ISO-10303-21;
HEADER;
/* Generated by software containing ST-Developer
 * from STEP Tools, Inc. (www.steptools.com) 
 */

FILE_DESCRIPTION(
/* description */ (
'Independent welded steel electronics enclosure with removable sealed 
lid, internal mounting tray and two threaded cable entries. 300 x 220 
mm body. No ingress or electrical safety rating assigned.'),
/* implementation_level */ '2;1');

FILE_NAME(
/* name */ 'Socket head cap screw M6x16.step',
/* time_stamp */ '2026-11-14T09:13:27-08:00',
/* author */ (''),
/* organization */ (''),
/* preprocessor_version */ 'ST-DEVELOPER v20.2',
/* originating_system */ 'Autodesk Translation Framework v15.17.0.0',
/* authorisation */ '');

FILE_SCHEMA (('AUTOMOTIVE_DESIGN { 1 0 10303 214 3 1 1 }'));
ENDSEC;

DATA;
#10=MECHANICAL_DESIGN_GEOMETRIC_PRESENTATION_REPRESENTATION('',(#976),#94412);
#152=CONICAL_SURFACE('',#8795,2.5,0.785398163397448);
#162=B_SPLINE_SURFACE_WITH_KNOTS('',3,3,((#69341,#69342,#69343,#69344,#69345,
#69346,#69347,#69348,#69349,#69350,#69351,#69352,#69353,#69354,#69355,#69356,
#69357,#69358,#69359,#69360,#69361,#69362,#69363,#69364,#69365,#69366,#69367,
#69368,#69369,#69370,#69371,#69372,#69373,#69374,#69375,#69376,#69377,#69378,
#69379,#69380,#69381,#69382,#69383,#69384,#69385,#69386,#69387,#69388,#69389,
#69390,#69391,#69392,#69393,#69394,#69395,#69396,#69397,#69398,#69399,#69400,
#69401,#69402,#69403,#69404,#69405,#69406,#69407,#69408,#69409,#69410,#69411,
#69412,#69413,#69414,#69415,#69416,#69417,#69418,#69419,#69420,#69421,#69422,
#69423,#69424,#69425,#69426,#69427,#69428,#69429,#69430,#69431,#69432,#69433,
#69434,#69435,#69436,#69437,#69438,#69439,#69440,#69441,#69442),(#69443,
#69444,#69445,#69446,#69447,#69448,#69449,#69450,#69451,#69452,#69453,#69454,
#69455,#69456,#69457,#69458,#69459,#69460,#69461,#69462,#69463,#69464,#69465,
#69466,#69467,#69468,#69469,#69470,#69471,#69472,#69473,#69474,#69475,#69476,
#69477,#69478,#69479,#69480,#69481,#69482,#69483,#69484,#69485,#69486,#69487,
#69488,#69489,#69490,#69491,#69492,#69493,#69494,#69495,#69496,#69497,#69498,
#69499,#69500,#69501,#69502,#69503,#69504,#69505,#69506,#69507,#69508,#69509,
#69510,#69511,#69512,#69513,#69514,#69515,#69516,#69517,#69518,#69519,#69520,
#69521,#69522,#69523,#69524,#69525,#69526,#69527,#69528,#69529,#69530,#69531,
#69532,#69533,#69534,#69535,#69536,#69537,#69538,#69539,#69540,#69541,#69542,
#69543,#69544),(#69545,#69546,#69547,#69548,#69549,#69550,#69551,#69552,
#69553,#69554,#69555,#69556,#69557,#69558,#69559,#69560,#69561,#69562,#69563,
#69564,#69565,#69566,#69567,#69568,#69569,#69570,#69571,#69572,#69573,#69574,
#69575,#69576,#69577,#69578,#69579,#69580,#69581,#69582,#69583,#69584,#69585,
#69586,#69587,#69588,#69589,#69590,#69591,#69592,#69593,#69594,#69595,#69596,
#69597,#69598,#69599,#69600,#69601,#69602,#69603,#69604,#69605,#69606,#69607,
#69608,#69609,#69610,#69611,#69612,#69613,#69614,#69615,#69616,#69617,#69618,
#69619,#69620,#69621,#69622,#69623,#69624,#69625,#69626,#69627,#69628,#69629,
#69630,#69631,#69632,#69633,#69634,#69635,#69636,#69637,#69638,#69639,#69640,
#69641,#69642,#69643,#69644,#69645,#69646),(#69647,#69648,#69649,#69650,
#69651,#69652,#69653,#69654,#69655,#69656,#69657,#69658,#69659,#69660,#69661,
#69662,#69663,#69664,#69665,#69666,#69667,#69668,#69669,#69670,#69671,#69672,
#69673,#69674,#69675,#69676,#69677,#69678,#69679,#69680,#69681,#69682,#69683,
#69684,#69685,#69686,#69687,#69688,#69689,#69690,#69691,#69692,#69693,#69694,
#69695,#69696,#69697,#69698,#69699,#69700,#69701,#69702,#69703,#69704,#69705,
#69706,#69707,#69708,#69709,#69710,#69711,#69712,#69713,#69714,#69715,#69716,
#69717,#69718,#69719,#69720,#69721,#69722,#69723,#69724,#69725,#69726,#69727,
#69728,#69729,#69730,#69731,#69732,#69733,#69734,#69735,#69736,#69737,#69738,
#69739,#69740,#69741,#69742,#69743,#69744,#69745,#69746,#69747,#69748)),
 .UNSPECIFIED.,.F.,.F.,.F.,(4,4),(4,1,1,1,1,1,1,1,1,1,1,1,1,1,1,1,1,1,1,
1,1,1,1,1,1,1,1,1,1,1,1,1,1,1,1,1,1,1,1,1,1,1,1,1,1,1,1,1,1,1,1,1,1,1,1,
1,1,1,1,1,1,1,1,1,1,1,1,1,1,1,1,1,1,1,1,1,1,1,1,1,1,1,1,1,1,1,1,1,1,1,1,
1,1,1,1,1,1,1,1,4),(-0.000429898909490116,0.0663250612852997),(11.6145561949038,
12.6069034617266,13.598774075635,14.5906446895433,15.5825153034517,16.5743859173601,
17.5662565312685,18.5581271451769,19.5499977590852,20.5418683729936,21.533738986902,
22.5256096008104,23.5174802147187,24.5093508286271,25.5012214425355,26.4930920564439,
27.4849626703523,28.4768332842606,29.468703898169,30.4605745120774,31.4524451259858,
32.4443157398941,33.4361863538025,34.4280569677109,35.4199275816193,36.4117981955277,
37.403668809436,38.3955394233444,39.3874100372528,40.3792806511612,41.3711512650695,
42.3630218789779,43.3548924928863,44.3467631067947,45.3386337207031,46.3305043346114,
47.3223749485198,48.3142455624282,49.3061161763366,50.2979867902449,51.2898574041533,
52.2817280180617,53.2735986319701,54.2654692458785,55.2573398597868,56.2492104736952,
57.2410810876036,58.232951701512,59.2248223154203,60.2166929293287,61.2085635432371,
62.2004341571455,63.1923047710539,64.1841753849622,65.1760459988706,66.167916612779,
67.1597872266874,68.1516578405957,69.1435284545041,70.1353990684125,71.1272696823209,
72.1191402962293,73.1110109101376,74.102881524046,75.0947521379544,76.0866227518628,
77.0784933657711,78.0703639796795,79.0622345935879,80.0541052074963,81.0459758214047,
82.037846435313,83.0297170492214,84.0215876631298,85.0134582770382,86.0053288909465,
86.9971995048549,87.9890701187633,88.9809407326717,89.9728113465801,90.9646819604884,
91.9565525743968,92.9484231883052,93.9402938022136,94.9321644161219,95.9240350300303,
96.9159056439387,97.9077762578471,98.8996468717555,99.8915174856638,100.883388099572,
101.875258713481,102.867129327389,103.858999941297,104.850870555206,105.842741169114,
106.834611783022,107.826482396931,108.818353010839,109.810701887832),
 .UNSPECIFIED.);
#163=B_SPLINE_SURFACE_WITH_KNOTS('',3,3,((#69837,#69838,#69839,#69840,#69841,
#69842,#69843,#69844,#69845,#69846,#69847,#69848,#69849,#69850,#69851,#69852,
#69853,#69854,#69855,#69856,#69857,#69858,#69859,#69860,#69861,#69862,#69863,
#69864,#69865,#69866,#69867,#69868,#69869,#69870,#69871,#69872,#69873,#69874,
#69875,#69876,#69877,#69878,#69879,#69880,#69881,#69882,#69883,#69884,#69885,
#69886,#69887,#69888,#69889,#69890,#69891,#69892,#69893,#69894,#69895,#69896,
#69897,#69898,#69899,#69900,#69901,#69902,#69903,#69904,#69905,#69906,#69907,
#69908,#69909,#69910,#69911,#69912,#69913,#69914,#69915,#69916,#69917,#69918,
#69919,#69920,#69921,#69922,#69923,#69924,#69925,#69926,#69927,#69928,#69929,
#69930,#69931,#69932,#69933,#69934,#69935,#69936,#69937,#69938,#69939,#69940),
(#69941,#69942,#69943,#69944,#69945,#69946,#69947,#69948,#69949,#69950,
#69951,#69952,#69953,#69954,#69955,#69956,#69957,#69958,#69959,#69960,#69961,
#69962,#69963,#69964,#69965,#69966,#69967,#69968,#69969,#69970,#69971,#69972,
#69973,#69974,#69975,#69976,#69977,#69978,#69979,#69980,#69981,#69982,#69983,
#69984,#69985,#69986,#69987,#69988,#69989,#69990,#69991,#69992,#69993,#69994,
#69995,#69996,#69997,#69998,#69999,#70000,#70001,#70002,#70003,#70004,#70005,
#70006,#70007,#70008,#70009,#70010,#70011,#70012,#70013,#70014,#70015,#70016,
#70017,#70018,#70019,#70020,#70021,#70022,#70023,#70024,#70025,#70026,#70027,
#70028,#70029,#70030,#70031,#70032,#70033,#70034,#70035,#70036,#70037,#70038,
#70039,#70040,#70041,#70042,#70043,#70044),(#70045,#70046,#70047,#70048,
#70049,#70050,#70051,#70052,#70053,#70054,#70055,#70056,#70057,#70058,#70059,
#70060,#70061,#70062,#70063,#70064,#70065,#70066,#70067,#70068,#70069,#70070,
#70071,#70072,#70073,#70074,#70075,#70076,#70077,#70078,#70079,#70080,#70081,
#70082,#70083,#70084,#70085,#70086,#70087,#70088,#70089,#70090,#70091,#70092,
#70093,#70094,#70095,#70096,#70097,#70098,#70099,#70100,#70101,#70102,#70103,
#70104,#70105,#70106,#70107,#70108,#70109,#70110,#70111,#70112,#70113,#70114,
#70115,#70116,#70117,#70118,#70119,#70120,#70121,#70122,#70123,#70124,#70125,
#70126,#70127,#70128,#70129,#70130,#70131,#70132,#70133,#70134,#70135,#70136,
#70137,#70138,#70139,#70140,#70141,#70142,#70143,#70144,#70145,#70146,#70147,
#70148),(#70149,#70150,#70151,#70152,#70153,#70154,#70155,#70156,#70157,
#70158,#70159,#70160,#70161,#70162,#70163,#70164,#70165,#70166,#70167,#70168,
#70169,#70170,#70171,#70172,#70173,#70174,#70175,#70176,#70177,#70178,#70179,
#70180,#70181,#70182,#70183,#70184,#70185,#70186,#70187,#70188,#70189,#70190,
#70191,#70192,#70193,#70194,#70195,#70196,#70197,#70198,#70199,#70200,#70201,
#70202,#70203,#70204,#70205,#70206,#70207,#70208,#70209,#70210,#70211,#70212,
#70213,#70214,#70215,#70216,#70217,#70218,#70219,#70220,#70221,#70222,#70223,
#70224,#70225,#70226,#70227,#70228,#70229,#70230,#70231,#70232,#70233,#70234,
#70235,#70236,#70237,#70238,#70239,#70240,#70241,#70242,#70243,#70244,#70245,
#70246,#70247,#70248,#70249,#70250,#70251,#70252)),.UNSPECIFIED.,.F.,.F.,
 .F.,(4,4),(4,1,1,1,1,1,1,1,1,1,1,1,1,1,1,1,1,1,1,1,1,1,1,1,1,1,1,1,1,1,
1,1,1,1,1,1,1,1,1,1,1,1,1,1,1,1,1,1,1,1,1,1,1,1,1,1,1,1,1,1,1,1,1,1,1,1,
1,1,1,1,1,1,1,1,1,1,1,1,1,1,1,1,1,1,1,1,1,1,1,1,1,1,1,1,1,1,1,1,1,1,1,4),
(-0.000478368004393251,0.0662783428032473),(8.30747755240101,9.30018873014199,
10.292899907883,11.2856110856239,12.2783222633649,13.2710334411059,14.2637446188469,
15.2564557965878,16.2491669743288,17.2418781520698,18.2345893298108,19.2273005075518,
20.2200116852927,21.2127228630337,22.2054340407747,23.1981452185157,24.1908563962566,
25.1835675739976,26.1762787517386,27.1689899294796,28.1617011072206,29.1544122849615,
30.1471234627025,31.1398346404435,32.1325458181845,33.1252569959254,34.1179681736664,
35.1106793514074,36.1033905291484,37.0961017068893,38.0888128846303,39.0815240623713,
40.0742352401123,41.0669464178533,42.0596575955942,43.0523687733352,44.0450799510762,
45.0377911288172,46.0305023065581,47.0232134842991,48.0159246620401,49.0086358397811,
50.001347017522,50.994058195263,51.986769373004,52.979480550745,53.972191728486,
54.9649029062269,55.9576140839679,56.9503252617089,57.9430364394499,58.9357476171908,
59.9284587949318,60.9211699726728,61.9138811504138,62.9065923281547,63.8993035058957,
64.8920146836367,65.8847258613777,66.8774370391187,67.8701482168596,68.8628593946006,
69.8555705723416,70.8482817500825,71.8409929278235,72.8337041055645,73.8264152833055,
74.8191264610465,75.8118376387874,76.8045488165284,77.7972599942694,78.7899711720104,
79.7826823497514,80.7753935274923,81.7681047052333,82.7608158829743,83.7535270607153,
84.7462382384562,85.7389494161972,86.7316605939382,87.7243717716792,88.7170829494201,
89.7097941271611,90.7025053049021,91.6952164826431,92.687927660384,93.680638838125,
94.673350015866,95.666061193607,96.658772371348,97.6514835490889,98.6441947268299,
99.6369059045709,100.629617082312,101.622328260053,102.615039437794,103.607750615535,
104.600461793276,105.593172971017,106.585884148758,107.578595326499,108.571784872244),
 .UNSPECIFIED.);
#660=B_SPLINE_CURVE_WITH_KNOTS('',3,(#59880,#59881,#59882,#59883,#59884,
#59885,#59886,#59887,#59888,#59889,#59890,#59891,#59892,#59893,#59894,#59895,
#59896,#59897,#59898,#59899,#59900,#59901,#59902,#59903,#59904,#59905,#59906,
#59907,#59908,#59909,#59910,#59911,#59912,#59913,#59914,#59915,#59916,#59917,
#59918,#59919,#59920,#59921,#59922,#59923,#59924,#59925,#59926,#59927,#59928,
#59929,#59930,#59931,#59932,#59933,#59934,#59935,#59936,#59937,#59938,#59939,
#59940,#59941,#59942,#59943,#59944,#59945,#59946,#59947,#59948,#59949,#59950,
#59951,#59952,#59953,#59954,#59955,#59956,#59957,#59958,#59959,#59960,#59961,
#59962,#59963,#59964,#59965,#59966,#59967,#59968,#59969,#59970,#59971,#59972,
#59973,#59974,#59975,#59976,#59977,#59978,#59979,#59980,#59981,#59982,#59983,
#59984,#59985,#59986,#59987,#59988,#59989,#59990,#59991,#59992,#59993,#59994,
#59995,#59996,#59997,#59998,#59999,#60000,#60001,#60002,#60003,#60004,#60005,
#60006,#60007,#60008,#60009,#60010,#60011,#60012,#60013,#60014,#60015,#60016,
#60017,#60018,#60019,#60020,#60021,#60022,#60023,#60024,#60025,#60026,#60027,
#60028,#60029,#60030,#60031,#60032,#60033,#60034,#60035,#60036,#60037,#60038,
#60039,#60040,#60041,#60042,#60043,#60044,#60045,#60046,#60047,#60048,#60049,
#60050,#60051,#60052,#60053,#60054,#60055,#60056,#60057,#60058,#60059,#60060,
#60061,#60062,#60063,#60064,#60065,#60066,#60067,#60068,#60069,#60070,#60071,
#60072,#60073,#60074,#60075,#60076,#60077,#60078,#60079,#60080,#60081,#60082,
#60083,#60084,#60085,#60086,#60087,#60088,#60089,#60090,#60091,#60092,#60093,
#60094,#60095,#60096,#60097,#60098,#60099),.UNSPECIFIED.,.F.,.F.,(4,2,2,
2,2,2,2,2,2,2,2,2,2,2,2,2,2,2,2,2,2,2,2,2,2,2,2,2,2,2,2,2,2,2,2,2,2,2,2,
2,2,2,2,2,2,2,2,2,2,2,2,2,2,2,2,2,2,2,2,2,2,2,2,2,2,2,2,2,2,2,2,2,2,2,2,
2,2,2,2,2,2,2,2,2,2,2,2,2,2,2,2,2,2,2,2,2,2,2,2,2,2,2,2,2,2,2,2,2,2,4),
(-1.25131977917524,-1.23656241881066,-1.20701295486785,-1.19935871676255,
-1.16998794161902,-1.16491791364363,-1.16206861960701,-1.15985345132094,
-1.15669994958711,-1.14996749086125,-1.12074390449838,-1.0680149534151,
-1.05340619187006,-1.04716889055948,-1.04274260344209,-1.03812375910127,
-1.03112895839771,-1.00928158984193,-0.968195495489653,-0.933932853647884,
-0.92881700987865,-0.925953556630634,-0.923730250269325,-0.920569233340291,
-0.913843744006523,-0.884771920553245,-0.832301822404733,-0.817786153245362,
-0.811551968163211,-0.807118490998376,-0.802483582653689,-0.795446646811962,
-0.773291417064023,-0.731159554570256,-0.698108987017462,-0.693006864744909,
-0.690148059879696,-0.687721451057466,-0.684473160784883,-0.677133693698043,
-0.666683646671541,-0.634103674058093,-0.589030563247094,-0.579716218945477,
-0.574137223679013,-0.569781993080877,-0.564995877635212,-0.557099295630797,
-0.522644451837198,-0.498367101298772,-0.491757393674209,-0.461620048853493,
-0.45655361502068,-0.453713766588345,-0.451501624306616,-0.448354019829487,
-0.441665163028119,-0.412925065500677,-0.361710023544992,-0.345200197292985,
-0.338660560506218,-0.334572225302417,-0.330068155759284,-0.323731329808694,
-0.307418910181425,-0.282201113022025,-0.22776757811646,-0.221258922839231,
-0.218103105280213,-0.215673498636336,-0.215595324444493,-0.215532309095076,
-0.215481049666447,-0.215439050839442,-0.215404439133561,-0.215346195470749,
-0.215290095264256,-0.215235966328501,-0.215183653324741,-0.215133015668737,
-0.215083925738375,-0.215036267342248,-0.214989934391034,-0.214944829751753,
-0.214900864254929,-0.214857955826897,-0.214816028731415,-0.214775012905456,
-0.214734843373777,-0.21469545973249,-0.214656805689996,-0.214618828661828,
-0.214581479411155,-0.214544711722475,-0.214508482116246,-0.214472749586117,
-0.214437475364664,-0.214402622713177,-0.211017314188223,-0.202128083903168,
-0.188616362646853,-0.128692901795126,-0.112341255688242,-0.105779734258138,
-0.10123828105323,-0.0965920861369307,-0.0897300410221464,-0.0697341073430826,
-0.0351736997662141,-0.00354544123312327),.UNSPECIFIED.);
#661=B_SPLINE_CURVE_WITH_KNOTS('',3,(#60102,#60103,#60104,#60105,#60106,
#60107,#60108,#60109,#60110,#60111,#60112,#60113,#60114,#60115,#60116,#60117,
#60118,#60119,#60120,#60121,#60122,#60123,#60124,#60125,#60126,#60127,#60128,
#60129,#60130,#60131,#60132,#60133,#60134,#60135,#60136,#60137,#60138,#60139,
#60140,#60141,#60142,#60143,#60144,#60145,#60146,#60147,#60148,#60149,#60150,
#60151,#60152,#60153,#60154,#60155,#60156,#60157,#60158,#60159,#60160,#60161,
#60162,#60163,#60164,#60165,#60166,#60167,#60168,#60169,#60170,#60171,#60172,
#60173,#60174,#60175,#60176,#60177,#60178,#60179,#60180,#60181,#60182,#60183,
#60184,#60185,#60186,#60187,#60188,#60189,#60190,#60191,#60192,#60193,#60194,
#60195,#60196,#60197,#60198,#60199,#60200,#60201,#60202,#60203,#60204,#60205,
#60206,#60207,#60208,#60209,#60210,#60211,#60212,#60213,#60214,#60215,#60216,
#60217,#60218,#60219,#60220,#60221,#60222,#60223,#60224,#60225),
 .UNSPECIFIED.,.F.,.F.,(4,3,3,3,3,3,3,3,3,3,3,3,3,3,3,3,3,3,3,3,3,3,3,3,
3,3,3,3,3,3,3,3,3,3,3,3,3,3,3,3,3,4),(11.6150328478182,11.7179446012586,
11.8207946212876,11.923634938576,12.0264737944964,12.1293362764885,12.2322474918762,
12.335310488753,12.4384541798223,12.5417938440493,12.6069034617266,12.706476373012,
12.8058907630902,12.9051721677229,13.0043802300127,13.103547378039,13.2027059877237,
13.3019580568064,13.4012539542961,13.5007320275801,13.598774075635,13.6995165720154,
13.8001157862556,13.9005997135967,14.0010206760435,14.1014095657536,14.2017972346013,
14.3022816451625,14.4028137969415,14.5035204650583,14.5906446895433,14.691401271234,
14.7920178477645,14.8925240235074,14.9929702101377,15.0933872721949,15.1938060367443,
15.2943259460171,15.3948960718821,15.4956444670245,15.5825153034517,15.63538085578),
 .UNSPECIFIED.);
#662=B_SPLINE_CURVE_WITH_KNOTS('',3,(#60230,#60231,#60232,#60233,#60234,
#60235,#60236,#60237,#60238,#60239,#60240,#60241,#60242,#60243,#60244,#60245,
#60246,#60247,#60248,#60249,#60250,#60251,#60252,#60253,#60254,#60255,#60256,
#60257,#60258,#60259,#60260,#60261,#60262,#60263,#60264,#60265,#60266,#60267,
#60268,#60269,#60270,#60271,#60272,#60273,#60274,#60275,#60276,#60277,#60278,
#60279,#60280,#60281,#60282,#60283,#60284,#60285,#60286,#60287,#60288,#60289,
#60290,#60291,#60292,#60293,#60294,#60295,#60296,#60297,#60298,#60299,#60300,
#60301,#60302,#60303,#60304,#60305,#60306,#60307,#60308,#60309,#60310,#60311,
#60312,#60313,#60314,#60315,#60316,#60317,#60318,#60319,#60320,#60321,#60322,
#60323,#60324,#60325,#60326,#60327,#60328,#60329,#60330,#60331,#60332,#60333,
#60334,#60335,#60336,#60337,#60338,#60339,#60340,#60341,#60342,#60343,#60344,
#60345,#60346,#60347,#60348,#60349,#60350,#60351,#60352,#60353,#60354,#60355,
#60356,#60357,#60358,#60359,#60360,#60361,#60362,#60363,#60364,#60365,#60366,
#60367,#60368,#60369,#60370,#60371,#60372,#60373,#60374,#60375,#60376,#60377,
#60378,#60379,#60380,#60381,#60382,#60383,#60384,#60385,#60386,#60387,#60388,
#60389,#60390,#60391,#60392,#60393,#60394,#60395,#60396,#60397,#60398,#60399,
#60400,#60401,#60402,#60403,#60404,#60405,#60406,#60407,#60408,#60409,#60410,
#60411,#60412,#60413,#60414,#60415,#60416,#60417,#60418,#60419,#60420,#60421,
#60422,#60423,#60424,#60425,#60426,#60427,#60428,#60429,#60430,#60431,#60432,
#60433,#60434,#60435,#60436,#60437),.UNSPECIFIED.,.F.,.F.,(4,2,2,2,2,2,
2,2,2,2,2,2,2,2,2,2,2,2,2,2,2,2,2,2,2,2,2,2,2,2,2,2,2,2,2,2,2,2,2,2,2,2,
2,2,2,2,2,2,2,2,2,2,2,2,2,2,2,2,2,2,2,2,2,2,2,2,2,2,2,2,2,2,2,2,2,2,2,2,
2,2,2,2,2,2,2,2,2,2,2,2,2,2,2,2,2,2,2,2,2,2,2,2,2,4),(-2.74540210132995,
-2.71148878064438,-2.70502039877798,-2.69915538242511,-2.69474829232318,
-2.68999575073976,-2.68235751778743,-2.65577199448838,-2.61843778059984,
-2.58646854578538,-2.58146128272585,-2.57906790744654,-2.57685167660375,
-2.5740019528062,-2.56893555598404,-2.53982230770332,-2.53176532679166,
-2.50196619744075,-2.48265943784217,-2.46910514556952,-2.46320930388327,
-2.45879747327701,-2.45405728408279,-2.44647752147774,-2.42140337771276,
-2.37665569015157,-2.35859977029646,-2.35122810245577,-2.3455848945712,
-2.34264415389782,-2.34019248203058,-2.33702027417077,-2.33042982937092,
-2.288215565947,-2.27425605039392,-2.24993867509917,-2.23401637799999,-2.22775355936165,
-2.22327975268266,-2.21920417986974,-2.21265335612755,-2.19593832494037,
-2.14529820496415,-2.11679946167232,-2.11014329207341,-2.10700360387211,
-2.1047891237258,-2.10192724727491,-2.09680631926088,-2.0620156496777,-2.03518318405526,
-2.01273978387739,-2.00245242345074,-1.99402362209504,-1.98910255041698,
-1.98473739185936,-1.97920515005959,-1.97033142881071,-1.91601554106387,
-1.87897954341978,-1.87342601186145,-1.87050375095237,-1.86805047724644,
-1.86490727860569,-1.85805079628739,-1.82035089359626,-1.78375010644519,
-1.76321164751351,-1.75635960175413,-1.7517712136186,-1.74732686040429,
-1.74098224081769,-1.72559708094449,-1.6736629840931,-1.64471559334932,
-1.63801146479455,-1.63486230392345,-1.63264573452409,-1.62978691323599,
-1.62468688200851,-1.59180961546464,-1.56425704241657,-1.52943407360889,
-1.52148361789708,-1.51666231162885,-1.51227240238779,-1.50664404484596,
-1.49723139443558,-1.45555750097605,-1.42076350483367,-1.40468769956954,
-1.40034876208145,-1.39768636854869,-1.39518354337576,-1.39147126710944,
-1.38196612464931,-1.31695904095716,-1.29241366120115,-1.28488616538071,
-1.28015964555661,-1.27574774387445,-1.26983247445604,-1.25614345626771,
-1.25131977917524),.UNSPECIFIED.);
#663=B_SPLINE_CURVE_WITH_KNOTS('',3,(#60439,#60440,#60441,#60442),
 .UNSPECIFIED.,.F.,.F.,(4,4),(15.63538085578,15.7079632679489),
 .UNSPECIFIED.);
#664=B_SPLINE_CURVE_WITH_KNOTS('',3,(#60443,#60444,#60445,#60446,#60447,
#60448,#60449,#60450,#60451,#60452,#60453,#60454,#60455,#60456,#60457,#60458,
#60459,#60460,#60461,#60462,#60463,#60464,#60465,#60466,#60467,#60468,#60469,
#60470,#60471,#60472,#60473,#60474,#60475,#60476,#60477,#60478,#60479,#60480,
#60481,#60482,#60483,#60484,#60485,#60486,#60487,#60488,#60489,#60490,#60491,
#60492,#60493,#60494,#60495,#60496,#60497,#60498,#60499,#60500,#60501,#60502,
#60503,#60504,#60505,#60506,#60507,#60508,#60509,#60510,#60511,#60512,#60513,
#60514,#60515,#60516,#60517,#60518,#60519,#60520,#60521,#60522,#60523,#60524,
#60525,#60526,#60527,#60528,#60529,#60530,#60531,#60532,#60533,#60534,#60535,
#60536,#60537,#60538,#60539,#60540,#60541,#60542,#60543,#60544,#60545,#60546,
#60547,#60548,#60549,#60550,#60551,#60552,#60553,#60554,#60555,#60556,#60557,
#60558,#60559,#60560,#60561,#60562,#60563,#60564,#60565,#60566,#60567,#60568,
#60569,#60570,#60571,#60572,#60573,#60574,#60575,#60576,#60577,#60578,#60579,
#60580,#60581,#60582,#60583,#60584,#60585,#60586,#60587,#60588,#60589,#60590,
#60591,#60592,#60593,#60594,#60595,#60596,#60597,#60598,#60599,#60600,#60601,
#60602,#60603,#60604,#60605,#60606,#60607,#60608,#60609,#60610,#60611,#60612,
#60613,#60614,#60615,#60616,#60617,#60618,#60619,#60620,#60621,#60622,#60623,
#60624,#60625,#60626,#60627,#60628,#60629,#60630,#60631,#60632,#60633,#60634,
#60635,#60636,#60637,#60638,#60639,#60640,#60641,#60642,#60643,#60644),
 .UNSPECIFIED.,.F.,.F.,(4,2,2,2,2,2,2,2,2,2,2,2,2,2,2,2,2,2,2,2,2,2,2,2,
2,2,2,2,2,2,2,2,2,2,2,2,2,2,2,2,2,2,2,2,2,2,2,2,2,2,2,2,2,2,2,2,2,2,2,2,
2,2,2,2,2,2,2,2,2,2,2,2,2,2,2,2,2,2,2,2,2,2,2,2,2,2,2,2,2,2,2,2,2,2,2,2,
2,2,2,2,4),(-2.98988513948328,-2.9890416521686,-2.92263169910402,-2.91052211338097,
-2.9048225881356,-2.90037948007852,-2.89542472032189,-2.88706812245068,
-2.84498674133361,-2.81330044732805,-2.79856800781766,-2.79208647956025,
-2.78714431285256,-2.78427320418269,-2.78176278084892,-2.77848125081889,
-2.77109437620559,-2.71703359952672,-2.69214521419253,-2.68109477778924,
-2.67214054105368,-2.66702812690655,-2.66255677049176,-2.65697043445206,
-2.64565031060122,-2.5895185263064,-2.56698077938366,-2.55846505756579,
-2.55213377816661,-2.54900629168709,-2.54649376766983,-2.54335120435105,
-2.53691296744397,-2.49073918797809,-2.44466978940957,-2.43626015740604,
-2.43127026806654,-2.42679216377246,-2.42104160876643,-2.40879222669042,
-2.3407514312561,-2.32660208625429,-2.31740882957647,-2.31379753759757,
-2.31124456163607,-2.30844073832737,-2.30362363718131,-2.28399700056034,
-2.24687156102182,-2.21489833999116,-2.20269571671468,-2.19695802201051,
-2.19248628526751,-2.18749989640427,-2.1790879421364,-2.13842309363864,
-2.1083431943885,-2.09199254371572,-2.08182672658222,-2.07807663020203,
-2.07549982550455,-2.07308939971531,-2.06886808333821,-2.05594812003229,
-2.00914412269069,-1.98453734522703,-1.97357278556821,-1.96467723026801,
-1.95958411605605,-1.95512177504329,-1.94953678494926,-1.94071360967437,
-1.87646035777905,-1.85749363828203,-1.84984564474205,-1.84401589113536,
-1.84099521807015,-1.83848503844687,-1.83523888030372,-1.82848788858546,
-1.78966867805449,-1.76999982516351,-1.74742136431683,-1.73703879719564,
-1.7285131056941,-1.72349915266241,-1.71902672977988,-1.71332117265768,
-1.70408025654224,-1.65409075944999,-1.62557319984512,-1.61580239479506,
-1.60878389507161,-1.60553432523165,-1.60326403243555,-1.60035323528149,
-1.59518844543772,-1.56351406666289,-1.55856664877721,-1.52619751615928,
-1.51264578802335),.UNSPECIFIED.);
#665=B_SPLINE_CURVE_WITH_KNOTS('',3,(#60650,#60651,#60652,#60653,#60654,
#60655,#60656,#60657,#60658,#60659,#60660),.UNSPECIFIED.,.F.,.F.,(4,1,1,
1,1,1,1,1,4),(21.9911485751285,22.2054340407747,23.1981452185157,24.1908563962566,
25.1835675739976,26.1762787517386,27.1689899294796,28.1617011072206,28.2016224877447),
 .UNSPECIFIED.);
#666=B_SPLINE_CURVE_WITH_KNOTS('',3,(#60661,#60662,#60663,#60664),
 .UNSPECIFIED.,.F.,.F.,(4,4),(-2.762961044583,-2.74540210132995),
 .UNSPECIFIED.);
#667=B_SPLINE_CURVE_WITH_KNOTS('',3,(#60665,#60666,#60667,#60668,#60669,
#60670,#60671,#60672,#60673,#60674,#60675,#60676,#60677,#60678,#60679,#60680,
#60681,#60682,#60683,#60684,#60685,#60686,#60687,#60688,#60689,#60690,#60691,
#60692,#60693,#60694,#60695,#60696,#60697,#60698,#60699,#60700,#60701,#60702,
#60703,#60704,#60705,#60706,#60707,#60708,#60709,#60710,#60711,#60712,#60713,
#60714,#60715,#60716,#60717,#60718,#60719,#60720,#60721,#60722,#60723,#60724,
#60725,#60726,#60727,#60728,#60729,#60730,#60731,#60732,#60733,#60734,#60735,
#60736,#60737,#60738,#60739,#60740,#60741,#60742,#60743,#60744,#60745,#60746,
#60747,#60748,#60749,#60750,#60751,#60752,#60753,#60754,#60755,#60756,#60757,
#60758,#60759,#60760,#60761,#60762,#60763,#60764,#60765,#60766,#60767,#60768,
#60769,#60770,#60771,#60772,#60773,#60774,#60775,#60776,#60777,#60778,#60779,
#60780,#60781,#60782,#60783,#60784,#60785,#60786,#60787,#60788,#60789,#60790,
#60791,#60792,#60793,#60794,#60795,#60796,#60797,#60798,#60799,#60800,#60801,
#60802,#60803,#60804,#60805,#60806,#60807,#60808,#60809,#60810,#60811,#60812,
#60813,#60814,#60815,#60816,#60817,#60818,#60819,#60820,#60821,#60822,#60823,
#60824,#60825,#60826,#60827,#60828,#60829,#60830,#60831,#60832,#60833,#60834,
#60835,#60836,#60837,#60838,#60839,#60840,#60841,#60842,#60843,#60844,#60845,
#60846,#60847,#60848,#60849,#60850,#60851,#60852,#60853,#60854,#60855,#60856,
#60857,#60858,#60859,#60860,#60861,#60862,#60863,#60864,#60865,#60866,#60867,
#60868,#60869,#60870,#60871,#60872,#60873,#60874,#60875,#60876,#60877,#60878,
#60879,#60880),.UNSPECIFIED.,.F.,.F.,(4,2,2,2,2,2,2,2,2,2,2,2,2,2,2,2,2,
2,2,2,2,2,2,2,2,2,2,2,2,2,2,2,2,2,2,2,2,2,2,2,2,2,2,2,2,2,2,2,2,2,2,2,2,
2,2,2,2,2,2,2,2,2,2,2,2,2,2,2,2,2,2,2,2,2,2,2,2,2,2,2,2,2,2,2,2,2,2,2,2,
2,2,2,2,2,2,2,2,2,2,2,2,2,2,2,2,2,2,4),(-1.51264578802335,-1.50824742685751,
-1.49533761970036,-1.48953443554317,-1.48503835802918,-1.48012834175573,
-1.47208960266296,-1.43768348666959,-1.41207448473708,-1.37709072636435,
-1.3718917214899,-1.36897323675787,-1.36670395455006,-1.36346509250798,
-1.35650637519991,-1.32565656373753,-1.26655813435419,-1.25736763246281,
-1.25215959838171,-1.24775061296511,-1.24234006042237,-1.2318878269114,
-1.21836221161977,-1.18325177190705,-1.1436904093263,-1.13694585630377,
-1.13370104690605,-1.13119171527509,-1.12817229721059,-1.12234305813237,
-1.09805717878198,-1.04539492736767,-1.02620490939015,-1.0192124889966,
-1.01499050691231,-1.01045185975469,-1.00426957108446,-0.989441746128937,
-0.967641506053302,-0.924403025948637,-0.904505636141447,-0.899659065410351,
-0.896847146869314,-0.894294815974935,-0.890693927051407,-0.881574126068692,
-0.867585440150397,-0.802323655848105,-0.78841984888466,-0.782832153608177,
-0.778671699346145,-0.774083128238035,-0.767614388424231,-0.750847631532854,
-0.724715793534429,-0.686591942583678,-0.668354451969255,-0.663623739851483,
-0.660837131401936,-0.658274547699032,-0.654612485700317,-0.645081672151302,
-0.580326066405161,-0.555678940085506,-0.548037582743291,-0.543212133210271,
-0.538686221769879,-0.532580758242613,-0.51823649151297,-0.497442371630394,
-0.469183815947758,-0.436055784894154,-0.429142947436221,-0.425912986079974,
-0.423405037435553,-0.420375001722253,-0.414491988616732,-0.374626674798603,
-0.324495723259461,-0.315268308078574,-0.309567249806176,-0.305096086043443,
-0.300081178282735,-0.29154798623774,-0.281152175522218,-0.258526113875507,
-0.218170322377199,-0.196907800629956,-0.191989462241814,-0.189162234580494,
-0.186615972927455,-0.186594270579785,-0.18657307999466,-0.186552377311534,
-0.186532140083982,-0.186512347162349,-0.183227486755542,-0.175322346189646,
-0.163544859603235,-0.122545419456931,-0.0852549480989891,-0.0769461251879338,
-0.0719788213987705,-0.0674979115811748,-0.0617113107814555,-0.0553956176738501,
-0.0447410390484928,-0.0182464691462297),.UNSPECIFIED.);
#668=B_SPLINE_CURVE_WITH_KNOTS('',3,(#60886,#60887,#60888,#60889,#60890,
#60891,#60892,#60893,#60894,#60895,#60896,#60897,#60898,#60899,#60900,#60901,
#60902,#60903,#60904,#60905,#60906,#60907,#60908,#60909,#60910,#60911,#60912,
#60913,#60914,#60915,#60916,#60917,#60918,#60919,#60920,#60921,#60922,#60923,
#60924,#60925,#60926,#60927,#60928,#60929,#60930,#60931,#60932,#60933,#60934,
#60935,#60936,#60937,#60938,#60939,#60940,#60941,#60942,#60943,#60944,#60945,
#60946,#60947,#60948,#60949,#60950,#60951,#60952,#60953,#60954,#60955,#60956,
#60957,#60958,#60959,#60960,#60961,#60962,#60963,#60964,#60965,#60966,#60967,
#60968,#60969,#60970,#60971,#60972,#60973,#60974,#60975,#60976,#60977,#60978,
#60979,#60980,#60981,#60982,#60983,#60984,#60985,#60986,#60987,#60988,#60989,
#60990,#60991,#60992,#60993,#60994,#60995,#60996,#60997,#60998,#60999,#61000,
#61001,#61002,#61003,#61004,#61005,#61006,#61007,#61008,#61009,#61010,#61011,
#61012,#61013,#61014,#61015,#61016,#61017,#61018,#61019,#61020,#61021,#61022,
#61023,#61024,#61025,#61026,#61027,#61028,#61029,#61030,#61031,#61032,#61033,
#61034,#61035,#61036,#61037,#61038,#61039,#61040,#61041,#61042,#61043,#61044,
#61045,#61046,#61047,#61048,#61049,#61050,#61051,#61052,#61053,#61054,#61055,
#61056,#61057,#61058,#61059,#61060,#61061,#61062,#61063,#61064,#61065,#61066,
#61067,#61068,#61069,#61070,#61071,#61072,#61073,#61074,#61075),
 .UNSPECIFIED.,.F.,.F.,(4,3,3,3,3,3,3,3,3,3,3,3,3,3,3,3,3,3,3,3,3,3,3,3,
3,3,3,3,3,3,3,3,3,3,3,3,3,3,3,3,3,3,3,3,3,3,3,3,3,3,3,3,3,3,3,3,3,3,3,3,
3,3,3,4),(28.2743341515405,28.373510423933,28.4725496186461,28.5715132139937,
28.6704339425324,28.7693444802945,28.8683439593539,28.9673864432613,29.0666027207686,
29.1544122849615,29.2549893084417,29.3554225402566,29.4557405947623,29.555995827914,
29.6562193813565,29.7564423567437,29.8567645084394,29.9571353509374,30.0576848454224,
30.1471234627025,30.2477004859965,30.348133717608,30.4484517718857,30.5487070047943,
30.6489305579792,30.7491535330941,30.8494756844967,30.9498465266896,31.0503960208528,
31.1398346404435,31.240411665129,31.3408448981566,31.441162953881,31.5414181882544,
31.6416417429197,31.741864719529,31.8421868724372,31.9425577161444,32.0431072118187,
32.1325458181845,32.2331228421251,32.3335560743984,32.4338741293577,32.5341293629598,
32.6343529168488,32.7345758926779,32.8348980448052,32.9352688877297,33.0358183826278,
33.1252569959254,33.2258340199109,33.3262672522277,33.4265853072283,33.5268405408702,
33.6270640947977,33.7272870706639,33.8276092228255,33.9279800657829,34.028529560711,
34.1179681736664,34.2266510107969,34.3350816319526,34.4431465276488,34.4851594650687),
 .UNSPECIFIED.);
#669=B_SPLINE_CURVE_WITH_KNOTS('',3,(#61076,#61077,#61078,#61079),
 .UNSPECIFIED.,.F.,.F.,(4,4),(28.2016224877447,28.2743338823081),
 .UNSPECIFIED.);
#670=B_SPLINE_CURVE_WITH_KNOTS('',3,(#61081,#61082,#61083,#61084),
 .UNSPECIFIED.,.F.,.F.,(4,4),(-0.0182464691462297,-0.000683907669467373),
 .UNSPECIFIED.);
#671=B_SPLINE_CURVE_WITH_KNOTS('',3,(#61085,#61086,#61087,#61088,#61089,
#61090,#61091,#61092,#61093,#61094,#61095,#61096,#61097,#61098,#61099,#61100,
#61101,#61102,#61103,#61104,#61105,#61106,#61107,#61108,#61109,#61110,#61111,
#61112,#61113,#61114,#61115,#61116,#61117,#61118,#61119,#61120,#61121,#61122,
#61123,#61124,#61125,#61126,#61127,#61128,#61129,#61130,#61131,#61132,#61133,
#61134,#61135,#61136,#61137,#61138,#61139,#61140,#61141,#61142,#61143,#61144,
#61145,#61146,#61147,#61148,#61149,#61150,#61151,#61152,#61153,#61154,#61155,
#61156,#61157,#61158,#61159,#61160,#61161,#61162,#61163,#61164,#61165,#61166,
#61167,#61168,#61169,#61170,#61171,#61172,#61173,#61174,#61175,#61176,#61177,
#61178,#61179,#61180,#61181,#61182,#61183,#61184,#61185,#61186,#61187,#61188,
#61189,#61190,#61191,#61192,#61193,#61194,#61195,#61196,#61197,#61198,#61199,
#61200,#61201,#61202,#61203,#61204,#61205,#61206,#61207,#61208,#61209,#61210,
#61211,#61212,#61213,#61214,#61215,#61216,#61217,#61218,#61219,#61220,#61221,
#61222,#61223,#61224,#61225,#61226,#61227,#61228,#61229,#61230,#61231,#61232,
#61233,#61234,#61235,#61236,#61237,#61238,#61239,#61240,#61241,#61242,#61243,
#61244,#61245,#61246,#61247,#61248,#61249,#61250,#61251,#61252,#61253,#61254,
#61255,#61256,#61257,#61258,#61259,#61260,#61261,#61262,#61263,#61264,#61265,
#61266,#61267,#61268,#61269,#61270,#61271,#61272,#61273,#61274,#61275,#61276),
 .UNSPECIFIED.,.F.,.F.,(4,2,2,2,2,2,2,2,2,2,2,2,2,2,2,2,2,2,2,2,2,2,2,2,
2,2,2,2,2,2,2,2,2,2,2,2,2,2,2,2,2,2,2,2,2,2,2,2,2,2,2,2,2,2,2,2,2,2,2,2,
2,2,2,2,2,2,2,2,2,2,2,2,2,2,2,2,2,2,2,2,2,2,2,2,2,2,2,2,2,2,2,2,2,2,2,4),
(-2.98929371686741,-2.95942260090057,-2.94908673202952,-2.94568016859995,
-2.94316029079119,-2.94062978415982,-2.93775045959017,-2.93272485907433,
-2.90843250200678,-2.87437961387487,-2.83806022771823,-2.82988827047787,
-2.82487872151955,-2.82040690508782,-2.81469754036461,-2.80544058838125,
-2.75593338036318,-2.7158543386228,-2.70972363013292,-2.70664396034991,
-2.70413863945052,-2.70096718609043,-2.69436491288393,-2.65053170443754,
-2.60255764740952,-2.59401548864488,-2.58899881337042,-2.58452817192148,
-2.5788306642466,-2.56961506201767,-2.51918854198363,-2.47993569648334,
-2.47381344470312,-2.47073541619546,-2.46822998609407,-2.46505657156555,
-2.45844424087166,-2.41492993222893,-2.36663326561542,-2.35809988403435,
-2.35308499392165,-2.34861390609176,-2.34291303084164,-2.33368600588134,
-2.28348667391634,-2.24385299524389,-2.23783757590937,-2.23478083512784,
-2.2322744837398,-2.22907669904788,-2.22233593505826,-2.17997121825981,
-2.13055414439691,-2.12210950622387,-2.11711337269429,-2.11263862408216,
-2.1069048595422,-2.09756380269823,-2.05062964505076,-2.00816461292868,
-2.0020088171623,-1.99892404087715,-1.99641868753577,-1.99325238957545,
-1.98667783099717,-1.94278275659959,-1.89622751751532,-1.88690136356124,
-1.88171981654142,-1.87726777759646,-1.87180809826288,-1.86340471640823,
-1.80448355847513,-1.77349374584792,-1.76652174530783,-1.76328075195105,
-1.7610114383161,-1.7580947528467,-1.75290379581136,-1.71823848535071,-1.6913656798286,
-1.66908442485546,-1.6540291179165,-1.64781178677845,-1.64326744954752,
-1.63848103257163,-1.63102546613321,-1.60757504267856,-1.55338306018242,
-1.54017386336012,-1.53141974456107,-1.52787527070329,-1.52533191440914,
-1.52249470265252,-1.51753139877423,-1.51249653208003),.UNSPECIFIED.);
#672=B_SPLINE_CURVE_WITH_KNOTS('',3,(#61282,#61283,#61284,#61285,#61286,
#61287,#61288,#61289,#61290,#61291,#61292,#61293,#61294,#61295,#61296,#61297,
#61298,#61299,#61300,#61301,#61302,#61303,#61304,#61305,#61306,#61307,#61308,
#61309,#61310,#61311,#61312,#61313,#61314,#61315,#61316,#61317,#61318,#61319,
#61320,#61321,#61322,#61323,#61324,#61325,#61326,#61327,#61328,#61329,#61330,
#61331,#61332,#61333,#61334,#61335,#61336,#61337,#61338,#61339,#61340,#61341,
#61342,#61343,#61344,#61345,#61346,#61347,#61348,#61349,#61350,#61351,#61352,
#61353,#61354,#61355,#61356,#61357,#61358,#61359,#61360,#61361,#61362,#61363,
#61364,#61365,#61366,#61367,#61368,#61369,#61370,#61371,#61372,#61373,#61374,
#61375,#61376,#61377,#61378,#61379,#61380,#61381,#61382,#61383,#61384,#61385,
#61386,#61387,#61388,#61389,#61390,#61391,#61392,#61393,#61394,#61395,#61396,
#61397,#61398,#61399,#61400,#61401,#61402,#61403,#61404,#61405,#61406,#61407,
#61408,#61409,#61410,#61411,#61412,#61413,#61414,#61415,#61416,#61417,#61418,
#61419,#61420,#61421,#61422,#61423,#61424,#61425,#61426,#61427,#61428,#61429,
#61430,#61431,#61432,#61433,#61434,#61435,#61436,#61437,#61438,#61439,#61440,
#61441,#61442,#61443,#61444,#61445,#61446,#61447,#61448,#61449,#61450,#61451,
#61452,#61453,#61454,#61455,#61456,#61457,#61458,#61459,#61460,#61461,#61462,
#61463,#61464,#61465,#61466,#61467,#61468,#61469,#61470,#61471,#61472,#61473,
#61474,#61475,#61476,#61477,#61478,#61479,#61480,#61481,#61482,#61483,#61484,
#61485,#61486,#61487,#61488,#61489,#61490,#61491,#61492,#61493),
 .UNSPECIFIED.,.F.,.F.,(4,2,2,2,2,2,2,2,2,2,2,2,2,2,2,2,2,2,2,2,2,2,2,2,
2,2,2,2,2,2,2,2,2,2,2,2,2,2,2,2,2,2,2,2,2,2,2,2,2,2,2,2,2,2,2,2,2,2,2,2,
2,2,2,2,2,2,2,2,2,2,2,2,2,2,2,2,2,2,2,2,2,2,2,2,2,2,2,2,2,2,2,2,2,2,2,2,
2,2,2,2,2,2,2,2,2,4),(-1.47764986309498,-1.44881698295396,-1.43952935990818,
-1.43393724919047,-1.42955351574726,-1.42471638787349,-1.41668651112816,
-1.38010143774755,-1.36673596052301,-1.3238902221451,-1.3173053247027,-1.31413388159894,
-1.31168179412128,-1.30873929395105,-1.30308979745928,-1.29570878360394,
-1.27762005080888,-1.23287911256112,-1.20786267104714,-1.20028680944599,
-1.19554653131156,-1.19113289607351,-1.18523203237493,-1.17165416714221,
-1.15230025713113,-1.12244653776663,-1.11456732622048,-1.0853317294815,
-1.08026094845732,-1.07740969601219,-1.07519282195167,-1.0720358270436,
-1.06528879051481,-1.03592788138144,-0.982763616052192,-0.96867115490706,
-0.963124607704263,-0.959037394949743,-0.954572856963394,-0.948364471522385,
-0.932819019168934,-0.909343910254935,-0.88178178658113,-0.849287754897747,
-0.844189428715838,-0.841332067872399,-0.839116256016836,-0.835968326961959,
-0.829269658035917,-0.80037308628289,-0.748574614133139,-0.73307883344986,
-0.72671348772298,-0.722265155154821,-0.717681504132227,-0.710853651652471,
-0.690533097450211,-0.654617291282131,-0.615826663941689,-0.609030837664496,
-0.605864859041756,-0.603413243436209,-0.600466773694076,-0.594797424277209,
-0.587382541278495,-0.569163338586325,-0.524253167997968,-0.499551149716652,
-0.492004393270059,-0.487270472516489,-0.482854716063843,-0.476938764594269,
-0.463268157125065,-0.443729201528938,-0.41412128665872,-0.406489302572081,
-0.377089580736931,-0.372015853250601,-0.369164033033085,-0.366947395512771,
-0.36379162035778,-0.357050598854746,-0.327745978010035,-0.27474717456546,
-0.260494257252249,-0.254924401431048,-0.250831639655306,-0.246372204598149,
-0.240191700280601,-0.224832490828784,-0.201766456536337,-0.175008249335334,
-0.141068520831317,-0.135961156695513,-0.13310186622085,-0.13088649291921,
-0.127741700869035,-0.121059297816463,-0.0923160942520134,-0.0460591495953894,
-0.0261999556201138,-0.0192392761083748,-0.0150892407283716,-0.0109091130635428,
-0.0059084454421249,-0.00068537780707878),.UNSPECIFIED.);
#673=B_SPLINE_CURVE_WITH_KNOTS('',3,(#61494,#61495,#61496,#61497),
 .UNSPECIFIED.,.F.,.F.,(4,4),(34.4851594650687,34.557519189258),
 .UNSPECIFIED.);
#674=B_SPLINE_CURVE_WITH_KNOTS('',3,(#61498,#61499,#61500,#61501,#61502,
#61503,#61504,#61505,#61506,#61507,#61508,#61509,#61510,#61511,#61512,#61513,
#61514,#61515,#61516,#61517,#61518,#61519,#61520,#61521,#61522,#61523,#61524,
#61525,#61526,#61527,#61528,#61529,#61530,#61531,#61532,#61533,#61534,#61535,
#61536,#61537,#61538,#61539,#61540,#61541,#61542,#61543,#61544,#61545,#61546,
#61547,#61548,#61549,#61550,#61551,#61552,#61553,#61554,#61555,#61556,#61557,
#61558,#61559,#61560,#61561,#61562,#61563,#61564,#61565,#61566,#61567,#61568,
#61569,#61570,#61571,#61572,#61573,#61574,#61575,#61576,#61577,#61578,#61579,
#61580,#61581,#61582,#61583,#61584,#61585,#61586,#61587,#61588,#61589,#61590,
#61591,#61592,#61593,#61594,#61595,#61596,#61597,#61598,#61599,#61600,#61601,
#61602,#61603,#61604,#61605,#61606,#61607,#61608,#61609,#61610,#61611,#61612,
#61613,#61614,#61615,#61616,#61617,#61618,#61619,#61620,#61621,#61622,#61623,
#61624,#61625,#61626,#61627,#61628,#61629,#61630,#61631,#61632,#61633,#61634,
#61635,#61636,#61637,#61638,#61639,#61640,#61641,#61642,#61643,#61644,#61645,
#61646,#61647,#61648,#61649,#61650,#61651,#61652,#61653,#61654,#61655,#61656,
#61657,#61658,#61659,#61660,#61661,#61662,#61663,#61664,#61665,#61666,#61667,
#61668,#61669,#61670,#61671,#61672,#61673,#61674,#61675,#61676,#61677,#61678,
#61679,#61680,#61681,#61682,#61683,#61684,#61685),.UNSPECIFIED.,.F.,.F.,
(4,2,2,2,2,2,2,2,2,2,2,2,2,2,2,2,2,2,2,2,2,2,2,2,2,2,2,2,2,2,2,2,2,2,2,
2,2,2,2,2,2,2,2,2,2,2,2,2,2,2,2,2,2,2,2,2,2,2,2,2,2,2,2,2,2,2,2,2,2,2,2,
2,2,2,2,2,2,2,2,2,2,2,2,2,2,2,2,2,2,2,2,2,2,4),(-1.51249653208003,-1.49532235228339,
-1.46458408338178,-1.42271694013379,-1.41433716581086,-1.4093543853258,
-1.40487617875404,-1.39911645151077,-1.38681096003889,-1.35206241795467,
-1.31023612226106,-1.29707975235174,-1.29283106324752,-1.2901496382989,
-1.28752206697662,-1.2835244523702,-1.27144029660535,-1.25023835607663,
-1.19930033730217,-1.18307841925596,-1.17650573344924,-1.17194350696784,
-1.16726573912676,-1.16033721323982,-1.13994895294347,-1.10402802489318,
-1.06568240683567,-1.05880163461925,-1.05557740777576,-1.05306950387456,
-1.05003415764808,-1.04412606768488,-1.01231876880348,-0.956134751789516,
-0.944651118225109,-0.93904235943167,-0.93457966203583,-0.92950623864646,
-0.920698109854971,-0.875213513816718,-0.829062597455482,-0.822617541309217,
-0.819475930441066,-0.816970753190448,-0.813862126005212,-0.807586417741081,
-0.799163071815572,-0.777007837465092,-0.722531516718579,-0.709667997760202,
-0.703783173293315,-0.699274966223604,-0.694402196525816,-0.686539012550412,
-0.655275588327369,-0.627014132778495,-0.593882809767509,-0.586969370135155,
-0.583739154616511,-0.581231009634986,-0.578200736404825,-0.572317327458206,
-0.532551298529391,-0.48230275119364,-0.473079938289183,-0.467379937167282,
-0.46290854034125,-0.457892265062286,-0.449353968788562,-0.401310764105049,
-0.357438847579887,-0.350857567516843,-0.347689830387979,-0.345184251086645,
-0.342100310645394,-0.335949489212392,-0.293906824364619,-0.246666962872415,
-0.23728011121668,-0.231532871480163,-0.227232089831868,-0.22247592499597,
-0.217439405894266,-0.199883383200268,-0.171834221934627,-0.128940005275336,
-0.117149301677165,-0.113066575360789,-0.110683308995864,-0.108081841643167,
-0.104212107675829,-0.0931671729726866,-0.0746899741359773,-0.0180297629229655),
 .UNSPECIFIED.);
#675=B_SPLINE_CURVE_WITH_KNOTS('',3,(#61690,#61691,#61692,#61693,#61694,
#61695,#61696,#61697,#61698,#61699,#61700,#61701,#61702,#61703,#61704,#61705,
#61706,#61707,#61708,#61709,#61710,#61711,#61712,#61713,#61714,#61715,#61716,
#61717,#61718,#61719,#61720,#61721,#61722,#61723,#61724,#61725,#61726,#61727,
#61728,#61729,#61730,#61731,#61732,#61733,#61734,#61735,#61736,#61737,#61738,
#61739,#61740,#61741,#61742,#61743,#61744,#61745,#61746,#61747,#61748,#61749,
#61750,#61751,#61752,#61753,#61754,#61755,#61756,#61757,#61758,#61759,#61760,
#61761,#61762,#61763,#61764,#61765,#61766,#61767,#61768,#61769,#61770,#61771,
#61772,#61773,#61774,#61775,#61776,#61777,#61778,#61779,#61780,#61781,#61782,
#61783,#61784,#61785,#61786,#61787,#61788,#61789,#61790,#61791,#61792,#61793,
#61794,#61795,#61796,#61797,#61798,#61799,#61800,#61801,#61802,#61803,#61804,
#61805,#61806,#61807,#61808,#61809,#61810,#61811,#61812,#61813,#61814,#61815,
#61816,#61817,#61818,#61819,#61820,#61821,#61822,#61823,#61824,#61825,#61826,
#61827,#61828,#61829,#61830,#61831,#61832,#61833,#61834,#61835,#61836,#61837,
#61838,#61839,#61840,#61841,#61842,#61843,#61844,#61845,#61846,#61847,#61848,
#61849,#61850,#61851,#61852,#61853,#61854,#61855,#61856,#61857,#61858,#61859,
#61860,#61861,#61862,#61863,#61864,#61865,#61866,#61867,#61868,#61869,#61870,
#61871,#61872,#61873,#61874,#61875,#61876,#61877,#61878,#61879,#61880,#61881,
#61882,#61883,#61884,#61885,#61886,#61887,#61888,#61889,#61890,#61891),
 .UNSPECIFIED.,.F.,.F.,(4,2,2,2,2,2,2,2,2,2,2,2,2,2,2,2,2,2,2,2,2,2,2,2,
2,2,2,2,2,2,2,2,2,2,2,2,2,2,2,2,2,2,2,2,2,2,2,2,2,2,2,2,2,2,2,2,2,2,2,2,
2,2,2,2,2,2,2,2,2,2,2,2,2,2,2,2,2,2,2,2,2,2,2,2,2,2,2,2,2,2,2,2,2,2,2,2,
2,2,2,2,4),(-2.97190100113565,-2.97131175839763,-2.96845623843134,-2.96614107326616,
-2.96368022360977,-2.96045676381779,-2.95314821990278,-2.9310116849298,
-2.8994834220475,-2.8741892507486,-2.85784077341721,-2.8515174500756,-2.84703296917863,
-2.84296937776516,-2.83648537192792,-2.82021859310396,-2.7691538133824,
-2.74783173551207,-2.73964661187022,-2.73353245624978,-2.73049709068879,
-2.72804986538015,-2.72498731645274,-2.71873425796821,-2.67134910166512,
-2.62584286662948,-2.61755510053169,-2.61266388972297,-2.60829333690894,
-2.60271046178093,-2.59366244347109,-2.53047808995372,-2.51090300052764,
-2.50314293653978,-2.4972728276138,-2.49428592775775,-2.4918372626154,-2.4887214702138,
-2.48219178918329,-2.43821677823288,-2.39005253042042,-2.38158662294442,
-2.37665736844077,-2.372292967894,-2.36677250990311,-2.35794023223671,-2.30319488462053,
-2.26702351366726,-2.26116128265609,-2.25817590582041,-2.2557270818585,
-2.25260930181604,-2.24606947775557,-2.20219743268914,-2.15388707018597,
-2.14545093407467,-2.14052788955146,-2.13616234341669,-2.13063143780608,
-2.12176362860523,-2.06738242309581,-2.03039970235347,-2.02484735762898,
-2.02192509490361,-2.01947146370955,-2.01632727476398,-2.00946641205748,
-1.97242088651315,-1.95327364695403,-1.92913718080272,-1.9132943332153,
-1.90704270160636,-1.90257066044696,-1.89849250452637,-1.89192825028888,
-1.87512632282246,-1.82456092977286,-1.79608646698237,-1.78943242359899,
-1.78629291450267,-1.78407810670438,-1.78121503164371,-1.77609084830558,
-1.74120126708856,-1.71422341379356,-1.69192515350075,-1.68167972891799,
-1.67327725702302,-1.66836091218807,-1.66399354090812,-1.65844976348067,
-1.6495391375974,-1.59560011757762,-1.55825787324151,-1.55269382525663,
-1.54976889499946,-1.54731514883066,-1.54417345713816,-1.53756924516136,
-1.49521188663987,-1.47764986309498),.UNSPECIFIED.);
#676=B_SPLINE_CURVE_WITH_KNOTS('',3,(#61893,#61894,#61895,#61896,#61897,
#61898,#61899,#61900),.UNSPECIFIED.,.F.,.F.,(4,2,2,4),(-0.0180297629229655,
-0.0117363126142654,-0.00498186049605689,-0.000717196793377947),
 .UNSPECIFIED.);
#677=B_SPLINE_CURVE_WITH_KNOTS('',3,(#61901,#61902,#61903,#61904,#61905,
#61906,#61907,#61908,#61909,#61910),.UNSPECIFIED.,.F.,.F.,(4,1,1,1,1,1,
1,4),(40.8407044966673,41.3711512650695,42.3630218789779,43.3548924928863,
44.3467631067947,45.3386337207031,46.3305043346114,47.0500693632372),
 .UNSPECIFIED.);
#678=B_SPLINE_CURVE_WITH_KNOTS('',3,(#61916,#61917,#61918,#61919,#61920,
#61921,#61922,#61923,#61924,#61925),.UNSPECIFIED.,.F.,.F.,(4,1,1,1,1,1,
1,4),(47.1238982701508,48.0159246620401,49.0086358397811,50.001347017522,
50.994058195263,51.986769373004,52.979480550745,53.334785281413),
 .UNSPECIFIED.);
#679=B_SPLINE_CURVE_WITH_KNOTS('',3,(#61926,#61927,#61928,#61929,#61930,
#61931),.UNSPECIFIED.,.F.,.F.,(4,2,4),(-2.98912319920029,-2.97800245941442,
-2.97190100113565),.UNSPECIFIED.);
#680=B_SPLINE_CURVE_WITH_KNOTS('',3,(#61933,#61934,#61935,#61936),
 .UNSPECIFIED.,.F.,.F.,(4,4),(47.0500693632372,47.1238868231314),
 .UNSPECIFIED.);
#681=B_SPLINE_CURVE_WITH_KNOTS('',3,(#61937,#61938,#61939,#61940,#61941,
#61942,#61943,#61944,#61945,#61946,#61947,#61948,#61949,#61950,#61951,#61952,
#61953,#61954,#61955,#61956,#61957,#61958,#61959,#61960,#61961,#61962,#61963,
#61964,#61965,#61966,#61967,#61968,#61969,#61970,#61971,#61972,#61973,#61974,
#61975,#61976,#61977,#61978,#61979,#61980,#61981,#61982,#61983,#61984,#61985,
#61986,#61987,#61988,#61989,#61990,#61991,#61992,#61993,#61994,#61995,#61996,
#61997,#61998,#61999,#62000,#62001,#62002,#62003,#62004,#62005,#62006,#62007,
#62008,#62009,#62010,#62011,#62012,#62013,#62014,#62015,#62016,#62017,#62018,
#62019,#62020,#62021,#62022,#62023,#62024,#62025,#62026,#62027,#62028,#62029,
#62030,#62031,#62032,#62033,#62034,#62035,#62036,#62037,#62038,#62039,#62040,
#62041,#62042,#62043,#62044,#62045,#62046,#62047,#62048,#62049,#62050,#62051,
#62052,#62053,#62054,#62055,#62056,#62057,#62058,#62059,#62060,#62061,#62062,
#62063,#62064,#62065,#62066,#62067,#62068,#62069,#62070,#62071,#62072,#62073,
#62074,#62075,#62076,#62077,#62078,#62079,#62080,#62081,#62082,#62083,#62084,
#62085,#62086,#62087,#62088,#62089,#62090,#62091,#62092,#62093,#62094,#62095,
#62096,#62097,#62098,#62099,#62100,#62101,#62102,#62103,#62104,#62105,#62106,
#62107,#62108,#62109,#62110,#62111,#62112,#62113,#62114,#62115,#62116,#62117,
#62118,#62119,#62120,#62121,#62122,#62123,#62124,#62125,#62126,#62127,#62128,
#62129,#62130,#62131,#62132),.UNSPECIFIED.,.F.,.F.,(4,2,2,2,2,2,2,2,2,2,
2,2,2,2,2,2,2,2,2,2,2,2,2,2,2,2,2,2,2,2,2,2,2,2,2,2,2,2,2,2,2,2,2,2,2,2,
2,2,2,2,2,2,2,2,2,2,2,2,2,2,2,2,2,2,2,2,2,2,2,2,2,2,2,2,2,2,2,2,2,2,2,2,
2,2,2,2,2,2,2,2,2,2,2,2,2,2,2,4),(-2.98909564641531,-2.96016523086049,-2.94987452961653,
-2.94645872464972,-2.94393562506273,-2.94140386423417,-2.93853047506777,
-2.93353056391019,-2.9097072416286,-2.87574585450262,-2.83957868726566,
-2.83099748365331,-2.82590079067047,-2.82144224541615,-2.81587122359658,
-2.80708918644641,-2.75168571123234,-2.71653949738635,-2.71046049087622,
-2.70739124745004,-2.70488575083645,-2.70170311196662,-2.69504130183218,
-2.65219393568004,-2.60317763100082,-2.59471946091289,-2.58972083401277,
-2.58524722022996,-2.57951958099087,-2.5701985894611,-2.5225942068571,-2.48058541046492,
-2.47454829458135,-2.47148738179386,-2.46898147804595,-2.46578917294243,
-2.45907649892798,-2.4163849241686,-2.36743409430002,-2.35889744843827,
-2.35388208983118,-2.34941146072798,-2.3437123742855,-2.33449081491071,
-2.28419526214826,-2.25591530249727,-2.2461917115635,-2.23919903320737,
-2.23595455218833,-2.23368514586778,-2.23077164283522,-2.22559364226457,
-2.19158596652003,-2.18795264412711,-2.14966417018502,-2.12854639265802,
-2.12153709128879,-2.11684371734355,-2.11229536734441,-2.10579395675903,
-2.08996220026183,-2.03860744878683,-2.01728738733133,-2.00906080850749,
-2.00289778220183,-1.9998117494116,-1.99730667387238,-1.99414236314651,
-1.9875772571877,-1.94357760116908,-1.89584018740329,-1.88723032427049,
-1.88219937517131,-1.87773130277114,-1.87205793923073,-1.86292562612946,
-1.80012982619518,-1.7736545022907,-1.76715992439133,-1.76400902932515,
-1.76150407853096,-1.75840518126524,-1.7521776128705,-1.70393705597441,
-1.66620796990811,-1.65375655302756,-1.64797126848625,-1.64349058091613,
-1.63852271118832,-1.63021101707353,-1.59282358972378,-1.54079007272048,
-1.53221975494757,-1.52870455191223,-1.52616578910238,-1.52331499820292,
-1.51828796833696,-1.51241459518593),.UNSPECIFIED.);
#682=B_SPLINE_CURVE_WITH_KNOTS('',3,(#62138,#62139,#62140,#62141,#62142,
#62143,#62144,#62145,#62146,#62147,#62148,#62149,#62150,#62151,#62152,#62153,
#62154,#62155,#62156,#62157,#62158,#62159,#62160,#62161,#62162,#62163,#62164,
#62165,#62166,#62167,#62168,#62169,#62170,#62171,#62172,#62173,#62174,#62175,
#62176,#62177,#62178,#62179,#62180,#62181,#62182,#62183,#62184,#62185,#62186,
#62187,#62188,#62189,#62190,#62191,#62192,#62193,#62194,#62195,#62196,#62197,
#62198,#62199,#62200,#62201,#62202,#62203,#62204,#62205,#62206,#62207,#62208,
#62209,#62210,#62211,#62212,#62213,#62214,#62215,#62216,#62217,#62218,#62219,
#62220,#62221,#62222,#62223,#62224,#62225,#62226,#62227,#62228,#62229,#62230,
#62231,#62232,#62233,#62234,#62235,#62236,#62237,#62238,#62239,#62240,#62241,
#62242,#62243,#62244,#62245,#62246,#62247,#62248,#62249,#62250,#62251,#62252,
#62253,#62254,#62255,#62256,#62257,#62258,#62259,#62260,#62261,#62262,#62263,
#62264,#62265,#62266,#62267,#62268,#62269,#62270,#62271,#62272,#62273,#62274,
#62275,#62276,#62277,#62278,#62279,#62280,#62281,#62282,#62283,#62284,#62285,
#62286,#62287,#62288,#62289,#62290,#62291,#62292,#62293,#62294,#62295,#62296,
#62297,#62298,#62299,#62300,#62301,#62302,#62303,#62304,#62305,#62306,#62307,
#62308,#62309,#62310,#62311,#62312,#62313,#62314,#62315,#62316,#62317,#62318,
#62319,#62320,#62321,#62322,#62323,#62324,#62325,#62326,#62327),
 .UNSPECIFIED.,.F.,.F.,(4,3,3,3,3,3,3,3,3,3,3,3,3,3,3,3,3,3,3,3,3,3,3,3,
3,3,3,3,3,3,3,3,3,3,3,3,3,3,3,3,3,3,3,3,3,3,3,3,3,3,3,3,3,3,3,3,3,3,3,3,
3,3,3,4),(53.4070751110264,53.5094895370782,53.611968539674,53.7146203178466,
53.8173674042498,53.9203240275781,53.972191728486,54.0727687525615,54.1732019849704,
54.2735200400656,54.3737752738037,54.4739988278287,54.5742218037934,54.6745439560551,
54.7749147991135,54.8754642941431,54.9649029062269,55.0654799303024,55.165913162711,
55.2662312178063,55.3664864515444,55.4667100055694,55.5669329815341,55.6672551337958,
55.7676259768542,55.8681754718837,55.9576140839679,56.0581911080434,56.1586243404524,
56.2589423955477,56.3591976292858,56.4594211833108,56.5596441592756,56.6599663115373,
56.7603371545958,56.8608866496254,56.9503252617089,57.0509022857844,57.1513355181932,
57.2516535732885,57.3519088070266,57.4521323610516,57.5523553370163,57.6526774892779,
57.7530483323363,57.8535978273659,57.9430364394499,58.0436134635254,58.1440466959342,
58.2443647510295,58.3446199847677,58.4448435387926,58.5450665147576,58.6453886670194,
58.7457595100778,58.8463090051074,58.9357476171908,59.0350728526044,59.1342668431611,
59.2333624091373,59.3324091722181,59.4314232994544,59.5304864406886,59.6164740057542),
 .UNSPECIFIED.);
#683=B_SPLINE_CURVE_WITH_KNOTS('',3,(#62328,#62329,#62330,#62331),
 .UNSPECIFIED.,.F.,.F.,(4,4),(53.334785281413,53.4070701237542),
 .UNSPECIFIED.);
#684=B_SPLINE_CURVE_WITH_KNOTS('',3,(#62332,#62333,#62334,#62335,#62336,
#62337,#62338,#62339,#62340,#62341,#62342,#62343,#62344,#62345,#62346,#62347,
#62348,#62349,#62350,#62351,#62352,#62353,#62354,#62355,#62356,#62357,#62358,
#62359,#62360,#62361,#62362,#62363,#62364,#62365,#62366,#62367,#62368,#62369,
#62370,#62371,#62372,#62373,#62374,#62375,#62376,#62377,#62378,#62379,#62380,
#62381,#62382,#62383,#62384,#62385,#62386,#62387,#62388,#62389,#62390,#62391,
#62392,#62393,#62394,#62395,#62396,#62397,#62398,#62399,#62400,#62401,#62402,
#62403,#62404,#62405,#62406,#62407,#62408,#62409,#62410,#62411,#62412,#62413,
#62414,#62415,#62416,#62417,#62418,#62419,#62420,#62421,#62422,#62423,#62424,
#62425,#62426,#62427,#62428,#62429,#62430,#62431,#62432,#62433,#62434,#62435,
#62436,#62437,#62438,#62439,#62440,#62441,#62442,#62443,#62444,#62445,#62446,
#62447,#62448,#62449,#62450,#62451,#62452,#62453,#62454,#62455,#62456,#62457,
#62458,#62459,#62460,#62461,#62462,#62463,#62464,#62465,#62466,#62467,#62468,
#62469,#62470,#62471,#62472,#62473,#62474,#62475,#62476,#62477,#62478,#62479,
#62480,#62481,#62482,#62483,#62484,#62485,#62486,#62487,#62488,#62489,#62490,
#62491,#62492,#62493,#62494,#62495,#62496,#62497,#62498,#62499,#62500,#62501,
#62502,#62503,#62504,#62505,#62506,#62507,#62508,#62509,#62510,#62511,#62512,
#62513,#62514,#62515,#62516,#62517),.UNSPECIFIED.,.F.,.F.,(4,2,2,2,2,2,
2,2,2,2,2,2,2,2,2,2,2,2,2,2,2,2,2,2,2,2,2,2,2,2,2,2,2,2,2,2,2,2,2,2,2,2,
2,2,2,2,2,2,2,2,2,2,2,2,2,2,2,2,2,2,2,2,2,2,2,2,2,2,2,2,2,2,2,2,2,2,2,2,
2,2,2,2,2,2,2,2,2,2,2,2,2,2,4),(-1.51241459518593,-1.49524509246308,-1.46505511337229,
-1.42360606407568,-1.41522311013593,-1.41023995122281,-1.40576233768265,
-1.40000467888127,-1.38770887107532,-1.35318820490325,-1.3117549439869,
-1.29808955902646,-1.29378382502586,-1.29109013811061,-1.28847284228217,
-1.28452410408607,-1.27284615938273,-1.25273662743795,-1.20569110063573,
-1.18525163153861,-1.17811502024508,-1.17339514153084,-1.16881191855104,
-1.16237214340507,-1.14581063957843,-1.12016133266688,-1.09611557475652,
-1.06394850766189,-1.05878169525847,-1.05587045934723,-1.05360024374072,
-1.05035130867201,-1.04333585878254,-1.03357148537055,-1.00508041225542,
-0.955137735674959,-0.945900910309668,-0.940196955583426,-0.935725252867187,
-0.930711542384892,-0.922184902475477,-0.873835482265823,-0.830306263634118,
-0.823689576972656,-0.820515143933244,-0.818009453206771,-0.81493175935616,
-0.808812116937569,-0.769760127189184,-0.719147160121579,-0.709943008732649,
-0.704248427502345,-0.699777641969742,-0.694758257362915,-0.686205127832704,
-0.637702076993659,-0.594420233382172,-0.58777320939651,-0.584592975690829,
-0.582087066564602,-0.579014465404662,-0.572920562333852,-0.536349612376319,
-0.48282439921669,-0.473828365994832,-0.468194089672247,-0.463729205340216,
-0.458672599772318,-0.449943755976233,-0.401925510290071,-0.35844253953196,
-0.351820136631256,-0.348644566767666,-0.346138781236953,-0.343061958930788,
-0.336946936495131,-0.298352707192188,-0.24724089508629,-0.238053169451893,
-0.232363258103448,-0.228092179612958,-0.223252127632017,-0.218161637497641,
-0.199900841164055,-0.170049856811425,-0.121938455918974,-0.115690262250876,
-0.112587085718642,-0.110081899281292,-0.106934758984033,-0.100460824792478,
-0.0741727939511685,-0.0180007184006807),.UNSPECIFIED.);
#685=B_SPLINE_CURVE_WITH_KNOTS('',3,(#62523,#62524,#62525,#62526,#62527,
#62528,#62529,#62530,#62531,#62532,#62533,#62534,#62535,#62536,#62537,#62538,
#62539,#62540,#62541,#62542,#62543,#62544,#62545,#62546,#62547,#62548,#62549,
#62550,#62551,#62552,#62553,#62554,#62555,#62556,#62557,#62558,#62559,#62560,
#62561,#62562,#62563,#62564,#62565,#62566,#62567,#62568,#62569,#62570,#62571,
#62572,#62573,#62574,#62575,#62576,#62577,#62578,#62579,#62580,#62581,#62582,
#62583,#62584,#62585,#62586,#62587,#62588,#62589,#62590,#62591,#62592,#62593,
#62594,#62595,#62596,#62597,#62598,#62599,#62600,#62601,#62602,#62603,#62604,
#62605,#62606,#62607,#62608,#62609,#62610,#62611,#62612,#62613,#62614,#62615,
#62616,#62617,#62618,#62619,#62620,#62621,#62622,#62623,#62624,#62625,#62626,
#62627,#62628,#62629,#62630,#62631,#62632,#62633,#62634,#62635,#62636,#62637,
#62638,#62639,#62640,#62641,#62642,#62643,#62644,#62645,#62646,#62647,#62648,
#62649,#62650,#62651,#62652,#62653,#62654,#62655,#62656,#62657,#62658,#62659,
#62660,#62661,#62662,#62663,#62664,#62665,#62666,#62667,#62668,#62669,#62670,
#62671,#62672,#62673,#62674,#62675,#62676,#62677,#62678,#62679,#62680,#62681,
#62682,#62683,#62684,#62685,#62686,#62687,#62688,#62689,#62690,#62691,#62692,
#62693,#62694,#62695,#62696,#62697,#62698,#62699,#62700,#62701,#62702,#62703,
#62704,#62705,#62706,#62707,#62708,#62709,#62710,#62711,#62712,#62713,#62714,
#62715,#62716,#62717,#62718,#62719,#62720,#62721,#62722,#62723,#62724,#62725,
#62726,#62727,#62728),.UNSPECIFIED.,.F.,.F.,(4,2,2,2,2,2,2,2,2,2,2,2,2,
2,2,2,2,2,2,2,2,2,2,2,2,2,2,2,2,2,2,2,2,2,2,2,2,2,2,2,2,2,2,2,2,2,2,2,2,
2,2,2,2,2,2,2,2,2,2,2,2,2,2,2,2,2,2,2,2,2,2,2,2,2,2,2,2,2,2,2,2,2,2,2,2,
2,2,2,2,2,2,2,2,2,2,2,2,2,2,2,2,2,4),(-1.47756856596777,-1.47667518010056,
-1.47402767376772,-1.47148251209158,-1.46769128329404,-1.4568569678724,
-1.43879538213463,-1.39408829884182,-1.36900200688479,-1.36141950416248,
-1.35667758649383,-1.35226412399069,-1.34636607086331,-1.3328068075458,
-1.31349037355033,-1.28358727468684,-1.27565553739564,-1.24644897713212,
-1.24137845605213,-1.23852713753658,-1.23631007987131,-1.23315265124239,
-1.22640402224165,-1.19703029445297,-1.14383034860837,-1.1297679363977,
-1.12422576203256,-1.1201394154692,-1.11567355010628,-1.10945906303664,
-1.09387420491701,-1.07031265089973,-1.04315932934328,-1.01039061091018,
-1.00529095439064,-1.00243317233192,-1.00021723432547,-0.997069386712347,
-0.990371887374177,-0.961489030219941,-0.909732843962621,-0.894191467386958,
-0.88781729693775,-0.883367104204696,-0.878785147064071,-0.871966779059083,
-0.851732597209932,-0.816087272756875,-0.776882310149309,-0.770104851823568,
-0.76694213732142,-0.764490561249494,-0.761541129569988,-0.755857930867351,
-0.748419638422406,-0.730111089011565,-0.670366855268694,-0.657149882358595,
-0.651745696304398,-0.647287261691925,-0.64271634239969,-0.635951725103874,
-0.616181514229606,-0.581942003030305,-0.540629896265991,-0.533934140365763,
-0.530786727433254,-0.52833615314165,-0.525374738656974,-0.519632322484477,
-0.512092865096358,-0.493391591500168,-0.429962513770676,-0.419414811119862,
-0.413991023162881,-0.409634379042546,-0.404639474259673,-0.395864875451135,
-0.348284159340901,-0.304211584097677,-0.297685142273985,-0.294569675055742,
-0.292120673318311,-0.289132619720033,-0.283258159864416,-0.275491752606876,
-0.255893014993365,-0.19283578273377,-0.183755819193247,-0.178163213947666,
-0.173790991041131,-0.168904058046772,-0.160966872435302,-0.128065793818931,
-0.0940482035040311,-0.0657814238749686,-0.0607335324943708,-0.0578875980400268,
-0.0556701326240175,-0.0525061282772593,-0.0490024008786595,-0.0389255836744063,
-0.000685810379229455),.UNSPECIFIED.);
#686=B_SPLINE_CURVE_WITH_KNOTS('',3,(#62729,#62730,#62731,#62732),
 .UNSPECIFIED.,.F.,.F.,(4,4),(59.6164740057542,59.690260418206),
 .UNSPECIFIED.);
#687=B_SPLINE_CURVE_WITH_KNOTS('',3,(#62734,#62735,#62736,#62737,#62738,
#62739,#62740,#62741),.UNSPECIFIED.,.F.,.F.,(4,2,2,4),(-0.0180007184006807,
-0.0122274356288746,-0.00513494177923378,-0.000683356472381724),
 .UNSPECIFIED.);
#688=B_SPLINE_CURVE_WITH_KNOTS('',3,(#62742,#62743,#62744,#62745,#62746,
#62747,#62748,#62749,#62750,#62751,#62752,#62753,#62754,#62755,#62756,#62757,
#62758,#62759,#62760,#62761,#62762,#62763,#62764,#62765,#62766,#62767,#62768,
#62769,#62770,#62771,#62772,#62773,#62774,#62775,#62776,#62777,#62778,#62779,
#62780,#62781,#62782,#62783,#62784,#62785,#62786,#62787,#62788,#62789,#62790,
#62791,#62792,#62793,#62794,#62795,#62796,#62797,#62798,#62799,#62800,#62801,
#62802,#62803,#62804,#62805,#62806,#62807,#62808,#62809,#62810,#62811,#62812,
#62813,#62814,#62815,#62816,#62817,#62818,#62819,#62820,#62821,#62822,#62823,
#62824,#62825,#62826,#62827,#62828,#62829,#62830,#62831,#62832,#62833,#62834,
#62835,#62836,#62837,#62838,#62839,#62840,#62841,#62842,#62843,#62844,#62845,
#62846,#62847,#62848,#62849,#62850,#62851,#62852,#62853,#62854,#62855,#62856,
#62857,#62858,#62859,#62860,#62861,#62862,#62863,#62864,#62865,#62866,#62867,
#62868,#62869,#62870,#62871,#62872,#62873,#62874,#62875,#62876,#62877,#62878,
#62879,#62880,#62881,#62882,#62883,#62884,#62885,#62886,#62887,#62888,#62889,
#62890,#62891,#62892,#62893,#62894,#62895,#62896,#62897,#62898,#62899,#62900,
#62901,#62902,#62903,#62904,#62905,#62906,#62907,#62908,#62909,#62910,#62911,
#62912,#62913,#62914,#62915,#62916,#62917,#62918,#62919,#62920,#62921,#62922,
#62923,#62924,#62925,#62926,#62927,#62928,#62929,#62930,#62931,#62932,#62933,
#62934,#62935,#62936,#62937,#62938,#62939,#62940,#62941,#62942,#62943,#62944,
#62945,#62946,#62947),.UNSPECIFIED.,.F.,.F.,(4,2,2,2,2,2,2,2,2,2,2,2,2,
2,2,2,2,2,2,2,2,2,2,2,2,2,2,2,2,2,2,2,2,2,2,2,2,2,2,2,2,2,2,2,2,2,2,2,2,
2,2,2,2,2,2,2,2,2,2,2,2,2,2,2,2,2,2,2,2,2,2,2,2,2,2,2,2,2,2,2,2,2,2,2,2,
2,2,2,2,2,2,2,2,2,2,2,2,2,2,2,2,2,4),(-2.98838788646982,-2.98528829418108,
-2.98146659002245,-2.97698691775857,-2.97081660209869,-2.95622861621512,
-2.94199447241219,-2.90215992325245,-2.88154888698576,-2.8734939388036,
-2.86742976418027,-2.86436410567773,-2.86185935104928,-2.85867488688888,
-2.8520000353513,-2.80903100507921,-2.7602925067911,-2.7517825329484,-2.74677398413034,
-2.74230405660114,-2.73659847599713,-2.7273506004005,-2.67725560329362,
-2.64889106712198,-2.63915262817281,-2.63215259343949,-2.62890746399829,
-2.62663866234702,-2.62372742221094,-2.61855671960823,-2.5850262691835,
-2.55849687775771,-2.53532586746911,-2.51986167747301,-2.5135841501213,
-2.50903140221415,-2.50483499055254,-2.49797458944606,-2.47973438304461,
-2.42604023861142,-2.40847775111068,-2.39780500766514,-2.39398502459098,
-2.39139427283262,-2.38866508409898,-2.38419332343814,-2.36890733353992,
-2.32348241613457,-2.29984068542966,-2.28416264700806,-2.27785303069014,
-2.27329462940184,-2.26910511197311,-2.26228360239454,-2.24431833420245,
-2.19031822096395,-2.17271683158259,-2.16202805560938,-2.15820588586896,
-2.15561466131597,-2.15288605412615,-2.14841716375823,-2.1331631205036,
-2.08771965115224,-2.06406438951804,-2.05337176105262,-2.04464970313674,
-2.03959597537389,-2.03513299238843,-2.02950025852013,-2.02050481739934,
-1.95707037668424,-1.93776486726977,-1.93003288892616,-1.92415534085002,
-1.92112698118282,-1.91861975919638,-1.91538991616257,-1.90847433297581,
-1.87503247989781,-1.84639674010233,-1.81583133899907,-1.80801480599274,
-1.8031531778308,-1.79864340372126,-1.79273940388295,-1.77922388291805,
-1.72525466950789,-1.70322992144778,-1.69483799623768,-1.68858116350246,
-1.68547694434599,-1.68297266310022,-1.67982885004434,-1.67336872111006,
-1.62750489725578,-1.58185642475913,-1.5730452000715,-1.56797224927187,
-1.56351126538561,-1.55790639166416,-1.54900779818947,-1.5120028941296),
 .UNSPECIFIED.);
#689=B_SPLINE_CURVE_WITH_KNOTS('',3,(#62952,#62953,#62954,#62955,#62956,
#62957,#62958,#62959,#62960,#62961,#62962,#62963,#62964,#62965,#62966,#62967,
#62968,#62969,#62970,#62971,#62972,#62973,#62974,#62975,#62976,#62977,#62978,
#62979,#62980,#62981,#62982,#62983,#62984,#62985,#62986,#62987,#62988,#62989,
#62990,#62991,#62992,#62993,#62994,#62995,#62996,#62997,#62998,#62999,#63000,
#63001,#63002,#63003,#63004,#63005,#63006,#63007,#63008,#63009,#63010,#63011,
#63012,#63013,#63014,#63015,#63016,#63017,#63018,#63019,#63020,#63021,#63022,
#63023,#63024,#63025,#63026,#63027,#63028,#63029,#63030,#63031,#63032,#63033,
#63034,#63035,#63036,#63037,#63038,#63039,#63040,#63041,#63042,#63043,#63044,
#63045,#63046,#63047,#63048,#63049,#63050,#63051,#63052,#63053,#63054,#63055,
#63056,#63057,#63058,#63059,#63060,#63061,#63062,#63063,#63064,#63065,#63066,
#63067,#63068,#63069,#63070,#63071,#63072,#63073,#63074,#63075,#63076,#63077,
#63078,#63079,#63080,#63081,#63082,#63083,#63084,#63085,#63086,#63087,#63088,
#63089,#63090,#63091,#63092,#63093,#63094,#63095,#63096,#63097,#63098,#63099,
#63100,#63101,#63102,#63103,#63104,#63105,#63106,#63107,#63108,#63109,#63110,
#63111,#63112,#63113,#63114,#63115,#63116,#63117,#63118,#63119,#63120,#63121,
#63122,#63123,#63124,#63125,#63126,#63127,#63128,#63129,#63130,#63131,#63132,
#63133,#63134,#63135,#63136,#63137,#63138,#63139,#63140,#63141,#63142,#63143,
#63144,#63145,#63146,#63147,#63148,#63149,#63150,#63151,#63152,#63153,#63154,
#63155,#63156,#63157,#63158,#63159,#63160,#63161,#63162,#63163,#63164,#63165,
#63166,#63167,#63168,#63169,#63170,#63171,#63172,#63173,#63174,#63175),
 .UNSPECIFIED.,.F.,.F.,(4,2,2,2,2,2,2,2,2,2,2,2,2,2,2,2,2,2,2,2,2,2,2,2,
2,2,2,2,2,2,2,2,2,2,2,2,2,2,2,2,2,2,2,2,2,2,2,2,2,2,2,2,2,2,2,2,2,2,2,2,
2,2,2,2,2,2,2,2,2,2,2,2,2,2,2,2,2,2,2,2,2,2,2,2,2,2,2,2,2,2,2,2,2,2,2,2,
2,2,2,2,2,2,2,2,2,2,2,2,2,2,2,4),(-2.97196931891727,-2.91428574589538,-2.89770718111958,
-2.89332752620021,-2.89065668856314,-2.8881571917411,-2.88506034809745,
-2.87733615891202,-2.83080695999882,-2.80140723545357,-2.78924401518633,
-2.78239363240096,-2.77683289895904,-2.77675093910441,-2.77666503218692,
-2.77657439665546,-2.77647809242424,-2.77637497071679,-2.77626360401267,
-2.77614218585477,-2.77600838367988,-2.77585911584778,-2.77569020139731,
-2.77151261174643,-2.76677917299566,-2.75923275586235,-2.73403288392933,
-2.68930540982225,-2.67126639267519,-2.66389889500036,-2.65825802425226,
-2.65531760896332,-2.65286580560208,-2.64969289432205,-2.64309896224071,
-2.60041906988531,-2.58694267669041,-2.56260522765195,-2.54667350710196,
-2.54040916226628,-2.53593496955431,-2.53131623922925,-2.52431587657374,
-2.50426004130823,-2.45668716948417,-2.43634704095623,-2.42839779910167,
-2.42241840095309,-2.41940947627274,-2.41696141396609,-2.4138698835983,
-2.40746814786311,-2.36129838918073,-2.35101771342128,-2.32659359258713,
-2.31062344486255,-2.3043534254354,-2.29987810058965,-2.29580359007659,
-2.28925989618402,-2.27259386323244,-2.22189897772901,-2.19337950611251,
-2.18672074475212,-2.18358037378002,-2.18136549643623,-2.1785030912631,
-2.17338182004744,-2.13861537134678,-2.11263585630217,-2.089649271752,-2.07432504692235,
-2.0681497711038,-2.06369119347227,-2.05959719771755,-2.05402254107939,
-2.04276512924811,-1.98170695539743,-1.96324744653309,-1.9557701536014,
-1.95006453590518,-1.94711055600451,-1.94465935321661,-1.94150247240344,
-1.93475626206012,-1.89437742870489,-1.85957041175885,-1.83960993084124,
-1.83282307632219,-1.82824748064158,-1.82379229001105,-1.81739122276488,
-1.80170578259206,-1.75006355372384,-1.72857959653916,-1.72035516172327,
-1.7142181717278,-1.71117772595403,-1.7087297468675,-1.70567042821201,-1.69943700442974,
-1.65149482931027,-1.60646578565236,-1.59818389317943,-1.59329293009228,
-1.588920634794,-1.58333282259018,-1.57427100609585,-1.5222212838022,-1.49481084704842,
-1.48094622016344,-1.47756856596777),.UNSPECIFIED.);
#690=B_SPLINE_CURVE_WITH_KNOTS('',3,(#63176,#63177,#63178,#63179,#63180,
#63181,#63182,#63183,#63184,#63185,#63186,#63187,#63188,#63189,#63190,#63191,
#63192,#63193,#63194,#63195,#63196,#63197,#63198,#63199,#63200,#63201,#63202,
#63203,#63204,#63205,#63206,#63207,#63208,#63209,#63210,#63211,#63212,#63213,
#63214,#63215,#63216,#63217,#63218,#63219,#63220,#63221,#63222,#63223,#63224,
#63225,#63226,#63227,#63228,#63229,#63230,#63231,#63232,#63233,#63234,#63235,
#63236,#63237,#63238,#63239,#63240,#63241,#63242,#63243,#63244,#63245,#63246,
#63247,#63248,#63249,#63250,#63251,#63252,#63253,#63254,#63255,#63256,#63257,
#63258,#63259,#63260,#63261,#63262,#63263,#63264,#63265,#63266,#63267,#63268,
#63269,#63270,#63271,#63272,#63273,#63274,#63275,#63276,#63277,#63278,#63279,
#63280,#63281,#63282,#63283,#63284,#63285,#63286,#63287,#63288,#63289,#63290,
#63291,#63292,#63293,#63294,#63295,#63296,#63297,#63298,#63299,#63300,#63301,
#63302,#63303,#63304,#63305,#63306,#63307,#63308,#63309,#63310,#63311,#63312,
#63313,#63314,#63315,#63316,#63317,#63318,#63319,#63320,#63321,#63322,#63323,
#63324,#63325,#63326,#63327,#63328,#63329,#63330,#63331,#63332,#63333,#63334,
#63335,#63336,#63337,#63338,#63339,#63340,#63341,#63342,#63343,#63344,#63345,
#63346,#63347,#63348,#63349,#63350,#63351,#63352,#63353,#63354,#63355,#63356,
#63357,#63358,#63359,#63360,#63361,#63362,#63363,#63364,#63365,#63366,#63367,
#63368,#63369,#63370,#63371,#63372,#63373,#63374,#63375,#63376,#63377,#63378,
#63379),.UNSPECIFIED.,.F.,.F.,(4,2,2,2,2,2,2,2,2,2,2,2,2,2,2,2,2,2,2,2,
2,2,2,2,2,2,2,2,2,2,2,2,2,2,2,2,2,2,2,2,2,2,2,2,2,2,2,2,2,2,2,2,2,2,2,2,
2,2,2,2,2,2,2,2,2,2,2,2,2,2,2,2,2,2,2,2,2,2,2,2,2,2,2,2,2,2,2,2,2,2,2,2,
2,2,2,2,2,2,2,2,2,4),(-1.5120028941296,-1.49444504748298,-1.48728459445354,
-1.45724761769968,-1.45209467100208,-1.4491869789942,-1.44691683246572,
-1.44366447210436,-1.43662765579084,-1.42682267054302,-1.39811444349937,
-1.34851334425224,-1.33926454099114,-1.33355789785115,-1.32908688024209,
-1.32407683922482,-1.31556370112943,-1.26712239155253,-1.22370563941062,
-1.21707857541056,-1.21390264893852,-1.21139751980532,-1.20832265762709,
-1.20221489895544,-1.16416629342023,-1.1124282396071,-1.10329512972379,
-1.09762185695204,-1.0931542402523,-1.08812420456324,-1.07951697127604,
-1.03267877083928,-0.987655116524005,-0.981141842507781,-0.977987636574164,
-0.975482995647184,-0.972388122203787,-0.966179543090284,-0.957873677743406,
-0.936216969035032,-0.883605726750471,-0.869115066171862,-0.863435418991197,
-0.859253556753791,-0.854686904773009,-0.848334975518078,-0.832377054725447,
-0.808109829651744,-0.761758703975713,-0.748010228477541,-0.743695910328262,
-0.741000695311787,-0.738385488167906,-0.734445219280618,-0.722832593392474,
-0.70289333577784,-0.656441201509723,-0.63532751128321,-0.628121469429759,
-0.6233878902741,-0.618815212573951,-0.612430104171281,-0.596245082914192,
-0.571463117374698,-0.517978298974142,-0.510303021561183,-0.507174599073968,
-0.50462776690422,-0.50187130991816,-0.497277351391218,-0.478702815592633,
-0.431620935217259,-0.401101540546551,-0.393087553320132,-0.388183410694565,
-0.383686678799748,-0.377774027577873,-0.364590799483157,-0.298543914095754,
-0.277389452300924,-0.272476340623328,-0.269650200824313,-0.267103474300365,
-0.263536057283984,-0.254632889000594,-0.241108764369719,-0.182931385201981,
-0.163200816634732,-0.156143039607164,-0.151909514214553,-0.147379338457002,
-0.141245807342578,-0.126724135291483,-0.0825275835693964,-0.0545755851130164,
-0.0404434800717171,-0.036087373177055,-0.0333827955054112,-0.0310247821076836,
-0.0284248721535145,-0.0248021682944244,-0.0178498417920879),
 .UNSPECIFIED.);
#691=B_SPLINE_CURVE_WITH_KNOTS('',3,(#63385,#63386,#63387,#63388,#63389,
#63390,#63391,#63392,#63393,#63394),.UNSPECIFIED.,.F.,.F.,(4,1,1,1,1,1,
1,4),(72.2566310325652,72.8337041055645,73.8264152833055,74.8191264610465,
75.8118376387874,76.8045488165284,77.7972599942694,78.4660953116528),
 .UNSPECIFIED.);
#692=B_SPLINE_CURVE_WITH_KNOTS('',3,(#63395,#63396,#63397,#63398),
 .UNSPECIFIED.,.F.,.F.,(4,4),(-2.98921828163543,-2.97196931891727),
 .UNSPECIFIED.);
#693=B_SPLINE_CURVE_WITH_KNOTS('',3,(#63400,#63401,#63402,#63403),
 .UNSPECIFIED.,.F.,.F.,(4,4),(-0.0178498417920879,-0.000682550733952316),
 .UNSPECIFIED.);
#694=B_SPLINE_CURVE_WITH_KNOTS('',3,(#63404,#63405,#63406,#63407,#63408,
#63409,#63410,#63411,#63412,#63413,#63414,#63415,#63416,#63417,#63418,#63419,
#63420,#63421,#63422,#63423,#63424,#63425,#63426,#63427,#63428,#63429,#63430,
#63431,#63432,#63433,#63434,#63435,#63436,#63437,#63438,#63439,#63440,#63441,
#63442,#63443,#63444,#63445,#63446,#63447,#63448,#63449,#63450,#63451,#63452,
#63453,#63454,#63455,#63456,#63457,#63458,#63459,#63460,#63461,#63462,#63463,
#63464,#63465,#63466,#63467,#63468,#63469,#63470,#63471,#63472,#63473,#63474,
#63475,#63476,#63477,#63478,#63479,#63480,#63481,#63482,#63483,#63484,#63485,
#63486,#63487,#63488,#63489,#63490,#63491,#63492,#63493,#63494,#63495,#63496,
#63497,#63498,#63499,#63500,#63501,#63502,#63503,#63504,#63505,#63506,#63507,
#63508,#63509,#63510,#63511,#63512,#63513,#63514,#63515,#63516,#63517,#63518,
#63519,#63520,#63521,#63522,#63523,#63524,#63525,#63526,#63527,#63528,#63529,
#63530,#63531,#63532,#63533,#63534,#63535,#63536,#63537,#63538,#63539,#63540,
#63541,#63542,#63543,#63544,#63545,#63546,#63547,#63548,#63549,#63550,#63551,
#63552,#63553,#63554,#63555,#63556,#63557,#63558,#63559,#63560,#63561,#63562,
#63563,#63564,#63565,#63566,#63567,#63568,#63569,#63570,#63571,#63572,#63573,
#63574,#63575,#63576,#63577,#63578,#63579,#63580,#63581,#63582,#63583,#63584,
#63585,#63586,#63587,#63588,#63589,#63590,#63591,#63592,#63593,#63594,#63595),
 .UNSPECIFIED.,.F.,.F.,(4,2,2,2,2,2,2,2,2,2,2,2,2,2,2,2,2,2,2,2,2,2,2,2,
2,2,2,2,2,2,2,2,2,2,2,2,2,2,2,2,2,2,2,2,2,2,2,2,2,2,2,2,2,2,2,2,2,2,2,2,
2,2,2,2,2,2,2,2,2,2,2,2,2,2,2,2,2,2,2,2,2,2,2,2,2,2,2,2,2,2,2,2,2,2,2,4),
(-2.98961608686735,-2.92955913902989,-2.91434706881341,-2.90810641341164,
-2.90355878245489,-2.89878126957801,-2.89136529818291,-2.86828728786766,
-2.81952199490476,-2.80265574864177,-2.79556266327165,-2.7902365920153,
-2.78738327906901,-2.78487795006288,-2.78170355459493,-2.77508552931107,
-2.73176464316543,-2.68325779438362,-2.67474161328496,-2.66973054623383,
-2.6652590592707,-2.65955243548637,-2.65030489731358,-2.60057345985161,
-2.57191013064851,-2.56211255982198,-2.55508008937664,-2.55182827136203,
-2.54955797523332,-2.54664928170565,-2.54149290374496,-2.51116381551174,
-2.50419149324638,-2.46562836721085,-2.44442895495745,-2.43741060940826,
-2.4327153431829,-2.42816825824175,-2.42167408142716,-2.40588093378539,
-2.35448508388209,-2.33315361186218,-2.32492426680635,-2.31875963743648,
-2.31567325629579,-2.31316814710835,-2.31000410779275,-2.30344058556475,
-2.25941788879275,-2.21217626815809,-2.20330445866743,-2.19821813770763,
-2.19375787644256,-2.18817045447724,-2.17933346841292,-2.12413724305368,
-2.08887880164089,-2.08279807846928,-2.07972831250716,-2.07722258152124,
-2.07403988823319,-2.06737877282502,-2.02426117147748,-1.97561129597601,
-1.96709475401779,-1.96208342366462,-1.95761167086137,-1.95190466527456,
-1.94265641734554,-1.89292608283016,-1.86425834913199,-1.85445968316169,
-1.847426521533,-1.84417446243856,-1.8419040278866,-1.8389951989531,-1.83383867288096,
-1.80352186809264,-1.79692428835465,-1.76704386674269,-1.74784768075342,
-1.73429599963488,-1.72832061537338,-1.72381459720499,-1.71893741187965,
-1.71105181699964,-1.68269328521487,-1.6335070501788,-1.61459848585955,
-1.60998049580903,-1.60721855136846,-1.60467387721262,-1.60096911118102,
-1.59390153680279,-1.54740719322482,-1.51254166440623),.UNSPECIFIED.);
#695=B_SPLINE_CURVE_WITH_KNOTS('',3,(#63601,#63602,#63603,#63604,#63605,
#63606,#63607,#63608,#63609,#63610,#63611,#63612,#63613,#63614,#63615,#63616,
#63617,#63618,#63619,#63620,#63621,#63622,#63623,#63624,#63625,#63626,#63627,
#63628,#63629,#63630,#63631,#63632,#63633,#63634,#63635,#63636,#63637,#63638,
#63639,#63640,#63641,#63642,#63643,#63644,#63645,#63646,#63647,#63648,#63649,
#63650,#63651,#63652,#63653,#63654,#63655,#63656,#63657,#63658,#63659,#63660,
#63661,#63662,#63663,#63664,#63665,#63666,#63667,#63668,#63669,#63670,#63671,
#63672,#63673,#63674,#63675,#63676,#63677,#63678,#63679,#63680,#63681,#63682,
#63683,#63684,#63685,#63686,#63687,#63688,#63689,#63690,#63691,#63692,#63693,
#63694,#63695,#63696,#63697,#63698,#63699,#63700,#63701,#63702,#63703,#63704,
#63705,#63706,#63707,#63708,#63709,#63710,#63711,#63712,#63713,#63714,#63715,
#63716,#63717,#63718,#63719,#63720,#63721,#63722,#63723,#63724,#63725,#63726,
#63727,#63728,#63729,#63730,#63731,#63732,#63733,#63734,#63735,#63736,#63737,
#63738,#63739,#63740,#63741,#63742,#63743,#63744,#63745,#63746,#63747,#63748,
#63749,#63750,#63751,#63752,#63753,#63754,#63755,#63756,#63757,#63758,#63759,
#63760,#63761,#63762,#63763,#63764,#63765,#63766,#63767,#63768,#63769,#63770,
#63771,#63772,#63773,#63774,#63775,#63776,#63777,#63778,#63779,#63780,#63781,
#63782,#63783,#63784,#63785,#63786,#63787,#63788,#63789,#63790),
 .UNSPECIFIED.,.F.,.F.,(4,3,3,3,3,3,3,3,3,3,3,3,3,3,3,3,3,3,3,3,3,3,3,3,
3,3,3,3,3,3,3,3,3,3,3,3,3,3,3,3,3,3,3,3,3,3,3,3,3,3,3,3,3,3,3,3,3,3,3,3,
3,3,3,4),(78.5398163397448,78.669184564488,78.7899711720104,78.8905481960992,
78.9909814285215,79.09129948363,79.1915547173813,79.2917782714196,79.3920012473976,
79.4923233996722,79.5926942427436,79.6932437377857,79.7826823497514,79.8832593738159,
79.9836926062141,80.0840106612987,80.1842658950263,80.2844894490409,80.3847124249955,
80.4850345772472,80.5854054202958,80.6859549153159,80.7753935274923,80.8759705515419,
80.9764037839248,81.0767218389937,81.1769770727055,81.277200626704,81.3774236026423,
81.4777457548775,81.5781165979097,81.6786660929132,81.7681047052333,81.8686817294026,
81.9691149619056,82.0694330170946,82.1696882509264,82.2699118050448,82.3701347811025,
82.4704569334559,82.5708277766054,82.6713772717241,82.7608158829743,82.8613929069483,
82.9618261392563,83.0621441942518,83.1623994278909,83.2626229818178,83.3628459576855,
83.4631681098523,83.563538952817,83.6640884477557,83.7535270607153,83.8541040846601,
83.9545373169367,84.0548553718979,84.1551106055011,84.2553341593904,84.3555571352188,
84.4558792873442,84.5562501302661,84.6567996251603,84.7462382384562,84.7500696323053),
 .UNSPECIFIED.);
#696=B_SPLINE_CURVE_WITH_KNOTS('',3,(#63791,#63792,#63793,#63794),
 .UNSPECIFIED.,.F.,.F.,(4,4),(78.4660953116528,78.5398163397448),
 .UNSPECIFIED.);
#697=B_SPLINE_CURVE_WITH_KNOTS('',3,(#63795,#63796,#63797,#63798,#63799,
#63800,#63801,#63802,#63803,#63804,#63805,#63806,#63807,#63808,#63809,#63810,
#63811,#63812,#63813,#63814,#63815,#63816,#63817,#63818,#63819,#63820,#63821,
#63822,#63823,#63824,#63825,#63826,#63827,#63828,#63829,#63830,#63831,#63832,
#63833,#63834,#63835,#63836,#63837,#63838,#63839,#63840,#63841,#63842,#63843,
#63844,#63845,#63846,#63847,#63848,#63849,#63850,#63851,#63852,#63853,#63854,
#63855,#63856,#63857,#63858,#63859,#63860,#63861,#63862,#63863,#63864,#63865,
#63866,#63867,#63868,#63869,#63870,#63871,#63872,#63873,#63874,#63875,#63876,
#63877,#63878,#63879,#63880,#63881,#63882,#63883,#63884,#63885,#63886,#63887,
#63888,#63889,#63890,#63891,#63892,#63893,#63894,#63895,#63896,#63897,#63898,
#63899,#63900,#63901,#63902,#63903,#63904,#63905,#63906,#63907,#63908,#63909,
#63910,#63911,#63912,#63913,#63914,#63915,#63916,#63917,#63918,#63919,#63920,
#63921,#63922,#63923,#63924,#63925,#63926,#63927,#63928,#63929,#63930,#63931,
#63932,#63933,#63934,#63935,#63936,#63937,#63938,#63939,#63940,#63941,#63942,
#63943,#63944,#63945,#63946,#63947,#63948,#63949,#63950,#63951,#63952,#63953,
#63954,#63955,#63956,#63957,#63958,#63959,#63960,#63961,#63962,#63963,#63964,
#63965,#63966,#63967,#63968,#63969,#63970,#63971,#63972,#63973,#63974,#63975,
#63976,#63977,#63978,#63979,#63980,#63981,#63982,#63983,#63984,#63985,#63986,
#63987,#63988,#63989,#63990,#63991,#63992,#63993,#63994,#63995,#63996,#63997,
#63998,#63999,#64000,#64001,#64002,#64003,#64004,#64005,#64006,#64007,#64008,
#64009,#64010,#64011,#64012,#64013,#64014,#64015,#64016,#64017,#64018,#64019,
#64020,#64021,#64022,#64023,#64024,#64025,#64026,#64027,#64028,#64029,#64030,
#64031,#64032,#64033,#64034,#64035,#64036,#64037,#64038,#64039,#64040,#64041,
#64042,#64043,#64044,#64045,#64046,#64047,#64048,#64049,#64050,#64051,#64052,
#64053,#64054,#64055,#64056,#64057,#64058,#64059,#64060),.UNSPECIFIED.,
 .F.,.F.,(4,2,2,2,2,2,2,2,2,2,2,2,2,2,2,2,2,2,2,2,2,2,2,2,2,2,2,2,2,2,2,
2,2,2,2,2,2,2,2,2,2,2,2,2,2,2,2,2,2,2,2,2,2,2,2,2,2,2,2,2,2,2,2,2,2,2,2,
2,2,2,2,2,2,2,2,2,2,2,2,2,2,2,2,2,2,2,2,2,2,2,2,2,2,2,2,2,2,2,2,2,2,2,2,
2,2,2,2,2,2,2,2,2,2,2,2,2,2,2,2,2,2,2,2,2,2,2,2,2,2,2,2,2,4),(-1.51254166440623,
-1.50358687733872,-1.49521768662821,-1.49023743753114,-1.48575918136067,
-1.47999613363582,-1.46767039141004,-1.43238520659278,-1.38960746151934,
-1.37767405555367,-1.3735732534584,-1.37118657045784,-1.36858843453146,
-1.36473510723931,-1.35381633081085,-1.33565393081433,-1.27696212473058,
-1.26307088832274,-1.25748537385371,-1.25332555565174,-1.24873671272699,
-1.24226571564178,-1.22548154805426,-1.19930777629856,-1.16107507700933,
-1.14299695310182,-1.1382776414061,-1.13549359618687,-1.13293007873679,
-1.12926199883559,-1.11968899045097,-1.05483920518293,-1.03021664517121,
-1.02264111850684,-1.01782981551288,-1.01329818103851,-1.0071553853881,
-0.992574997544352,-0.971291801131024,-0.928899172051115,-0.907462969713808,
-0.902536198441425,-0.899707147346546,-0.897161522018309,-0.893600777255911,
-0.884740280170151,-0.871306797053486,-0.81431481812923,-0.793507373232208,
-0.786332615335024,-0.78160518115067,-0.777027760574175,-0.77061818250404,
-0.754265956675427,-0.729101403556005,-0.674411365757629,-0.667761866795157,
-0.664581318302855,-0.662075593307231,-0.659003749268963,-0.652912891037507,
-0.616590240131492,-0.562768921474694,-0.553800789239317,-0.548174885242987,
-0.543711091212179,-0.538649814232322,-0.529897606858921,-0.481156763813978,
-0.438618535914785,-0.431885478227617,-0.428689115376463,-0.426182796879897,
-0.423124751072955,-0.417102966785914,-0.409123661148039,-0.388828131798958,
-0.341126501054896,-0.321439833701956,-0.314386989202548,-0.310154259528849,
-0.30562332056504,-0.299485886361556,-0.284940522597808,-0.263730620661781,
-0.236097740513245,-0.203010952122292,-0.196119542944986,-0.192893608593384,
-0.190385934214598,-0.190331662082248,-0.190279979933743,-0.190230688356025,
-0.190183607911403,-0.190138576699426,-0.190095448269347,-0.190054089815314,
-0.190014380625071,-0.189976210726914,-0.18993947971519,-0.189904095729544,
-0.189869974564239,-0.189837038875559,-0.189805217494056,-0.189774444819543,
-0.189744660278097,-0.189715807843964,-0.189687835624076,-0.189660695471361,
-0.189634342651879,-0.189608735545615,-0.189583835371524,-0.189559605951785,
-0.189536013493062,-0.189513026385609,-0.189490615029967,-0.189468751676441,
-0.189447410277488,-0.189426566364043,-0.189406196915075,-0.189386280251627,
-0.186109378997095,-0.178221264837677,-0.16649512808658,-0.125880405963827,
-0.0881332296270172,-0.0798166726120481,-0.0748477520311481,-0.0703672557747848,
-0.0645838298938687,-0.0582726373553926,-0.0476295332544095,-0.018241527118741),
 .UNSPECIFIED.);
#698=B_SPLINE_CURVE_WITH_KNOTS('',3,(#64066,#64067,#64068,#64069,#64070,
#64071,#64072,#64073,#64074,#64075,#64076,#64077,#64078,#64079,#64080,#64081,
#64082,#64083,#64084,#64085,#64086,#64087,#64088,#64089,#64090,#64091,#64092,
#64093,#64094,#64095,#64096,#64097,#64098,#64099,#64100,#64101,#64102,#64103,
#64104,#64105,#64106,#64107,#64108,#64109,#64110,#64111,#64112,#64113,#64114,
#64115,#64116,#64117,#64118,#64119,#64120,#64121,#64122,#64123,#64124,#64125,
#64126,#64127,#64128,#64129,#64130,#64131,#64132,#64133,#64134,#64135,#64136,
#64137,#64138,#64139,#64140,#64141,#64142,#64143,#64144,#64145,#64146,#64147,
#64148,#64149,#64150,#64151,#64152,#64153,#64154,#64155,#64156,#64157,#64158,
#64159,#64160,#64161,#64162,#64163,#64164,#64165,#64166,#64167,#64168,#64169,
#64170,#64171,#64172,#64173,#64174,#64175,#64176,#64177,#64178,#64179,#64180,
#64181,#64182,#64183,#64184,#64185,#64186,#64187,#64188,#64189,#64190,#64191,
#64192,#64193,#64194,#64195,#64196,#64197,#64198,#64199,#64200,#64201,#64202,
#64203,#64204,#64205,#64206,#64207,#64208,#64209,#64210,#64211,#64212,#64213,
#64214,#64215,#64216,#64217,#64218,#64219,#64220,#64221,#64222,#64223,#64224,
#64225,#64226,#64227,#64228,#64229,#64230,#64231,#64232,#64233,#64234,#64235,
#64236,#64237,#64238,#64239,#64240,#64241,#64242,#64243,#64244,#64245,#64246,
#64247,#64248,#64249,#64250,#64251,#64252,#64253,#64254,#64255,#64256,#64257,
#64258,#64259,#64260,#64261,#64262,#64263,#64264,#64265,#64266,#64267,#64268,
#64269,#64270,#64271,#64272,#64273,#64274,#64275,#64276,#64277,#64278,#64279,
#64280,#64281,#64282,#64283,#64284,#64285,#64286,#64287,#64288,#64289,#64290,
#64291,#64292,#64293,#64294,#64295,#64296,#64297,#64298,#64299,#64300,#64301,
#64302,#64303,#64304,#64305,#64306,#64307,#64308,#64309,#64310,#64311,#64312,
#64313,#64314,#64315,#64316,#64317,#64318,#64319,#64320,#64321,#64322,#64323,
#64324,#64325,#64326,#64327,#64328,#64329,#64330,#64331,#64332,#64333,#64334,
#64335,#64336,#64337,#64338,#64339),.UNSPECIFIED.,.F.,.F.,(4,2,2,2,2,2,
2,2,2,2,2,2,2,2,2,2,2,2,2,2,2,2,2,2,2,2,2,2,2,2,2,2,2,2,2,2,2,2,2,2,2,2,
2,2,2,2,2,2,2,2,2,2,2,2,2,2,2,2,2,2,2,2,2,2,2,2,2,2,2,2,2,2,2,2,2,2,2,2,
2,2,2,2,2,2,2,2,2,2,2,2,2,2,2,2,2,2,2,2,2,2,2,2,2,2,2,2,2,2,2,2,2,2,2,2,
2,2,2,2,2,2,2,2,2,2,2,2,2,2,2,2,2,2,2,2,2,2,4),(-1.47758203553868,-1.42899975050051,
-1.40713396065841,-1.40225440817748,-1.39947453781305,-1.3969931931183,
-1.39355802552855,-1.38519875808859,-1.37273993155273,-1.32570381463777,
-1.29475606810944,-1.28681911537627,-1.28200235399692,-1.27761433094251,
-1.27188949146447,-1.2593428096774,-1.2227452640396,-1.17694041345732,-1.16840489189888,
-1.16484135947674,-1.16236394737657,-1.15964851340514,-1.15506554840041,
-1.13569936181252,-1.08283230436195,-1.05794342324226,-1.05038012635333,
-1.04564311339815,-1.04122940714009,-1.03532371679027,-1.02171241288969,
-1.00229058451556,-0.972532735680228,-0.964753332609068,-0.93546001536075,
-0.930388941922798,-0.927537948770019,-0.925321539766668,-0.922165550488369,
-0.915421990420157,-0.886087943674784,-0.832997115617142,-0.818845009136248,
-0.813290140658679,-0.809201415034091,-0.804739670631151,-0.798543469926555,
-0.783075299601176,-0.759768673717856,-0.731919319327381,-0.699458372272132,
-0.694361092433451,-0.691504288722078,-0.689288891172297,-0.686141527371202,
-0.67944397083235,-0.650551410103965,-0.598758518977501,-0.583269703219454,
-0.576906316715529,-0.57245896232353,-0.567875990948625,-0.561048516978307,
-0.540723772421731,-0.504789693549326,-0.466042391789734,-0.459247212219221,
-0.456081713271364,-0.453630552682631,-0.450684730797207,-0.445016901202972,
-0.437604183251857,-0.419391363518556,-0.374493515410956,-0.349789149628837,
-0.342243162330127,-0.337509995168157,-0.333095125730737,-0.327180643448004,
-0.313514765506184,-0.293983788171101,-0.26437545984912,-0.230141940365606,
-0.223269271662711,-0.220123160218621,-0.217765263502421,-0.217724439695203,
-0.217668032038743,-0.217614643452261,-0.217564008431681,-0.21751589221921,
-0.217470086422374,-0.217426405360392,-0.217384683009115,-0.217344770432778,
-0.217306533610085,-0.217269851581783,-0.217234614873007,-0.217200724139939,
-0.217168089011508,-0.217136627076906,-0.217106263010309,-0.217076927817307,
-0.217048558167393,-0.217021095815192,-0.21699448709232,-0.216968682453933,
-0.216943636077767,-0.216919305522286,-0.216895651408788,-0.216872637143664,
-0.216850228665975,-0.216828394236927,-0.216807104224317,-0.216786330941784,
-0.216766048473687,-0.216746232539398,-0.216726860360167,-0.216707910535952,
-0.21668936293948,-0.216671198627902,-0.216653399739507,-0.216635949424207,
-0.21661883176486,-0.213409431385154,-0.209564823591307,-0.202719038906595,
-0.186615837149335,-0.156725257244662,-0.115182717864199,-0.106906053210041,
-0.102017091908541,-0.0976459234138118,-0.0920586358523389,-0.0802794519782047,
-0.0133182801247358,-0.000686390217275949),.UNSPECIFIED.);
#699=B_SPLINE_CURVE_WITH_KNOTS('',3,(#64340,#64341,#64342,#64343),
 .UNSPECIFIED.,.F.,.F.,(4,4),(84.7500696323053,84.8230016469244),
 .UNSPECIFIED.);
#700=B_SPLINE_CURVE_WITH_KNOTS('',3,(#64345,#64346,#64347,#64348),
 .UNSPECIFIED.,.F.,.F.,(4,4),(-0.018241527118741,-0.00068348472876189),
 .UNSPECIFIED.);
#701=B_SPLINE_CURVE_WITH_KNOTS('',3,(#64349,#64350,#64351,#64352,#64353,
#64354,#64355,#64356,#64357,#64358,#64359,#64360,#64361,#64362,#64363,#64364,
#64365,#64366,#64367,#64368,#64369,#64370,#64371,#64372,#64373,#64374,#64375,
#64376,#64377,#64378,#64379,#64380,#64381,#64382,#64383,#64384,#64385,#64386,
#64387,#64388,#64389,#64390,#64391,#64392,#64393,#64394,#64395,#64396,#64397,
#64398,#64399,#64400,#64401,#64402,#64403,#64404,#64405,#64406,#64407,#64408,
#64409,#64410,#64411,#64412,#64413,#64414,#64415,#64416,#64417,#64418,#64419,
#64420,#64421,#64422,#64423,#64424,#64425,#64426,#64427,#64428,#64429,#64430,
#64431,#64432,#64433,#64434,#64435,#64436,#64437,#64438,#64439,#64440,#64441,
#64442,#64443,#64444,#64445,#64446,#64447,#64448,#64449,#64450,#64451,#64452,
#64453,#64454,#64455,#64456,#64457,#64458,#64459,#64460,#64461,#64462,#64463,
#64464,#64465,#64466,#64467,#64468,#64469,#64470,#64471,#64472,#64473,#64474,
#64475,#64476,#64477,#64478,#64479,#64480,#64481,#64482,#64483,#64484,#64485,
#64486,#64487,#64488,#64489,#64490,#64491,#64492,#64493,#64494,#64495,#64496,
#64497,#64498,#64499,#64500,#64501,#64502,#64503,#64504,#64505,#64506,#64507,
#64508,#64509,#64510,#64511,#64512,#64513,#64514,#64515,#64516,#64517,#64518,
#64519,#64520,#64521,#64522,#64523,#64524,#64525,#64526,#64527,#64528,#64529,
#64530,#64531,#64532,#64533,#64534,#64535,#64536,#64537,#64538,#64539,#64540,
#64541,#64542,#64543,#64544,#64545,#64546,#64547,#64548,#64549,#64550,#64551,
#64552,#64553,#64554),.UNSPECIFIED.,.F.,.F.,(4,2,2,2,2,2,2,2,2,2,2,2,2,
2,2,2,2,2,2,2,2,2,2,2,2,2,2,2,2,2,2,2,2,2,2,2,2,2,2,2,2,2,2,2,2,2,2,2,2,
2,2,2,2,2,2,2,2,2,2,2,2,2,2,2,2,2,2,2,2,2,2,2,2,2,2,2,2,2,2,2,2,2,2,2,2,
2,2,2,2,2,2,2,2,2,2,2,2,2,2,2,2,2,4),(-2.98941746380008,-2.96248487704949,
-2.95231218207499,-2.94882509966526,-2.94627588425307,-2.94373207430651,
-2.94089801440436,-2.93594791514604,-2.91432438045648,-2.8836342351491,
-2.85719872258917,-2.85385350591768,-2.84108214507179,-2.83289489716619,
-2.82788178193595,-2.82341030018426,-2.81770620487656,-2.80846815849808,
-2.75850278040354,-2.7299945269286,-2.72022646336742,-2.71320971940145,
-2.70996065224898,-2.70769055209363,-2.70477968793288,-2.69961414476861,
-2.66748843187319,-2.62506845358489,-2.60279592023616,-2.59566308670309,
-2.59094421025465,-2.58641306322525,-2.58000852807909,-2.56478878050303,
-2.5128242690168,-2.49133668963146,-2.48307011798251,-2.47688417195004,
-2.47379346268617,-2.47128830746959,-2.46812857314816,-2.4615881171433,
-2.41718024451569,-2.3710766057594,-2.3617565374957,-2.35657631550999,-2.35212428603858,
-2.34666319032082,-2.33825485350738,-2.2793750251368,-2.24835956015106,
-2.24138509149896,-2.2381436810177,-2.23587435621901,-2.2329580516155,-2.22776864658227,
-2.19316842332354,-2.16639978102874,-2.1440154174088,-2.13369023897457,
-2.12520137845459,-2.12019559056495,-2.11572225121708,-2.11000420519358,
-2.10071871235496,-2.05192667878566,-2.01107833642564,-2.00500291545911,
-2.00193397183937,-1.99942787532982,-1.99624340477556,-1.98957420302857,
-1.94650761390652,-1.89783660757977,-1.88930258607995,-1.88428713949085,
-1.87981544634602,-1.87411364917727,-1.86488481127286,-1.81469155770055,
-1.78633021881076,-1.77659001368226,-1.76958804112824,-1.7663414572083,
-1.76407142606589,-1.76115830980542,-1.75598361612362,-1.72232344586827,
-1.68106494468326,-1.65910026878054,-1.65199894354638,-1.64728615091001,
-1.6427500366689,-1.63631989534542,-1.6209137889279,-1.55749218930709,-1.54360611773456,
-1.53453442609139,-1.53094071300473,-1.52838945582394,-1.52557417449396,
-1.52071262104022,-1.5126288124337),.UNSPECIFIED.);
#702=B_SPLINE_CURVE_WITH_KNOTS('',3,(#64559,#64560,#64561,#64562,#64563,
#64564,#64565,#64566,#64567,#64568,#64569,#64570,#64571,#64572,#64573,#64574,
#64575,#64576,#64577,#64578,#64579,#64580,#64581,#64582,#64583,#64584,#64585,
#64586,#64587,#64588,#64589,#64590,#64591,#64592,#64593,#64594,#64595,#64596,
#64597,#64598,#64599,#64600,#64601,#64602,#64603,#64604,#64605,#64606,#64607,
#64608,#64609,#64610,#64611,#64612,#64613,#64614,#64615,#64616,#64617,#64618,
#64619,#64620,#64621,#64622,#64623,#64624,#64625,#64626,#64627,#64628,#64629,
#64630,#64631,#64632,#64633,#64634,#64635,#64636,#64637,#64638,#64639,#64640,
#64641,#64642,#64643,#64644,#64645,#64646,#64647,#64648,#64649,#64650,#64651,
#64652,#64653,#64654,#64655,#64656,#64657,#64658,#64659,#64660,#64661,#64662,
#64663,#64664,#64665,#64666,#64667,#64668,#64669,#64670,#64671,#64672,#64673,
#64674,#64675,#64676,#64677,#64678,#64679,#64680,#64681,#64682,#64683,#64684,
#64685,#64686,#64687,#64688,#64689,#64690,#64691,#64692,#64693,#64694,#64695,
#64696,#64697,#64698,#64699,#64700,#64701,#64702,#64703,#64704,#64705,#64706,
#64707,#64708,#64709,#64710,#64711,#64712,#64713,#64714,#64715,#64716,#64717,
#64718,#64719,#64720,#64721,#64722,#64723,#64724,#64725,#64726,#64727,#64728,
#64729,#64730,#64731,#64732,#64733,#64734,#64735,#64736,#64737,#64738,#64739,
#64740,#64741,#64742,#64743,#64744,#64745,#64746,#64747,#64748,#64749,#64750,
#64751,#64752,#64753,#64754,#64755,#64756,#64757,#64758,#64759,#64760,#64761,
#64762,#64763,#64764,#64765,#64766,#64767,#64768,#64769,#64770),
 .UNSPECIFIED.,.F.,.F.,(4,2,2,2,2,2,2,2,2,2,2,2,2,2,2,2,2,2,2,2,2,2,2,2,
2,2,2,2,2,2,2,2,2,2,2,2,2,2,2,2,2,2,2,2,2,2,2,2,2,2,2,2,2,2,2,2,2,2,2,2,
2,2,2,2,2,2,2,2,2,2,2,2,2,2,2,2,2,2,2,2,2,2,2,2,2,2,2,2,2,2,2,2,2,2,2,2,
2,2,2,2,2,2,2,2,2,4),(-2.97123293200389,-2.96018209535889,-2.94653467953259,
-2.94079549607278,-2.93646395987323,-2.93205085822967,-2.92731797038154,
-2.91976888812843,-2.89452044756518,-2.85305399826597,-2.83095702050522,
-2.82093864347159,-2.81719917840001,-2.81466532553443,-2.81200479945457,
-2.80766912760509,-2.79316376233238,-2.74654337121384,-2.72285941677932,
-2.70722156330017,-2.70100199176108,-2.6965374885075,-2.69245577118526,
-2.68692507089546,-2.6729220767887,-2.61967055034795,-2.59028083733551,
-2.58353308211964,-2.58037710025521,-2.57816148795362,-2.57531257791512,
-2.57024769457214,-2.54114604092698,-2.53307565643954,-2.50305994527748,
-2.47424683310716,-2.46665470925122,-2.46191282517589,-2.45750347458752,
-2.45171891303322,-2.43844732353472,-2.37841434063925,-2.36007289003813,
-2.35262755738223,-2.34694137947838,-2.34399231281459,-2.34154212281015,
-2.33838262903737,-2.33161714927247,-2.29182937796836,-2.27299017606512,
-2.25029265179837,-2.23993149663796,-2.23145590628294,-2.22652531930293,
-2.22216229783813,-2.21664703612831,-2.20783025530979,-2.15296321683991,
-2.11638120526222,-2.11084257064889,-2.10792360009756,-2.10547035317752,
-2.1023236770765,-2.09544626523312,-2.05969758416929,-2.02174087186709,
-2.00078955048243,-1.99389317820185,-1.98929664490684,-1.98486034402827,
-1.97855490257305,-1.96340147311525,-1.9112460583597,-1.88222542586457,
-1.87551505987632,-1.87236556510723,-1.87015021318367,-1.86729558461131,
-1.86220703159483,-1.83158661124563,-1.82167068961519,-1.7851724584713,
-1.76466958750591,-1.7578226795325,-1.75323610498249,-1.74879229022575,
-1.74244630831792,-1.72704898276516,-1.67513483577027,-1.646196369831,-1.63949441442758,
-1.63634640075441,-1.63413112420566,-1.63127522924421,-1.62618137293291,
-1.59446744729977,-1.5896706765963,-1.56069768784271,-1.53039679859945,
-1.52270284543596,-1.51793834871118,-1.5135352569642,-1.50779809362037,
-1.49481626177982,-1.47758203553868),.UNSPECIFIED.);
#703=B_SPLINE_CURVE_WITH_KNOTS('',3,(#64771,#64772,#64773,#64774,#64775,
#64776,#64777,#64778,#64779,#64780,#64781,#64782,#64783,#64784,#64785,#64786,
#64787,#64788,#64789,#64790,#64791,#64792,#64793,#64794,#64795,#64796,#64797,
#64798,#64799,#64800,#64801,#64802,#64803,#64804,#64805,#64806,#64807,#64808,
#64809,#64810,#64811,#64812,#64813,#64814,#64815,#64816,#64817,#64818,#64819,
#64820,#64821,#64822,#64823,#64824,#64825,#64826,#64827,#64828,#64829,#64830,
#64831,#64832,#64833,#64834,#64835,#64836,#64837,#64838,#64839,#64840,#64841,
#64842,#64843,#64844,#64845,#64846,#64847,#64848,#64849,#64850,#64851,#64852,
#64853,#64854,#64855,#64856,#64857,#64858,#64859,#64860,#64861,#64862,#64863,
#64864,#64865,#64866,#64867,#64868,#64869,#64870,#64871,#64872,#64873,#64874,
#64875,#64876,#64877,#64878,#64879,#64880,#64881,#64882,#64883,#64884,#64885,
#64886,#64887,#64888,#64889,#64890,#64891,#64892,#64893,#64894,#64895,#64896,
#64897,#64898,#64899,#64900,#64901,#64902,#64903,#64904,#64905,#64906,#64907,
#64908,#64909,#64910,#64911,#64912,#64913,#64914,#64915,#64916,#64917,#64918,
#64919,#64920,#64921,#64922,#64923,#64924,#64925,#64926,#64927,#64928,#64929,
#64930,#64931,#64932,#64933,#64934,#64935,#64936,#64937,#64938,#64939,#64940,
#64941,#64942,#64943,#64944,#64945,#64946,#64947,#64948,#64949,#64950,#64951,
#64952,#64953,#64954,#64955,#64956,#64957,#64958,#64959,#64960,#64961,#64962,
#64963,#64964,#64965,#64966,#64967,#64968),.UNSPECIFIED.,.F.,.F.,(4,2,2,
2,2,2,2,2,2,2,2,2,2,2,2,2,2,2,2,2,2,2,2,2,2,2,2,2,2,2,2,2,2,2,2,2,2,2,2,
2,2,2,2,2,2,2,2,2,2,2,2,2,2,2,2,2,2,2,2,2,2,2,2,2,2,2,2,2,2,2,2,2,2,2,2,
2,2,2,2,2,2,2,2,2,2,2,2,2,2,2,2,2,2,2,2,2,2,2,4),(-1.5126288124337,-1.50038114054109,
-1.49546479199589,-1.44606412386808,-1.42366624092399,-1.41631822307126,
-1.4115541165769,-1.40699740606741,-1.40070895674774,-1.38518831930661,
-1.36189724087179,-1.33558914890058,-1.30191823245816,-1.2967426740572,
-1.29382928014378,-1.29155911992285,-1.28831253492428,-1.28131112506051,
-1.27157323930674,-1.24322194045223,-1.19306223892939,-1.18383415560942,
-1.17813236805072,-1.17366044373705,-1.16864448607963,-1.16010901161033,
-1.11197953383842,-1.06819237216739,-1.06160211412162,-1.05843249665659,
-1.05592666101242,-1.05284392336975,-1.046699957856,-1.00536760922362,-0.957249337814812,
-0.947943166028995,-0.942218832374047,-0.937744412304101,-0.93274138091446,
-0.924267106080874,-0.875232155528154,-0.832413316551177,-0.825706622371078,
-0.82251486321443,-0.820008271450277,-0.816945132400755,-0.810899680953753,
-0.802879772017047,-0.782420659953794,-0.734145338154514,-0.71508205717588,
-0.708106128584507,-0.703886922727287,-0.699345825018686,-0.693150408393322,
-0.678240186779483,-0.656266216843191,-0.612830331704289,-0.593349426309233,
-0.588537752568741,-0.585733238735222,-0.583177617711738,-0.579558131695105,
-0.570316762160553,-0.556064258954025,-0.485626409173881,-0.476148484033475,
-0.470375057600833,-0.465895201878667,-0.460919756707715,-0.452574728771954,
-0.409888181588814,-0.365730445953171,-0.355471964610801,-0.351597197392485,
-0.349252732260916,-0.346607310085745,-0.342525237517454,-0.329701962106306,
-0.306408896864487,-0.247724994857589,-0.239296265007748,-0.233828769446615,
-0.229375971070713,-0.227916074284677,-0.227172544964561,-0.22641533902017,
-0.219485513050008,-0.199084759498255,-0.163124337587808,-0.124902246056914,
-0.117977158098232,-0.11474477389471,-0.112236499212788,-0.109207970221842,
-0.103333172622581,-0.0956076681871372,-0.0763324108419592,-0.0180105444581843),
 .UNSPECIFIED.);
#704=B_SPLINE_CURVE_WITH_KNOTS('',3,(#64974,#64975,#64976,#64977,#64978,
#64979,#64980,#64981,#64982,#64983),.UNSPECIFIED.,.F.,.F.,(4,1,1,1,1,1,
1,4),(97.3893749664237,97.6514835490889,98.6441947268299,99.6369059045709,
100.629617082312,101.622328260053,102.615039437794,103.599566372989),
 .UNSPECIFIED.);
#705=B_SPLINE_CURVE_WITH_KNOTS('',3,(#64984,#64985,#64986,#64987),
 .UNSPECIFIED.,.F.,.F.,(4,4),(-2.98877382828685,-2.97123293200389),
 .UNSPECIFIED.);
#706=B_SPLINE_CURVE_WITH_KNOTS('',3,(#64989,#64990,#64991,#64992,#64993,
#64994,#64995,#64996),.UNSPECIFIED.,.F.,.F.,(4,2,2,4),(-0.0180105444581843,
-0.0141561210882267,-0.00572761886439141,-0.000683821560827492),
 .UNSPECIFIED.);
#707=B_SPLINE_CURVE_WITH_KNOTS('',3,(#64997,#64998,#64999,#65000,#65001,
#65002,#65003,#65004,#65005,#65006,#65007,#65008,#65009,#65010,#65011,#65012,
#65013,#65014,#65015,#65016,#65017,#65018,#65019,#65020,#65021,#65022,#65023,
#65024,#65025,#65026,#65027,#65028,#65029,#65030,#65031,#65032,#65033,#65034,
#65035,#65036,#65037,#65038,#65039,#65040,#65041,#65042,#65043,#65044,#65045,
#65046,#65047,#65048,#65049,#65050,#65051,#65052,#65053,#65054,#65055,#65056,
#65057,#65058,#65059,#65060,#65061,#65062,#65063,#65064,#65065,#65066,#65067,
#65068,#65069,#65070,#65071,#65072,#65073,#65074,#65075,#65076,#65077,#65078,
#65079,#65080,#65081,#65082,#65083,#65084,#65085,#65086,#65087,#65088,#65089,
#65090,#65091,#65092,#65093,#65094,#65095,#65096,#65097,#65098,#65099,#65100,
#65101,#65102,#65103,#65104,#65105,#65106,#65107,#65108,#65109,#65110,#65111,
#65112,#65113,#65114,#65115,#65116,#65117,#65118,#65119,#65120,#65121,#65122,
#65123,#65124,#65125,#65126,#65127,#65128,#65129,#65130,#65131,#65132,#65133,
#65134,#65135,#65136,#65137,#65138,#65139,#65140,#65141,#65142,#65143,#65144,
#65145,#65146,#65147,#65148,#65149,#65150,#65151,#65152,#65153,#65154,#65155,
#65156,#65157,#65158,#65159,#65160,#65161,#65162,#65163,#65164,#65165,#65166,
#65167,#65168,#65169,#65170,#65171,#65172,#65173,#65174,#65175,#65176,#65177,
#65178,#65179,#65180,#65181,#65182,#65183,#65184,#65185,#65186),
 .UNSPECIFIED.,.F.,.F.,(4,3,3,3,3,3,3,3,3,3,3,3,3,3,3,3,3,3,3,3,3,3,3,3,
3,3,3,3,3,3,3,3,3,3,3,3,3,3,3,3,3,3,3,3,3,3,3,3,3,3,3,3,3,3,3,3,3,3,3,3,
3,3,3,4),(97.3893722612836,97.493384673513,97.5976334276354,97.7019998579112,
97.8066354474768,97.9077762578471,98.0083650106068,98.1088102098943,98.2091404938834,
98.3094081259277,98.4096442296323,98.5098798887576,98.6102146041844,98.7105981065155,
98.8111596237581,98.8996468717555,99.000231660288,99.1006728858691,99.2009992006014,
99.301262868009,99.4014950171848,99.5017267373846,99.6020575655355,99.7024372028987,
99.8029949370643,99.8915174856638,99.9921074860471,100.092553907656,100.192885370718,
100.293154154975,100.393391382668,100.493628136167,100.593963892524,100.694348408067,
100.794910880808,100.883388099572,100.983981673788,101.08443173694,101.184766925044,
101.285039483294,101.385280528212,101.485521136495,101.585860778769,101.686249203348,
101.786815578012,101.875258713481,101.975825805746,102.076249303367,102.176557925544,
102.27680393036,102.377018471189,102.477232661605,102.57754620383,102.677908662145,
102.778449594122,102.867129327389,102.96625050879,103.065243338486,103.164140823337,
103.262975843551,103.361809067418,103.4606412558,103.559547384382,103.598719667128),
 .UNSPECIFIED.);
#708=B_SPLINE_CURVE_WITH_KNOTS('',3,(#65190,#65191,#65192,#65193,#65194,
#65195),.UNSPECIFIED.,.F.,.F.,(4,1,1,4),(-4.09293042013066,-3.96748245563351,
-2.97561184172513,-2.06906822660971),.UNSPECIFIED.);
#709=B_SPLINE_CURVE_WITH_KNOTS('',3,(#65199,#65200,#65201,#65202,#65203),
 .UNSPECIFIED.,.F.,.F.,(4,1,4),(0.,0.992711177740983,1.1173004083682),
 .UNSPECIFIED.);
#710=B_SPLINE_CURVE_WITH_KNOTS('',3,(#65205,#65206,#65207,#65208,#65209,
#65210,#65211,#65212,#65213,#65214,#65215,#65216,#65217,#65218,#65219,#65220,
#65221,#65222,#65223,#65224,#65225,#65226,#65227,#65228,#65229,#65230,#65231,
#65232,#65233,#65234,#65235,#65236,#65237,#65238,#65239,#65240,#65241,#65242,
#65243,#65244,#65245,#65246,#65247,#65248,#65249,#65250,#65251,#65252,#65253,
#65254,#65255,#65256,#65257,#65258,#65259,#65260,#65261,#65262,#65263,#65264,
#65265,#65266,#65267,#65268,#65269,#65270,#65271,#65272,#65273,#65274,#65275,
#65276,#65277,#65278,#65279,#65280,#65281,#65282,#65283,#65284,#65285,#65286,
#65287,#65288,#65289,#65290,#65291,#65292,#65293,#65294,#65295,#65296,#65297,
#65298,#65299,#65300,#65301,#65302,#65303,#65304,#65305,#65306,#65307,#65308,
#65309,#65310,#65311,#65312,#65313,#65314,#65315,#65316,#65317,#65318,#65319,
#65320,#65321,#65322,#65323,#65324,#65325,#65326,#65327,#65328,#65329,#65330,
#65331,#65332,#65333,#65334,#65335,#65336,#65337,#65338,#65339,#65340,#65341,
#65342,#65343,#65344,#65345,#65346,#65347,#65348,#65349,#65350,#65351,#65352,
#65353,#65354,#65355,#65356,#65357,#65358,#65359,#65360,#65361,#65362,#65363,
#65364,#65365,#65366,#65367,#65368,#65369,#65370,#65371,#65372,#65373,#65374,
#65375,#65376,#65377,#65378,#65379,#65380,#65381,#65382,#65383,#65384,#65385,
#65386,#65387,#65388,#65389,#65390,#65391,#65392,#65393,#65394,#65395,#65396,
#65397,#65398,#65399,#65400,#65401,#65402,#65403,#65404,#65405,#65406,#65407,
#65408,#65409,#65410,#65411,#65412,#65413,#65414,#65415),.UNSPECIFIED.,
 .F.,.F.,(4,3,3,3,3,3,3,3,3,3,3,3,3,3,3,3,3,3,3,3,3,3,3,3,3,3,3,3,3,3,3,
3,3,3,3,3,3,3,3,3,3,3,3,3,3,3,3,3,3,3,3,3,3,3,3,3,3,3,3,3,3,3,3,3,3,3,3,
3,3,3,4),(1.1173004083682,1.21032980834395,1.3072163767362,1.4000398708129,
1.49281995955612,1.58558508021891,1.6783636479266,1.77123897043941,1.8641715077765,
1.95724799133377,1.98542235548196,2.08087078878419,2.17618953906202,2.27140784073711,
2.3665583879355,2.46167490015914,2.55678364613916,2.65191088024338,2.74713937184165,
2.84242574410779,2.93785940901966,2.97813353322293,3.07359703316209,3.16893382142426,
3.26917268261672,3.36434619530356,3.45948972117081,3.55462950391444,3.64979177626171,
3.74505982279029,3.84038921166125,3.93586752489477,3.97084471096391,4.06602029899652,
4.16106424190066,4.25600618469319,4.35087925914523,4.44571772712217,4.54054821730625,
4.63539734391196,4.73034964786798,4.82536054310032,4.92052244082011,4.96355588870488,
5.05888749329321,5.15408932749402,5.24919080357482,5.3442251834698,5.43922599598654,
5.53421966847994,5.62923261450247,5.72434871738995,5.81952363603612,5.91484834628159,
5.95626706644586,6.05158819173318,6.14677979675512,6.24187130762467,6.33689615981954,
6.43188772174665,6.52687243390915,6.62187672325866,6.71698468340639,6.81215174233597,
6.90746910348022,6.94897824418683,7.05133621204183,7.1533540140597,7.25515818809801,
7.35665992559863,7.40048571532638),.UNSPECIFIED.);
#711=B_SPLINE_CURVE_WITH_KNOTS('',3,(#65417,#65418,#65419,#65420,#65421,
#65422,#65423,#65424,#65425,#65426,#65427,#65428,#65429,#65430,#65431,#65432,
#65433,#65434,#65435,#65436,#65437,#65438,#65439,#65440,#65441,#65442,#65443,
#65444,#65445,#65446,#65447,#65448,#65449,#65450,#65451,#65452,#65453,#65454,
#65455,#65456,#65457,#65458,#65459,#65460,#65461,#65462,#65463,#65464,#65465,
#65466,#65467,#65468,#65469,#65470,#65471,#65472,#65473,#65474,#65475,#65476,
#65477,#65478,#65479,#65480,#65481,#65482,#65483,#65484,#65485,#65486,#65487,
#65488,#65489,#65490,#65491,#65492,#65493,#65494,#65495,#65496,#65497,#65498,
#65499,#65500,#65501,#65502,#65503,#65504,#65505,#65506,#65507,#65508,#65509,
#65510,#65511,#65512,#65513,#65514,#65515,#65516,#65517,#65518,#65519,#65520,
#65521,#65522,#65523,#65524,#65525,#65526,#65527,#65528,#65529,#65530,#65531,
#65532,#65533,#65534,#65535,#65536,#65537,#65538,#65539,#65540,#65541,#65542,
#65543,#65544,#65545,#65546,#65547,#65548,#65549,#65550,#65551,#65552,#65553,
#65554,#65555,#65556,#65557,#65558,#65559,#65560,#65561,#65562,#65563,#65564,
#65565,#65566,#65567,#65568,#65569,#65570,#65571,#65572,#65573,#65574,#65575,
#65576,#65577,#65578,#65579,#65580,#65581,#65582,#65583,#65584,#65585,#65586,
#65587,#65588,#65589,#65590,#65591,#65592,#65593,#65594,#65595,#65596,#65597,
#65598,#65599,#65600,#65601,#65602,#65603,#65604,#65605,#65606,#65607,#65608,
#65609,#65610,#65611,#65612,#65613,#65614,#65615,#65616,#65617,#65618,#65619,
#65620,#65621,#65622,#65623,#65624,#65625,#65626,#65627),.UNSPECIFIED.,
 .F.,.F.,(4,3,3,3,3,3,3,3,3,3,3,3,3,3,3,3,3,3,3,3,3,3,3,3,3,3,3,3,3,3,3,
3,3,3,3,3,3,3,3,3,3,3,3,3,3,3,3,3,3,3,3,3,3,3,3,3,3,3,3,3,3,3,3,3,3,3,3,
3,3,3,4),(7.40048571554779,7.49824612985645,7.59608965728392,7.69411743523722,
7.79224606749592,7.89057934795509,7.94168942192781,8.03699764920788,8.13217600279553,
8.22725392955767,8.32226475962273,8.41724203232331,8.51221220555734,8.60720172346273,
8.7022946487693,8.79744650061537,8.89274853363321,8.93440059966879,9.02970523102217,
9.12487999259607,9.21995433644279,9.31496161266825,9.40993535119827,9.50490201456794,
9.59988805157463,9.69497756112813,9.79012602969033,9.8854247615887,9.92711177740977,
10.0224119143356,10.1175820941002,10.212651775755,10.3076542898582,10.4026232059893,
10.4975849926482,10.5925661045524,10.6876506453834,10.7827941131637,10.8780878423386,
10.9198229551507,11.015126647672,11.1103004319231,11.2053737615344,11.3003799727728,
11.3953526151215,11.4903181524017,11.5853030346704,11.680391352975,11.7755386076768,
11.870836102385,11.9125341328917,12.0078370228027,12.1030100004079,12.1980825205225,
12.2930879215015,12.3880597534642,12.4830244812746,12.5780085560348,12.6730960747126,
12.7682425331656,12.8635392443914,12.9052453106327,13.0025485246029,13.0963989586797,
13.1901630945498,13.2838688632371,13.3775441272426,13.4712489108769,13.5649722634797,
13.6587806403493,13.6836710223941),.UNSPECIFIED.);
#712=B_SPLINE_CURVE_WITH_KNOTS('',3,(#65629,#65630,#65631,#65632,#65633,
#65634,#65635,#65636,#65637,#65638,#65639,#65640,#65641,#65642,#65643,#65644,
#65645,#65646,#65647,#65648,#65649,#65650,#65651,#65652,#65653,#65654,#65655,
#65656,#65657,#65658,#65659,#65660,#65661,#65662,#65663,#65664,#65665,#65666,
#65667,#65668,#65669,#65670,#65671,#65672,#65673,#65674,#65675,#65676,#65677,
#65678,#65679,#65680,#65681,#65682,#65683,#65684,#65685,#65686,#65687,#65688,
#65689,#65690,#65691,#65692,#65693,#65694,#65695,#65696,#65697,#65698,#65699,
#65700,#65701,#65702,#65703,#65704,#65705,#65706,#65707,#65708,#65709,#65710,
#65711,#65712,#65713,#65714,#65715,#65716,#65717,#65718,#65719,#65720,#65721,
#65722,#65723,#65724,#65725,#65726,#65727,#65728,#65729,#65730,#65731,#65732,
#65733,#65734,#65735,#65736,#65737,#65738,#65739,#65740,#65741,#65742,#65743,
#65744,#65745,#65746,#65747,#65748,#65749,#65750,#65751,#65752,#65753,#65754,
#65755,#65756,#65757,#65758,#65759,#65760,#65761,#65762,#65763,#65764,#65765,
#65766,#65767,#65768,#65769,#65770,#65771,#65772,#65773,#65774,#65775,#65776,
#65777,#65778,#65779,#65780,#65781,#65782,#65783,#65784,#65785,#65786,#65787,
#65788,#65789,#65790,#65791,#65792,#65793,#65794,#65795,#65796,#65797,#65798,
#65799,#65800,#65801,#65802,#65803,#65804,#65805,#65806,#65807,#65808,#65809,
#65810,#65811,#65812,#65813,#65814,#65815,#65816,#65817,#65818,#65819,#65820,
#65821,#65822,#65823,#65824,#65825,#65826,#65827,#65828,#65829,#65830,#65831,
#65832,#65833,#65834,#65835,#65836),.UNSPECIFIED.,.F.,.F.,(4,3,3,3,3,3,
3,3,3,3,3,3,3,3,3,3,3,3,3,3,3,3,3,3,3,3,3,3,3,3,3,3,3,3,3,3,3,3,3,3,3,3,
3,3,3,3,3,3,3,3,3,3,3,3,3,3,3,3,3,3,3,3,3,3,3,3,3,3,3,4),(13.6836710227274,
13.8145638300528,13.8979564883737,13.9932593777273,14.0884323511339,14.1835048634302,
14.2785102512182,14.3734820666447,14.4684467745816,14.5634308261355,14.6585183166849,
14.7536647441496,14.8489614202729,14.8906676661147,14.9859704022949,15.0811432213058,
15.1762155782123,15.2712208097971,15.3661924685803,15.4611570196336,15.5561409142636,
15.6512282487803,15.7463745205009,15.8416710428038,15.8833788438556,15.9786815267226,
16.0738542910791,16.1689265920748,16.2639317661137,16.3589033663558,16.4538678579444,
16.5488516922565,16.6439389655255,16.7390851753785,16.8343816354455,16.8760900215966,
16.971392776919,17.0665656148329,17.1616379903769,17.2566432401223,17.3516149167606,
17.4465794853395,17.5415633971411,17.6366507481872,17.7317970360928,17.8270935738962,
17.8688011993376,17.9641039278211,18.0592767386331,18.1543490868526,18.249354309059,
18.3443259580365,18.4392904988676,18.5342743828697,18.6293617062065,18.7245079664151,
18.8198044768031,18.8615123770786,18.9568151010649,19.0519879072284,19.1470602506551,
19.2420654678741,19.337037111745,19.4320016473566,19.5269855260317,19.6220728439113,
19.7172190985804,19.8125156033542,19.8542235548195,19.966856329907),
 .UNSPECIFIED.);
#713=B_SPLINE_CURVE_WITH_KNOTS('',3,(#65838,#65839,#65840,#65841,#65842,
#65843,#65844,#65845,#65846,#65847),.UNSPECIFIED.,.F.,.F.,(4,1,1,1,1,1,
1,4),(19.9668647663903,20.8469347325605,21.8396459103015,22.8323570880425,
23.8250682657834,24.8177794435244,25.8104906212654,26.2500416370865),
 .UNSPECIFIED.);
#714=B_SPLINE_CURVE_WITH_KNOTS('',3,(#65849,#65850,#65851,#65852,#65853,
#65854,#65855,#65856,#65857,#65858),.UNSPECIFIED.,.F.,.F.,(4,1,1,1,1,1,
1,4),(26.2500416370865,26.8032017990064,27.7959129767474,28.7886241544883,
29.7813353322293,30.7740465099703,31.7667576877113,32.5332265095628),
 .UNSPECIFIED.);
#715=B_SPLINE_CURVE_WITH_KNOTS('',3,(#65860,#65861,#65862,#65863,#65864,
#65865,#65866,#65867,#65868,#65869,#65870,#65871,#65872,#65873,#65874,#65875,
#65876,#65877,#65878,#65879,#65880,#65881,#65882,#65883,#65884,#65885,#65886,
#65887,#65888,#65889,#65890,#65891,#65892,#65893,#65894,#65895,#65896,#65897,
#65898,#65899,#65900,#65901,#65902,#65903,#65904,#65905,#65906,#65907,#65908,
#65909,#65910,#65911,#65912,#65913,#65914,#65915,#65916,#65917,#65918,#65919,
#65920,#65921,#65922,#65923,#65924,#65925,#65926,#65927,#65928,#65929,#65930,
#65931,#65932,#65933,#65934,#65935,#65936,#65937,#65938,#65939,#65940,#65941,
#65942,#65943,#65944,#65945,#65946,#65947,#65948,#65949,#65950,#65951,#65952,
#65953,#65954,#65955,#65956,#65957,#65958,#65959,#65960,#65961,#65962,#65963,
#65964,#65965,#65966,#65967,#65968,#65969,#65970,#65971,#65972,#65973,#65974,
#65975,#65976,#65977,#65978,#65979,#65980,#65981,#65982,#65983,#65984,#65985,
#65986,#65987,#65988,#65989,#65990,#65991,#65992,#65993,#65994,#65995,#65996,
#65997,#65998,#65999,#66000,#66001,#66002,#66003,#66004,#66005,#66006,#66007,
#66008,#66009,#66010,#66011,#66012,#66013,#66014,#66015,#66016,#66017,#66018,
#66019,#66020,#66021,#66022,#66023,#66024,#66025,#66026,#66027,#66028,#66029,
#66030,#66031,#66032,#66033,#66034,#66035,#66036,#66037,#66038,#66039,#66040,
#66041,#66042,#66043,#66044,#66045,#66046,#66047,#66048,#66049,#66050,#66051,
#66052,#66053,#66054,#66055,#66056,#66057,#66058,#66059,#66060,#66061,#66062,
#66063,#66064,#66065,#66066,#66067),.UNSPECIFIED.,.F.,.F.,(4,3,3,3,3,3,
3,3,3,3,3,3,3,3,3,3,3,3,3,3,3,3,3,3,3,3,3,3,3,3,3,3,3,3,3,3,3,3,3,3,3,3,
3,3,3,3,3,3,3,3,3,3,3,3,3,3,3,3,3,3,3,3,3,3,3,3,3,3,3,4),(32.5332269442661,
32.6610063604515,32.7594688654522,32.8547715954818,32.9499444077968,33.0450167574743,
33.140021981065,33.2349936313803,33.329958173501,33.4249420587423,33.5200293832342,
33.6151756445514,33.7104721559659,33.7521800431932,33.8474827732234,33.9426555855391,
34.0377279352173,34.1327331588088,34.2277048091247,34.3226693512461,34.417653236488,
34.5127405609806,34.6078868222985,34.7031833337137,34.7448912209342,34.8401939509647,
34.9353667632806,35.030439112959,35.1254443365508,35.220415986867,35.3153805289887,
35.4103644142309,35.5054517387237,35.6005980000419,35.6958945114574,35.7376023986752,
35.8329051287053,35.9280779410209,36.0231502906989,36.1181555142903,36.2131271646062,
36.3080917067275,36.4030755919693,36.4981629164617,36.5933091777795,36.6886056891946,
36.7303135764161,36.8256163064463,36.920789118762,37.0158614684403,37.1108666920318,
37.2058383423478,37.3008028844693,37.3957867697112,37.4908740942038,37.5860203555218,
37.681316866937,37.7230247541571,37.8183274841874,37.9135002965031,38.0085726461813,
38.1035778697729,38.198549520089,38.2935140622104,38.3884979474524,38.483585271945,
38.5787315332631,38.6740280446784,38.7157359318981,38.8164122514457),
 .UNSPECIFIED.);
#716=B_SPLINE_CURVE_WITH_KNOTS('',3,(#66069,#66070,#66071,#66072,#66073,
#66074,#66075,#66076,#66077,#66078,#66079,#66080,#66081,#66082,#66083,#66084,
#66085,#66086,#66087,#66088,#66089,#66090,#66091,#66092,#66093,#66094,#66095,
#66096,#66097,#66098,#66099,#66100,#66101,#66102,#66103,#66104,#66105,#66106,
#66107,#66108,#66109,#66110,#66111,#66112,#66113,#66114,#66115,#66116,#66117,
#66118,#66119,#66120,#66121,#66122,#66123,#66124,#66125,#66126,#66127,#66128,
#66129,#66130,#66131,#66132,#66133,#66134,#66135,#66136,#66137,#66138,#66139,
#66140,#66141,#66142,#66143,#66144,#66145,#66146,#66147,#66148,#66149,#66150,
#66151,#66152,#66153,#66154,#66155,#66156,#66157,#66158,#66159,#66160,#66161,
#66162,#66163,#66164,#66165,#66166,#66167,#66168,#66169,#66170,#66171,#66172,
#66173,#66174,#66175,#66176,#66177,#66178,#66179,#66180,#66181,#66182,#66183,
#66184,#66185,#66186,#66187,#66188,#66189,#66190,#66191,#66192,#66193,#66194,
#66195,#66196,#66197,#66198,#66199,#66200,#66201,#66202,#66203,#66204,#66205,
#66206,#66207,#66208,#66209,#66210,#66211,#66212,#66213,#66214,#66215,#66216,
#66217,#66218,#66219,#66220,#66221,#66222,#66223,#66224,#66225,#66226,#66227,
#66228,#66229,#66230,#66231,#66232,#66233,#66234,#66235,#66236,#66237,#66238,
#66239,#66240,#66241,#66242,#66243,#66244,#66245,#66246,#66247,#66248,#66249,
#66250,#66251,#66252,#66253,#66254,#66255,#66256,#66257,#66258,#66259,#66260,
#66261,#66262,#66263,#66264,#66265,#66266,#66267,#66268,#66269,#66270,#66271,
#66272,#66273,#66274,#66275,#66276,#66277,#66278,#66279),.UNSPECIFIED.,
 .F.,.F.,(4,3,3,3,3,3,3,3,3,3,3,3,3,3,3,3,3,3,3,3,3,3,3,3,3,3,3,3,3,3,3,
3,3,3,3,3,3,3,3,3,3,3,3,3,3,3,3,3,3,3,3,3,3,3,3,3,3,3,3,3,3,3,3,3,3,3,3,
3,3,3,4),(38.8164122516606,38.9104710740768,39.0044137650042,39.0982701591792,
39.1920814649995,39.2858754296552,39.3796797770884,39.4735791389773,39.5675317808481,
39.6616329706406,39.7084471096391,39.8037498396694,39.8989226519849,39.993995001663,
40.0890002252545,40.1839718755706,40.2789364176921,40.3739203029341,40.4690076274267,
40.5641538887446,40.6594504001598,40.7011582873801,40.7964610174103,40.8916338297258,
40.9867061794043,41.0817114029959,41.1766830533118,41.2716475954333,41.3666314806755,
41.4617188051681,41.5568650664861,41.6521615779013,41.693869465121,41.7891721951512,
41.8843450074669,41.9794173571453,42.0744225807369,42.1693942310528,42.2643587731741,
42.3593426584158,42.4544299829083,42.5495762442263,42.6448727556416,42.686580642862,
42.7818833728922,42.8770561852078,42.972128534886,43.0671337584776,43.1621054087936,
43.2570699509149,43.3520538361566,43.4471411606493,43.542287421967,43.6375839333822,
43.679291820603,43.7745945506333,43.8697673629495,43.9648397126277,44.0598449362192,
44.1548165865352,44.2497811286566,44.3447650138982,44.4398523383908,44.5349985997084,
44.6302951111235,44.672002998344,44.778901555894,44.8823115123222,44.985464121309,
45.0882552304087,45.099597228544),.UNSPECIFIED.);
#717=B_SPLINE_CURVE_WITH_KNOTS('',3,(#66281,#66282,#66283,#66284,#66285,
#66286,#66287,#66288,#66289,#66290),.UNSPECIFIED.,.F.,.F.,(4,1,1,1,1,1,
1,4),(45.0995975586253,45.6647141760849,46.6574253538259,47.6501365315669,
48.6428477093079,49.6355588870488,50.6282700647898,51.3827828658049),
 .UNSPECIFIED.);
#718=B_SPLINE_CURVE_WITH_KNOTS('',3,(#66292,#66293,#66294,#66295,#66296,
#66297,#66298,#66299,#66300,#66301,#66302),.UNSPECIFIED.,.F.,.F.,(4,1,1,
1,1,1,1,1,4),(51.3827828658049,51.6209812425308,52.6136924202718,53.6064035980127,
54.5991147757537,55.5918259534947,56.5845371312357,57.5772483089767,57.6659681729845),
 .UNSPECIFIED.);
#719=B_SPLINE_CURVE_WITH_KNOTS('',3,(#66304,#66305,#66306,#66307,#66308,
#66309,#66310,#66311,#66312,#66313,#66314,#66315,#66316,#66317,#66318,#66319,
#66320,#66321,#66322,#66323,#66324,#66325,#66326,#66327,#66328,#66329,#66330,
#66331,#66332,#66333,#66334,#66335,#66336,#66337,#66338,#66339,#66340,#66341,
#66342,#66343,#66344,#66345,#66346,#66347,#66348,#66349,#66350,#66351,#66352,
#66353,#66354,#66355,#66356,#66357,#66358,#66359,#66360,#66361,#66362,#66363,
#66364,#66365,#66366,#66367,#66368,#66369,#66370,#66371,#66372,#66373,#66374,
#66375,#66376,#66377,#66378,#66379,#66380,#66381,#66382,#66383,#66384,#66385,
#66386,#66387,#66388,#66389,#66390,#66391,#66392,#66393,#66394,#66395,#66396,
#66397,#66398,#66399,#66400,#66401,#66402,#66403,#66404,#66405,#66406,#66407,
#66408,#66409,#66410,#66411,#66412,#66413,#66414,#66415,#66416,#66417,#66418,
#66419,#66420,#66421,#66422,#66423,#66424,#66425,#66426,#66427,#66428,#66429,
#66430,#66431,#66432,#66433,#66434,#66435,#66436,#66437,#66438,#66439,#66440,
#66441,#66442,#66443,#66444,#66445,#66446,#66447,#66448,#66449,#66450,#66451,
#66452,#66453,#66454,#66455,#66456,#66457,#66458,#66459,#66460,#66461,#66462,
#66463,#66464,#66465,#66466,#66467,#66468,#66469,#66470,#66471,#66472,#66473,
#66474,#66475,#66476,#66477,#66478,#66479,#66480,#66481,#66482,#66483,#66484,
#66485,#66486,#66487,#66488,#66489,#66490,#66491,#66492,#66493,#66494,#66495,
#66496,#66497,#66498,#66499,#66500,#66501,#66502,#66503,#66504,#66505,#66506,
#66507,#66508,#66509,#66510,#66511),.UNSPECIFIED.,.F.,.F.,(4,3,3,3,3,3,
3,3,3,3,3,3,3,3,3,3,3,3,3,3,3,3,3,3,3,3,3,3,3,3,3,3,3,3,3,3,3,3,3,3,3,3,
3,3,3,3,3,3,3,3,3,3,3,3,3,3,3,3,3,3,3,3,3,3,3,3,3,3,3,4),(57.6659681729845,
57.7601239022619,57.8541607955583,57.9481076140006,58.0420067651304,58.1358859245011,
58.229772741962,58.3237532139684,58.4177843761107,58.5119675653933,58.5699594867177,
58.665262216748,58.7604350290637,58.8555073787417,58.9505126023331,59.0454842526491,
59.1404487947705,59.2354326800123,59.330520004505,59.425666265823,59.5209627772383,
59.5626706644586,59.6579733944888,59.7531462068047,59.8482185564831,59.9432237800747,
60.0381954303908,60.133159972512,60.2281438577538,60.3232311822464,60.4183774435642,
60.5136739549794,60.5553818421996,60.6506845722298,60.7458573845455,60.8409297342235,
60.935934957815,61.0309066081311,61.1258711502524,61.2208550354948,61.3159423599874,
61.4110886213055,61.5063851327206,61.5480930199406,61.6433957499709,61.7385685622864,
61.833640911965,61.9286461355565,62.0236177858725,62.118582327994,62.2135662132359,
62.3086535377286,62.4037997990464,62.4990963104617,62.5408041976816,62.6361069277118,
62.7312797400277,62.826352089706,62.9213573132975,63.0163289636135,63.111293505735,
63.206277390977,63.3013647154696,63.3965109767875,63.4918074882025,63.5335153754225,
63.6379533631389,63.7421227640998,63.8458245660772,63.9491534799855),
 .UNSPECIFIED.);
#720=B_SPLINE_CURVE_WITH_KNOTS('',3,(#66513,#66514,#66515,#66516,#66517,
#66518,#66519,#66520,#66521,#66522,#66523,#66524,#66525,#66526,#66527,#66528,
#66529,#66530,#66531,#66532,#66533,#66534,#66535,#66536,#66537,#66538,#66539,
#66540,#66541,#66542,#66543,#66544,#66545,#66546,#66547,#66548,#66549,#66550,
#66551,#66552,#66553,#66554,#66555,#66556,#66557,#66558,#66559,#66560,#66561,
#66562,#66563,#66564,#66565,#66566,#66567,#66568,#66569,#66570,#66571,#66572,
#66573,#66574,#66575,#66576,#66577,#66578,#66579,#66580,#66581,#66582,#66583,
#66584,#66585,#66586,#66587,#66588,#66589,#66590,#66591,#66592,#66593,#66594,
#66595,#66596,#66597,#66598,#66599,#66600,#66601,#66602,#66603,#66604,#66605,
#66606,#66607,#66608,#66609,#66610,#66611,#66612,#66613,#66614,#66615,#66616,
#66617,#66618,#66619,#66620,#66621,#66622,#66623,#66624,#66625,#66626,#66627,
#66628,#66629,#66630,#66631,#66632,#66633,#66634,#66635,#66636,#66637,#66638,
#66639,#66640,#66641,#66642,#66643,#66644,#66645,#66646,#66647,#66648,#66649,
#66650,#66651,#66652,#66653,#66654,#66655,#66656,#66657,#66658,#66659,#66660,
#66661,#66662,#66663,#66664,#66665,#66666,#66667,#66668,#66669,#66670,#66671,
#66672,#66673,#66674,#66675,#66676,#66677,#66678,#66679,#66680,#66681,#66682,
#66683,#66684,#66685,#66686,#66687,#66688,#66689,#66690,#66691,#66692,#66693,
#66694,#66695,#66696,#66697,#66698,#66699,#66700,#66701,#66702,#66703,#66704,
#66705,#66706,#66707,#66708,#66709,#66710,#66711,#66712,#66713,#66714,#66715,
#66716,#66717,#66718,#66719,#66720),.UNSPECIFIED.,.F.,.F.,(4,3,3,3,3,3,
3,3,3,3,3,3,3,3,3,3,3,3,3,3,3,3,3,3,3,3,3,3,3,3,3,3,3,3,3,3,3,3,3,3,3,3,
3,3,3,3,3,3,3,3,3,3,3,3,3,3,3,3,3,3,3,3,3,3,3,3,3,3,3,4),(63.9491534801641,
64.0458634592205,64.1426193688178,64.2395234686266,64.3365021408146,64.4336819362929,
64.5262265531635,64.6215292831939,64.7167020955097,64.811774445188,64.9067796687797,
65.0017513190958,65.0967158612177,65.1916997464599,65.2867870709527,65.3819333322708,
65.4772298436862,65.5189377309045,65.6142404609347,65.7094132732503,65.8044856229284,
65.8994908465199,65.9944624968358,66.0894270389571,66.1844109241988,66.2794982486914,
66.3746445100095,66.4699410214246,66.5116489086455,66.6069516386749,66.70212445099,
66.797196800667,66.8922020242578,66.987173674573,67.0821382166934,67.1771221019346,
67.2722094264265,67.3673556877436,67.4626521991581,67.5043600863864,67.5996628164186,
67.694835628736,67.789907978416,67.8849132020092,67.979884852327,68.07484939445,
68.1698332796939,68.2649206041882,68.3600668655079,68.4553633769248,68.4970712641274,
68.5923739941569,68.6875468064717,68.7826191561489,68.8776243797395,68.9725960300548,
69.0675605721757,69.1625444574167,69.2576317819083,69.3527780432254,69.4480745546398,
69.4897824418684,69.5839866200001,69.6780732484959,69.7720701604336,69.8660050891807,
69.9599324042788,70.0538503457583,70.1478411652905,70.2323387873437),
 .UNSPECIFIED.);
#721=B_SPLINE_CURVE_WITH_KNOTS('',3,(#66722,#66723,#66724,#66725,#66726,
#66727,#66728,#66729,#66730,#66731,#66732),.UNSPECIFIED.,.F.,.F.,(4,1,1,
1,1,1,1,1,4),(70.2323404852416,70.4824936196094,71.4752047973503,72.4679159750913,
73.4606271528323,74.4533383305733,75.4460495083142,76.4387606860552,76.5155240945233),
 .UNSPECIFIED.);
#722=B_SPLINE_CURVE_WITH_KNOTS('',3,(#66734,#66735,#66736,#66737,#66738,
#66739,#66740,#66741,#66742,#66743),.UNSPECIFIED.,.F.,.F.,(4,1,1,1,1,1,
1,4),(76.5155240945233,77.4314718637962,78.4241830415372,79.4168942192782,
80.4096053970191,81.4023165747601,82.3950277525011,82.7987030501078),
 .UNSPECIFIED.);
#723=B_SPLINE_CURVE_WITH_KNOTS('',3,(#66745,#66746,#66747,#66748,#66749,
#66750,#66751,#66752,#66753,#66754,#66755,#66756,#66757,#66758,#66759,#66760,
#66761,#66762,#66763,#66764,#66765,#66766,#66767,#66768,#66769,#66770,#66771,
#66772,#66773,#66774,#66775,#66776,#66777,#66778,#66779,#66780,#66781,#66782,
#66783,#66784,#66785,#66786,#66787,#66788,#66789,#66790,#66791,#66792,#66793,
#66794,#66795,#66796,#66797,#66798,#66799,#66800,#66801,#66802,#66803,#66804,
#66805,#66806,#66807,#66808,#66809,#66810,#66811,#66812,#66813,#66814,#66815,
#66816,#66817,#66818,#66819,#66820,#66821,#66822,#66823,#66824,#66825,#66826,
#66827,#66828,#66829,#66830,#66831,#66832,#66833,#66834,#66835,#66836,#66837,
#66838,#66839,#66840,#66841,#66842,#66843,#66844,#66845,#66846,#66847,#66848,
#66849,#66850,#66851,#66852,#66853,#66854,#66855,#66856,#66857,#66858,#66859,
#66860,#66861,#66862,#66863,#66864,#66865,#66866,#66867,#66868,#66869,#66870,
#66871,#66872,#66873,#66874,#66875,#66876,#66877,#66878,#66879,#66880,#66881,
#66882,#66883,#66884,#66885,#66886,#66887,#66888,#66889,#66890,#66891,#66892,
#66893,#66894,#66895,#66896,#66897,#66898,#66899,#66900,#66901,#66902,#66903,
#66904,#66905,#66906,#66907,#66908,#66909,#66910,#66911,#66912,#66913,#66914,
#66915,#66916,#66917,#66918,#66919,#66920,#66921,#66922,#66923,#66924,#66925,
#66926,#66927,#66928,#66929,#66930,#66931,#66932,#66933,#66934,#66935,#66936,
#66937,#66938,#66939,#66940,#66941,#66942,#66943,#66944,#66945,#66946,#66947,
#66948,#66949,#66950,#66951,#66952),.UNSPECIFIED.,.F.,.F.,(4,3,3,3,3,3,
3,3,3,3,3,3,3,3,3,3,3,3,3,3,3,3,3,3,3,3,3,3,3,3,3,3,3,3,3,3,3,3,3,3,3,3,
3,3,3,3,3,3,3,3,3,3,3,3,3,3,3,3,3,3,3,3,3,3,3,3,3,3,3,4),(82.7987094017029,
82.895106815508,82.9915395652103,83.0905894064683,83.1872287620549,83.2874838461485,
83.3877389302421,83.4830416091242,83.5782143703192,83.6732866689735,83.7682918418933,
83.863263441777,83.9582279337673,84.0532117692414,84.148299044809,84.2434452576144,
84.338741721605,84.380450107983,84.4757528488978,84.5709256716648,84.6659980313535,
84.7610032642682,84.8559749234772,84.9509394740533,85.0459233673026,85.1410106990881,
85.2361569673007,85.3314534849416,85.373161285724,85.468464179738,85.5636371568421,
85.6587096718769,85.7537150609738,85.8486868768196,85.9436515842866,86.0386356344819,
86.1337231223428,86.2288695463545,86.324166217889,86.365872463465,86.4611748113714,
86.5563472414657,86.6514192093459,86.7464240533369,86.841395325572,86.9363594915972,
87.031343003194,87.126429959959,87.2215758564116,87.3168720107783,87.358583641206,
87.4538865705107,87.5490595793686,87.6441321226302,87.7391375346734,87.8341093701794,
87.9290740940189,88.0240581572941,88.1191456532476,88.2142920825123,88.3095887549497,
88.351294818947,88.4456074585947,88.5398015981657,88.6339049701896,88.7279452082351,
88.8219735339946,88.9159914878525,89.0100736649993,89.0818947088825),
 .UNSPECIFIED.);
#724=B_SPLINE_CURVE_WITH_KNOTS('',3,(#66954,#66955,#66956,#66957,#66958,
#66959,#66960,#66961,#66962,#66963,#66964,#66965,#66966,#66967,#66968,#66969,
#66970,#66971,#66972,#66973,#66974,#66975,#66976,#66977,#66978,#66979,#66980,
#66981,#66982,#66983,#66984,#66985,#66986,#66987,#66988,#66989,#66990,#66991,
#66992,#66993,#66994,#66995,#66996,#66997,#66998,#66999,#67000,#67001,#67002,
#67003,#67004,#67005,#67006,#67007,#67008,#67009,#67010,#67011,#67012,#67013,
#67014,#67015,#67016,#67017,#67018,#67019,#67020,#67021,#67022,#67023,#67024,
#67025,#67026,#67027,#67028,#67029,#67030,#67031,#67032,#67033,#67034,#67035,
#67036,#67037,#67038,#67039,#67040,#67041,#67042,#67043,#67044,#67045,#67046,
#67047,#67048,#67049,#67050,#67051,#67052,#67053,#67054,#67055,#67056,#67057,
#67058,#67059,#67060,#67061,#67062,#67063,#67064,#67065,#67066,#67067,#67068,
#67069,#67070,#67071,#67072,#67073,#67074,#67075,#67076,#67077,#67078,#67079,
#67080,#67081,#67082,#67083,#67084,#67085,#67086,#67087,#67088,#67089,#67090,
#67091,#67092,#67093,#67094,#67095,#67096,#67097,#67098,#67099,#67100,#67101,
#67102,#67103,#67104,#67105,#67106,#67107,#67108,#67109,#67110,#67111,#67112,
#67113,#67114,#67115,#67116,#67117,#67118,#67119,#67120,#67121,#67122,#67123,
#67124,#67125,#67126,#67127,#67128,#67129,#67130,#67131,#67132,#67133,#67134,
#67135,#67136,#67137),.UNSPECIFIED.,.F.,.F.,(4,3,3,3,3,3,3,3,3,3,3,3,3,
3,3,3,3,3,3,3,3,3,3,3,3,3,3,3,3,3,3,3,3,3,3,3,3,3,3,3,3,3,3,3,3,3,3,3,3,
3,3,3,3,3,3,3,3,3,3,3,3,4),(89.0818947090523,89.2010772987298,89.3225086931315,
89.3440059966879,89.4393059557034,89.5344759943235,89.6295455714376,89.72454803557,
89.819516935694,89.9144787402817,90.0094599040507,90.1045445475032,90.1996881470965,
90.2949820514435,90.3367171744289,90.4320221177038,90.5271971267366,90.622271653863,
90.7172790176911,90.8122527842734,90.9072194161947,91.0022053622507,91.0972946918649,
91.1924429293055,91.287741354068,91.3294283521699,91.4247365779264,91.5199149303054,
91.6149928561725,91.7100036858097,91.8049809583734,91.899951131761,91.9949406501105,
92.0900335762961,92.1851854292711,92.2804874637891,92.3221395299109,92.4174227169089,
92.5125759541894,92.607628723862,92.702614440878,92.7975666381309,92.8925118047009,
92.9874764159754,93.0825447346589,93.1776721164449,93.2729501198545,93.3148507076518,
93.4101742137088,93.505367707397,93.6004606169913,93.6954861375727,93.7904779132753,
93.8854623849804,93.9804659796295,94.0755725658572,94.1707378601395,94.266052876599,
94.3075618853928,94.4222874520932,94.5356827162139,94.6122043555102),
 .UNSPECIFIED.);
#725=B_SPLINE_CURVE_WITH_KNOTS('',3,(#67141,#67142,#67143,#67144,#67145,
#67146,#67147,#67148,#67149,#67150,#67151,#67152,#67153,#67154,#67155,#67156,
#67157,#67158,#67159,#67160,#67161,#67162,#67163,#67164,#67165,#67166,#67167,
#67168,#67169,#67170,#67171,#67172,#67173,#67174,#67175,#67176,#67177,#67178,
#67179,#67180,#67181,#67182,#67183,#67184,#67185,#67186,#67187,#67188,#67189,
#67190,#67191,#67192,#67193,#67194,#67195,#67196,#67197,#67198,#67199,#67200,
#67201,#67202,#67203,#67204,#67205,#67206,#67207,#67208,#67209,#67210,#67211,
#67212,#67213,#67214,#67215,#67216,#67217,#67218,#67219,#67220,#67221,#67222,
#67223,#67224,#67225,#67226,#67227,#67228,#67229,#67230,#67231,#67232,#67233,
#67234,#67235,#67236,#67237,#67238,#67239,#67240,#67241,#67242,#67243,#67244,
#67245,#67246,#67247,#67248,#67249,#67250,#67251,#67252,#67253,#67254,#67255,
#67256,#67257,#67258,#67259,#67260,#67261,#67262,#67263,#67264,#67265,#67266,
#67267,#67268,#67269,#67270,#67271,#67272,#67273,#67274,#67275,#67276,#67277,
#67278,#67279,#67280,#67281,#67282,#67283,#67284,#67285,#67286,#67287,#67288,
#67289,#67290,#67291,#67292,#67293,#67294),.UNSPECIFIED.,.F.,.F.,(4,3,3,
3,3,3,3,3,3,3,3,3,3,3,3,3,3,3,3,3,3,3,3,3,3,3,3,3,3,3,3,3,3,3,3,3,3,3,3,
3,3,3,3,3,3,3,3,3,3,3,3,4),(-96.6808311787084,-96.5809449266008,-96.480745285623,
-96.3803817017057,-96.2797248066616,-96.2114495491126,-96.1159900242025,
-96.0206599529141,-95.9205248257004,-95.8253649156292,-95.730237536908,
-95.6351164381511,-95.5399753811037,-95.4447324428179,-95.3494303233826,
-95.2539827866144,-95.2195789352043,-95.1241060636225,-95.0287597025951,
-94.9286282799327,-94.8334447617397,-94.7382911316415,-94.6431411596734,
-94.5479686267728,-94.452690465454,-94.357350914987,-94.2618629298127,-94.2277083212959,
-94.1325225818946,-94.03746828344,-93.9425157966575,-93.8476319848257,-93.7527826436286,
-93.6579411577424,-93.5630809262139,-93.4681176414075,-93.3730956835252,
-93.2779232583095,-93.2358377073875,-93.140495698385,-93.0452832460174,
-92.9501709549859,-92.8551255574552,-92.7601135863588,-92.665108628832,
-92.5700842857123,-92.4749569070836,-92.3797706305332,-92.2844350940134,
-92.2439670934791,-92.1042237372444,-92.0575247206449),.UNSPECIFIED.);
#726=B_SPLINE_CURVE_WITH_KNOTS('',3,(#67296,#67297,#67298,#67299,#67300,
#67301,#67302,#67303,#67304,#67305),.UNSPECIFIED.,.F.,.F.,(4,1,1,1,1,1,
1,4),(-92.0575206890591,-91.2520964795708,-90.2602258656624,-89.268355251754,
-88.2764846378456,-87.2846140239373,-86.2927434100289,-85.7743394134653),
 .UNSPECIFIED.);
#727=B_SPLINE_CURVE_WITH_KNOTS('',3,(#67307,#67308,#67309,#67310,#67311,
#67312,#67313,#67314,#67315,#67316,#67317,#67318,#67319,#67320,#67321,#67322,
#67323,#67324,#67325,#67326,#67327,#67328,#67329,#67330,#67331,#67332,#67333,
#67334,#67335,#67336,#67337,#67338,#67339,#67340,#67341,#67342,#67343,#67344,
#67345,#67346,#67347,#67348,#67349,#67350,#67351,#67352,#67353,#67354,#67355,
#67356,#67357,#67358,#67359,#67360,#67361,#67362,#67363,#67364,#67365,#67366,
#67367,#67368,#67369,#67370,#67371,#67372,#67373,#67374,#67375,#67376,#67377,
#67378,#67379,#67380,#67381,#67382,#67383,#67384,#67385,#67386,#67387,#67388,
#67389,#67390,#67391,#67392,#67393,#67394,#67395,#67396,#67397,#67398,#67399,
#67400,#67401,#67402,#67403,#67404,#67405,#67406,#67407,#67408,#67409,#67410,
#67411,#67412,#67413,#67414,#67415,#67416,#67417,#67418,#67419,#67420,#67421,
#67422,#67423,#67424,#67425,#67426,#67427,#67428,#67429,#67430,#67431,#67432,
#67433,#67434,#67435,#67436,#67437,#67438,#67439,#67440,#67441,#67442,#67443,
#67444,#67445,#67446,#67447,#67448,#67449,#67450,#67451,#67452,#67453,#67454,
#67455,#67456,#67457,#67458,#67459,#67460,#67461,#67462,#67463,#67464,#67465,
#67466,#67467,#67468,#67469,#67470,#67471,#67472,#67473,#67474,#67475,#67476,
#67477,#67478,#67479,#67480,#67481,#67482,#67483,#67484,#67485,#67486,#67487,
#67488,#67489,#67490,#67491,#67492,#67493,#67494,#67495,#67496,#67497,#67498,
#67499,#67500,#67501,#67502,#67503,#67504,#67505,#67506,#67507,#67508,#67509,
#67510,#67511,#67512,#67513,#67514),.UNSPECIFIED.,.F.,.F.,(4,3,3,3,3,3,
3,3,3,3,3,3,3,3,3,3,3,3,3,3,3,3,3,3,3,3,3,3,3,3,3,3,3,3,3,3,3,3,3,3,3,3,
3,3,3,3,3,3,3,3,3,3,3,3,3,3,3,3,3,3,3,3,3,3,3,3,3,3,3,4),(-85.7743392960028,
-85.6739374733394,-85.5732262312564,-85.472355561626,-85.371202429377,-85.3008727961205,
-85.2055602958256,-85.1103775106317,-85.0152950012911,-84.9202794272017,
-84.8252972923522,-84.7303221451598,-84.635327547713,-84.5402296359904,
-84.4450727078759,-84.3497660603351,-84.3090021822121,-84.2136891674468,
-84.1185058602982,-84.023422822308,-83.9284067118599,-83.8334240360757,
-83.7384483440533,-83.6434531985585,-83.5483547372275,-83.4531972578332,
-83.3578900616534,-83.3171315683037,-83.2218187096071,-83.1266355598024,
-83.0315526801975,-82.9365367290044,-82.8415542129483,-82.7465786809226,
-82.6515836954888,-82.5564853933454,-82.4613280728628,-82.3660210336682,
-82.3252609543953,-82.2299481472722,-82.1347650503614,-82.0396822248883,
-81.9446663294413,-81.8496838701141,-81.754708395731,-81.6597134687846,
-81.5646152260565,-81.4694579656052,-81.3741509868217,-81.333390340487,
-81.2380774610597,-81.1428942907392,-81.0478113908618,-80.9527954198476,
-80.8578128842607,-80.7628373330209,-80.6678423287162,-80.5727440083377,
-80.4775866699588,-80.382279613558,-80.3415197265786,-80.2475783950597,
-80.1530253589629,-80.0593194743372,-79.9656701712186,-79.8720495386157,
-79.7768256805332,-79.6831364418205,-79.5871452740531,-79.4911541062857),
 .UNSPECIFIED.);
#728=B_SPLINE_CURVE_WITH_KNOTS('',3,(#67516,#67517,#67518,#67519,#67520,
#67521,#67522,#67523,#67524,#67525,#67526),.UNSPECIFIED.,.F.,.F.,(4,1,1,
1,1,1,1,1,4),(-79.4911541062857,-79.3496491126702,-78.3577784987618,-77.3659078848535,
-76.3740372709451,-75.3821666570367,-74.3902960431283,-73.3984254292199,
-73.2079687991062),.UNSPECIFIED.);
#729=B_SPLINE_CURVE_WITH_KNOTS('',3,(#67528,#67529,#67530,#67531,#67532,
#67533,#67534,#67535,#67536,#67537,#67538,#67539,#67540,#67541,#67542,#67543,
#67544,#67545,#67546,#67547,#67548,#67549,#67550,#67551,#67552,#67553,#67554,
#67555,#67556,#67557,#67558,#67559,#67560,#67561,#67562,#67563,#67564,#67565,
#67566,#67567,#67568,#67569,#67570,#67571,#67572,#67573,#67574,#67575,#67576,
#67577,#67578,#67579,#67580,#67581,#67582,#67583,#67584,#67585,#67586,#67587,
#67588,#67589,#67590,#67591,#67592,#67593,#67594,#67595,#67596,#67597,#67598,
#67599,#67600,#67601,#67602,#67603,#67604,#67605,#67606,#67607,#67608,#67609,
#67610,#67611,#67612,#67613,#67614,#67615,#67616,#67617,#67618,#67619,#67620,
#67621,#67622,#67623,#67624,#67625,#67626,#67627,#67628,#67629,#67630,#67631,
#67632,#67633,#67634,#67635,#67636,#67637,#67638,#67639,#67640,#67641,#67642,
#67643,#67644,#67645,#67646,#67647,#67648,#67649,#67650,#67651,#67652,#67653,
#67654,#67655,#67656,#67657,#67658,#67659,#67660,#67661,#67662,#67663,#67664,
#67665,#67666,#67667,#67668,#67669,#67670,#67671,#67672,#67673,#67674,#67675,
#67676,#67677,#67678,#67679,#67680,#67681,#67682,#67683,#67684,#67685,#67686,
#67687,#67688,#67689,#67690,#67691,#67692,#67693,#67694,#67695,#67696,#67697,
#67698,#67699,#67700,#67701,#67702,#67703,#67704,#67705,#67706,#67707,#67708,
#67709,#67710,#67711,#67712,#67713,#67714,#67715,#67716,#67717,#67718,#67719,
#67720,#67721,#67722,#67723,#67724,#67725,#67726,#67727,#67728,#67729,#67730,
#67731,#67732,#67733,#67734,#67735,#67736,#67737,#67738),.UNSPECIFIED.,
 .F.,.F.,(4,3,3,3,3,3,3,3,3,3,3,3,3,3,3,3,3,3,3,3,3,3,3,3,3,3,3,3,3,3,3,
3,3,3,3,3,3,3,3,3,3,3,3,3,3,3,3,3,3,3,3,3,3,3,3,3,3,3,3,3,3,3,3,3,3,3,3,
3,3,3,4),(-73.2079687991062,-73.1141930383266,-73.0205086469885,-72.9268725476114,
-72.8332568363415,-72.7396336360451,-72.6459179993694,-72.5521513863378,
-72.4582359235161,-72.4065548153116,-72.3112419613016,-72.2160588167084,
-72.1209759428295,-72.0259599981062,-71.9309774889811,-71.8360019643406,
-71.7410069867394,-71.6459086930605,-71.5507513814166,-71.4554443515525,
-71.4146842014032,-71.3193713475026,-71.2241882030198,-71.1291053292529,
-71.0340893846429,-70.9391068756322,-70.8441313511065,-70.7491363736211,
-70.6540380800576,-70.5588807685294,-70.4635737387803,-70.4228135874948,
-70.3275007335772,-70.2323175890775,-70.1372347152933,-70.0422187706665,
-69.9472362616387,-69.8522607370961,-69.7572657595937,-69.662167466014,
-69.5670101544696,-69.4717031247048,-69.4309429735864,-69.3356301196485,
-69.2404469751282,-69.145364101323,-69.0503481566748,-68.9553656476253,
-68.8603901230612,-68.7653951455369,-68.670296851935,-68.5751395403683,
-68.4798325105811,-68.4390723596781,-68.3437595057564,-68.2485763612523,
-68.1534934874637,-68.0584775428324,-67.9634950338001,-67.8685195092529,
-67.7735245317458,-67.678426238161,-67.5832689266113,-67.4879618968412,
-67.4472017457697,-67.3481553896538,-67.249282246638,-67.1506135548848,
-67.0520677119532,-66.9536573933733,-66.9247834919266),.UNSPECIFIED.);
#730=B_SPLINE_CURVE_WITH_KNOTS('',3,(#67740,#67741,#67742,#67743,#67744,
#67745,#67746,#67747,#67748,#67749,#67750,#67751,#67752,#67753,#67754,#67755,
#67756,#67757,#67758,#67759,#67760,#67761,#67762,#67763,#67764,#67765,#67766,
#67767,#67768,#67769,#67770,#67771,#67772,#67773,#67774,#67775,#67776,#67777,
#67778,#67779,#67780,#67781,#67782,#67783,#67784,#67785,#67786,#67787,#67788,
#67789,#67790,#67791,#67792,#67793,#67794,#67795,#67796,#67797,#67798,#67799,
#67800,#67801,#67802,#67803,#67804,#67805,#67806,#67807,#67808,#67809,#67810,
#67811,#67812,#67813,#67814,#67815,#67816,#67817,#67818,#67819,#67820,#67821,
#67822,#67823,#67824,#67825,#67826,#67827,#67828,#67829,#67830,#67831,#67832,
#67833,#67834,#67835,#67836,#67837,#67838,#67839,#67840,#67841,#67842,#67843,
#67844,#67845,#67846,#67847,#67848,#67849,#67850,#67851,#67852,#67853,#67854,
#67855,#67856,#67857,#67858,#67859,#67860,#67861,#67862,#67863,#67864,#67865,
#67866,#67867,#67868,#67869,#67870,#67871,#67872,#67873,#67874,#67875,#67876,
#67877,#67878,#67879,#67880,#67881,#67882,#67883,#67884,#67885,#67886,#67887,
#67888,#67889,#67890,#67891,#67892,#67893,#67894,#67895,#67896,#67897,#67898,
#67899,#67900,#67901,#67902,#67903,#67904,#67905,#67906,#67907,#67908,#67909,
#67910,#67911,#67912,#67913,#67914,#67915,#67916,#67917,#67918,#67919,#67920,
#67921,#67922,#67923,#67924,#67925,#67926,#67927,#67928,#67929,#67930,#67931,
#67932,#67933,#67934,#67935,#67936,#67937,#67938,#67939,#67940,#67941,#67942,
#67943,#67944,#67945,#67946,#67947),.UNSPECIFIED.,.F.,.F.,(4,3,3,3,3,3,
3,3,3,3,3,3,3,3,3,3,3,3,3,3,3,3,3,3,3,3,3,3,3,3,3,3,3,3,3,3,3,3,3,3,3,3,
3,3,3,3,3,3,3,3,3,3,3,3,3,3,3,3,3,3,3,3,3,3,3,3,3,3,3,4),(-66.9247834916582,
-66.8241972479502,-66.7232917051859,-66.6222208880497,-66.5208647849073,
-66.4553311318613,-66.3600182779336,-66.2648351334237,-66.1697522596294,
-66.0747363149919,-65.9797538059533,-65.8847782813999,-65.7897833038863,
-65.6946850102952,-65.5995276987392,-65.5042206689629,-65.4634605179529,
-65.3681476640275,-65.2729645195198,-65.1778816457278,-65.0828657010926,
-64.9878831920564,-64.8929076675055,-64.7979126899944,-64.7028143964057,
-64.6076570848523,-64.5123500550785,-64.4715899040445,-64.3762770501184,
-64.2810939056101,-64.1860110318173,-64.0909950871814,-63.9960125781445,
-63.9010370535929,-63.8060420760811,-63.7109437824917,-63.6157864709376,
-63.5204794411631,-63.4797192901362,-63.3844064362099,-63.2892232917013,
-63.1941404179083,-63.0991244732721,-63.004141964235,-62.9091664396831,
-62.8141714621711,-62.7190731685814,-62.623915857027,-62.5286088272522,
-62.4878486762278,-62.3925358223018,-62.2973526777935,-62.2022698040008,
-62.107253859365,-62.0122713503281,-61.9172958257766,-61.8223008482649,
-61.7272025546755,-61.6320452431215,-61.5367382133469,-61.4959780623194,
-61.4020258640311,-61.3069724041206,-61.2132558463476,-61.1195956834216,
-61.0259640136845,-60.9298725564501,-60.8361708089317,-60.7388844968393,
-60.641598184747),.UNSPECIFIED.);
#731=B_SPLINE_CURVE_WITH_KNOTS('',3,(#67949,#67950,#67951,#67952,#67953,
#67954,#67955,#67956,#67957,#67958,#67959),.UNSPECIFIED.,.F.,.F.,(4,1,1,
1,1,1,1,1,4),(-60.641598184747,-60.5041074484111,-59.5122368345027,-58.5203662205943,
-57.5284956066859,-56.5366249927775,-55.5447543788692,-54.5528837649608,
-54.3584128775674),.UNSPECIFIED.);
#732=B_SPLINE_CURVE_WITH_KNOTS('',3,(#67961,#67962,#67963,#67964,#67965,
#67966,#67967,#67968,#67969,#67970,#67971,#67972,#67973,#67974,#67975,#67976,
#67977,#67978,#67979,#67980,#67981,#67982,#67983,#67984,#67985,#67986,#67987,
#67988,#67989,#67990,#67991,#67992,#67993,#67994,#67995,#67996,#67997,#67998,
#67999,#68000,#68001,#68002,#68003,#68004,#68005,#68006,#68007,#68008,#68009,
#68010,#68011,#68012,#68013,#68014,#68015,#68016,#68017,#68018,#68019,#68020,
#68021,#68022,#68023,#68024,#68025,#68026,#68027,#68028,#68029,#68030,#68031,
#68032,#68033,#68034,#68035,#68036,#68037,#68038,#68039,#68040,#68041,#68042,
#68043,#68044,#68045,#68046,#68047,#68048,#68049,#68050,#68051,#68052,#68053,
#68054,#68055,#68056,#68057,#68058,#68059,#68060,#68061,#68062,#68063,#68064,
#68065,#68066,#68067,#68068,#68069,#68070,#68071,#68072,#68073,#68074,#68075,
#68076,#68077,#68078,#68079,#68080,#68081,#68082,#68083,#68084,#68085,#68086,
#68087,#68088,#68089,#68090,#68091,#68092,#68093,#68094,#68095,#68096,#68097,
#68098,#68099,#68100,#68101,#68102,#68103,#68104,#68105,#68106,#68107,#68108,
#68109,#68110,#68111,#68112,#68113,#68114,#68115,#68116,#68117,#68118,#68119,
#68120,#68121,#68122,#68123,#68124,#68125,#68126,#68127,#68128,#68129,#68130,
#68131,#68132,#68133,#68134,#68135,#68136,#68137,#68138,#68139,#68140,#68141,
#68142,#68143,#68144,#68145,#68146,#68147,#68148,#68149,#68150,#68151,#68152,
#68153,#68154,#68155,#68156,#68157,#68158,#68159,#68160,#68161,#68162,#68163,
#68164,#68165,#68166,#68167,#68168,#68169,#68170,#68171),.UNSPECIFIED.,
 .F.,.F.,(4,3,3,3,3,3,3,3,3,3,3,3,3,3,3,3,3,3,3,3,3,3,3,3,3,3,3,3,3,3,3,
3,3,3,3,3,3,3,3,3,3,3,3,3,3,3,3,3,3,3,3,3,3,3,3,3,3,3,3,3,3,3,3,3,3,3,3,
3,3,3,4),(-54.3584128775674,-54.2646323366795,-54.1709411722708,-54.0772969876914,
-53.9836718890636,-53.8900380078539,-53.7963108600296,-53.7025315890191,
-53.6086045466861,-53.5610131510524,-53.4657002971262,-53.3705171526179,
-53.2754342788251,-53.1804183341892,-53.0854358251522,-52.9904603006004,
-52.8954653230883,-52.8003670294989,-52.7052097179446,-52.60990268817,-52.569142537144,
-52.4738296832179,-52.3786465387095,-52.2835636649166,-52.1885477202807,
-52.0935652112438,-51.9985896866921,-51.9035947091802,-51.8084964155908,
-51.7133391040365,-51.6180320742619,-51.5772719232356,-51.4819590693095,
-51.3867759248012,-51.2916930510088,-51.1966771063729,-51.101694597336,
-51.0067190727841,-50.9117240952724,-50.8166258016831,-50.7214684901288,
-50.6261614603543,-50.5854013093273,-50.4900884554012,-50.394905310893,
-50.2998224371,-50.2048064924641,-50.1098239834272,-50.0148484588757,-49.9198534813636,
-49.8247551877742,-49.7295978762199,-49.6342908464453,-49.5935306954189,
-49.4982178414929,-49.4030346969844,-49.3079518231912,-49.2129358785552,
-49.1179533695183,-49.0229778449664,-48.9279828674541,-48.8328845738646,
-48.7377272623104,-48.6424202325358,-48.6016600815105,-48.5027680424292,
-48.4040468426938,-48.3055256886538,-48.2071242950924,-48.1088534778964,
-48.0752275703878),.UNSPECIFIED.);
#733=B_SPLINE_CURVE_WITH_KNOTS('',3,(#68173,#68174,#68175,#68176,#68177,
#68178,#68179,#68180,#68181,#68182,#68183,#68184,#68185,#68186,#68187,#68188,
#68189,#68190,#68191,#68192,#68193,#68194,#68195,#68196,#68197,#68198,#68199,
#68200,#68201,#68202,#68203,#68204,#68205,#68206,#68207,#68208,#68209,#68210,
#68211,#68212,#68213,#68214,#68215,#68216,#68217,#68218,#68219,#68220,#68221,
#68222,#68223,#68224,#68225,#68226,#68227,#68228,#68229,#68230,#68231,#68232,
#68233,#68234,#68235,#68236,#68237,#68238,#68239,#68240,#68241,#68242,#68243,
#68244,#68245,#68246,#68247,#68248,#68249,#68250,#68251,#68252,#68253,#68254,
#68255,#68256,#68257,#68258,#68259,#68260,#68261,#68262,#68263,#68264,#68265,
#68266,#68267,#68268,#68269,#68270,#68271,#68272,#68273,#68274,#68275,#68276,
#68277,#68278,#68279,#68280,#68281,#68282,#68283,#68284,#68285,#68286,#68287,
#68288,#68289,#68290,#68291,#68292,#68293,#68294,#68295,#68296,#68297,#68298,
#68299,#68300,#68301,#68302,#68303,#68304,#68305,#68306,#68307,#68308,#68309,
#68310,#68311,#68312,#68313,#68314,#68315,#68316,#68317,#68318,#68319,#68320,
#68321,#68322,#68323,#68324,#68325,#68326,#68327,#68328,#68329,#68330,#68331,
#68332,#68333,#68334,#68335,#68336,#68337,#68338,#68339,#68340,#68341,#68342,
#68343,#68344,#68345,#68346,#68347,#68348,#68349,#68350,#68351,#68352,#68353,
#68354,#68355,#68356,#68357,#68358,#68359,#68360,#68361,#68362,#68363,#68364,
#68365,#68366,#68367,#68368,#68369,#68370,#68371,#68372,#68373,#68374,#68375,
#68376,#68377,#68378,#68379,#68380),.UNSPECIFIED.,.F.,.F.,(4,3,3,3,3,3,
3,3,3,3,3,3,3,3,3,3,3,3,3,3,3,3,3,3,3,3,3,3,3,3,3,3,3,3,3,3,3,3,3,3,3,3,
3,3,3,3,3,3,3,3,3,3,3,3,3,3,3,3,3,3,3,3,3,3,3,3,3,3,3,4),(-48.0752275700803,
-47.9744522344853,-47.8733473108059,-47.772071053497,-47.6705065609339,
-47.6097894676021,-47.5144766136761,-47.4192934691677,-47.3242105953751,
-47.2291946507392,-47.1342121417024,-47.0392366171508,-46.944241639639,
-46.8491433460497,-46.7539860344955,-46.6586790047209,-46.6179188536938,
-46.5226059997677,-46.4274228552593,-46.3323399814666,-46.2373240368307,
-46.1423415277937,-46.0473660032421,-45.9523710257302,-45.8572727321408,
-45.7621154205866,-45.666808390812,-45.6260482397854,-45.5307353858593,
-45.4355522413509,-45.3404693675581,-45.2454534229221,-45.1504709138852,
-45.0554953893335,-44.9605004118216,-44.8654021182322,-44.770244806678,
-44.6749377769034,-44.634177625877,-44.5388647719509,-44.4436816274425,
-44.3485987536498,-44.2535828090139,-44.1586002999769,-44.0636247754252,
-43.9686297979134,-43.873531504324,-43.7783741927699,-43.6830671629953,
-43.6423070119686,-43.5469941580425,-43.4518110135341,-43.3567281397412,
-43.2617121951052,-43.1667296860683,-43.0717541615167,-42.9767591840048,
-42.8816608904153,-42.7865035788611,-42.6911965490865,-42.6504363980602,
-42.5564717447825,-42.4609180595857,-42.3671892541391,-42.2735166658413,
-42.1798724036703,-42.0829148685548,-41.9891990816263,-41.8906206724173,
-41.7920422632082),.UNSPECIFIED.);
#734=B_SPLINE_CURVE_WITH_KNOTS('',3,(#68382,#68383,#68384,#68385,#68386,
#68387,#68388,#68389,#68390,#68391,#68392),.UNSPECIFIED.,.F.,.F.,(4,1,1,
1,1,1,1,1,4),(-41.7920422632082,-41.6585657841519,-40.6666951702435,-39.6748245563351,
-38.6829539424267,-37.6910833285184,-36.69921271461,-35.7073421007016,-35.5088569560286),
 .UNSPECIFIED.);
#735=B_SPLINE_CURVE_WITH_KNOTS('',3,(#68394,#68395,#68396,#68397,#68398,
#68399,#68400,#68401,#68402,#68403,#68404,#68405,#68406,#68407,#68408,#68409,
#68410,#68411,#68412,#68413,#68414,#68415,#68416,#68417,#68418,#68419,#68420,
#68421,#68422,#68423,#68424,#68425,#68426,#68427,#68428,#68429,#68430,#68431,
#68432,#68433,#68434,#68435,#68436,#68437,#68438,#68439,#68440,#68441,#68442,
#68443,#68444,#68445,#68446,#68447,#68448,#68449,#68450,#68451,#68452,#68453,
#68454,#68455,#68456,#68457,#68458,#68459,#68460,#68461,#68462,#68463,#68464,
#68465,#68466,#68467,#68468,#68469,#68470,#68471,#68472,#68473,#68474,#68475,
#68476,#68477,#68478,#68479,#68480,#68481,#68482,#68483,#68484,#68485,#68486,
#68487,#68488,#68489,#68490,#68491,#68492,#68493,#68494,#68495,#68496,#68497,
#68498,#68499,#68500,#68501,#68502,#68503,#68504,#68505,#68506,#68507,#68508,
#68509,#68510,#68511,#68512,#68513,#68514,#68515,#68516,#68517,#68518,#68519,
#68520,#68521,#68522,#68523,#68524,#68525,#68526,#68527,#68528,#68529,#68530,
#68531,#68532,#68533,#68534,#68535,#68536,#68537,#68538,#68539,#68540,#68541,
#68542,#68543,#68544,#68545,#68546,#68547,#68548,#68549,#68550,#68551,#68552,
#68553,#68554,#68555,#68556,#68557,#68558,#68559,#68560,#68561,#68562,#68563,
#68564,#68565,#68566,#68567,#68568,#68569,#68570,#68571,#68572,#68573,#68574,
#68575,#68576,#68577,#68578,#68579,#68580,#68581,#68582,#68583,#68584,#68585,
#68586,#68587,#68588,#68589,#68590,#68591,#68592,#68593,#68594,#68595,#68596,
#68597,#68598,#68599,#68600,#68601,#68602,#68603,#68604),.UNSPECIFIED.,
 .F.,.F.,(4,3,3,3,3,3,3,3,3,3,3,3,3,3,3,3,3,3,3,3,3,3,3,3,3,3,3,3,3,3,3,
3,3,3,3,3,3,3,3,3,3,3,3,3,3,3,3,3,3,3,3,3,3,3,3,3,3,3,3,3,3,3,3,3,3,3,3,
3,3,3,4),(-35.5088569560286,-35.4150700759351,-35.321370554688,-35.2277166821189,
-35.1340805756398,-35.0404343766173,-34.9466940692927,-34.8529004798333,
-34.758960180959,-34.7154714867932,-34.6201586328671,-34.5249754883587,
-34.429892614566,-34.3348766699301,-34.2398941608932,-34.1449186363415,
-34.0499236588296,-33.9548253652401,-33.859668053686,-33.7643610239114,
-33.7236008728848,-33.6282880189595,-33.5331048744518,-33.4380220006598,
-33.3430060560246,-33.2480235469885,-33.1530480224376,-33.0580530449264,
-32.9629547513378,-32.8677974397844,-32.7724904100105,-32.7317302589765,
-32.6364174050486,-32.5412342605387,-32.4461513867441,-32.3511354421064,
-32.2561529330677,-32.1611774085145,-32.0661824310004,-31.9710841374094,
-31.8759268258537,-31.7806197960775,-31.7398596450681,-31.6445467911428,
-31.5493636466353,-31.4542807728439,-31.3592648282087,-31.2642823191725,
-31.1693067946216,-31.0743118171102,-30.9792135235215,-30.8840562119678,
-30.7887491821939,-30.7479890311597,-30.6526761772381,-30.5574930327345,
-30.4624101589461,-30.3673942143148,-30.2724117052827,-30.1774361807356,
-30.0824412032285,-29.9873429096436,-29.8921855980939,-29.7968785683237,
-29.7561184172513,-29.6573775631943,-29.5588052664884,-29.4604287441025,
-29.3621690345465,-29.2640350167219,-29.225671648849),.UNSPECIFIED.);
#736=B_SPLINE_CURVE_WITH_KNOTS('',3,(#68606,#68607,#68608,#68609,#68610,
#68611,#68612,#68613,#68614,#68615),.UNSPECIFIED.,.F.,.F.,(4,1,1,1,1,1,
1,4),(-29.2256689641518,-28.764247803343,-27.7723771894346,-26.7805065755262,
-25.7886359616178,-24.7967653477094,-23.8048947338011,-22.9424863416694),
 .UNSPECIFIED.);
#737=B_SPLINE_CURVE_WITH_KNOTS('',3,(#68617,#68618,#68619,#68620,#68621,
#68622,#68623,#68624,#68625,#68626,#68627),.UNSPECIFIED.,.F.,.F.,(4,1,1,
1,1,1,1,1,4),(-22.9424863416694,-22.8130241198927,-21.8211535059843,-20.8292828920759,
-19.8374122781676,-18.8455416642592,-17.8536710503508,-16.8618004364424,
-16.6593010344898),.UNSPECIFIED.);
#738=B_SPLINE_CURVE_WITH_KNOTS('',3,(#68629,#68630,#68631,#68632,#68633,
#68634,#68635,#68636,#68637,#68638,#68639,#68640,#68641,#68642,#68643,#68644,
#68645,#68646,#68647,#68648,#68649,#68650,#68651,#68652,#68653,#68654,#68655,
#68656,#68657,#68658,#68659,#68660,#68661,#68662,#68663,#68664,#68665,#68666,
#68667,#68668,#68669,#68670,#68671,#68672,#68673,#68674,#68675,#68676,#68677,
#68678,#68679,#68680,#68681,#68682,#68683,#68684,#68685,#68686,#68687,#68688,
#68689,#68690,#68691,#68692,#68693,#68694,#68695,#68696,#68697,#68698,#68699,
#68700,#68701,#68702,#68703,#68704,#68705,#68706,#68707,#68708,#68709,#68710,
#68711,#68712,#68713,#68714,#68715,#68716,#68717,#68718,#68719,#68720,#68721,
#68722,#68723,#68724,#68725,#68726,#68727,#68728,#68729,#68730,#68731,#68732,
#68733,#68734,#68735,#68736,#68737,#68738,#68739,#68740,#68741,#68742,#68743,
#68744,#68745,#68746,#68747,#68748,#68749,#68750,#68751,#68752,#68753,#68754,
#68755,#68756,#68757,#68758,#68759,#68760,#68761,#68762,#68763,#68764,#68765,
#68766,#68767,#68768,#68769,#68770,#68771,#68772,#68773,#68774,#68775,#68776,
#68777,#68778,#68779,#68780,#68781,#68782,#68783,#68784,#68785,#68786,#68787,
#68788,#68789,#68790,#68791,#68792,#68793,#68794,#68795,#68796,#68797,#68798,
#68799,#68800,#68801,#68802,#68803,#68804,#68805,#68806,#68807,#68808,#68809,
#68810,#68811,#68812,#68813,#68814,#68815,#68816,#68817,#68818,#68819,#68820,
#68821,#68822,#68823,#68824,#68825,#68826,#68827,#68828,#68829,#68830,#68831,
#68832,#68833,#68834,#68835,#68836,#68837,#68838,#68839),.UNSPECIFIED.,
 .F.,.F.,(4,3,3,3,3,3,3,3,3,3,3,3,3,3,3,3,3,3,3,3,3,3,3,3,3,3,3,3,3,3,3,
3,3,3,3,3,3,3,3,3,3,3,3,3,3,3,3,3,3,3,3,3,3,3,3,3,3,3,3,3,3,3,3,3,3,3,3,
3,3,3,4),(-16.6593010344898,-16.5606296329953,-16.4669232014932,-16.3732596170644,
-16.2796110115953,-16.1859495380336,-16.0921922443136,-15.9983791947975,
-15.9044217971492,-15.869929822534,-15.774616959187,-15.6794338056938,-15.5843509233581,
-15.4893349708615,-15.3943524543906,-15.2993769228379,-15.2043819387649,
-15.1092836393092,-15.0141263222782,-14.9188192876671,-14.8780592086257,
-14.7827461890252,-14.6875628780416,-14.592479837212,-14.4974637254086,
-14.402481049193,-14.3075053576623,-14.2125102135824,-14.1174117550459,
-14.0222542792401,-13.9269470878258,-13.8861885947173,-13.7908761215009,
-13.6956933577844,-13.6006108643442,-13.5055952978454,-13.4106131654119,
-13.3156380154653,-13.2206434100938,-13.1255454827213,-13.0303885345095,
-12.9350818602807,-12.8943179808089,-12.7990049356622,-12.7038216026842,
-12.6087385433885,-12.5137224183594,-12.4187397321764,-12.3237640339271,
-12.2287688863699,-12.1336704292036,-12.0385129575439,-11.9432057744304,
-11.9024473669005,-11.8071335232423,-11.7119493829509,-11.6168655087749,
-11.5218485611603,-11.4268650479544,-11.3318885193192,-11.2368925390841,
-11.1417932508704,-11.046634947928,-10.9513269410766,-10.9105767529922,
-10.8119870552616,-10.7135637207956,-10.6153319956712,-10.5172142509035,
-10.4192173278538,-10.3761157273102),.UNSPECIFIED.);
#739=B_SPLINE_CURVE_WITH_KNOTS('',3,(#68840,#68841,#68842,#68843,#68844,
#68845,#68846,#68847,#68848,#68849),.UNSPECIFIED.,.F.,.F.,(4,1,1,1,1,1,
1,4),(-10.3761127482158,-9.91870613908378,-8.9268355251754,-7.93496491126702,
-6.94309429735864,-5.95122368345026,-4.95935306954189,-4.09293042013066),
 .UNSPECIFIED.);
#740=B_SPLINE_CURVE_WITH_KNOTS('',3,(#68852,#68853,#68854,#68855),
 .UNSPECIFIED.,.F.,.F.,(4,4),(103.598719667128,103.672557568218),
 .UNSPECIFIED.);
#741=B_SPLINE_CURVE_WITH_KNOTS('',3,(#68857,#68858,#68859,#68860,#68861,
#68862,#68863,#68864,#68865,#68866,#68867,#68868,#68869,#68870,#68871,#68872,
#68873,#68874,#68875,#68876,#68877,#68878,#68879,#68880,#68881,#68882,#68883,
#68884,#68885,#68886,#68887,#68888,#68889,#68890,#68891,#68892,#68893,#68894,
#68895,#68896,#68897,#68898,#68899,#68900,#68901,#68902,#68903,#68904,#68905,
#68906,#68907,#68908,#68909,#68910,#68911,#68912,#68913,#68914,#68915,#68916,
#68917,#68918,#68919,#68920,#68921,#68922,#68923,#68924,#68925,#68926,#68927,
#68928,#68929,#68930,#68931,#68932,#68933,#68934,#68935,#68936,#68937,#68938,
#68939,#68940,#68941,#68942,#68943,#68944,#68945,#68946,#68947,#68948,#68949,
#68950,#68951,#68952,#68953,#68954,#68955,#68956,#68957,#68958,#68959,#68960,
#68961,#68962,#68963,#68964,#68965,#68966,#68967,#68968,#68969,#68970,#68971,
#68972,#68973,#68974,#68975,#68976,#68977,#68978,#68979,#68980,#68981,#68982,
#68983,#68984,#68985,#68986,#68987,#68988,#68989,#68990,#68991,#68992,#68993,
#68994,#68995,#68996,#68997,#68998,#68999,#69000,#69001,#69002,#69003,#69004,
#69005,#69006,#69007,#69008,#69009,#69010,#69011,#69012,#69013,#69014,#69015,
#69016,#69017,#69018,#69019,#69020,#69021,#69022,#69023,#69024,#69025,#69026,
#69027,#69028,#69029,#69030,#69031,#69032,#69033,#69034,#69035,#69036,#69037,
#69038,#69039,#69040,#69041,#69042,#69043),.UNSPECIFIED.,.F.,.F.,(4,3,3,
3,3,3,3,3,3,3,3,3,3,3,3,3,3,3,3,3,3,3,3,3,3,3,3,3,3,3,3,3,3,3,3,3,3,3,3,
3,3,3,3,3,3,3,3,3,3,3,3,3,3,3,3,3,3,3,3,3,3,3,4),(103.672557568463,103.820034675392,
103.858999941297,103.959617585576,104.060092020312,104.160451913393,104.260749367129,
104.361015461365,104.461281236281,104.561646050319,104.662059688377,104.762651052579,
104.850870555206,104.951316799698,105.051619155889,105.151806756723,105.251931866953,
105.352025803237,105.452119842625,105.552314769,105.652559264494,105.752984690398,
105.842741169114,105.943516664012,106.044148018232,106.144662702836,106.245113571047,
106.34553149369,106.44594730048,106.546458311783,106.647016259314,106.747747136848,
106.834611783022,106.935344605953,107.035936261338,107.136415835605,107.236834401933,
107.337222849264,107.437612028115,107.538100986795,107.638639364,107.739354989191,
107.826482396931,107.925989483572,108.025352284445,108.124603771469,108.223795063832,
108.322958565098,108.422126641208,108.521408812288,108.620746084475,108.720284355729,
108.818353010839,108.921718483103,109.024920625112,109.127960648325,109.230905205988,
109.333779542361,109.436608819253,109.539447067769,109.642285379207,109.745194616777,
109.810223624748),.UNSPECIFIED.);
#742=B_SPLINE_CURVE_WITH_KNOTS('',3,(#69047,#69048,#69049,#69050,#69051,
#69052,#69053,#69054,#69055,#69056,#69057,#69058,#69059,#69060,#69061,#69062,
#69063,#69064,#69065,#69066,#69067,#69068,#69069,#69070,#69071,#69072,#69073,
#69074,#69075,#69076,#69077,#69078,#69079,#69080,#69081,#69082,#69083,#69084,
#69085,#69086,#69087,#69088,#69089,#69090,#69091,#69092,#69093,#69094,#69095,
#69096,#69097,#69098,#69099,#69100,#69101,#69102,#69103,#69104,#69105,#69106,
#69107,#69108,#69109,#69110,#69111,#69112,#69113,#69114,#69115,#69116,#69117,
#69118,#69119,#69120,#69121,#69122,#69123,#69124,#69125,#69126,#69127,#69128,
#69129,#69130,#69131,#69132,#69133,#69134,#69135,#69136,#69137,#69138,#69139,
#69140,#69141,#69142,#69143,#69144,#69145,#69146,#69147,#69148,#69149,#69150,
#69151,#69152,#69153,#69154,#69155,#69156,#69157,#69158,#69159,#69160,#69161,
#69162,#69163,#69164,#69165,#69166,#69167,#69168,#69169,#69170,#69171,#69172,
#69173,#69174,#69175,#69176,#69177,#69178,#69179,#69180,#69181,#69182,#69183,
#69184,#69185,#69186,#69187,#69188,#69189,#69190,#69191,#69192,#69193,#69194,
#69195,#69196,#69197),.UNSPECIFIED.,.F.,.F.,(4,3,3,3,3,3,3,3,3,3,3,3,3,
3,3,3,3,3,3,3,3,3,3,3,3,3,3,3,3,3,3,3,3,3,3,3,3,3,3,3,3,3,3,3,3,3,3,3,3,
3,4),(103.67255780872,103.772028396805,103.875582571364,103.974810689988,
104.073986558126,104.173142610607,104.272311252423,104.371585990288,104.47092364339,
104.570421796513,104.600461793276,104.701227449666,104.8018487344,104.902353090162,
105.002793462484,105.103200738506,105.203605764118,105.304106096047,105.404653264734,
105.50537395965,105.593172971017,105.693893970835,105.794473571861,105.894940843091,
105.995346945599,106.095722787311,106.196099237591,106.296575605139,106.397101306063,
106.497804905763,106.585884148758,106.685379877789,106.784731096122,106.883970749977,
106.98315003858,107.082301377603,107.181457144904,107.280741690303,107.380066654784,
107.47959327395,107.578595326499,107.681954817579,107.785150670333,107.888184011499,
107.991121663445,108.093988893523,108.196810886437,108.299641785865,108.402472625654,
108.505374666306,108.57130650424),.UNSPECIFIED.);
#743=B_SPLINE_CURVE_WITH_KNOTS('',3,(#69198,#69199,#69200,#69201,#69202),
 .UNSPECIFIED.,.F.,.F.,(4,1,4),(103.599566372989,103.607750615535,103.672557568463),
 .UNSPECIFIED.);
#744=B_SPLINE_CURVE_WITH_KNOTS('',3,(#69205,#69206,#69207,#69208,#69209,
#69210,#69211,#69212,#69213,#69214,#69215,#69216,#69217,#69218,#69219,#69220,
#69221,#69222,#69223,#69224,#69225,#69226,#69227,#69228,#69229,#69230,#69231,
#69232,#69233,#69234),.UNSPECIFIED.,.F.,.F.,(4,2,2,2,2,2,2,2,2,2,2,2,2,
2,4),(-2.23305280487553,-1.97896579953537,-1.73577232135028,-1.53430986639811,
-1.37974696990534,-1.21783860833472,-1.04897899044366,-0.891695760805949,
-0.708676356012324,-0.554482474707368,-0.368500908541818,-0.241956806614549,
-0.138087935175818,-0.0732023944895521,-0.00018678784649391),
 .UNSPECIFIED.);
#745=B_SPLINE_CURVE_WITH_KNOTS('',3,(#69235,#69236,#69237,#69238,#69239,
#69240,#69241,#69242,#69243,#69244,#69245,#69246,#69247,#69248,#69249,#69250,
#69251,#69252,#69253,#69254,#69255,#69256,#69257,#69258,#69259,#69260,#69261,
#69262,#69263,#69264,#69265,#69266,#69267,#69268,#69269,#69270,#69271,#69272,
#69273,#69274,#69275,#69276,#69277,#69278,#69279,#69280,#69281,#69282,#69283,
#69284,#69285,#69286,#69287,#69288,#69289,#69290,#69291,#69292,#69293,#69294,
#69295,#69296,#69297,#69298),.UNSPECIFIED.,.F.,.F.,(4,3,3,3,3,3,3,3,3,3,
3,3,3,3,3,3,3,3,3,3,3,4),(-0.410648750433038,-0.381296088292737,-0.350882391849445,
-0.328072119516976,-0.310964415267624,-0.305842993500878,-0.301661871504881,
-0.274116258800685,-0.259641302519569,-0.231392457082299,-0.202468399947011,
-0.198019208917011,-0.170841895434807,-0.143725312403613,-0.117042212888725,
-0.102411936277635,-0.097195049751494,-0.0935363835720784,-0.0677899334604712,
-0.0424347820407558,-0.0178142542830924,0.),.UNSPECIFIED.);
#746=B_SPLINE_CURVE_WITH_KNOTS('',3,(#69300,#69301,#69302,#69303,#69304,
#69305,#69306,#69307,#69308,#69309,#69310,#69311,#69312,#69313,#69314,#69315,
#69316,#69317,#69318,#69319,#69320,#69321,#69322,#69323,#69324,#69325,#69326,
#69327,#69328,#69329,#69330,#69331,#69332,#69333),.UNSPECIFIED.,.F.,.F.,
(4,3,3,3,3,3,3,3,3,3,3,4),(-0.219677966288016,-0.201006229477425,-0.173906949584204,
-0.172158028090248,-0.142713390739092,-0.124874216896705,-0.114789665948937,
-0.110082687886506,-0.0803547102951982,-0.0502957032480209,-0.0203907630638487,
0.),.UNSPECIFIED.);
#747=B_SPLINE_CURVE_WITH_KNOTS('',3,(#69334,#69335,#69336,#69337),
 .UNSPECIFIED.,.F.,.F.,(4,4),(-0.00018678784649391,-7.03322184060005E-5),
 .UNSPECIFIED.);
#748=B_SPLINE_CURVE_WITH_KNOTS('',3,(#69749,#69750,#69751,#69752,#69753,
#69754,#69755,#69756,#69757,#69758,#69759,#69760,#69761,#69762,#69763,#69764,
#69765,#69766,#69767,#69768,#69769,#69770,#69771,#69772,#69773,#69774,#69775,
#69776,#69777,#69778,#69779,#69780,#69781,#69782,#69783,#69784,#69785,#69786,
#69787,#69788,#69789,#69790,#69791,#69792,#69793,#69794,#69795,#69796,#69797,
#69798,#69799,#69800,#69801,#69802,#69803,#69804,#69805,#69806,#69807,#69808,
#69809,#69810,#69811,#69812,#69813,#69814,#69815,#69816,#69817,#69818,#69819,
#69820,#69821,#69822,#69823,#69824,#69825,#69826,#69827,#69828,#69829,#69830,
#69831,#69832,#69833,#69834,#69835,#69836),.UNSPECIFIED.,.F.,.F.,(4,3,3,
3,3,3,3,3,3,3,3,3,3,3,3,3,3,3,3,3,3,3,3,3,3,3,3,3,3,4),(-0.552745378375041,
-0.527830263536694,-0.499859837592608,-0.485874624620565,-0.477192997531472,
-0.471889411648522,-0.442927810370459,-0.413963015571315,-0.408336266644177,
-0.40114435110069,-0.397446251891128,-0.369166582261538,-0.341169387622816,
-0.31397908943666,-0.298150853306366,-0.293754274173184,-0.266922432865955,
-0.250809444272419,-0.223156811908825,-0.19550417954523,-0.19139998392206,
-0.16479071965233,-0.138164593557966,-0.111921701546741,-0.097931488853398,
-0.091170251499608,-0.0656115897288642,-0.0404467470576775,-0.0160684028764294,
0.),.UNSPECIFIED.);
#749=B_SPLINE_CURVE_WITH_KNOTS('',3,(#70254,#70255,#70256,#70257,#70258,
#70259,#70260,#70261,#70262,#70263,#70264,#70265,#70266,#70267,#70268,#70269,
#70270,#70271,#70272,#70273,#70274,#70275,#70276,#70277,#70278,#70279,#70280,
#70281,#70282,#70283,#70284,#70285,#70286,#70287,#70288,#70289,#70290,#70291,
#70292,#70293,#70294,#70295,#70296,#70297,#70298,#70299,#70300,#70301,#70302,
#70303,#70304,#70305,#70306,#70307,#70308,#70309,#70310,#70311,#70312,#70313,
#70314,#70315,#70316,#70317,#70318,#70319,#70320,#70321,#70322,#70323,#70324,
#70325,#70326,#70327,#70328,#70329,#70330,#70331,#70332,#70333,#70334,#70335,
#70336,#70337,#70338,#70339,#70340,#70341,#70342,#70343,#70344),
 .UNSPECIFIED.,.F.,.F.,(4,3,3,3,3,3,3,3,3,3,3,3,3,3,3,3,3,3,3,3,3,3,3,3,
3,3,3,3,3,3,4),(-0.555272788399392,-0.535208229286056,-0.510357943747353,
-0.495927663091087,-0.490771565699598,-0.465394215383921,-0.439311463621092,
-0.431518091480653,-0.425427657470475,-0.415445052851753,-0.3887274389215,
-0.361614454556187,-0.341463747205989,-0.332379220304646,-0.326285899706679,
-0.321326754662703,-0.293412801441296,-0.281011625155395,-0.25378286604002,
-0.226554106924644,-0.220947145848259,-0.216688100237889,-0.188776530116757,
-0.160380134586806,-0.131653127387196,-0.114279480489655,-0.109581292141837,
-0.0801117384511105,-0.0505679692699675,-0.0215915474950309,-5.6663350074274E-15),
 .UNSPECIFIED.);
#750=B_SPLINE_CURVE_WITH_KNOTS('',3,(#70345,#70346,#70347,#70348),
 .UNSPECIFIED.,.F.,.F.,(4,4),(-0.0122626075766948,0.),.UNSPECIFIED.);
#946=SHAPE_REPRESENTATION_RELATIONSHIP('SRR','None',#94498,#961);
#961=ADVANCED_BREP_SHAPE_REPRESENTATION('',(#991),#94407);
#976=STYLED_ITEM('',(#94578),#991);
#991=MANIFOLD_SOLID_BREP('Body1',#8261);
#1043=FACE_BOUND('',#1827,.T.);
#1044=FACE_BOUND('',#1830,.T.);
#1131=PLANE('',#8797);
#1132=PLANE('',#8798);
#1133=PLANE('',#8799);
#1134=PLANE('',#8800);
#1135=PLANE('',#8801);
#1136=PLANE('',#8802);
#1137=PLANE('',#8803);
#1138=PLANE('',#8804);
#1139=PLANE('',#8808);
#1140=PLANE('',#8809);
#1396=FACE_OUTER_BOUND('',#1799,.T.);
#1397=FACE_OUTER_BOUND('',#1800,.T.);
#1398=FACE_OUTER_BOUND('',#1801,.T.);
#1399=FACE_OUTER_BOUND('',#1802,.T.);
#1400=FACE_OUTER_BOUND('',#1803,.T.);
#1401=FACE_OUTER_BOUND('',#1804,.T.);
#1402=FACE_OUTER_BOUND('',#1805,.T.);
#1403=FACE_OUTER_BOUND('',#1806,.T.);
#1404=FACE_OUTER_BOUND('',#1807,.T.);
#1405=FACE_OUTER_BOUND('',#1808,.T.);
#1406=FACE_OUTER_BOUND('',#1809,.T.);
#1407=FACE_OUTER_BOUND('',#1810,.T.);
#1408=FACE_OUTER_BOUND('',#1811,.T.);
#1409=FACE_OUTER_BOUND('',#1812,.T.);
#1410=FACE_OUTER_BOUND('',#1813,.T.);
#1411=FACE_OUTER_BOUND('',#1814,.T.);
#1412=FACE_OUTER_BOUND('',#1815,.T.);
#1413=FACE_OUTER_BOUND('',#1816,.T.);
#1414=FACE_OUTER_BOUND('',#1817,.T.);
#1415=FACE_OUTER_BOUND('',#1818,.T.);
#1416=FACE_OUTER_BOUND('',#1819,.T.);
#1417=FACE_OUTER_BOUND('',#1820,.T.);
#1418=FACE_OUTER_BOUND('',#1821,.T.);
#1419=FACE_OUTER_BOUND('',#1822,.T.);
#1420=FACE_OUTER_BOUND('',#1823,.T.);
#1421=FACE_OUTER_BOUND('',#1824,.T.);
#1422=FACE_OUTER_BOUND('',#1825,.T.);
#1423=FACE_OUTER_BOUND('',#1826,.T.);
#1424=FACE_OUTER_BOUND('',#1828,.T.);
#1425=FACE_OUTER_BOUND('',#1829,.T.);
#1426=FACE_OUTER_BOUND('',#1831,.T.);
#1799=EDGE_LOOP('',(#6812,#6813,#6814,#6815));
#1800=EDGE_LOOP('',(#6816,#6817,#6818,#6819,#6820));
#1801=EDGE_LOOP('',(#6821,#6822,#6823,#6824,#6825));
#1802=EDGE_LOOP('',(#6826,#6827,#6828,#6829,#6830,#6831));
#1803=EDGE_LOOP('',(#6832,#6833,#6834,#6835,#6836));
#1804=EDGE_LOOP('',(#6837,#6838,#6839,#6840,#6841));
#1805=EDGE_LOOP('',(#6842,#6843,#6844,#6845,#6846,#6847));
#1806=EDGE_LOOP('',(#6848,#6849,#6850,#6851,#6852));
#1807=EDGE_LOOP('',(#6853,#6854,#6855,#6856,#6857,#6858));
#1808=EDGE_LOOP('',(#6859,#6860,#6861,#6862));
#1809=EDGE_LOOP('',(#6863,#6864,#6865,#6866,#6867,#6868));
#1810=EDGE_LOOP('',(#6869,#6870,#6871,#6872,#6873));
#1811=EDGE_LOOP('',(#6874,#6875,#6876,#6877,#6878,#6879));
#1812=EDGE_LOOP('',(#6880,#6881,#6882,#6883));
#1813=EDGE_LOOP('',(#6884,#6885,#6886,#6887,#6888,#6889));
#1814=EDGE_LOOP('',(#6890,#6891,#6892,#6893,#6894,#6895,#6896,#6897,#6898,
#6899,#6900,#6901,#6902,#6903,#6904,#6905,#6906,#6907,#6908,#6909,#6910,
#6911,#6912,#6913,#6914,#6915,#6916,#6917,#6918,#6919,#6920,#6921,#6922,
#6923));
#1815=EDGE_LOOP('',(#6924,#6925,#6926,#6927,#6928,#6929));
#1816=EDGE_LOOP('',(#6930,#6931,#6932,#6933,#6934,#6935,#6936,#6937,#6938));
#1817=EDGE_LOOP('',(#6939,#6940,#6941,#6942,#6943,#6944,#6945,#6946,#6947,
#6948,#6949,#6950,#6951,#6952,#6953,#6954,#6955,#6956,#6957,#6958,#6959,
#6960,#6961,#6962,#6963,#6964,#6965,#6966,#6967,#6968,#6969,#6970,#6971,
#6972,#6973,#6974,#6975,#6976,#6977,#6978,#6979,#6980,#6981));
#1818=EDGE_LOOP('',(#6982,#6983,#6984,#6985,#6986,#6987,#6988,#6989,#6990,
#6991,#6992,#6993,#6994,#6995,#6996,#6997,#6998,#6999,#7000,#7001,#7002,
#7003,#7004,#7005,#7006,#7007,#7008,#7009,#7010,#7011,#7012,#7013,#7014,
#7015,#7016,#7017,#7018,#7019,#7020,#7021,#7022,#7023,#7024,#7025,#7026,
#7027,#7028,#7029));
#1819=EDGE_LOOP('',(#7030,#7031,#7032,#7033));
#1820=EDGE_LOOP('',(#7034,#7035,#7036,#7037));
#1821=EDGE_LOOP('',(#7038,#7039,#7040,#7041));
#1822=EDGE_LOOP('',(#7042,#7043,#7044,#7045));
#1823=EDGE_LOOP('',(#7046,#7047,#7048,#7049));
#1824=EDGE_LOOP('',(#7050,#7051,#7052,#7053));
#1825=EDGE_LOOP('',(#7054,#7055,#7056,#7057,#7058,#7059));
#1826=EDGE_LOOP('',(#7060));
#1827=EDGE_LOOP('',(#7061,#7062,#7063,#7064,#7065));
#1828=EDGE_LOOP('',(#7066,#7067,#7068,#7069));
#1829=EDGE_LOOP('',(#7070));
#1830=EDGE_LOOP('',(#7071,#7072,#7073,#7074,#7075,#7076));
#1831=EDGE_LOOP('',(#7077));
#2219=LINE('',#59878,#2617);
#2220=LINE('',#60229,#2618);
#2221=LINE('',#60648,#2619);
#2222=LINE('',#60884,#2620);
#2223=LINE('',#61280,#2621);
#2224=LINE('',#61689,#2622);
#2225=LINE('',#61914,#2623);
#2226=LINE('',#62136,#2624);
#2227=LINE('',#62521,#2625);
#2228=LINE('',#62951,#2626);
#2229=LINE('',#63383,#2627);
#2230=LINE('',#63599,#2628);
#2231=LINE('',#64064,#2629);
#2232=LINE('',#64558,#2630);
#2233=LINE('',#64972,#2631);
#2234=LINE('',#69339,#2632);
#2235=LINE('',#70352,#2633);
#2236=LINE('',#70354,#2634);
#2237=LINE('',#70356,#2635);
#2238=LINE('',#70357,#2636);
#2239=LINE('',#70360,#2637);
#2240=LINE('',#70362,#2638);
#2241=LINE('',#70363,#2639);
#2242=LINE('',#70366,#2640);
#2243=LINE('',#70368,#2641);
#2244=LINE('',#70369,#2642);
#2245=LINE('',#70372,#2643);
#2246=LINE('',#70374,#2644);
#2247=LINE('',#70375,#2645);
#2248=LINE('',#70378,#2646);
#2249=LINE('',#70380,#2647);
#2250=LINE('',#70381,#2648);
#2251=LINE('',#70383,#2649);
#2252=LINE('',#70384,#2650);
#2253=LINE('',#70391,#2651);
#2617=VECTOR('',#9915,2.37175);
#2618=VECTOR('',#9920,2.37175);
#2619=VECTOR('',#9923,2.37175);
#2620=VECTOR('',#9926,2.37175);
#2621=VECTOR('',#9929,2.37175);
#2622=VECTOR('',#9932,2.37175);
#2623=VECTOR('',#9935,2.37175);
#2624=VECTOR('',#9938,2.37175);
#2625=VECTOR('',#9941,2.37175);
#2626=VECTOR('',#9944,2.37175);
#2627=VECTOR('',#9947,2.37175);
#2628=VECTOR('',#9950,2.37175);
#2629=VECTOR('',#9953,2.37175);
#2630=VECTOR('',#9956,2.37175);
#2631=VECTOR('',#9959,2.37175);
#2632=VECTOR('',#9972,2.5);
#2633=VECTOR('',#9977,10.);
#2634=VECTOR('',#9978,10.);
#2635=VECTOR('',#9979,10.);
#2636=VECTOR('',#9980,10.);
#2637=VECTOR('',#9983,10.);
#2638=VECTOR('',#9984,10.);
#2639=VECTOR('',#9985,10.);
#2640=VECTOR('',#9988,9.99999999999999);
#2641=VECTOR('',#9989,10.);
#2642=VECTOR('',#9990,10.);
#2643=VECTOR('',#9993,10.);
#2644=VECTOR('',#9994,10.);
#2645=VECTOR('',#9995,10.);
#2646=VECTOR('',#9998,10.);
#2647=VECTOR('',#9999,10.);
#2648=VECTOR('',#10000,10.);
#2649=VECTOR('',#10003,10.);
#2650=VECTOR('',#10004,10.);
#2651=VECTOR('',#10013,5.);
#2810=CIRCLE('',#8775,2.37175);
#2811=CIRCLE('',#8791,2.942);
#2812=CIRCLE('',#8792,2.942);
#2813=CIRCLE('',#8794,2.37175);
#2814=CIRCLE('',#8796,2.);
#2815=CIRCLE('',#8805,5.);
#2816=CIRCLE('',#8807,5.);
#3492=VERTEX_POINT('',#59876);
#3493=VERTEX_POINT('',#59877);
#3494=VERTEX_POINT('',#59879);
#3495=VERTEX_POINT('',#60100);
#3496=VERTEX_POINT('',#60227);
#3497=VERTEX_POINT('',#60228);
#3498=VERTEX_POINT('',#60438);
#3499=VERTEX_POINT('',#60646);
#3500=VERTEX_POINT('',#60647);
#3501=VERTEX_POINT('',#60649);
#3502=VERTEX_POINT('',#60882);
#3503=VERTEX_POINT('',#60883);
#3504=VERTEX_POINT('',#60885);
#3505=VERTEX_POINT('',#61080);
#3506=VERTEX_POINT('',#61278);
#3507=VERTEX_POINT('',#61279);
#3508=VERTEX_POINT('',#61281);
#3509=VERTEX_POINT('',#61687);
#3510=VERTEX_POINT('',#61688);
#3511=VERTEX_POINT('',#61892);
#3512=VERTEX_POINT('',#61912);
#3513=VERTEX_POINT('',#61913);
#3514=VERTEX_POINT('',#61915);
#3515=VERTEX_POINT('',#61932);
#3516=VERTEX_POINT('',#62134);
#3517=VERTEX_POINT('',#62135);
#3518=VERTEX_POINT('',#62137);
#3519=VERTEX_POINT('',#62519);
#3520=VERTEX_POINT('',#62520);
#3521=VERTEX_POINT('',#62522);
#3522=VERTEX_POINT('',#62733);
#3523=VERTEX_POINT('',#62949);
#3524=VERTEX_POINT('',#62950);
#3525=VERTEX_POINT('',#63381);
#3526=VERTEX_POINT('',#63382);
#3527=VERTEX_POINT('',#63384);
#3528=VERTEX_POINT('',#63399);
#3529=VERTEX_POINT('',#63597);
#3530=VERTEX_POINT('',#63598);
#3531=VERTEX_POINT('',#63600);
#3532=VERTEX_POINT('',#64062);
#3533=VERTEX_POINT('',#64063);
#3534=VERTEX_POINT('',#64065);
#3535=VERTEX_POINT('',#64344);
#3536=VERTEX_POINT('',#64556);
#3537=VERTEX_POINT('',#64557);
#3538=VERTEX_POINT('',#64970);
#3539=VERTEX_POINT('',#64971);
#3540=VERTEX_POINT('',#64973);
#3541=VERTEX_POINT('',#64988);
#3542=VERTEX_POINT('',#65188);
#3543=VERTEX_POINT('',#65189);
#3544=VERTEX_POINT('',#65196);
#3545=VERTEX_POINT('',#65198);
#3546=VERTEX_POINT('',#65204);
#3547=VERTEX_POINT('',#65416);
#3548=VERTEX_POINT('',#65628);
#3549=VERTEX_POINT('',#65837);
#3550=VERTEX_POINT('',#65848);
#3551=VERTEX_POINT('',#65859);
#3552=VERTEX_POINT('',#66068);
#3553=VERTEX_POINT('',#66280);
#3554=VERTEX_POINT('',#66291);
#3555=VERTEX_POINT('',#66303);
#3556=VERTEX_POINT('',#66512);
#3557=VERTEX_POINT('',#66721);
#3558=VERTEX_POINT('',#66733);
#3559=VERTEX_POINT('',#66744);
#3560=VERTEX_POINT('',#66953);
#3561=VERTEX_POINT('',#67138);
#3562=VERTEX_POINT('',#67140);
#3563=VERTEX_POINT('',#67295);
#3564=VERTEX_POINT('',#67306);
#3565=VERTEX_POINT('',#67515);
#3566=VERTEX_POINT('',#67527);
#3567=VERTEX_POINT('',#67739);
#3568=VERTEX_POINT('',#67948);
#3569=VERTEX_POINT('',#67960);
#3570=VERTEX_POINT('',#68172);
#3571=VERTEX_POINT('',#68381);
#3572=VERTEX_POINT('',#68393);
#3573=VERTEX_POINT('',#68605);
#3574=VERTEX_POINT('',#68616);
#3575=VERTEX_POINT('',#68628);
#3576=VERTEX_POINT('',#68851);
#3577=VERTEX_POINT('',#68856);
#3578=VERTEX_POINT('',#69044);
#3579=VERTEX_POINT('',#69046);
#3580=VERTEX_POINT('',#69204);
#3581=VERTEX_POINT('',#69299);
#3582=VERTEX_POINT('',#69338);
#3583=VERTEX_POINT('',#70253);
#3584=VERTEX_POINT('',#70350);
#3585=VERTEX_POINT('',#70351);
#3586=VERTEX_POINT('',#70353);
#3587=VERTEX_POINT('',#70355);
#3588=VERTEX_POINT('',#70359);
#3589=VERTEX_POINT('',#70361);
#3590=VERTEX_POINT('',#70365);
#3591=VERTEX_POINT('',#70367);
#3592=VERTEX_POINT('',#70371);
#3593=VERTEX_POINT('',#70373);
#3594=VERTEX_POINT('',#70377);
#3595=VERTEX_POINT('',#70379);
#3596=VERTEX_POINT('',#70387);
#3597=VERTEX_POINT('',#70390);
#4671=EDGE_CURVE('',#3492,#3493,#2219,.T.);
#4672=EDGE_CURVE('',#3494,#3492,#660,.F.);
#4673=EDGE_CURVE('',#3495,#3494,#2810,.T.);
#4674=EDGE_CURVE('',#3495,#3493,#661,.T.);
#4675=EDGE_CURVE('',#3496,#3497,#2220,.T.);
#4676=EDGE_CURVE('',#3492,#3496,#662,.F.);
#4677=EDGE_CURVE('',#3493,#3498,#663,.T.);
#4678=EDGE_CURVE('',#3498,#3497,#664,.T.);
#4679=EDGE_CURVE('',#3499,#3500,#2221,.T.);
#4680=EDGE_CURVE('',#3501,#3499,#665,.T.);
#4681=EDGE_CURVE('',#3496,#3501,#666,.F.);
#4682=EDGE_CURVE('',#3497,#3500,#667,.T.);
#4683=EDGE_CURVE('',#3502,#3503,#2222,.T.);
#4684=EDGE_CURVE('',#3504,#3502,#668,.T.);
#4685=EDGE_CURVE('',#3499,#3504,#669,.T.);
#4686=EDGE_CURVE('',#3500,#3505,#670,.T.);
#4687=EDGE_CURVE('',#3505,#3503,#671,.T.);
#4688=EDGE_CURVE('',#3506,#3507,#2223,.T.);
#4689=EDGE_CURVE('',#3508,#3506,#672,.F.);
#4690=EDGE_CURVE('',#3502,#3508,#673,.T.);
#4691=EDGE_CURVE('',#3503,#3507,#674,.T.);
#4692=EDGE_CURVE('',#3509,#3510,#2224,.T.);
#4693=EDGE_CURVE('',#3506,#3509,#675,.F.);
#4694=EDGE_CURVE('',#3507,#3511,#676,.T.);
#4695=EDGE_CURVE('',#3511,#3510,#677,.T.);
#4696=EDGE_CURVE('',#3512,#3513,#2225,.T.);
#4697=EDGE_CURVE('',#3514,#3512,#678,.T.);
#4698=EDGE_CURVE('',#3509,#3514,#679,.F.);
#4699=EDGE_CURVE('',#3510,#3515,#680,.T.);
#4700=EDGE_CURVE('',#3515,#3513,#681,.T.);
#4701=EDGE_CURVE('',#3516,#3517,#2226,.T.);
#4702=EDGE_CURVE('',#3518,#3516,#682,.T.);
#4703=EDGE_CURVE('',#3512,#3518,#683,.T.);
#4704=EDGE_CURVE('',#3513,#3517,#684,.T.);
#4705=EDGE_CURVE('',#3519,#3520,#2227,.T.);
#4706=EDGE_CURVE('',#3521,#3519,#685,.F.);
#4707=EDGE_CURVE('',#3516,#3521,#686,.T.);
#4708=EDGE_CURVE('',#3517,#3522,#687,.T.);
#4709=EDGE_CURVE('',#3522,#3520,#688,.T.);
#4710=EDGE_CURVE('',#3523,#3524,#2228,.T.);
#4711=EDGE_CURVE('',#3519,#3523,#689,.F.);
#4712=EDGE_CURVE('',#3520,#3524,#690,.T.);
#4713=EDGE_CURVE('',#3525,#3526,#2229,.T.);
#4714=EDGE_CURVE('',#3527,#3525,#691,.T.);
#4715=EDGE_CURVE('',#3523,#3527,#692,.F.);
#4716=EDGE_CURVE('',#3524,#3528,#693,.T.);
#4717=EDGE_CURVE('',#3528,#3526,#694,.T.);
#4718=EDGE_CURVE('',#3529,#3530,#2230,.T.);
#4719=EDGE_CURVE('',#3531,#3529,#695,.T.);
#4720=EDGE_CURVE('',#3525,#3531,#696,.T.);
#4721=EDGE_CURVE('',#3526,#3530,#697,.T.);
#4722=EDGE_CURVE('',#3532,#3533,#2231,.T.);
#4723=EDGE_CURVE('',#3534,#3532,#698,.F.);
#4724=EDGE_CURVE('',#3529,#3534,#699,.T.);
#4725=EDGE_CURVE('',#3530,#3535,#700,.T.);
#4726=EDGE_CURVE('',#3535,#3533,#701,.T.);
#4727=EDGE_CURVE('',#3536,#3537,#2232,.T.);
#4728=EDGE_CURVE('',#3532,#3536,#702,.F.);
#4729=EDGE_CURVE('',#3533,#3537,#703,.T.);
#4730=EDGE_CURVE('',#3538,#3539,#2233,.T.);
#4731=EDGE_CURVE('',#3540,#3538,#704,.T.);
#4732=EDGE_CURVE('',#3536,#3540,#705,.F.);
#4733=EDGE_CURVE('',#3537,#3541,#706,.T.);
#4734=EDGE_CURVE('',#3541,#3539,#707,.T.);
#4735=EDGE_CURVE('',#3542,#3543,#708,.T.);
#4736=EDGE_CURVE('',#3543,#3544,#2811,.F.);
#4737=EDGE_CURVE('',#3544,#3545,#709,.T.);
#4738=EDGE_CURVE('',#3545,#3546,#710,.T.);
#4739=EDGE_CURVE('',#3546,#3547,#711,.T.);
#4740=EDGE_CURVE('',#3547,#3548,#712,.T.);
#4741=EDGE_CURVE('',#3548,#3549,#713,.T.);
#4742=EDGE_CURVE('',#3549,#3550,#714,.T.);
#4743=EDGE_CURVE('',#3550,#3551,#715,.T.);
#4744=EDGE_CURVE('',#3551,#3552,#716,.T.);
#4745=EDGE_CURVE('',#3552,#3553,#717,.T.);
#4746=EDGE_CURVE('',#3553,#3554,#718,.T.);
#4747=EDGE_CURVE('',#3554,#3555,#719,.T.);
#4748=EDGE_CURVE('',#3555,#3556,#720,.T.);
#4749=EDGE_CURVE('',#3556,#3557,#721,.T.);
#4750=EDGE_CURVE('',#3557,#3558,#722,.T.);
#4751=EDGE_CURVE('',#3558,#3559,#723,.T.);
#4752=EDGE_CURVE('',#3559,#3560,#724,.T.);
#4753=EDGE_CURVE('',#3560,#3561,#2812,.T.);
#4754=EDGE_CURVE('',#3561,#3562,#725,.T.);
#4755=EDGE_CURVE('',#3562,#3563,#726,.T.);
#4756=EDGE_CURVE('',#3563,#3564,#727,.T.);
#4757=EDGE_CURVE('',#3564,#3565,#728,.T.);
#4758=EDGE_CURVE('',#3565,#3566,#729,.T.);
#4759=EDGE_CURVE('',#3566,#3567,#730,.T.);
#4760=EDGE_CURVE('',#3567,#3568,#731,.T.);
#4761=EDGE_CURVE('',#3568,#3569,#732,.T.);
#4762=EDGE_CURVE('',#3569,#3570,#733,.T.);
#4763=EDGE_CURVE('',#3570,#3571,#734,.T.);
#4764=EDGE_CURVE('',#3571,#3572,#735,.T.);
#4765=EDGE_CURVE('',#3572,#3573,#736,.T.);
#4766=EDGE_CURVE('',#3573,#3574,#737,.T.);
#4767=EDGE_CURVE('',#3574,#3575,#738,.T.);
#4768=EDGE_CURVE('',#3575,#3542,#739,.T.);
#4769=EDGE_CURVE('',#3539,#3576,#740,.T.);
#4770=EDGE_CURVE('',#3576,#3577,#741,.T.);
#4771=EDGE_CURVE('',#3577,#3578,#2813,.T.);
#4772=EDGE_CURVE('',#3579,#3578,#742,.T.);
#4773=EDGE_CURVE('',#3538,#3579,#743,.T.);
#4774=EDGE_CURVE('',#3578,#3580,#744,.T.);
#4775=EDGE_CURVE('',#3561,#3577,#745,.T.);
#4776=EDGE_CURVE('',#3581,#3560,#746,.T.);
#4777=EDGE_CURVE('',#3580,#3581,#747,.T.);
#4778=EDGE_CURVE('',#3580,#3582,#2234,.T.);
#4779=EDGE_CURVE('',#3582,#3582,#2814,.T.);
#4780=EDGE_CURVE('',#3543,#3495,#748,.T.);
#4781=EDGE_CURVE('',#3583,#3544,#749,.T.);
#4782=EDGE_CURVE('',#3583,#3494,#750,.T.);
#4783=EDGE_CURVE('',#3584,#3585,#2235,.T.);
#4784=EDGE_CURVE('',#3584,#3586,#2236,.T.);
#4785=EDGE_CURVE('',#3586,#3587,#2237,.T.);
#4786=EDGE_CURVE('',#3585,#3587,#2238,.T.);
#4787=EDGE_CURVE('',#3588,#3584,#2239,.T.);
#4788=EDGE_CURVE('',#3588,#3589,#2240,.T.);
#4789=EDGE_CURVE('',#3589,#3586,#2241,.T.);
#4790=EDGE_CURVE('',#3590,#3588,#2242,.T.);
#4791=EDGE_CURVE('',#3590,#3591,#2243,.T.);
#4792=EDGE_CURVE('',#3591,#3589,#2244,.T.);
#4793=EDGE_CURVE('',#3592,#3590,#2245,.T.);
#4794=EDGE_CURVE('',#3592,#3593,#2246,.T.);
#4795=EDGE_CURVE('',#3593,#3591,#2247,.T.);
#4796=EDGE_CURVE('',#3594,#3592,#2248,.T.);
#4797=EDGE_CURVE('',#3594,#3595,#2249,.T.);
#4798=EDGE_CURVE('',#3595,#3593,#2250,.T.);
#4799=EDGE_CURVE('',#3585,#3594,#2251,.T.);
#4800=EDGE_CURVE('',#3587,#3595,#2252,.T.);
#4801=EDGE_CURVE('',#3596,#3596,#2815,.T.);
#4802=EDGE_CURVE('',#3596,#3597,#2253,.T.);
#4803=EDGE_CURVE('',#3597,#3597,#2816,.T.);
#6812=ORIENTED_EDGE('',*,*,#4671,.F.);
#6813=ORIENTED_EDGE('',*,*,#4672,.F.);
#6814=ORIENTED_EDGE('',*,*,#4673,.F.);
#6815=ORIENTED_EDGE('',*,*,#4674,.T.);
#6816=ORIENTED_EDGE('',*,*,#4675,.F.);
#6817=ORIENTED_EDGE('',*,*,#4676,.F.);
#6818=ORIENTED_EDGE('',*,*,#4671,.T.);
#6819=ORIENTED_EDGE('',*,*,#4677,.T.);
#6820=ORIENTED_EDGE('',*,*,#4678,.T.);
#6821=ORIENTED_EDGE('',*,*,#4679,.F.);
#6822=ORIENTED_EDGE('',*,*,#4680,.F.);
#6823=ORIENTED_EDGE('',*,*,#4681,.F.);
#6824=ORIENTED_EDGE('',*,*,#4675,.T.);
#6825=ORIENTED_EDGE('',*,*,#4682,.T.);
#6826=ORIENTED_EDGE('',*,*,#4683,.F.);
#6827=ORIENTED_EDGE('',*,*,#4684,.F.);
#6828=ORIENTED_EDGE('',*,*,#4685,.F.);
#6829=ORIENTED_EDGE('',*,*,#4679,.T.);
#6830=ORIENTED_EDGE('',*,*,#4686,.T.);
#6831=ORIENTED_EDGE('',*,*,#4687,.T.);
#6832=ORIENTED_EDGE('',*,*,#4688,.F.);
#6833=ORIENTED_EDGE('',*,*,#4689,.F.);
#6834=ORIENTED_EDGE('',*,*,#4690,.F.);
#6835=ORIENTED_EDGE('',*,*,#4683,.T.);
#6836=ORIENTED_EDGE('',*,*,#4691,.T.);
#6837=ORIENTED_EDGE('',*,*,#4692,.F.);
#6838=ORIENTED_EDGE('',*,*,#4693,.F.);
#6839=ORIENTED_EDGE('',*,*,#4688,.T.);
#6840=ORIENTED_EDGE('',*,*,#4694,.T.);
#6841=ORIENTED_EDGE('',*,*,#4695,.T.);
#6842=ORIENTED_EDGE('',*,*,#4696,.F.);
#6843=ORIENTED_EDGE('',*,*,#4697,.F.);
#6844=ORIENTED_EDGE('',*,*,#4698,.F.);
#6845=ORIENTED_EDGE('',*,*,#4692,.T.);
#6846=ORIENTED_EDGE('',*,*,#4699,.T.);
#6847=ORIENTED_EDGE('',*,*,#4700,.T.);
#6848=ORIENTED_EDGE('',*,*,#4701,.F.);
#6849=ORIENTED_EDGE('',*,*,#4702,.F.);
#6850=ORIENTED_EDGE('',*,*,#4703,.F.);
#6851=ORIENTED_EDGE('',*,*,#4696,.T.);
#6852=ORIENTED_EDGE('',*,*,#4704,.T.);
#6853=ORIENTED_EDGE('',*,*,#4705,.F.);
#6854=ORIENTED_EDGE('',*,*,#4706,.F.);
#6855=ORIENTED_EDGE('',*,*,#4707,.F.);
#6856=ORIENTED_EDGE('',*,*,#4701,.T.);
#6857=ORIENTED_EDGE('',*,*,#4708,.T.);
#6858=ORIENTED_EDGE('',*,*,#4709,.T.);
#6859=ORIENTED_EDGE('',*,*,#4710,.F.);
#6860=ORIENTED_EDGE('',*,*,#4711,.F.);
#6861=ORIENTED_EDGE('',*,*,#4705,.T.);
#6862=ORIENTED_EDGE('',*,*,#4712,.T.);
#6863=ORIENTED_EDGE('',*,*,#4713,.F.);
#6864=ORIENTED_EDGE('',*,*,#4714,.F.);
#6865=ORIENTED_EDGE('',*,*,#4715,.F.);
#6866=ORIENTED_EDGE('',*,*,#4710,.T.);
#6867=ORIENTED_EDGE('',*,*,#4716,.T.);
#6868=ORIENTED_EDGE('',*,*,#4717,.T.);
#6869=ORIENTED_EDGE('',*,*,#4718,.F.);
#6870=ORIENTED_EDGE('',*,*,#4719,.F.);
#6871=ORIENTED_EDGE('',*,*,#4720,.F.);
#6872=ORIENTED_EDGE('',*,*,#4713,.T.);
#6873=ORIENTED_EDGE('',*,*,#4721,.T.);
#6874=ORIENTED_EDGE('',*,*,#4722,.F.);
#6875=ORIENTED_EDGE('',*,*,#4723,.F.);
#6876=ORIENTED_EDGE('',*,*,#4724,.F.);
#6877=ORIENTED_EDGE('',*,*,#4718,.T.);
#6878=ORIENTED_EDGE('',*,*,#4725,.T.);
#6879=ORIENTED_EDGE('',*,*,#4726,.T.);
#6880=ORIENTED_EDGE('',*,*,#4727,.F.);
#6881=ORIENTED_EDGE('',*,*,#4728,.F.);
#6882=ORIENTED_EDGE('',*,*,#4722,.T.);
#6883=ORIENTED_EDGE('',*,*,#4729,.T.);
#6884=ORIENTED_EDGE('',*,*,#4730,.F.);
#6885=ORIENTED_EDGE('',*,*,#4731,.F.);
#6886=ORIENTED_EDGE('',*,*,#4732,.F.);
#6887=ORIENTED_EDGE('',*,*,#4727,.T.);
#6888=ORIENTED_EDGE('',*,*,#4733,.T.);
#6889=ORIENTED_EDGE('',*,*,#4734,.T.);
#6890=ORIENTED_EDGE('',*,*,#4735,.T.);
#6891=ORIENTED_EDGE('',*,*,#4736,.T.);
#6892=ORIENTED_EDGE('',*,*,#4737,.T.);
#6893=ORIENTED_EDGE('',*,*,#4738,.T.);
#6894=ORIENTED_EDGE('',*,*,#4739,.T.);
#6895=ORIENTED_EDGE('',*,*,#4740,.T.);
#6896=ORIENTED_EDGE('',*,*,#4741,.T.);
#6897=ORIENTED_EDGE('',*,*,#4742,.T.);
#6898=ORIENTED_EDGE('',*,*,#4743,.T.);
#6899=ORIENTED_EDGE('',*,*,#4744,.T.);
#6900=ORIENTED_EDGE('',*,*,#4745,.T.);
#6901=ORIENTED_EDGE('',*,*,#4746,.T.);
#6902=ORIENTED_EDGE('',*,*,#4747,.T.);
#6903=ORIENTED_EDGE('',*,*,#4748,.T.);
#6904=ORIENTED_EDGE('',*,*,#4749,.T.);
#6905=ORIENTED_EDGE('',*,*,#4750,.T.);
#6906=ORIENTED_EDGE('',*,*,#4751,.T.);
#6907=ORIENTED_EDGE('',*,*,#4752,.T.);
#6908=ORIENTED_EDGE('',*,*,#4753,.T.);
#6909=ORIENTED_EDGE('',*,*,#4754,.T.);
#6910=ORIENTED_EDGE('',*,*,#4755,.T.);
#6911=ORIENTED_EDGE('',*,*,#4756,.T.);
#6912=ORIENTED_EDGE('',*,*,#4757,.T.);
#6913=ORIENTED_EDGE('',*,*,#4758,.T.);
#6914=ORIENTED_EDGE('',*,*,#4759,.T.);
#6915=ORIENTED_EDGE('',*,*,#4760,.T.);
#6916=ORIENTED_EDGE('',*,*,#4761,.T.);
#6917=ORIENTED_EDGE('',*,*,#4762,.T.);
#6918=ORIENTED_EDGE('',*,*,#4763,.T.);
#6919=ORIENTED_EDGE('',*,*,#4764,.T.);
#6920=ORIENTED_EDGE('',*,*,#4765,.T.);
#6921=ORIENTED_EDGE('',*,*,#4766,.T.);
#6922=ORIENTED_EDGE('',*,*,#4767,.T.);
#6923=ORIENTED_EDGE('',*,*,#4768,.T.);
#6924=ORIENTED_EDGE('',*,*,#4730,.T.);
#6925=ORIENTED_EDGE('',*,*,#4769,.T.);
#6926=ORIENTED_EDGE('',*,*,#4770,.T.);
#6927=ORIENTED_EDGE('',*,*,#4771,.T.);
#6928=ORIENTED_EDGE('',*,*,#4772,.F.);
#6929=ORIENTED_EDGE('',*,*,#4773,.F.);
#6930=ORIENTED_EDGE('',*,*,#4774,.F.);
#6931=ORIENTED_EDGE('',*,*,#4771,.F.);
#6932=ORIENTED_EDGE('',*,*,#4775,.F.);
#6933=ORIENTED_EDGE('',*,*,#4753,.F.);
#6934=ORIENTED_EDGE('',*,*,#4776,.F.);
#6935=ORIENTED_EDGE('',*,*,#4777,.F.);
#6936=ORIENTED_EDGE('',*,*,#4778,.T.);
#6937=ORIENTED_EDGE('',*,*,#4779,.F.);
#6938=ORIENTED_EDGE('',*,*,#4778,.F.);
#6939=ORIENTED_EDGE('',*,*,#4775,.T.);
#6940=ORIENTED_EDGE('',*,*,#4770,.F.);
#6941=ORIENTED_EDGE('',*,*,#4769,.F.);
#6942=ORIENTED_EDGE('',*,*,#4734,.F.);
#6943=ORIENTED_EDGE('',*,*,#4733,.F.);
#6944=ORIENTED_EDGE('',*,*,#4729,.F.);
#6945=ORIENTED_EDGE('',*,*,#4726,.F.);
#6946=ORIENTED_EDGE('',*,*,#4725,.F.);
#6947=ORIENTED_EDGE('',*,*,#4721,.F.);
#6948=ORIENTED_EDGE('',*,*,#4717,.F.);
#6949=ORIENTED_EDGE('',*,*,#4716,.F.);
#6950=ORIENTED_EDGE('',*,*,#4712,.F.);
#6951=ORIENTED_EDGE('',*,*,#4709,.F.);
#6952=ORIENTED_EDGE('',*,*,#4708,.F.);
#6953=ORIENTED_EDGE('',*,*,#4704,.F.);
#6954=ORIENTED_EDGE('',*,*,#4700,.F.);
#6955=ORIENTED_EDGE('',*,*,#4699,.F.);
#6956=ORIENTED_EDGE('',*,*,#4695,.F.);
#6957=ORIENTED_EDGE('',*,*,#4694,.F.);
#6958=ORIENTED_EDGE('',*,*,#4691,.F.);
#6959=ORIENTED_EDGE('',*,*,#4687,.F.);
#6960=ORIENTED_EDGE('',*,*,#4686,.F.);
#6961=ORIENTED_EDGE('',*,*,#4682,.F.);
#6962=ORIENTED_EDGE('',*,*,#4678,.F.);
#6963=ORIENTED_EDGE('',*,*,#4677,.F.);
#6964=ORIENTED_EDGE('',*,*,#4674,.F.);
#6965=ORIENTED_EDGE('',*,*,#4780,.F.);
#6966=ORIENTED_EDGE('',*,*,#4735,.F.);
#6967=ORIENTED_EDGE('',*,*,#4768,.F.);
#6968=ORIENTED_EDGE('',*,*,#4767,.F.);
#6969=ORIENTED_EDGE('',*,*,#4766,.F.);
#6970=ORIENTED_EDGE('',*,*,#4765,.F.);
#6971=ORIENTED_EDGE('',*,*,#4764,.F.);
#6972=ORIENTED_EDGE('',*,*,#4763,.F.);
#6973=ORIENTED_EDGE('',*,*,#4762,.F.);
#6974=ORIENTED_EDGE('',*,*,#4761,.F.);
#6975=ORIENTED_EDGE('',*,*,#4760,.F.);
#6976=ORIENTED_EDGE('',*,*,#4759,.F.);
#6977=ORIENTED_EDGE('',*,*,#4758,.F.);
#6978=ORIENTED_EDGE('',*,*,#4757,.F.);
#6979=ORIENTED_EDGE('',*,*,#4756,.F.);
#6980=ORIENTED_EDGE('',*,*,#4755,.F.);
#6981=ORIENTED_EDGE('',*,*,#4754,.F.);
#6982=ORIENTED_EDGE('',*,*,#4774,.T.);
#6983=ORIENTED_EDGE('',*,*,#4777,.T.);
#6984=ORIENTED_EDGE('',*,*,#4776,.T.);
#6985=ORIENTED_EDGE('',*,*,#4752,.F.);
#6986=ORIENTED_EDGE('',*,*,#4751,.F.);
#6987=ORIENTED_EDGE('',*,*,#4750,.F.);
#6988=ORIENTED_EDGE('',*,*,#4749,.F.);
#6989=ORIENTED_EDGE('',*,*,#4748,.F.);
#6990=ORIENTED_EDGE('',*,*,#4747,.F.);
#6991=ORIENTED_EDGE('',*,*,#4746,.F.);
#6992=ORIENTED_EDGE('',*,*,#4745,.F.);
#6993=ORIENTED_EDGE('',*,*,#4744,.F.);
#6994=ORIENTED_EDGE('',*,*,#4743,.F.);
#6995=ORIENTED_EDGE('',*,*,#4742,.F.);
#6996=ORIENTED_EDGE('',*,*,#4741,.F.);
#6997=ORIENTED_EDGE('',*,*,#4740,.F.);
#6998=ORIENTED_EDGE('',*,*,#4739,.F.);
#6999=ORIENTED_EDGE('',*,*,#4738,.F.);
#7000=ORIENTED_EDGE('',*,*,#4737,.F.);
#7001=ORIENTED_EDGE('',*,*,#4781,.F.);
#7002=ORIENTED_EDGE('',*,*,#4782,.T.);
#7003=ORIENTED_EDGE('',*,*,#4672,.T.);
#7004=ORIENTED_EDGE('',*,*,#4676,.T.);
#7005=ORIENTED_EDGE('',*,*,#4681,.T.);
#7006=ORIENTED_EDGE('',*,*,#4680,.T.);
#7007=ORIENTED_EDGE('',*,*,#4685,.T.);
#7008=ORIENTED_EDGE('',*,*,#4684,.T.);
#7009=ORIENTED_EDGE('',*,*,#4690,.T.);
#7010=ORIENTED_EDGE('',*,*,#4689,.T.);
#7011=ORIENTED_EDGE('',*,*,#4693,.T.);
#7012=ORIENTED_EDGE('',*,*,#4698,.T.);
#7013=ORIENTED_EDGE('',*,*,#4697,.T.);
#7014=ORIENTED_EDGE('',*,*,#4703,.T.);
#7015=ORIENTED_EDGE('',*,*,#4702,.T.);
#7016=ORIENTED_EDGE('',*,*,#4707,.T.);
#7017=ORIENTED_EDGE('',*,*,#4706,.T.);
#7018=ORIENTED_EDGE('',*,*,#4711,.T.);
#7019=ORIENTED_EDGE('',*,*,#4715,.T.);
#7020=ORIENTED_EDGE('',*,*,#4714,.T.);
#7021=ORIENTED_EDGE('',*,*,#4720,.T.);
#7022=ORIENTED_EDGE('',*,*,#4719,.T.);
#7023=ORIENTED_EDGE('',*,*,#4724,.T.);
#7024=ORIENTED_EDGE('',*,*,#4723,.T.);
#7025=ORIENTED_EDGE('',*,*,#4728,.T.);
#7026=ORIENTED_EDGE('',*,*,#4732,.T.);
#7027=ORIENTED_EDGE('',*,*,#4731,.T.);
#7028=ORIENTED_EDGE('',*,*,#4773,.T.);
#7029=ORIENTED_EDGE('',*,*,#4772,.T.);
#7030=ORIENTED_EDGE('',*,*,#4783,.F.);
#7031=ORIENTED_EDGE('',*,*,#4784,.T.);
#7032=ORIENTED_EDGE('',*,*,#4785,.T.);
#7033=ORIENTED_EDGE('',*,*,#4786,.F.);
#7034=ORIENTED_EDGE('',*,*,#4787,.F.);
#7035=ORIENTED_EDGE('',*,*,#4788,.T.);
#7036=ORIENTED_EDGE('',*,*,#4789,.T.);
#7037=ORIENTED_EDGE('',*,*,#4784,.F.);
#7038=ORIENTED_EDGE('',*,*,#4790,.F.);
#7039=ORIENTED_EDGE('',*,*,#4791,.T.);
#7040=ORIENTED_EDGE('',*,*,#4792,.T.);
#7041=ORIENTED_EDGE('',*,*,#4788,.F.);
#7042=ORIENTED_EDGE('',*,*,#4793,.F.);
#7043=ORIENTED_EDGE('',*,*,#4794,.T.);
#7044=ORIENTED_EDGE('',*,*,#4795,.T.);
#7045=ORIENTED_EDGE('',*,*,#4791,.F.);
#7046=ORIENTED_EDGE('',*,*,#4796,.F.);
#7047=ORIENTED_EDGE('',*,*,#4797,.T.);
#7048=ORIENTED_EDGE('',*,*,#4798,.T.);
#7049=ORIENTED_EDGE('',*,*,#4794,.F.);
#7050=ORIENTED_EDGE('',*,*,#4799,.F.);
#7051=ORIENTED_EDGE('',*,*,#4786,.T.);
#7052=ORIENTED_EDGE('',*,*,#4800,.T.);
#7053=ORIENTED_EDGE('',*,*,#4797,.F.);
#7054=ORIENTED_EDGE('',*,*,#4800,.F.);
#7055=ORIENTED_EDGE('',*,*,#4785,.F.);
#7056=ORIENTED_EDGE('',*,*,#4789,.F.);
#7057=ORIENTED_EDGE('',*,*,#4792,.F.);
#7058=ORIENTED_EDGE('',*,*,#4795,.F.);
#7059=ORIENTED_EDGE('',*,*,#4798,.F.);
#7060=ORIENTED_EDGE('',*,*,#4801,.T.);
#7061=ORIENTED_EDGE('',*,*,#4780,.T.);
#7062=ORIENTED_EDGE('',*,*,#4673,.T.);
#7063=ORIENTED_EDGE('',*,*,#4782,.F.);
#7064=ORIENTED_EDGE('',*,*,#4781,.T.);
#7065=ORIENTED_EDGE('',*,*,#4736,.F.);
#7066=ORIENTED_EDGE('',*,*,#4801,.F.);
#7067=ORIENTED_EDGE('',*,*,#4802,.T.);
#7068=ORIENTED_EDGE('',*,*,#4803,.T.);
#7069=ORIENTED_EDGE('',*,*,#4802,.F.);
#7070=ORIENTED_EDGE('',*,*,#4803,.F.);
#7071=ORIENTED_EDGE('',*,*,#4783,.T.);
#7072=ORIENTED_EDGE('',*,*,#4799,.T.);
#7073=ORIENTED_EDGE('',*,*,#4796,.T.);
#7074=ORIENTED_EDGE('',*,*,#4793,.T.);
#7075=ORIENTED_EDGE('',*,*,#4790,.T.);
#7076=ORIENTED_EDGE('',*,*,#4787,.T.);
#7077=ORIENTED_EDGE('',*,*,#4779,.T.);
#7814=CYLINDRICAL_SURFACE('',#8774,2.37175);
#7815=CYLINDRICAL_SURFACE('',#8776,2.37175);
#7816=CYLINDRICAL_SURFACE('',#8777,2.37175);
#7817=CYLINDRICAL_SURFACE('',#8778,2.37175);
#7818=CYLINDRICAL_SURFACE('',#8779,2.37175);
#7819=CYLINDRICAL_SURFACE('',#8780,2.37175);
#7820=CYLINDRICAL_SURFACE('',#8781,2.37175);
#7821=CYLINDRICAL_SURFACE('',#8782,2.37175);
#7822=CYLINDRICAL_SURFACE('',#8783,2.37175);
#7823=CYLINDRICAL_SURFACE('',#8784,2.37175);
#7824=CYLINDRICAL_SURFACE('',#8785,2.37175);
#7825=CYLINDRICAL_SURFACE('',#8786,2.37175);
#7826=CYLINDRICAL_SURFACE('',#8787,2.37175);
#7827=CYLINDRICAL_SURFACE('',#8788,2.37175);
#7828=CYLINDRICAL_SURFACE('',#8789,2.37175);
#7829=CYLINDRICAL_SURFACE('',#8790,2.942);
#7830=CYLINDRICAL_SURFACE('',#8793,2.37175);
#7831=CYLINDRICAL_SURFACE('',#8806,5.);
#8133=ADVANCED_FACE('',(#1396),#7814,.T.);
#8134=ADVANCED_FACE('',(#1397),#7815,.T.);
#8135=ADVANCED_FACE('',(#1398),#7816,.T.);
#8136=ADVANCED_FACE('',(#1399),#7817,.T.);
#8137=ADVANCED_FACE('',(#1400),#7818,.T.);
#8138=ADVANCED_FACE('',(#1401),#7819,.T.);
#8139=ADVANCED_FACE('',(#1402),#7820,.T.);
#8140=ADVANCED_FACE('',(#1403),#7821,.T.);
#8141=ADVANCED_FACE('',(#1404),#7822,.T.);
#8142=ADVANCED_FACE('',(#1405),#7823,.T.);
#8143=ADVANCED_FACE('',(#1406),#7824,.T.);
#8144=ADVANCED_FACE('',(#1407),#7825,.T.);
#8145=ADVANCED_FACE('',(#1408),#7826,.T.);
#8146=ADVANCED_FACE('',(#1409),#7827,.T.);
#8147=ADVANCED_FACE('',(#1410),#7828,.T.);
#8148=ADVANCED_FACE('',(#1411),#7829,.T.);
#8149=ADVANCED_FACE('',(#1412),#7830,.T.);
#8150=ADVANCED_FACE('',(#1413),#152,.T.);
#8151=ADVANCED_FACE('',(#1414),#162,.F.);
#8152=ADVANCED_FACE('',(#1415),#163,.F.);
#8153=ADVANCED_FACE('',(#1416),#1131,.F.);
#8154=ADVANCED_FACE('',(#1417),#1132,.F.);
#8155=ADVANCED_FACE('',(#1418),#1133,.F.);
#8156=ADVANCED_FACE('',(#1419),#1134,.F.);
#8157=ADVANCED_FACE('',(#1420),#1135,.F.);
#8158=ADVANCED_FACE('',(#1421),#1136,.F.);
#8159=ADVANCED_FACE('',(#1422),#1137,.F.);
#8160=ADVANCED_FACE('',(#1423,#1043),#1138,.T.);
#8161=ADVANCED_FACE('',(#1424),#7831,.T.);
#8162=ADVANCED_FACE('',(#1425,#1044),#1139,.F.);
#8163=ADVANCED_FACE('',(#1426),#1140,.T.);
#8261=CLOSED_SHELL('',(#8133,#8134,#8135,#8136,#8137,#8138,#8139,#8140,
#8141,#8142,#8143,#8144,#8145,#8146,#8147,#8148,#8149,#8150,#8151,#8152,
#8153,#8154,#8155,#8156,#8157,#8158,#8159,#8160,#8161,#8162,#8163));
#8773=AXIS2_PLACEMENT_3D('',#59874,#9911,#9912);
#8774=AXIS2_PLACEMENT_3D('',#59875,#9913,#9914);
#8775=AXIS2_PLACEMENT_3D('',#60101,#9916,#9917);
#8776=AXIS2_PLACEMENT_3D('',#60226,#9918,#9919);
#8777=AXIS2_PLACEMENT_3D('',#60645,#9921,#9922);
#8778=AXIS2_PLACEMENT_3D('',#60881,#9924,#9925);
#8779=AXIS2_PLACEMENT_3D('',#61277,#9927,#9928);
#8780=AXIS2_PLACEMENT_3D('',#61686,#9930,#9931);
#8781=AXIS2_PLACEMENT_3D('',#61911,#9933,#9934);
#8782=AXIS2_PLACEMENT_3D('',#62133,#9936,#9937);
#8783=AXIS2_PLACEMENT_3D('',#62518,#9939,#9940);
#8784=AXIS2_PLACEMENT_3D('',#62948,#9942,#9943);
#8785=AXIS2_PLACEMENT_3D('',#63380,#9945,#9946);
#8786=AXIS2_PLACEMENT_3D('',#63596,#9948,#9949);
#8787=AXIS2_PLACEMENT_3D('',#64061,#9951,#9952);
#8788=AXIS2_PLACEMENT_3D('',#64555,#9954,#9955);
#8789=AXIS2_PLACEMENT_3D('',#64969,#9957,#9958);
#8790=AXIS2_PLACEMENT_3D('',#65187,#9960,#9961);
#8791=AXIS2_PLACEMENT_3D('',#65197,#9962,#9963);
#8792=AXIS2_PLACEMENT_3D('',#67139,#9964,#9965);
#8793=AXIS2_PLACEMENT_3D('',#68850,#9966,#9967);
#8794=AXIS2_PLACEMENT_3D('',#69045,#9968,#9969);
#8795=AXIS2_PLACEMENT_3D('',#69203,#9970,#9971);
#8796=AXIS2_PLACEMENT_3D('',#69340,#9973,#9974);
#8797=AXIS2_PLACEMENT_3D('',#70349,#9975,#9976);
#8798=AXIS2_PLACEMENT_3D('',#70358,#9981,#9982);
#8799=AXIS2_PLACEMENT_3D('',#70364,#9986,#9987);
#8800=AXIS2_PLACEMENT_3D('',#70370,#9991,#9992);
#8801=AXIS2_PLACEMENT_3D('',#70376,#9996,#9997);
#8802=AXIS2_PLACEMENT_3D('',#70382,#10001,#10002);
#8803=AXIS2_PLACEMENT_3D('',#70385,#10005,#10006);
#8804=AXIS2_PLACEMENT_3D('',#70386,#10007,#10008);
#8805=AXIS2_PLACEMENT_3D('',#70388,#10009,#10010);
#8806=AXIS2_PLACEMENT_3D('',#70389,#10011,#10012);
#8807=AXIS2_PLACEMENT_3D('',#70392,#10014,#10015);
#8808=AXIS2_PLACEMENT_3D('',#70393,#10016,#10017);
#8809=AXIS2_PLACEMENT_3D('',#70394,#10018,#10019);
#9911=DIRECTION('axis',(0.,0.,1.));
#9912=DIRECTION('refdir',(1.,0.,0.));
#9913=DIRECTION('center_axis',(0.,0.,1.));
#9914=DIRECTION('ref_axis',(0.997339946684471,-0.0728905394918792,0.));
#9915=DIRECTION('',(0.,0.,-1.));
#9916=DIRECTION('center_axis',(0.,0.,-1.));
#9917=DIRECTION('ref_axis',(1.,1.10476514494527E-13,0.));
#9918=DIRECTION('center_axis',(0.,0.,1.));
#9919=DIRECTION('ref_axis',(0.997339946684471,-0.0728905394918792,0.));
#9920=DIRECTION('',(0.,0.,-1.));
#9921=DIRECTION('center_axis',(0.,0.,1.));
#9922=DIRECTION('ref_axis',(0.997339946684471,-0.0728905394918792,0.));
#9923=DIRECTION('',(0.,0.,-1.));
#9924=DIRECTION('center_axis',(0.,0.,1.));
#9925=DIRECTION('ref_axis',(0.997339946684471,-0.0728905394918792,0.));
#9926=DIRECTION('',(0.,0.,-1.));
#9927=DIRECTION('center_axis',(0.,0.,1.));
#9928=DIRECTION('ref_axis',(0.997339946684471,-0.0728905394918792,0.));
#9929=DIRECTION('',(0.,0.,-1.));
#9930=DIRECTION('center_axis',(0.,0.,1.));
#9931=DIRECTION('ref_axis',(0.997339946684471,-0.0728905394918792,0.));
#9932=DIRECTION('',(0.,0.,-1.));
#9933=DIRECTION('center_axis',(0.,0.,1.));
#9934=DIRECTION('ref_axis',(0.997339946684471,-0.0728905394918792,0.));
#9935=DIRECTION('',(0.,0.,-1.));
#9936=DIRECTION('center_axis',(0.,0.,1.));
#9937=DIRECTION('ref_axis',(0.997339946684471,-0.0728905394918792,0.));
#9938=DIRECTION('',(0.,0.,-1.));
#9939=DIRECTION('center_axis',(0.,0.,1.));
#9940=DIRECTION('ref_axis',(0.997339946684471,-0.0728905394918792,0.));
#9941=DIRECTION('',(0.,0.,-1.));
#9942=DIRECTION('center_axis',(0.,0.,1.));
#9943=DIRECTION('ref_axis',(0.997339946684471,-0.0728905394918792,0.));
#9944=DIRECTION('',(0.,0.,-1.));
#9945=DIRECTION('center_axis',(0.,0.,1.));
#9946=DIRECTION('ref_axis',(0.997339946684471,-0.0728905394918792,0.));
#9947=DIRECTION('',(0.,0.,-1.));
#9948=DIRECTION('center_axis',(0.,0.,1.));
#9949=DIRECTION('ref_axis',(0.997339946684471,-0.0728905394918792,0.));
#9950=DIRECTION('',(0.,0.,-1.));
#9951=DIRECTION('center_axis',(0.,0.,1.));
#9952=DIRECTION('ref_axis',(0.997339946684471,-0.0728905394918792,0.));
#9953=DIRECTION('',(0.,0.,-1.));
#9954=DIRECTION('center_axis',(0.,0.,1.));
#9955=DIRECTION('ref_axis',(0.997339946684471,-0.0728905394918792,0.));
#9956=DIRECTION('',(0.,0.,-1.));
#9957=DIRECTION('center_axis',(0.,0.,1.));
#9958=DIRECTION('ref_axis',(0.997339946684471,-0.0728905394918792,0.));
#9959=DIRECTION('',(0.,0.,-1.));
#9960=DIRECTION('center_axis',(0.,0.,1.));
#9961=DIRECTION('ref_axis',(1.,0.,0.));
#9962=DIRECTION('center_axis',(0.,0.,-1.));
#9963=DIRECTION('ref_axis',(1.,0.,0.));
#9964=DIRECTION('center_axis',(0.,0.,-1.));
#9965=DIRECTION('ref_axis',(1.,0.,0.));
#9966=DIRECTION('center_axis',(0.,0.,1.));
#9967=DIRECTION('ref_axis',(0.997339946684471,-0.0728905394918792,0.));
#9968=DIRECTION('center_axis',(0.,0.,-1.));
#9969=DIRECTION('ref_axis',(1.,1.10476514494527E-13,0.));
#9970=DIRECTION('center_axis',(0.,0.,-1.));
#9971=DIRECTION('ref_axis',(1.,0.,0.));
#9972=DIRECTION('',(0.707106781186547,-8.65956056235493E-17,0.707106781186548));
#9973=DIRECTION('center_axis',(0.,0.,1.));
#9974=DIRECTION('ref_axis',(1.,0.,0.));
#9975=DIRECTION('center_axis',(-1.92296268638356E-16,-1.,0.));
#9976=DIRECTION('ref_axis',(1.,-1.92296268638356E-16,0.));
#9977=DIRECTION('',(1.,-1.92296268638356E-16,0.));
#9978=DIRECTION('',(0.,0.,1.));
#9979=DIRECTION('',(1.,-1.92296268638356E-16,0.));
#9980=DIRECTION('',(0.,0.,1.));
#9981=DIRECTION('center_axis',(-0.866025403784439,-0.5,0.));
#9982=DIRECTION('ref_axis',(0.5,-0.866025403784439,0.));
#9983=DIRECTION('',(0.5,-0.866025403784439,0.));
#9984=DIRECTION('',(0.,0.,1.));
#9985=DIRECTION('',(0.5,-0.866025403784439,0.));
#9986=DIRECTION('center_axis',(-0.866025403784439,0.5,0.));
#9987=DIRECTION('ref_axis',(-0.5,-0.866025403784439,0.));
#9988=DIRECTION('',(-0.5,-0.866025403784439,0.));
#9989=DIRECTION('',(0.,0.,1.));
#9990=DIRECTION('',(-0.5,-0.866025403784439,0.));
#9991=DIRECTION('center_axis',(1.92296268638356E-16,1.,0.));
#9992=DIRECTION('ref_axis',(-1.,1.92296268638356E-16,0.));
#9993=DIRECTION('',(-1.,1.92296268638356E-16,0.));
#9994=DIRECTION('',(0.,0.,1.));
#9995=DIRECTION('',(-1.,1.92296268638356E-16,0.));
#9996=DIRECTION('center_axis',(0.866025403784439,0.5,0.));
#9997=DIRECTION('ref_axis',(-0.5,0.866025403784439,0.));
#9998=DIRECTION('',(-0.5,0.866025403784439,0.));
#9999=DIRECTION('',(0.,0.,1.));
#10000=DIRECTION('',(-0.5,0.866025403784439,0.));
#10001=DIRECTION('center_axis',(0.866025403784439,-0.5,0.));
#10002=DIRECTION('ref_axis',(0.5,0.866025403784439,0.));
#10003=DIRECTION('',(0.5,0.866025403784439,0.));
#10004=DIRECTION('',(0.5,0.866025403784439,0.));
#10005=DIRECTION('center_axis',(0.,0.,1.));
#10006=DIRECTION('ref_axis',(1.,0.,0.));
#10007=DIRECTION('center_axis',(0.,0.,1.));
#10008=DIRECTION('ref_axis',(1.,0.,0.));
#10009=DIRECTION('center_axis',(0.,0.,1.));
#10010=DIRECTION('ref_axis',(1.,0.,0.));
#10011=DIRECTION('center_axis',(0.,0.,1.));
#10012=DIRECTION('ref_axis',(1.,0.,0.));
#10013=DIRECTION('',(0.,0.,-1.));
#10014=DIRECTION('center_axis',(0.,0.,1.));
#10015=DIRECTION('ref_axis',(1.,0.,0.));
#10016=DIRECTION('center_axis',(0.,0.,1.));
#10017=DIRECTION('ref_axis',(1.,0.,0.));
#10018=DIRECTION('center_axis',(0.,0.,1.));
#10019=DIRECTION('ref_axis',(1.,0.,0.));
#59874=CARTESIAN_POINT('',(0.,0.,0.));
#59875=CARTESIAN_POINT('Origin',(0.,0.,-1.84858989190501));
#59876=CARTESIAN_POINT('',(-2.3654410179195,0.172878145651696,0.838781724910481));
#59877=CARTESIAN_POINT('',(-2.36544101854889,0.172878137039861,0.639858258416768));
#59878=CARTESIAN_POINT('',(-2.36544101854889,0.172878137039864,-1.84858989190501));
#59879=CARTESIAN_POINT('',(-1.35356952483514,-1.9475748006014,6.39245600897453E-15));
#59880=CARTESIAN_POINT('Ctrl Pts',(-2.3654410179195,0.172878145651696,0.838781724910481));
#59881=CARTESIAN_POINT('Ctrl Pts',(-2.36186465939432,0.221812411566921,
0.835334615307093));
#59882=CARTESIAN_POINT('Ctrl Pts',(-2.35677062881215,0.270624944567347,
0.83184711542494));
#59883=CARTESIAN_POINT('Ctrl Pts',(-2.33694122097281,0.416601558032087,
0.821281086510961));
#59884=CARTESIAN_POINT('Ctrl Pts',(-2.31768037501523,0.513036883753267,
0.814113668653049));
#59885=CARTESIAN_POINT('Ctrl Pts',(-2.28597334870978,0.632591079542157,
0.805094650590239));
#59886=CARTESIAN_POINT('Ctrl Pts',(-2.27905450086233,0.657081597685872,
0.803240261822677));
#59887=CARTESIAN_POINT('Ctrl Pts',(-2.24368658420091,0.774986184855901,
0.79428990008055));
#59888=CARTESIAN_POINT('Ctrl Pts',(-2.20987773177701,0.866705066958452,
0.787253905998845));
#59889=CARTESIAN_POINT('Ctrl Pts',(-2.16370961226913,0.971515839898839,
0.779308765321606));
#59890=CARTESIAN_POINT('Ctrl Pts',(-2.15674863856911,0.986872668338088,
0.778147236898505));
#59891=CARTESIAN_POINT('Ctrl Pts',(-2.14562043767858,1.01074269110853,0.776347313985111));
#59892=CARTESIAN_POINT('Ctrl Pts',(-2.1415651017538,1.01930700623228,0.775702640310355));
#59893=CARTESIAN_POINT('Ctrl Pts',(-2.1342657730286,1.03448632025165,0.774562320316757));
#59894=CARTESIAN_POINT('Ctrl Pts',(-2.13104224434626,1.04111060490884,0.774065492034439));
#59895=CARTESIAN_POINT('Ctrl Pts',(-2.12315470361223,1.05712920905827,0.772865916939248));
#59896=CARTESIAN_POINT('Ctrl Pts',(-2.11845917407976,1.06650775813566,0.772165100716468));
#59897=CARTESIAN_POINT('Ctrl Pts',(-2.10354419647061,1.09581078519145,0.769979200043173));
#59898=CARTESIAN_POINT('Ctrl Pts',(-2.09310436995499,1.11562253840262,0.768506828631546));
#59899=CARTESIAN_POINT('Ctrl Pts',(-2.03585578615508,1.22063023879177,0.760716543072306));
#59900=CARTESIAN_POINT('Ctrl Pts',(-1.98411825460355,1.30304485762746,0.754649036969893));
#59901=CARTESIAN_POINT('Ctrl Pts',(-1.82523675449555,1.52462596590747,0.73781782639295));
#59902=CARTESIAN_POINT('Ctrl Pts',(-1.70751693198461,1.65540217462058,0.727216805660831));
#59903=CARTESIAN_POINT('Ctrl Pts',(-1.54014420431978,1.80430483693017,0.71294069687559));
#59904=CARTESIAN_POINT('Ctrl Pts',(-1.50285088494264,1.83548326581983,0.709806324549395));
#59905=CARTESIAN_POINT('Ctrl Pts',(-1.44830866409291,1.87830523736781,0.705269145107943));
#59906=CARTESIAN_POINT('Ctrl Pts',(-1.43182222859937,1.89090285637174,0.703903594004995));
#59907=CARTESIAN_POINT('Ctrl Pts',(-1.40335800852905,1.91206724097651,0.701554667561739));
#59908=CARTESIAN_POINT('Ctrl Pts',(-1.39146164491344,1.92074186406775,0.700575504311545));
#59909=CARTESIAN_POINT('Ctrl Pts',(-1.3669883754162,1.93824066317396,0.698565893624467));
#59910=CARTESIAN_POINT('Ctrl Pts',(-1.35440497340061,1.94705450255701,0.697535116827317));
#59911=CARTESIAN_POINT('Ctrl Pts',(-1.32255276290548,1.96890667932377,0.694931662709459));
#59912=CARTESIAN_POINT('Ctrl Pts',(-1.30317644214468,1.98178465450931,0.693353118980663));
#59913=CARTESIAN_POINT('Ctrl Pts',(-1.22251483217302,2.03369986455857,0.686800868590589));
#59914=CARTESIAN_POINT('Ctrl Pts',(-1.15964659263396,2.0701921476143,0.681736995118589));
#59915=CARTESIAN_POINT('Ctrl Pts',(-0.974025572717844,2.16682660700429,
0.666903549043471));
#59916=CARTESIAN_POINT('Ctrl Pts',(-0.847628386542998,2.21932032730963,
0.656928480850742));
#59917=CARTESIAN_POINT('Ctrl Pts',(-0.608857015404388,2.29509626347655,
0.638676939884996));
#59918=CARTESIAN_POINT('Ctrl Pts',(-0.497928917510556,2.32169037878113,
0.63042264113472));
#59919=CARTESIAN_POINT('Ctrl Pts',(-0.368722491334158,2.34297486041688,
0.621337489821968));
#59920=CARTESIAN_POINT('Ctrl Pts',(-0.351906811332879,2.34555944485181,
0.620165382005684));
#59921=CARTESIAN_POINT('Ctrl Pts',(-0.325636997874695,2.34930825775137,
0.618351786208036));
#59922=CARTESIAN_POINT('Ctrl Pts',(-0.316201580846568,2.35059679921502,
0.617703900088474));
#59923=CARTESIAN_POINT('Ctrl Pts',(-0.299426413398389,2.35278485180953,
0.616558557540844));
#59924=CARTESIAN_POINT('Ctrl Pts',(-0.292090115237561,2.35370688542672,
0.616059906008229));
#59925=CARTESIAN_POINT('Ctrl Pts',(-0.274312432938551,2.35585680236328,
0.614856832197766));
#59926=CARTESIAN_POINT('Ctrl Pts',(-0.263867029304125,2.35704959329835,
0.614154336940135));
#59927=CARTESIAN_POINT('Ctrl Pts',(-0.231173137377478,2.36056294180309,
0.611968257993204));
#59928=CARTESIAN_POINT('Ctrl Pts',(-0.208898801954638,2.36263831335565,
0.610497273355312));
#59929=CARTESIAN_POINT('Ctrl Pts',(-0.0901970347951604,2.3720062147553,
0.602740154966611));
#59930=CARTESIAN_POINT('Ctrl Pts',(0.00658955635311563,2.37371221252312,
0.596700305590679));
#59931=CARTESIAN_POINT('Ctrl Pts',(0.277620911008778,2.3619056561937,0.579940780284691));
#59932=CARTESIAN_POINT('Ctrl Pts',(0.45063895407541,2.33507883443648,0.569381696653995));
#59933=CARTESIAN_POINT('Ctrl Pts',(0.665760870418325,2.27690415666136,0.555174641919089));
#59934=CARTESIAN_POINT('Ctrl Pts',(0.711978684101656,2.26287779766201,0.552059447160011));
#59935=CARTESIAN_POINT('Ctrl Pts',(0.777384766086199,2.24082597310604,0.547542726857982));
#59936=CARTESIAN_POINT('Ctrl Pts',(0.796947413607959,2.23394335017341,0.546177747699829));
#59937=CARTESIAN_POINT('Ctrl Pts',(0.830262568694626,2.22172896717452,0.543827785225058));
#59938=CARTESIAN_POINT('Ctrl Pts',(0.844060421028905,2.21652374805786,0.542846979719771));
#59939=CARTESIAN_POINT('Ctrl Pts',(0.872181368903933,2.20561451497476,0.540832104435277));
#59940=CARTESIAN_POINT('Ctrl Pts',(0.886499157016149,2.19989885094293,0.53979768831023));
#59941=CARTESIAN_POINT('Ctrl Pts',(0.922411289486603,2.18515520503335,0.537181033875542));
#59942=CARTESIAN_POINT('Ctrl Pts',(0.94392919767036,2.17594656630374,0.535592847532929));
#59943=CARTESIAN_POINT('Ctrl Pts',(1.03261188561223,2.13643163428384,0.528960334959937));
#59944=CARTESIAN_POINT('Ctrl Pts',(1.09847615585474,2.10332488825453,0.523823248821254));
#59945=CARTESIAN_POINT('Ctrl Pts',(1.28479577714394,1.99853074367456,0.50866291455141));
#59946=CARTESIAN_POINT('Ctrl Pts',(1.400568999181,1.91917292343225,0.498422231341662));
#59947=CARTESIAN_POINT('Ctrl Pts',(1.59343553547025,1.76018036745042,0.480216392171473));
#59948=CARTESIAN_POINT('Ctrl Pts',(1.67327078380359,1.68447082225648,0.472264799607404));
#59949=CARTESIAN_POINT('Ctrl Pts',(1.75904547110874,1.59098867026052,0.46346266878034));
#59950=CARTESIAN_POINT('Ctrl Pts',(1.77038197576315,1.57836422253609,0.462293725146222));
#59951=CARTESIAN_POINT('Ctrl Pts',(1.78785822205109,1.55847727827402,0.460484314870678));
#59952=CARTESIAN_POINT('Ctrl Pts',(1.79409116127325,1.55129796040275,0.459837482885743));
#59953=CARTESIAN_POINT('Ctrl Pts',(1.8055348617662,1.53795547858139,0.458647411994184));
#59954=CARTESIAN_POINT('Ctrl Pts',(1.81075742223906,1.53180310505493,0.458103359185067));
#59955=CARTESIAN_POINT('Ctrl Pts',(1.82289788713066,1.51735232074527,0.456836317763363));
#59956=CARTESIAN_POINT('Ctrl Pts',(1.82979061394445,1.5090331648348,0.456115119859604));
#59957=CARTESIAN_POINT('Ctrl Pts',(1.85207183462001,1.48176377159186,0.453776654939211));
#59958=CARTESIAN_POINT('Ctrl Pts',(1.86722522808072,1.46262230823132,0.452174989712506));
#59959=CARTESIAN_POINT('Ctrl Pts',(1.90323310391704,1.41566594541722,0.448331753756019));
#59960=CARTESIAN_POINT('Ctrl Pts',(1.92377729464535,1.3876193606771,0.446107150673477));
#59961=CARTESIAN_POINT('Ctrl Pts',(2.00580677077071,1.27030858976154,0.437044047431806));
#59962=CARTESIAN_POINT('Ctrl Pts',(2.0617580284874,1.17732824700928,0.430418002240968));
#59963=CARTESIAN_POINT('Ctrl Pts',(2.17949645139178,0.947355357133899,0.414575239300669));
#59964=CARTESIAN_POINT('Ctrl Pts',(2.23501525973239,0.807704694744713,0.405358809755413));
#59965=CARTESIAN_POINT('Ctrl Pts',(2.28564882371701,0.634009141522768,0.393697410790794));
#59966=CARTESIAN_POINT('Ctrl Pts',(2.29373617921035,0.604096296483124,0.391683546812165));
#59967=CARTESIAN_POINT('Ctrl Pts',(2.30572646189051,0.556028716525917,0.388433843836277));
#59968=CARTESIAN_POINT('Ctrl Pts',(2.31000638695124,0.537971105572854,0.387210004757949));
#59969=CARTESIAN_POINT('Ctrl Pts',(2.31724914193221,0.505731481000089,0.385018734083788));
#59970=CARTESIAN_POINT('Ctrl Pts',(2.3202947920383,0.491568895307345,0.384053993826783));
#59971=CARTESIAN_POINT('Ctrl Pts',(2.3264145786531,0.461786404806506,0.382020351837113));
#59972=CARTESIAN_POINT('Ctrl Pts',(2.32946156243208,0.446161723188248,0.380950640249393));
#59973=CARTESIAN_POINT('Ctrl Pts',(2.3371181763739,0.404680691314672,0.378102723669877));
#59974=CARTESIAN_POINT('Ctrl Pts',(2.34145589000034,0.37877704702966,0.376316059820126));
#59975=CARTESIAN_POINT('Ctrl Pts',(2.36240761185764,0.239496083503416,0.36666180589382));
#59976=CARTESIAN_POINT('Ctrl Pts',(2.37121640096425,0.125115428188706,0.358554181236972));
#59977=CARTESIAN_POINT('Ctrl Pts',(2.37208590174046,-0.0701559832253248,
0.344460763667022));
#59978=CARTESIAN_POINT('Ctrl Pts',(2.36832452413327,-0.15083597370437,0.338567564366654));
#59979=CARTESIAN_POINT('Ctrl Pts',(2.3583160822561,-0.253033992601144,0.331077217486314));
#59980=CARTESIAN_POINT('Ctrl Pts',(2.35587046312243,-0.274873276325728,
0.329475255686216));
#59981=CARTESIAN_POINT('Ctrl Pts',(2.34058849647143,-0.396084236037446,
0.320584684156407));
#59982=CARTESIAN_POINT('Ctrl Pts',(2.32176704570386,-0.494610412207226,
0.313355661202691));
#59983=CARTESIAN_POINT('Ctrl Pts',(2.29256371229504,-0.607974945883795,
0.305232625040322));
#59984=CARTESIAN_POINT('Ctrl Pts',(2.28818697311984,-0.62424540525134,0.304071677629845));
#59985=CARTESIAN_POINT('Ctrl Pts',(2.28108675276386,-0.649561761547126,
0.302274392641359));
#59986=CARTESIAN_POINT('Ctrl Pts',(2.27848208575926,-0.658639999028936,
0.301631742024198));
#59987=CARTESIAN_POINT('Ctrl Pts',(2.27375202965481,-0.674762103304527,
0.300494032106262));
#59988=CARTESIAN_POINT('Ctrl Pts',(2.27164807206643,-0.681811723835021,
0.299997801779754));
#59989=CARTESIAN_POINT('Ctrl Pts',(2.26647084315136,-0.698868775290624,
0.298800006210314));
#59990=CARTESIAN_POINT('Ctrl Pts',(2.26336406876574,-0.708865819725888,
0.298100362408445));
#59991=CARTESIAN_POINT('Ctrl Pts',(2.25344844462857,-0.740042628486866,
0.295924944364));
#59992=CARTESIAN_POINT('Ctrl Pts',(2.24640750639646,-0.761148071253899,
0.294461675014972));
#59993=CARTESIAN_POINT('Ctrl Pts',(2.20754460552579,-0.872401054242493,
0.286782909472146));
#59994=CARTESIAN_POINT('Ctrl Pts',(2.17058763224998,-0.960671714941174,
0.280809617470508));
#59995=CARTESIAN_POINT('Ctrl Pts',(2.05321737489586,-1.19938722330217,0.264379801525432));
#59996=CARTESIAN_POINT('Ctrl Pts',(1.96178249514218,-1.34374047907669,0.254085718735529));
#59997=CARTESIAN_POINT('Ctrl Pts',(1.82146627338783,-1.52002483927286,0.239783986318725));
#59998=CARTESIAN_POINT('Ctrl Pts',(1.78578007342064,-1.56179502658402,0.236252038611432));
#59999=CARTESIAN_POINT('Ctrl Pts',(1.73398202190576,-1.61832556601315,0.231240622171423));
#60000=CARTESIAN_POINT('Ctrl Pts',(1.71906622591561,-1.63416111497828,0.22981005575489));
#60001=CARTESIAN_POINT('Ctrl Pts',(1.69447570596016,-1.65955869886622,0.227470265242845));
#60002=CARTESIAN_POINT('Ctrl Pts',(1.68493261901047,-1.66924685099942,0.226566669843765));
#60003=CARTESIAN_POINT('Ctrl Pts',(1.66470238026997,-1.68943436842655,0.22466001872677));
#60004=CARTESIAN_POINT('Ctrl Pts',(1.65399803861146,-1.69991557756897,0.223656236176726));
#60005=CARTESIAN_POINT('Ctrl Pts',(1.62799686676017,-1.7248966581399,0.221229656098395));
#60006=CARTESIAN_POINT('Ctrl Pts',(1.61260487707393,-1.73929518507195,0.219802663854785));
#60007=CARTESIAN_POINT('Ctrl Pts',(1.55691336642268,-1.79001736624349,0.214671506218182));
#60008=CARTESIAN_POINT('Ctrl Pts',(1.51556466329592,-1.82515871740052,0.210919954734751));
#60009=CARTESIAN_POINT('Ctrl Pts',(1.40732622083025,-1.91093256998107,0.20123776794873));
#60010=CARTESIAN_POINT('Ctrl Pts',(1.33889205141778,-1.95948874306921,0.195240521769358));
#60011=CARTESIAN_POINT('Ctrl Pts',(1.11509172694683,-2.10107668246895,0.176082573805482));
#60012=CARTESIAN_POINT('Ctrl Pts',(0.951572376105325,-2.18001548031892,
0.162689781931049));
#60013=CARTESIAN_POINT('Ctrl Pts',(0.760226426510909,-2.24671364647345,
0.148548789202375));
#60014=CARTESIAN_POINT('Ctrl Pts',(0.739693156082017,-2.25355730876224,
0.147050772190553));
#60015=CARTESIAN_POINT('Ctrl Pts',(0.709067926405305,-2.2633008786137,0.144848072967571));
#60016=CARTESIAN_POINT('Ctrl Pts',(0.699046384328166,-2.26641619174735,
0.144132259535063));
#60017=CARTESIAN_POINT('Ctrl Pts',(0.68127301687442,-2.27181214462059,0.142871943229718));
#60018=CARTESIAN_POINT('Ctrl Pts',(0.673529949131877,-2.27411977604542,
0.142325983721347));
#60019=CARTESIAN_POINT('Ctrl Pts',(0.665525343622258,-2.276460881958,0.141764746676507));
#60020=CARTESIAN_POINT('Ctrl Pts',(0.665275806655039,-2.27653381946505,
0.141747253714633));
#60021=CARTESIAN_POINT('Ctrl Pts',(0.664825098788998,-2.27666547706024,
0.141715663995405));
#60022=CARTESIAN_POINT('Ctrl Pts',(0.664623932141617,-2.27672421150266,
0.141701566438231));
#60023=CARTESIAN_POINT('Ctrl Pts',(0.664259113498333,-2.27683067479652,
0.141676004002107));
#60024=CARTESIAN_POINT('Ctrl Pts',(0.664095464169348,-2.27687841265838,
0.141664538621842));
#60025=CARTESIAN_POINT('Ctrl Pts',(0.663797721166953,-2.27696523192209,
0.141643680996446));
#60026=CARTESIAN_POINT('Ctrl Pts',(0.663663629200559,-2.27700431911861,
0.14163428842895));
#60027=CARTESIAN_POINT('Ctrl Pts',(0.663419024160122,-2.27707559692949,
0.141617156539464));
#60028=CARTESIAN_POINT('Ctrl Pts',(0.663308512208448,-2.27710779133997,
0.141609417006726));
#60029=CARTESIAN_POINT('Ctrl Pts',(0.663012027299088,-2.27719414009332,
0.141588654789123));
#60030=CARTESIAN_POINT('Ctrl Pts',(0.662826049999859,-2.27724827971398,
0.141575632921399));
#60031=CARTESIAN_POINT('Ctrl Pts',(0.662460926474542,-2.2773545218526,0.141550070886846));
#60032=CARTESIAN_POINT('Ctrl Pts',(0.662281780735279,-2.27740662601438,
0.141537530629021));
#60033=CARTESIAN_POINT('Ctrl Pts',(0.661929771916511,-2.27750896199234,
0.141512893053815));
#60034=CARTESIAN_POINT('Ctrl Pts',(0.661756909271774,-2.27755919526496,
0.141500795656101));
#60035=CARTESIAN_POINT('Ctrl Pts',(0.661416971848513,-2.27765793790856,
0.141477008845056));
#60036=CARTESIAN_POINT('Ctrl Pts',(0.661249897450439,-2.27770644857693,
0.141465319359927));
#60037=CARTESIAN_POINT('Ctrl Pts',(0.660921088649673,-2.27780188019891,
0.141442316745847));
#60038=CARTESIAN_POINT('Ctrl Pts',(0.660759354592563,-2.27784880230845,
0.141431003553344));
#60039=CARTESIAN_POINT('Ctrl Pts',(0.660440819886888,-2.27794117847227,
0.141408724823067));
#60040=CARTESIAN_POINT('Ctrl Pts',(0.660284019537088,-2.27798663356405,
0.141397759227762));
#60041=CARTESIAN_POINT('Ctrl Pts',(0.659974982005834,-2.27807618633512,
0.14137614956625));
#60042=CARTESIAN_POINT('Ctrl Pts',(0.659822745097611,-2.27812028494385,
0.141365505448848));
#60043=CARTESIAN_POINT('Ctrl Pts',(0.659522496367177,-2.27820722565541,
0.141344514895681));
#60044=CARTESIAN_POINT('Ctrl Pts',(0.659374484794813,-2.27825006859312,
0.14133416841421));
#60045=CARTESIAN_POINT('Ctrl Pts',(0.659082377178886,-2.27833459024196,
0.141313751305601));
#60046=CARTESIAN_POINT('Ctrl Pts',(0.658938281357462,-2.27837626970667,
0.14130368063709));
#60047=CARTESIAN_POINT('Ctrl Pts',(0.658653721032273,-2.27845854903023,
0.14128379512159));
#60048=CARTESIAN_POINT('Ctrl Pts',(0.658513256728526,-2.27849914957005,
0.141273980237223));
#60049=CARTESIAN_POINT('Ctrl Pts',(0.658235697815475,-2.27857934884532,
0.141254587855974));
#60050=CARTESIAN_POINT('Ctrl Pts',(0.658098603388054,-2.27861894819685,
0.141245010325362));
#60051=CARTESIAN_POINT('Ctrl Pts',(0.657827542788207,-2.27869721680865,
0.14122607564583));
#60052=CARTESIAN_POINT('Ctrl Pts',(0.657693576778667,-2.27873588662801,
0.141216718466227));
#60053=CARTESIAN_POINT('Ctrl Pts',(0.657428549634764,-2.27881236244484,
0.141198208760571));
#60054=CARTESIAN_POINT('Ctrl Pts',(0.657297488648413,-2.27885016894986,
0.1411890562067));
#60055=CARTESIAN_POINT('Ctrl Pts',(0.657038064372579,-2.27892497952696,
0.141170941170318));
#60056=CARTESIAN_POINT('Ctrl Pts',(0.656909701217583,-2.27896198406044,
0.141161978662544));
#60057=CARTESIAN_POINT('Ctrl Pts',(0.656655479978541,-2.27903524770222,
0.141144230165295));
#60058=CARTESIAN_POINT('Ctrl Pts',(0.656529622019303,-2.27907150722968,
0.141135444153025));
#60059=CARTESIAN_POINT('Ctrl Pts',(0.656280231644268,-2.27914333392576,
0.14111803601988));
#60060=CARTESIAN_POINT('Ctrl Pts',(0.656156699343588,-2.27917890147566,
0.14110941387837));
#60061=CARTESIAN_POINT('Ctrl Pts',(0.655911792584199,-2.27924939372603,
0.141092321695904));
#60062=CARTESIAN_POINT('Ctrl Pts',(0.655790418221921,-2.27928431877636,
0.141083851635575));
#60063=CARTESIAN_POINT('Ctrl Pts',(0.655549670267695,-2.27935357234028,
0.141067052576089));
#60064=CARTESIAN_POINT('Ctrl Pts',(0.655430296770329,-2.27938790117085,
0.141058723559758));
#60065=CARTESIAN_POINT('Ctrl Pts',(0.655193403125064,-2.27945600570688,
0.141042196231044));
#60066=CARTESIAN_POINT('Ctrl Pts',(0.655075883056496,-2.27948978170325,
0.141033997902541));
#60067=CARTESIAN_POINT('Ctrl Pts',(0.654842557535596,-2.27955682137068,
0.141017722206349));
#60068=CARTESIAN_POINT('Ctrl Pts',(0.654726752161155,-2.27959008530523,
0.141009644824376));
#60069=CARTESIAN_POINT('Ctrl Pts',(0.654496725180476,-2.27965613927842,
0.140993601835456));
#60070=CARTESIAN_POINT('Ctrl Pts',(0.654382503647127,-2.27968892955646,
0.140985636215651));
#60071=CARTESIAN_POINT('Ctrl Pts',(0.654155520629878,-2.2797540725024,0.140969808069232));
#60072=CARTESIAN_POINT('Ctrl Pts',(0.654042759215101,-2.27978642538729,
0.140961945531126));
#60073=CARTESIAN_POINT('Ctrl Pts',(0.65381857920301,-2.27985072788195,0.140946315324815));
#60074=CARTESIAN_POINT('Ctrl Pts',(0.653707160658574,-2.27988267769168,
0.140938547645489));
#60075=CARTESIAN_POINT('Ctrl Pts',(0.642773200295821,-2.28301717661147,
0.140176332963112));
#60076=CARTESIAN_POINT('Ctrl Pts',(0.631928448548873,-2.28604270820098,
0.139426072922503));
#60077=CARTESIAN_POINT('Ctrl Pts',(0.592529711468753,-2.29673260205386,
0.136719772349793));
#60078=CARTESIAN_POINT('Ctrl Pts',(0.56385333062162,-2.30394047482028,0.134786759720534));
#60079=CARTESIAN_POINT('Ctrl Pts',(0.491264066821116,-2.32074934483806,
0.129968638040957));
#60080=CARTESIAN_POINT('Ctrl Pts',(0.447198071601828,-2.32964208558751,
0.127112106876457));
#60081=CARTESIAN_POINT('Ctrl Pts',(0.206461101231627,-2.3711407062007,0.111748819003527));
#60082=CARTESIAN_POINT('Ctrl Pts',(0.00653527505048171,-2.38010438082522,
0.0997909555847822));
#60083=CARTESIAN_POINT('Ctrl Pts',(-0.246381698433964,-2.35954515023386,
0.0836589002354788));
#60084=CARTESIAN_POINT('Ctrl Pts',(-0.300430197833493,-2.35327394798437,
0.0801577623923198));
#60085=CARTESIAN_POINT('Ctrl Pts',(-0.375793933479163,-2.34189098148609,
0.0751743064046654));
#60086=CARTESIAN_POINT('Ctrl Pts',(-0.397328822786406,-2.33833363864016,
0.0737386488176271));
#60087=CARTESIAN_POINT('Ctrl Pts',(-0.433679534887422,-2.33181223780764,
0.0712939858783489));
#60088=CARTESIAN_POINT('Ctrl Pts',(-0.448521963182565,-2.32900285154338,
0.0702897638987183));
#60089=CARTESIAN_POINT('Ctrl Pts',(-0.478492233631729,-2.32303294478006,
0.068249272422422));
#60090=CARTESIAN_POINT('Ctrl Pts',(-0.493618024999703,-2.31986596737215,
0.0672128480493124));
#60091=CARTESIAN_POINT('Ctrl Pts',(-0.531003292032719,-2.31165621452894,
0.0646342634396861));
#60092=CARTESIAN_POINT('Ctrl Pts',(-0.553222583331075,-2.30643960723948,
0.0630867719150712));
#60093=CARTESIAN_POINT('Ctrl Pts',(-0.639877970586715,-2.28477061351907,
0.0569907455003847));
#60094=CARTESIAN_POINT('Ctrl Pts',(-0.703680470963905,-2.26593312002907,
0.052368842208252));
#60095=CARTESIAN_POINT('Ctrl Pts',(-0.875354877752572,-2.20729670813393,
0.0395571363453451));
#60096=CARTESIAN_POINT('Ctrl Pts',(-0.981253416593894,-2.16230011210438,
0.0312298997291111));
#60097=CARTESIAN_POINT('Ctrl Pts',(-1.17700219292696,-2.06177611854969,
0.0151851737384018));
#60098=CARTESIAN_POINT('Ctrl Pts',(-1.26723605846899,-2.00757678307237,
0.0074963326966278));
#60099=CARTESIAN_POINT('Ctrl Pts',(-1.35356952483514,-1.9475748006014,6.39245600897453E-15));
#60100=CARTESIAN_POINT('',(1.37702479013102,-1.93106208855765,0.));
#60101=CARTESIAN_POINT('Origin',(0.,0.,0.));
#60102=CARTESIAN_POINT('Ctrl Pts',(1.37702479013102,-1.93106208855765,-3.33066907387547E-15));
#60103=CARTESIAN_POINT('Ctrl Pts',(1.44326778530957,-1.88382474332991,0.00545963808742537));
#60104=CARTESIAN_POINT('Ctrl Pts',(1.50712417061229,-1.83314207740384,0.0109192761748538));
#60105=CARTESIAN_POINT('Ctrl Pts',(1.56823230173022,-1.77928230202797,0.0163789142622826));
#60106=CARTESIAN_POINT('Ctrl Pts',(1.62930377606925,-1.7254548353783,0.0218352772905245));
#60107=CARTESIAN_POINT('Ctrl Pts',(1.68762994983901,-1.66845433970544,0.027291640318767));
#60108=CARTESIAN_POINT('Ctrl Pts',(1.74288236953678,-1.60858916708334,0.0327480033470089));
#60109=CARTESIAN_POINT('Ctrl Pts',(1.79812957679123,-1.54872964206582,0.0382038516288718));
#60110=CARTESIAN_POINT('Ctrl Pts',(1.85030330341389,-1.48600629137094,0.0436596999107342));
#60111=CARTESIAN_POINT('Ctrl Pts',(1.89911260932967,-1.42076365366836,0.0491155481925971));
#60112=CARTESIAN_POINT('Ctrl Pts',(1.94792122166181,-1.3555219430682,0.0545713189464766));
#60113=CARTESIAN_POINT('Ctrl Pts',(1.99336524640357,-1.28776136609834,0.060027089700356));
#60114=CARTESIAN_POINT('Ctrl Pts',(2.0351954503436,-1.21785776731141,0.0654828604542355));
#60115=CARTESIAN_POINT('Ctrl Pts',(2.07703526430301,-1.14793810895803,0.0709398846101495));
#60116=CARTESIAN_POINT('Ctrl Pts',(2.11525938183687,-1.07587482429233,0.0763969087660638));
#60117=CARTESIAN_POINT('Ctrl Pts',(2.14966370056128,-1.00206987630064,0.0818539329219778));
#60118=CARTESIAN_POINT('Ctrl Pts',(2.18408431909924,-0.92822996156826,0.0873135424648312));
#60119=CARTESIAN_POINT('Ctrl Pts',(2.21468135480373,-0.852647137883284,
0.092773152007684));
#60120=CARTESIAN_POINT('Ctrl Pts',(2.24129860351498,-0.77574392191096,0.0982327615505374));
#60121=CARTESIAN_POINT('Ctrl Pts',(2.26795510942114,-0.698727283076209,
0.103700423351469));
#60122=CARTESIAN_POINT('Ctrl Pts',(2.290619963958,-0.620386776580873,0.109168085152402));
#60123=CARTESIAN_POINT('Ctrl Pts',(2.30918670871589,-0.541160610900181,
0.114635746953334));
#60124=CARTESIAN_POINT('Ctrl Pts',(2.3277679904902,-0.461872414309592,0.120107689714143));
#60125=CARTESIAN_POINT('Ctrl Pts',(2.34224469032866,-0.381697606332208,
0.125579632474952));
#60126=CARTESIAN_POINT('Ctrl Pts',(2.35256183899474,-0.301082806227277,
0.131051575235762));
#60127=CARTESIAN_POINT('Ctrl Pts',(2.36289859025774,-0.220314837889131,
0.136533914695488));
#60128=CARTESIAN_POINT('Ctrl Pts',(2.36905996623431,-0.139105642971568,
0.142016254155214));
#60129=CARTESIAN_POINT('Ctrl Pts',(2.37104302952243,-0.0579052212937533,
0.147498593614941));
#60130=CARTESIAN_POINT('Ctrl Pts',(2.37229246741722,-0.00674453241181939,
0.150952766113663));
#60131=CARTESIAN_POINT('Ctrl Pts',(2.37188429523822,0.0444126803724593,
0.154406938612386));
#60132=CARTESIAN_POINT('Ctrl Pts',(2.36982835395112,0.0954548862516559,
0.157861111111109));
#60133=CARTESIAN_POINT('Ctrl Pts',(2.36668417853294,0.173514337668007,0.163143618120815));
#60134=CARTESIAN_POINT('Ctrl Pts',(2.35967183891541,0.251594288586149,0.168426125130522));
#60135=CARTESIAN_POINT('Ctrl Pts',(2.3487818857182,0.329274529567723,0.173708632140229));
#60136=CARTESIAN_POINT('Ctrl Pts',(2.33790926945034,0.406831102722223,0.1789827293387));
#60137=CARTESIAN_POINT('Ctrl Pts',(2.32317135634299,0.48398875988057,0.184256826537171));
#60138=CARTESIAN_POINT('Ctrl Pts',(2.30461067786112,0.56032819488984,0.189530923735642));
#60139=CARTESIAN_POINT('Ctrl Pts',(2.28607482777778,0.636565511546182,0.194797965837111));
#60140=CARTESIAN_POINT('Ctrl Pts',(2.26372648220335,0.711986318125151,0.200065007938579));
#60141=CARTESIAN_POINT('Ctrl Pts',(2.23765962166701,0.786179038171995,0.205332050040048));
#60142=CARTESIAN_POINT('Ctrl Pts',(2.21161201755268,0.86031694968811,0.210595201209378));
#60143=CARTESIAN_POINT('Ctrl Pts',(2.18185150513484,0.933228124097077,0.215858352378709));
#60144=CARTESIAN_POINT('Ctrl Pts',(2.14852221092795,1.00451499324265,0.221121503548039));
#60145=CARTESIAN_POINT('Ctrl Pts',(2.11520666201045,1.07577246306641,0.226382484148276));
#60146=CARTESIAN_POINT('Ctrl Pts',(2.0783254543951,1.14540652368449,0.231643464748513));
#60147=CARTESIAN_POINT('Ctrl Pts',(2.03807065845716,1.21304000496109,0.236904445348749));
#60148=CARTESIAN_POINT('Ctrl Pts',(1.99781932847753,1.2806676629607,0.242164972975893));
#60149=CARTESIAN_POINT('Ctrl Pts',(1.9541952328856,1.34629467288068,0.247425500603037));
#60150=CARTESIAN_POINT('Ctrl Pts',(1.90743535172774,1.40957030384415,0.252686028230181));
#60151=CARTESIAN_POINT('Ctrl Pts',(1.86063139824614,1.47290557362668,0.257951514032385));
#60152=CARTESIAN_POINT('Ctrl Pts',(1.81068603974131,1.53388465079858,0.263216999834587));
#60153=CARTESIAN_POINT('Ctrl Pts',(1.757877954138,1.59218816754038,0.268482485636791));
#60154=CARTESIAN_POINT('Ctrl Pts',(1.70504654917932,1.6505174303476,0.273750296608203));
#60155=CARTESIAN_POINT('Ctrl Pts',(1.64935023909496,1.70616844123663,0.279018107579616));
#60156=CARTESIAN_POINT('Ctrl Pts',(1.59110425956814,1.758859089775,0.284285918551029));
#60157=CARTESIAN_POINT('Ctrl Pts',(1.53275141754399,1.81164640857858,0.289563394248496));
#60158=CARTESIAN_POINT('Ctrl Pts',(1.47183993167519,1.86146220983978,0.294840869945963));
#60159=CARTESIAN_POINT('Ctrl Pts',(1.40871752970107,1.90806524626725,0.30011834564343));
#60160=CARTESIAN_POINT('Ctrl Pts',(1.3465063371901,1.95399554011085,0.305319637836361));
#60161=CARTESIAN_POINT('Ctrl Pts',(1.28214806856191,1.99680506618771,0.310520930029293));
#60162=CARTESIAN_POINT('Ctrl Pts',(1.21599894108394,2.03630661683911,0.315722222222224));
#60163=CARTESIAN_POINT('Ctrl Pts',(1.14802781677833,2.07689618939975,0.321066777648344));
#60164=CARTESIAN_POINT('Ctrl Pts',(1.07789839973257,2.1141527057923,0.326411333074464));
#60165=CARTESIAN_POINT('Ctrl Pts',(1.00597032896329,2.14784118587606,0.331755888500584));
#60166=CARTESIAN_POINT('Ctrl Pts',(0.934144558695706,2.18148175214291,0.337092842573081));
#60167=CARTESIAN_POINT('Ctrl Pts',(0.860525634521335,2.21156416519094,0.342429796645578));
#60168=CARTESIAN_POINT('Ctrl Pts',(0.785499756332435,2.23789816464058,0.347766750718074));
#60169=CARTESIAN_POINT('Ctrl Pts',(0.710559857948801,2.26420198527461,0.353097588630614));
#60170=CARTESIAN_POINT('Ctrl Pts',(0.634216647943832,2.28676577651481,0.358428426543155));
#60171=CARTESIAN_POINT('Ctrl Pts',(0.556877001243562,2.30544704298016,0.363759264455695));
#60172=CARTESIAN_POINT('Ctrl Pts',(0.479585816847761,2.32411660345433,0.369086761976844));
#60173=CARTESIAN_POINT('Ctrl Pts',(0.401299887304215,2.33890835972766,0.374414259497993));
#60174=CARTESIAN_POINT('Ctrl Pts',(0.322440839336424,2.34972976480872,0.379741757019143));
#60175=CARTESIAN_POINT('Ctrl Pts',(0.243606977598816,2.3605477137182,0.385067553028768));
#60176=CARTESIAN_POINT('Ctrl Pts',(0.164200822520171,2.36739776666325,0.390393349038394));
#60177=CARTESIAN_POINT('Ctrl Pts',(0.0846523363143929,2.37023881591213,
0.39571914504802));
#60178=CARTESIAN_POINT('Ctrl Pts',(0.00510481752400763,2.37307983061006,
0.401044876288883));
#60179=CARTESIAN_POINT('Ctrl Pts',(-0.0745845630179324,2.37191192337,0.406370607529746));
#60180=CARTESIAN_POINT('Ctrl Pts',(-0.153984063945952,2.36674607225843,
0.411696338770609));
#60181=CARTESIAN_POINT('Ctrl Pts',(-0.233460080683629,2.36157524291304,
0.417027202318768));
#60182=CARTESIAN_POINT('Ctrl Pts',(-0.312645193559593,2.35239880416356,
0.422358065866927));
#60183=CARTESIAN_POINT('Ctrl Pts',(-0.391111612601996,2.33927975432351,
0.427688929415086));
#60184=CARTESIAN_POINT('Ctrl Pts',(-0.469615311879154,2.3261544714826,0.433022325713522));
#60185=CARTESIAN_POINT('Ctrl Pts',(-0.547399181006083,2.30908294519053,
0.438355722011956));
#60186=CARTESIAN_POINT('Ctrl Pts',(-0.624046927172358,2.2881790784785,0.443689118310392));
#60187=CARTESIAN_POINT('Ctrl Pts',(-0.700827728124772,2.26723892420874,
0.449031772988093));
#60188=CARTESIAN_POINT('Ctrl Pts',(-0.776468021395321,2.24245328232575,
0.454374427665795));
#60189=CARTESIAN_POINT('Ctrl Pts',(-0.850568189023652,2.21398550544511,
0.459717082343496));
#60190=CARTESIAN_POINT('Ctrl Pts',(-0.914674367487779,2.18935721587982,
0.464339166006773));
#60191=CARTESIAN_POINT('Ctrl Pts',(-0.977627989544473,2.16197390682528,
0.468961249670049));
#60192=CARTESIAN_POINT('Ctrl Pts',(-1.03918531674208,2.13196902884814,0.473583333333325));
#60193=CARTESIAN_POINT('Ctrl Pts',(-1.11037453998178,2.09726927735084,0.478928636008362));
#60194=CARTESIAN_POINT('Ctrl Pts',(-1.1799508286317,2.05893811340978,0.4842739386834));
#60195=CARTESIAN_POINT('Ctrl Pts',(-1.24752088426758,2.01714890521653,0.489619241358437));
#60196=CARTESIAN_POINT('Ctrl Pts',(-1.3149970487025,1.9754177647414,0.494957116529044));
#60197=CARTESIAN_POINT('Ctrl Pts',(-1.38047212392445,1.93023836733986,0.50029499169965));
#60198=CARTESIAN_POINT('Ctrl Pts',(-1.44357582915885,1.88183072776707,0.505632866870257));
#60199=CARTESIAN_POINT('Ctrl Pts',(-1.50661029432368,1.83347620311549,0.510964885097174));
#60200=CARTESIAN_POINT('Ctrl Pts',(-1.56727819271147,1.78190075845812,0.516296903324091));
#60201=CARTESIAN_POINT('Ctrl Pts',(-1.62523800314883,1.72736779396306,0.521628921551007));
#60202=CARTESIAN_POINT('Ctrl Pts',(-1.68316321911901,1.67286737855393,0.526957757256653));
#60203=CARTESIAN_POINT('Ctrl Pts',(-1.73838321742658,1.61541326635611,0.532286592962297));
#60204=CARTESIAN_POINT('Ctrl Pts',(-1.79059031382657,1.55530845510801,0.537615428667943));
#60205=CARTESIAN_POINT('Ctrl Pts',(-1.84278227267436,1.49522107137036,0.542942719266998));
#60206=CARTESIAN_POINT('Ctrl Pts',(-1.89196275933862,1.43248486673609,0.548270009866054));
#60207=CARTESIAN_POINT('Ctrl Pts',(-1.9378626713541,1.36743787042495,0.553597300465109));
#60208=CARTESIAN_POINT('Ctrl Pts',(-1.98376336156647,1.30238977129319,0.558924681384183));
#60209=CARTESIAN_POINT('Ctrl Pts',(-2.02638309921908,1.23503118430805,0.564252062303258));
#60210=CARTESIAN_POINT('Ctrl Pts',(-2.06549547725366,1.16573002704086,0.569579443222332));
#60211=CARTESIAN_POINT('Ctrl Pts',(-2.10464725042194,1.09635906761656,0.574912190035637));
#60212=CARTESIAN_POINT('Ctrl Pts',(-2.14028437834377,1.02504203662645,0.580244936848942));
#60213=CARTESIAN_POINT('Ctrl Pts',(-2.17222620810871,0.952171918986102,
0.585577683662246));
#60214=CARTESIAN_POINT('Ctrl Pts',(-2.20418399500941,0.879265397721765,
0.590913094548508));
#60215=CARTESIAN_POINT('Ctrl Pts',(-2.23244264048258,0.804804680306168,
0.59624850543477));
#60216=CARTESIAN_POINT('Ctrl Pts',(-2.25687043503204,0.729200865316473,
0.601583916321033));
#60217=CARTESIAN_POINT('Ctrl Pts',(-2.28134152996764,0.653463036002394,
0.606928784686197));
#60218=CARTESIAN_POINT('Ctrl Pts',(-2.30196808540654,0.576578511717898,
0.612273653051362));
#60219=CARTESIAN_POINT('Ctrl Pts',(-2.31866893201719,0.498971388155922,
0.617618521416527));
#60220=CARTESIAN_POINT('Ctrl Pts',(-2.33306932531436,0.43205423551041,0.622227162425831));
#60221=CARTESIAN_POINT('Ctrl Pts',(-2.34455183302236,0.364600187711573,
0.626835803435136));
#60222=CARTESIAN_POINT('Ctrl Pts',(-2.35309545095156,0.296883581915646,
0.63144444444444));
#60223=CARTESIAN_POINT('Ctrl Pts',(-2.35829469962102,0.255674403848179,
0.634249049101883));
#60224=CARTESIAN_POINT('Ctrl Pts',(-2.36241188740593,0.214324853083953,
0.637053653759326));
#60225=CARTESIAN_POINT('Ctrl Pts',(-2.36544101854889,0.172878137039861,
0.639858258416768));
#60226=CARTESIAN_POINT('Origin',(0.,0.,-1.84858989190501));
#60227=CARTESIAN_POINT('',(-2.36544098584031,0.172878584581258,1.83759047784057));
#60228=CARTESIAN_POINT('',(-2.3654410189124,0.172878132066172,1.63813797379334));
#60229=CARTESIAN_POINT('',(-2.36544101854889,0.172878137039864,-1.84858989190501));
#60230=CARTESIAN_POINT('Ctrl Pts',(-2.36544098584031,0.172878584581292,
1.83759047784057));
#60231=CARTESIAN_POINT('Ctrl Pts',(-2.35722714105123,0.285265929505931,
1.83063249560928));
#60232=CARTESIAN_POINT('Ctrl Pts',(-2.34100928488915,0.396994903760292,
1.82357843620098));
#60233=CARTESIAN_POINT('Ctrl Pts',(-2.31227652442218,0.52824094054548,1.8148787327713));
#60234=CARTESIAN_POINT('Ctrl Pts',(-2.30738827607898,0.549199883895431,
1.81347699129859));
#60235=CARTESIAN_POINT('Ctrl Pts',(-2.29752545332533,0.589029365526151,
1.81078751172885));
#60236=CARTESIAN_POINT('Ctrl Pts',(-2.29260185398925,0.607910769652914,
1.80950144430633));
#60237=CARTESIAN_POINT('Ctrl Pts',(-2.28357172865025,0.640869081213229,
1.80723600928146));
#60238=CARTESIAN_POINT('Ctrl Pts',(-2.27956653457981,0.65497283704039,1.8062599236483));
#60239=CARTESIAN_POINT('Ctrl Pts',(-2.27097111447355,0.684206267933738,
1.80422246971128));
#60240=CARTESIAN_POINT('Ctrl Pts',(-2.26635986087931,0.699328949850444,
1.80316046570306));
#60241=CARTESIAN_POINT('Ctrl Pts',(-2.25394441030967,0.738632695028761,
1.80037880936328));
#60242=CARTESIAN_POINT('Ctrl Pts',(-2.24590238571254,0.762735898173374,
1.79865154530968));
#60243=CARTESIAN_POINT('Ctrl Pts',(-2.20814253065937,0.87012912299293,1.7908564441645));
#60244=CARTESIAN_POINT('Ctrl Pts',(-2.17417092653295,0.951837996609212,
1.78465223068797));
#60245=CARTESIAN_POINT('Ctrl Pts',(-2.08172617652505,1.14325385041396,1.76945955502235));
#60246=CARTESIAN_POINT('Ctrl Pts',(-2.01903828739529,1.2506373141881,1.76037551377554));
#60247=CARTESIAN_POINT('Ctrl Pts',(-1.88761543876851,1.43993272900011,1.74359744154145));
#60248=CARTESIAN_POINT('Ctrl Pts',(-1.8211818356568,1.5230889692512,1.73591354639221));
#60249=CARTESIAN_POINT('Ctrl Pts',(-1.73814036513874,1.61379784220138,1.72737990089503));
#60250=CARTESIAN_POINT('Ctrl Pts',(-1.72676564206465,1.62596305624391,1.72623214380853));
#60251=CARTESIAN_POINT('Ctrl Pts',(-1.70976545426397,1.64376504579486,1.72454897917922));
#60252=CARTESIAN_POINT('Ctrl Pts',(-1.70423852282264,1.64949461844379,1.72400669198597));
#60253=CARTESIAN_POINT('Ctrl Pts',(-1.69353818286094,1.66047608467419,1.72296643431434));
#60254=CARTESIAN_POINT('Ctrl Pts',(-1.68836899431332,1.66573183587551,1.72246818024996));
#60255=CARTESIAN_POINT('Ctrl Pts',(-1.67649671226384,1.67769088152275,1.72133361594357));
#60256=CARTESIAN_POINT('Ctrl Pts',(-1.66977784756702,1.68437818428432,1.72069854002105));
#60257=CARTESIAN_POINT('Ctrl Pts',(-1.65100253843425,1.70284254248132,1.71894258893228));
#60258=CARTESIAN_POINT('Ctrl Pts',(-1.6388601144059,1.71453191023563,1.71782814421354));
#60259=CARTESIAN_POINT('Ctrl Pts',(-1.55610667644027,1.79251516904905,1.71036567796915));
#60260=CARTESIAN_POINT('Ctrl Pts',(-1.48160808908416,1.85456750822954,1.7042889607379));
#60261=CARTESIAN_POINT('Ctrl Pts',(-1.38190249563347,1.92776096707279,1.69663401602998));
#60262=CARTESIAN_POINT('Ctrl Pts',(-1.3600226948554,1.94325890111906,1.69498167754051));
#60263=CARTESIAN_POINT('Ctrl Pts',(-1.25600581148036,2.01431885573764,1.68723283380043));
#60264=CARTESIAN_POINT('Ctrl Pts',(-1.17070152113985,2.06506379246464,1.68117968707572));
#60265=CARTESIAN_POINT('Ctrl Pts',(-1.02530954692287,2.13964150449271,1.67101943787669));
#60266=CARTESIAN_POINT('Ctrl Pts',(-0.966982132491316,2.16662643473258,
1.66698306976667));
#60267=CARTESIAN_POINT('Ctrl Pts',(-0.865969100204142,2.20846766216718,
1.65999314870265));
#60268=CARTESIAN_POINT('Ctrl Pts',(-0.823822533234024,2.22453318997038,
1.65707703022371));
#60269=CARTESIAN_POINT('Ctrl Pts',(-0.762725631891272,2.24584781549101,
1.65283637414099));
#60270=CARTESIAN_POINT('Ctrl Pts',(-0.744126607086938,2.25207867415585,
1.6515437360367));
#60271=CARTESIAN_POINT('Ctrl Pts',(-0.71147943220595,2.26256723456253,1.64927072063327));
#60272=CARTESIAN_POINT('Ctrl Pts',(-0.697464879150606,2.26692659770059,
1.64829369425624));
#60273=CARTESIAN_POINT('Ctrl Pts',(-0.668311197724116,2.27569920143619,
1.64625815145276));
#60274=CARTESIAN_POINT('Ctrl Pts',(-0.653166749350483,2.28009207914493,
1.64519903366324));
#60275=CARTESIAN_POINT('Ctrl Pts',(-0.613695568138675,2.2911157852552,1.64243363732617));
#60276=CARTESIAN_POINT('Ctrl Pts',(-0.589305441430633,2.29751013143529,
1.64071991203987));
#60277=CARTESIAN_POINT('Ctrl Pts',(-0.483816048245487,2.32337599829674,
1.63328412701791));
#60278=CARTESIAN_POINT('Ctrl Pts',(-0.401831269856879,2.33894908193943,
1.62744204829056));
#60279=CARTESIAN_POINT('Ctrl Pts',(-0.17174776317778,2.37019944214391,1.61088154295688));
#60280=CARTESIAN_POINT('Ctrl Pts',(-0.0227404602583429,2.37630367796558,
1.59994901974875));
#60281=CARTESIAN_POINT('Ctrl Pts',(0.185791845559624,2.36522386247665,1.5847982339267));
#60282=CARTESIAN_POINT('Ctrl Pts',(0.245605832468564,2.35976295507623,1.58047398159062));
#60283=CARTESIAN_POINT('Ctrl Pts',(0.329462113747185,2.34888350770507,1.57449178450488));
#60284=CARTESIAN_POINT('Ctrl Pts',(0.353723429490974,2.34535260763826,1.57277063107814));
#60285=CARTESIAN_POINT('Ctrl Pts',(0.396454823485551,2.33845544601771,1.56976097179854));
#60286=CARTESIAN_POINT('Ctrl Pts',(0.414947592733761,2.33524492287473,1.56846574669954));
#60287=CARTESIAN_POINT('Ctrl Pts',(0.443017285872127,2.33002777115706,1.56651275317212));
#60288=CARTESIAN_POINT('Ctrl Pts',(0.452622637003993,2.32818093947422,1.56584677116821));
#60289=CARTESIAN_POINT('Ctrl Pts',(0.470214826024624,2.32468547952722,1.56463163238418));
#60290=CARTESIAN_POINT('Ctrl Pts',(0.478204731948126,2.32305505731711,1.56408153280828));
#60291=CARTESIAN_POINT('Ctrl Pts',(0.496513982854802,2.31922039995022,1.56282492822785));
#60292=CARTESIAN_POINT('Ctrl Pts',(0.506827199798709,2.31698847617451,1.56211997180643));
#60293=CARTESIAN_POINT('Ctrl Pts',(0.538520564101027,2.30990784755526,1.55996143902869));
#60294=CARTESIAN_POINT('Ctrl Pts',(0.559849333984127,2.30483133183948,1.55851983863276));
#60295=CARTESIAN_POINT('Ctrl Pts',(0.717259587323752,2.26505156234966,1.54794172717568));
#60296=CARTESIAN_POINT('Ctrl Pts',(0.850107205491825,2.21861398032677,1.53934359629095));
#60297=CARTESIAN_POINT('Ctrl Pts',(1.02039547770398,2.14152956179533,1.5278678166501));
#60298=CARTESIAN_POINT('Ctrl Pts',(1.06214085299248,2.12113472626287,1.52501700945994));
#60299=CARTESIAN_POINT('Ctrl Pts',(1.17488916859823,2.06188772611835,1.51715773494356));
#60300=CARTESIAN_POINT('Ctrl Pts',(1.24454096549887,2.02060928815572,1.51212144239303));
#60301=CARTESIAN_POINT('Ctrl Pts',(1.35607655238759,1.94655102578013,1.50360905416926));
#60302=CARTESIAN_POINT('Ctrl Pts',(1.3992126373164,1.91577865398202,1.50019764934463));
#60303=CARTESIAN_POINT('Ctrl Pts',(1.45782661280982,1.87092857254056,1.49536931809172));
#60304=CARTESIAN_POINT('Ctrl Pts',(1.4742052332523,1.85805033344258,1.49399823369769));
#60305=CARTESIAN_POINT('Ctrl Pts',(1.50198860296427,1.83560610934965,1.49163324786386));
#60306=CARTESIAN_POINT('Ctrl Pts',(1.51347704636193,1.82614532971459,1.49064353872654));
#60307=CARTESIAN_POINT('Ctrl Pts',(1.535259276613,1.80786083949195,1.48874391459932));
#60308=CARTESIAN_POINT('Ctrl Pts',(1.54556796274832,1.79905573033828,1.48783477526325));
#60309=CARTESIAN_POINT('Ctrl Pts',(1.57224742187303,1.77586906168157,1.48545492341814));
#60310=CARTESIAN_POINT('Ctrl Pts',(1.58849617293463,1.76134969095868,1.48397859767628));
#60311=CARTESIAN_POINT('Ctrl Pts',(1.64548479942085,1.70899644201354,1.47870243595983));
#60312=CARTESIAN_POINT('Ctrl Pts',(1.68508914509912,1.66995891020658,1.47485273911037));
#60313=CARTESIAN_POINT('Ctrl Pts',(1.83899512925561,1.50720201689521,1.4591221784128));
#60314=CARTESIAN_POINT('Ctrl Pts',(1.94133221807234,1.37287138593709,1.44679758164857));
#60315=CARTESIAN_POINT('Ctrl Pts',(2.07766343437612,1.1478201046207,1.42765017478009));
#60316=CARTESIAN_POINT('Ctrl Pts',(2.12186195971634,1.06389926357105,1.42080585024223));
#60317=CARTESIAN_POINT('Ctrl Pts',(2.17004694041861,0.957384090435737,1.41264330451139));
#60318=CARTESIAN_POINT('Ctrl Pts',(2.17888783742548,0.937089056085034,1.41111076392095));
#60319=CARTESIAN_POINT('Ctrl Pts',(2.19147944336146,0.907041865247635,1.40887809186221));
#60320=CARTESIAN_POINT('Ctrl Pts',(2.19545165433309,0.897384610812732,1.40816595864972));
#60321=CARTESIAN_POINT('Ctrl Pts',(2.20211670982261,0.880871332978508,1.4069579136309));
#60322=CARTESIAN_POINT('Ctrl Pts',(2.20484155890789,0.874028611861918,1.40646015305633));
#60323=CARTESIAN_POINT('Ctrl Pts',(2.2110149531686,0.858313199521728,1.40532348104106));
#60324=CARTESIAN_POINT('Ctrl Pts',(2.21444200813456,0.849432323408591,1.40468583332721));
#60325=CARTESIAN_POINT('Ctrl Pts',(2.22385210444035,0.82460294586158,1.40291549840315));
#60326=CARTESIAN_POINT('Ctrl Pts',(2.22971708258325,0.80860990161976,1.40178941354801));
#60327=CARTESIAN_POINT('Ctrl Pts',(2.27408239626158,0.683477004093835,1.39307879589059));
#60328=CARTESIAN_POINT('Ctrl Pts',(2.30472511693814,0.571699924214598,1.38588439733219));
#60329=CARTESIAN_POINT('Ctrl Pts',(2.34433034938688,0.370519105607558,1.37325544362029));
#60330=CARTESIAN_POINT('Ctrl Pts',(2.35661537045364,0.282016126448506,1.36780542369962));
#60331=CARTESIAN_POINT('Ctrl Pts',(2.36995951427631,0.118602623711337,1.35766390741791));
#60332=CARTESIAN_POINT('Ctrl Pts',(2.37251835609022,0.0439329213658409,
1.35300050716303));
#60333=CARTESIAN_POINT('Ctrl Pts',(2.37110747847136,-0.064952209819849,
1.34606382877371));
#60334=CARTESIAN_POINT('Ctrl Pts',(2.36992332403909,-0.0991601109507234,
1.34386521466893));
#60335=CARTESIAN_POINT('Ctrl Pts',(2.36642314971465,-0.161325126519403,
1.33982614468255));
#60336=CARTESIAN_POINT('Ctrl Pts',(2.36435055432993,-0.18928990745626,1.33799309353948));
#60337=CARTESIAN_POINT('Ctrl Pts',(2.36028353797204,-0.233511578513536,
1.33506574764054));
#60338=CARTESIAN_POINT('Ctrl Pts',(2.35861564770367,-0.24979639893873,1.33398156687636));
#60339=CARTESIAN_POINT('Ctrl Pts',(2.35515049221901,-0.280490737932346,
1.33192578644221));
#60340=CARTESIAN_POINT('Ctrl Pts',(2.35338920180665,-0.294903618020155,
1.33095535002486));
#60341=CARTESIAN_POINT('Ctrl Pts',(2.34909597992227,-0.327543516644778,
1.32874561706829));
#60342=CARTESIAN_POINT('Ctrl Pts',(2.34648405947798,-0.345758881250932,
1.32750388109208));
#60343=CARTESIAN_POINT('Ctrl Pts',(2.33913153662566,-0.393106638576622,
1.3242531182976));
#60344=CARTESIAN_POINT('Ctrl Pts',(2.33405873737489,-0.422183432552812,
1.32223391206511));
#60345=CARTESIAN_POINT('Ctrl Pts',(2.29408248164245,-0.628503021377255,
1.30773756136826));
#60346=CARTESIAN_POINT('Ctrl Pts',(2.23957705021871,-0.801312713206304,
1.29463731563116));
#60347=CARTESIAN_POINT('Ctrl Pts',(2.11584767113732,-1.07867882313158,1.27249052091164));
#60348=CARTESIAN_POINT('Ctrl Pts',(2.05699900424848,-1.18706392674639,1.2635321868307));
#60349=CARTESIAN_POINT('Ctrl Pts',(1.97994558575719,-1.30589225498314,1.25368860738171));
#60350=CARTESIAN_POINT('Ctrl Pts',(1.96971706077336,-1.32126978952174,1.25241452320485));
#60351=CARTESIAN_POINT('Ctrl Pts',(1.95383317693645,-1.34455510223488,1.25048674429816));
#60352=CARTESIAN_POINT('Ctrl Pts',(1.94830736053536,-1.35254979334937,1.24982514168341));
#60353=CARTESIAN_POINT('Ctrl Pts',(1.93805222333603,-1.36719355255494,1.24861413085931));
#60354=CARTESIAN_POINT('Ctrl Pts',(1.93333766282671,-1.37385229025253,1.24806382482572));
#60355=CARTESIAN_POINT('Ctrl Pts',(1.92250399042443,-1.38898731060532,1.2468136891501));
#60356=CARTESIAN_POINT('Ctrl Pts',(1.91636309994222,-1.39744760959839,1.24611533474814));
#60357=CARTESIAN_POINT('Ctrl Pts',(1.8966488747823,-1.42423353108166,1.24390478237288));
#60358=CARTESIAN_POINT('Ctrl Pts',(1.8828666275923,-1.4424047493233,1.24240590526639));
#60359=CARTESIAN_POINT('Ctrl Pts',(1.79161041667228,-1.55918418160259,1.23275745516874));
#60360=CARTESIAN_POINT('Ctrl Pts',(1.70667211832771,-1.65172675898231,1.22503098673496));
#60361=CARTESIAN_POINT('Ctrl Pts',(1.52561312465911,-1.8200361549536,1.20984467067568));
#60362=CARTESIAN_POINT('Ctrl Pts',(1.43017505512048,-1.89594942000968,1.20240340108188));
#60363=CARTESIAN_POINT('Ctrl Pts',(1.27274617037463,-2.00249445076763,1.19042861772049));
#60364=CARTESIAN_POINT('Ctrl Pts',(1.21453509175683,-2.03832530050755,1.18606045651479));
#60365=CARTESIAN_POINT('Ctrl Pts',(1.13495443083451,-2.08268960768377,1.18011513547858));
#60366=CARTESIAN_POINT('Ctrl Pts',(1.11488806527567,-2.09349996541952,1.17861830051763));
#60367=CARTESIAN_POINT('Ctrl Pts',(1.0811305049346,-2.11106319627428,1.17610228673514));
#60368=CARTESIAN_POINT('Ctrl Pts',(1.0675240366116,-2.11797625112552,1.17508873679286));
#60369=CARTESIAN_POINT('Ctrl Pts',(1.04060926264119,-2.13132562942958,1.17308446435479));
#60370=CARTESIAN_POINT('Ctrl Pts',(1.02730561190618,-2.13776980495989,1.17209406940381));
#60371=CARTESIAN_POINT('Ctrl Pts',(0.99486657594864,-2.15311027226794,1.16967938558323));
#60372=CARTESIAN_POINT('Ctrl Pts',(0.975671314050858,-2.16187621890714,
1.16825073997559));
#60373=CARTESIAN_POINT('Ctrl Pts',(0.909539128102713,-2.19101682348607,
1.16332800091282));
#60374=CARTESIAN_POINT('Ctrl Pts',(0.862064033008021,-2.21012693362633,
1.15979244659638));
#60375=CARTESIAN_POINT('Ctrl Pts',(0.651803798343957,-2.28695741254817,
1.14411833223436));
#60376=CARTESIAN_POINT('Ctrl Pts',(0.483626682876532,-2.32832801224491,
1.13148938972811));
#60377=CARTESIAN_POINT('Ctrl Pts',(0.217087657648068,-2.363753747955,1.11191829219545));
#60378=CARTESIAN_POINT('Ctrl Pts',(0.121000722839993,-2.370616215204,1.10496314684639));
#60379=CARTESIAN_POINT('Ctrl Pts',(0.0024641159692989,-2.37185347444286,
1.09668494617114));
#60380=CARTESIAN_POINT('Ctrl Pts',(-0.0198294107899865,-2.37177188177341,
1.09514135820286));
#60381=CARTESIAN_POINT('Ctrl Pts',(-0.0525898389896183,-2.37119000401645,
1.09289572903689));
#60382=CARTESIAN_POINT('Ctrl Pts',(-0.0630591383815335,-2.37093468524795,
1.09218149660046));
#60383=CARTESIAN_POINT('Ctrl Pts',(-0.0808943114277315,-2.37038151097527,
1.0909709412764));
#60384=CARTESIAN_POINT('Ctrl Pts',(-0.088260910713815,-2.37011864980122,
1.09047275216746));
#60385=CARTESIAN_POINT('Ctrl Pts',(-0.105126233550873,-2.36943810421742,
1.08933639109983));
#60386=CARTESIAN_POINT('Ctrl Pts',(-0.114623797917891,-2.36899764614722,
1.08869947147881));
#60387=CARTESIAN_POINT('Ctrl Pts',(-0.141057145050599,-2.36761243544618,
1.08693456521219));
#60388=CARTESIAN_POINT('Ctrl Pts',(-0.157986211095145,-2.36654308218753,
1.08581310422719));
#60389=CARTESIAN_POINT('Ctrl Pts',(-0.283956293560617,-2.3572281497173,
1.07752458613099));
#60390=CARTESIAN_POINT('Ctrl Pts',(-0.392336216701509,-2.34163066935196,
1.07070497611412));
#60391=CARTESIAN_POINT('Ctrl Pts',(-0.588875322105803,-2.29930996560503,
1.05830382807689));
#60392=CARTESIAN_POINT('Ctrl Pts',(-0.677291713564731,-2.27483548045842,
1.05271113445951));
#60393=CARTESIAN_POINT('Ctrl Pts',(-0.873746232327288,-2.20798267310153,
1.03988680254655));
#60394=CARTESIAN_POINT('Ctrl Pts',(-0.980527711062764,-2.16267899830609,
1.03262502884645));
#60395=CARTESIAN_POINT('Ctrl Pts',(-1.10708865651824,-2.09767779686214,
1.02337968054841));
#60396=CARTESIAN_POINT('Ctrl Pts',(-1.13040849121314,-2.08520358370078,
1.02164861153288));
#60397=CARTESIAN_POINT('Ctrl Pts',(-1.16752584057593,-2.06454320128883,
1.01884605116049));
#60398=CARTESIAN_POINT('Ctrl Pts',(-1.18145778590585,-2.05660222148821,
1.01778319770985));
#60399=CARTESIAN_POINT('Ctrl Pts',(-1.20791865551661,-2.04116235567341,
1.01574297939982));
#60400=CARTESIAN_POINT('Ctrl Pts',(-1.22046099428596,-2.03368782898244,
1.01476652014516));
#60401=CARTESIAN_POINT('Ctrl Pts',(-1.24892416837596,-2.01636724884487,
1.01252856722221));
#60402=CARTESIAN_POINT('Ctrl Pts',(-1.26479888151332,-2.0064476607514,1.01126445309901));
#60403=CARTESIAN_POINT('Ctrl Pts',(-1.30690261543567,-1.97944020139196,
1.00786795665786));
#60404=CARTESIAN_POINT('Ctrl Pts',(-1.33291277430861,-1.96201970757236,
1.00572355125666));
#60405=CARTESIAN_POINT('Ctrl Pts',(-1.47216311538605,-1.86470875723151,
0.993984702995008));
#60406=CARTESIAN_POINT('Ctrl Pts',(-1.57856315593311,-1.77553662127184,
0.984046110716758));
#60407=CARTESIAN_POINT('Ctrl Pts',(-1.75837430822803,-1.59583753871045,
0.965549759989945));
#60408=CARTESIAN_POINT('Ctrl Pts',(-1.83410167163593,-1.50819435381047,
0.95706534680311));
#60409=CARTESIAN_POINT('Ctrl Pts',(-1.93502778995027,-1.37248751380129,
0.944961901987382));
#60410=CARTESIAN_POINT('Ctrl Pts',(-1.96546643445939,-1.32853197026797,
0.941185821270263));
#60411=CARTESIAN_POINT('Ctrl Pts',(-2.00220433016033,-1.27144958344077,
0.936495923685183));
#60412=CARTESIAN_POINT('Ctrl Pts',(-2.00990195840806,-1.25924595146886,
0.935505288100589));
#60413=CARTESIAN_POINT('Ctrl Pts',(-2.02214279624241,-1.23944138970281,
0.933917862388022));
#60414=CARTESIAN_POINT('Ctrl Pts',(-2.02675550552619,-1.23188415614345,
0.933316806956642));
#60415=CARTESIAN_POINT('Ctrl Pts',(-2.03562233701832,-1.2171725594088,0.932156073891346));
#60416=CARTESIAN_POINT('Ctrl Pts',(-2.03988126613385,-1.21002138867156,
0.931596114676016));
#60417=CARTESIAN_POINT('Ctrl Pts',(-2.0503636154985,-1.19220783350347,0.930211449886934));
#60418=CARTESIAN_POINT('Ctrl Pts',(-2.05654171318131,-1.18151879896961,
0.929389576069711));
#60419=CARTESIAN_POINT('Ctrl Pts',(-2.07824100601197,-1.14328985623197,
0.92648026688112));
#60420=CARTESIAN_POINT('Ctrl Pts',(-2.09329549230765,-1.11548715223054,
0.924419572581565));
#60421=CARTESIAN_POINT('Ctrl Pts',(-2.2069236663899,-0.895231001562671,
0.908456322006391));
#60422=CARTESIAN_POINT('Ctrl Pts',(-2.27932482143577,-0.690399886668755,
0.895663885715221));
#60423=CARTESIAN_POINT('Ctrl Pts',(-2.33944284874626,-0.398589840733198,
0.877036953899787));
#60424=CARTESIAN_POINT('Ctrl Pts',(-2.35177732393919,-0.317817602165625,
0.871852055914454));
#60425=CARTESIAN_POINT('Ctrl Pts',(-2.36241924832637,-0.211660932493143,
0.864909099738889));
#60426=CARTESIAN_POINT('Ctrl Pts',(-2.36452210844591,-0.186708801712192,
0.86326818950181));
#60427=CARTESIAN_POINT('Ctrl Pts',(-2.36730150719752,-0.146043841907032,
0.860577149244879));
#60428=CARTESIAN_POINT('Ctrl Pts',(-2.36821755008672,-0.13034893653533,
0.859534462298416));
#60429=CARTESIAN_POINT('Ctrl Pts',(-2.36968681167995,-0.0999890842487386,
0.857509125154726));
#60430=CARTESIAN_POINT('Ctrl Pts',(-2.37026009007793,-0.0853257949025577,
0.856527144055823));
#60431=CARTESIAN_POINT('Ctrl Pts',(-2.37128337384001,-0.0509930647768157,
0.8542186455999));
#60432=CARTESIAN_POINT('Ctrl Pts',(-2.37162476824478,-0.0313217203434785,
0.852888834174311));
#60433=CARTESIAN_POINT('Ctrl Pts',(-2.37194500005966,0.033877598813773,
0.848456482579792));
#60434=CARTESIAN_POINT('Ctrl Pts',(-2.37085769533092,0.0793982044377964,
0.845321642107885));
#60435=CARTESIAN_POINT('Ctrl Pts',(-2.3676168457696,0.140875261515083,0.841030930904592));
#60436=CARTESIAN_POINT('Ctrl Pts',(-2.36661000737738,0.156883205384554,
0.839908467310091));
#60437=CARTESIAN_POINT('Ctrl Pts',(-2.3654410179195,0.172878145651696,0.838781724910481));
#60438=CARTESIAN_POINT('',(-2.37174937133752,0.00172686423176496,0.651410108094986));
#60439=CARTESIAN_POINT('Ctrl Pts',(-2.36544101854889,0.172878137039861,
0.639858258416768));
#60440=CARTESIAN_POINT('Ctrl Pts',(-2.36959990151614,0.115973356999348,
0.643708874976174));
#60441=CARTESIAN_POINT('Ctrl Pts',(-2.37170775441788,0.0588853258924011,
0.64755949153558));
#60442=CARTESIAN_POINT('Ctrl Pts',(-2.37174937133752,0.00172686423176496,
0.651410108094986));
#60443=CARTESIAN_POINT('Ctrl Pts',(-2.37174930856301,0.00181103033629052,
0.65275631368545));
#60444=CARTESIAN_POINT('Ctrl Pts',(-2.37175145119913,-0.000994994296776971,
0.652931750428388));
#60445=CARTESIAN_POINT('Ctrl Pts',(-2.37174861411466,-0.0038010296480299,
0.65310707081996));
#60446=CARTESIAN_POINT('Ctrl Pts',(-2.37112535322287,-0.227533331300736,
0.667076921649127));
#60447=CARTESIAN_POINT('Ctrl Pts',(-2.3396475745453,-0.447280622863168,
0.680222654294109));
#60448=CARTESIAN_POINT('Ctrl Pts',(-2.26701041577751,-0.698201160524075,
0.696978619706972));
#60449=CARTESIAN_POINT('Ctrl Pts',(-2.25482443388412,-0.736605426184959,
0.699589963336822));
#60450=CARTESIAN_POINT('Ctrl Pts',(-2.23547414284124,-0.79259881954743,
0.703476454847408));
#60451=CARTESIAN_POINT('Ctrl Pts',(-2.22906688871707,-0.810443275725124,
0.704727032771976));
#60452=CARTESIAN_POINT('Ctrl Pts',(-2.21728559275687,-0.842057655345016,
0.706965036564985));
#60453=CARTESIAN_POINT('Ctrl Pts',(-2.21199541292227,-0.855857915296851,
0.707949648076686));
#60454=CARTESIAN_POINT('Ctrl Pts',(-2.20053398961831,-0.884940584850265,
0.710041373015548));
#60455=CARTESIAN_POINT('Ctrl Pts',(-2.19433175983725,-0.900209854596918,
0.711149478850414));
#60456=CARTESIAN_POINT('Ctrl Pts',(-2.1772431631345,-0.941054105058062,
0.714140902870466));
#60457=CARTESIAN_POINT('Ctrl Pts',(-2.16606579647482,-0.96650373606868,
0.716033903290692));
#60458=CARTESIAN_POINT('Ctrl Pts',(-2.09592106749537,-1.11888374959912,
0.72754969047471));
#60459=CARTESIAN_POINT('Ctrl Pts',(-2.02626992352521,-1.24056600855936,
0.737538388265311));
#60460=CARTESIAN_POINT('Ctrl Pts',(-1.88610855465222,-1.44183616444756,
0.755361002526343));
#60461=CARTESIAN_POINT('Ctrl Pts',(-1.82021019388062,-1.52418242029779,
0.763091497800347));
#60462=CARTESIAN_POINT('Ctrl Pts',(-1.71597217196654,-1.63799784157414,
0.774239643714896));
#60463=CARTESIAN_POINT('Ctrl Pts',(-1.68177576093693,-1.67308944643683,
0.777748092669314));
#60464=CARTESIAN_POINT('Ctrl Pts',(-1.63100221906363,-1.7220610750296,0.782721029860509));
#60465=CARTESIAN_POINT('Ctrl Pts',(-1.61528547457365,-1.7368118760284,0.784229542336085));
#60466=CARTESIAN_POINT('Ctrl Pts',(-1.58723310654433,-1.76242992664603,
0.786865083629891));
#60467=CARTESIAN_POINT('Ctrl Pts',(-1.57498167654345,-1.7733868547831,0.787997558657892));
#60468=CARTESIAN_POINT('Ctrl Pts',(-1.55543372395288,-1.79050695851107,
0.78977407154451));
#60469=CARTESIAN_POINT('Ctrl Pts',(-1.54821244273485,-1.79675470731068,
0.790423903869768));
#60470=CARTESIAN_POINT('Ctrl Pts',(-1.53460640982889,-1.80838351629775,
0.791635967312343));
#60471=CARTESIAN_POINT('Ctrl Pts',(-1.52823093181423,-1.81377451641353,
0.792198873503901));
#60472=CARTESIAN_POINT('Ctrl Pts',(-1.51345564143206,-1.82613504532349,
0.79349209079308));
#60473=CARTESIAN_POINT('Ctrl Pts',(-1.50503600681029,-1.83308041613884,
0.794220696915092));
#60474=CARTESIAN_POINT('Ctrl Pts',(-1.47750783631063,-1.8554709157772,0.79657709530287));
#60475=CARTESIAN_POINT('Ctrl Pts',(-1.45820648725909,-1.87067786653943,
0.79818930663787));
#60476=CARTESIAN_POINT('Ctrl Pts',(-1.29570412667248,-1.99466472928793,
0.811467235141947));
#60477=CARTESIAN_POINT('Ctrl Pts',(-1.14077572060438,-2.08714754920945,
0.822279528123996));
#60478=CARTESIAN_POINT('Ctrl Pts',(-0.901402159325332,-2.19534279964806,
0.838480786284841));
#60479=CARTESIAN_POINT('Ctrl Pts',(-0.824210523956122,-2.22547329304567,
0.843630086845949));
#60480=CARTESIAN_POINT('Ctrl Pts',(-0.71070527866864,-2.26306157493698,
0.851227276449663));
#60481=CARTESIAN_POINT('Ctrl Pts',(-0.675542240663434,-2.27380565457656,
0.853583816804143));
#60482=CARTESIAN_POINT('Ctrl Pts',(-0.611462431899902,-2.291767677618,0.857894237503964));
#60483=CARTESIAN_POINT('Ctrl Pts',(-0.582632010190856,-2.29926623238359,
0.859839279339637));
#60484=CARTESIAN_POINT('Ctrl Pts',(-0.537132610243582,-2.31018956688958,
0.862921663067962));
#60485=CARTESIAN_POINT('Ctrl Pts',(-0.52055435672148,-2.31398150655587,
0.864047393429071));
#60486=CARTESIAN_POINT('Ctrl Pts',(-0.489403537832321,-2.32075493128074,
0.866168253421457));
#60487=CARTESIAN_POINT('Ctrl Pts',(-0.474840849986072,-2.32377826481472,
0.867162009843196));
#60488=CARTESIAN_POINT('Ctrl Pts',(-0.44202294155307,-2.33027016550626,
0.86940706460838));
#60489=CARTESIAN_POINT('Ctrl Pts',(-0.423753631734454,-2.3336615331005,
0.870660714478425));
#60490=CARTESIAN_POINT('Ctrl Pts',(-0.368349914117364,-2.34327420698001,
0.874475125812053));
#60491=CARTESIAN_POINT('Ctrl Pts',(-0.331106960801865,-2.34882599866167,
0.877056346144162));
#60492=CARTESIAN_POINT('Ctrl Pts',(-0.108508777858752,-2.37660946758394,
0.89259391120447));
#60493=CARTESIAN_POINT('Ctrl Pts',(0.0787862494267347,-2.37777541526812,
0.906194176431287));
#60494=CARTESIAN_POINT('Ctrl Pts',(0.338701600130435,-2.34863653959509,
0.925228823579191));
#60495=CARTESIAN_POINT('Ctrl Pts',(0.412730920049532,-2.33676418864128,
0.930658280309585));
#60496=CARTESIAN_POINT('Ctrl Pts',(0.513791275463868,-2.31560322649303,
0.9379919636375));
#60497=CARTESIAN_POINT('Ctrl Pts',(0.541399989981951,-2.30930421884901,
0.939987080227885));
#60498=CARTESIAN_POINT('Ctrl Pts',(0.589329175876271,-2.29746217065792,
0.943428813460818));
#60499=CARTESIAN_POINT('Ctrl Pts',(0.609700583562067,-2.29214017379983,
0.944884702820515));
#60500=CARTESIAN_POINT('Ctrl Pts',(0.64002627596649,-2.28378471009155,0.947038914525128));
#60501=CARTESIAN_POINT('Ctrl Pts',(0.650035245989951,-2.2809560331226,0.947747764708422));
#60502=CARTESIAN_POINT('Ctrl Pts',(0.668051382498788,-2.27573619618193,
0.949019421197831));
#60503=CARTESIAN_POINT('Ctrl Pts',(0.676064835806887,-2.27336847605512,
0.949583480546604));
#60504=CARTESIAN_POINT('Ctrl Pts',(0.694073563047986,-2.26794382423523,
0.95084759754205));
#60505=CARTESIAN_POINT('Ctrl Pts',(0.704061309954511,-2.26486312672848,
0.951546302645843));
#60506=CARTESIAN_POINT('Ctrl Pts',(0.734448791757013,-2.25526973532177,
0.953665748998557));
#60507=CARTESIAN_POINT('Ctrl Pts',(0.754781608827425,-2.24854650991014,
0.955075153725061));
#60508=CARTESIAN_POINT('Ctrl Pts',(0.920177439180745,-2.19136045754968,
0.966489355638334));
#60509=CARTESIAN_POINT('Ctrl Pts',(1.06013575415447,-2.12718412074107,0.975844663725485));
#60510=CARTESIAN_POINT('Ctrl Pts',(1.32540086451254,-1.97281678311415,0.994700298363149));
#60511=CARTESIAN_POINT('Ctrl Pts',(1.45008064551625,-1.88306970722863,1.00416530319755));
#60512=CARTESIAN_POINT('Ctrl Pts',(1.58624245144136,-1.76346692311956,1.01592490926147));
#60513=CARTESIAN_POINT('Ctrl Pts',(1.60693195699883,-1.74463471338083,1.01775413549386));
#60514=CARTESIAN_POINT('Ctrl Pts',(1.63935811861069,-1.71405324532737,1.02069279639434));
#60515=CARTESIAN_POINT('Ctrl Pts',(1.65131325205398,-1.70253871884271,1.02179235589651));
#60516=CARTESIAN_POINT('Ctrl Pts',(1.67376568906253,-1.68045480513513,1.02388890427318));
#60517=CARTESIAN_POINT('Ctrl Pts',(1.68428623817782,-1.66991011275184,1.02488479768518));
#60518=CARTESIAN_POINT('Ctrl Pts',(1.70808782140226,-1.64560016510896,1.02716951056766));
#60519=CARTESIAN_POINT('Ctrl Pts',(1.72130291198352,-1.63177209114302,1.02846107307362));
#60520=CARTESIAN_POINT('Ctrl Pts',(1.76213870827008,-1.58799403877477,1.03252619501467));
#60521=CARTESIAN_POINT('Ctrl Pts',(1.78915461323599,-1.55749263669784,1.03532449500998));
#60522=CARTESIAN_POINT('Ctrl Pts',(1.96098850704832,-1.35311626841625,1.05386768113877));
#60523=CARTESIAN_POINT('Ctrl Pts',(2.08105502521308,-1.15998796730692,1.07059680633053));
#60524=CARTESIAN_POINT('Ctrl Pts',(2.19082625303358,-0.909775230626747,
1.09030199113213));
#60525=CARTESIAN_POINT('Ctrl Pts',(2.20843932542779,-0.866144855839831,
1.09366573769639));
#60526=CARTESIAN_POINT('Ctrl Pts',(2.23533767686969,-0.793345947717991,
1.09913120919846));
#60527=CARTESIAN_POINT('Ctrl Pts',(2.24537671694182,-0.764471016807144,
1.10126176680796));
#60528=CARTESIAN_POINT('Ctrl Pts',(2.25857867154093,-0.72399215680235,1.10418951621238));
#60529=CARTESIAN_POINT('Ctrl Pts',(2.26221538892767,-0.712547407553803,
1.10501079124258));
#60530=CARTESIAN_POINT('Ctrl Pts',(2.26827457703349,-0.692965062538959,
1.10640437699663));
#60531=CARTESIAN_POINT('Ctrl Pts',(2.27074053361962,-0.684841275819829,
1.10697910006482));
#60532=CARTESIAN_POINT('Ctrl Pts',(2.27582330671087,-0.667767385879586,
1.10817966718811));
#60533=CARTESIAN_POINT('Ctrl Pts',(2.27843103380718,-0.658814872792653,
1.10880500419741));
#60534=CARTESIAN_POINT('Ctrl Pts',(2.28537541982347,-0.634439833165862,
1.11049689161909));
#60535=CARTESIAN_POINT('Ctrl Pts',(2.28960881789367,-0.618988050506459,
1.11155778868104));
#60536=CARTESIAN_POINT('Ctrl Pts',(2.31029520318116,-0.540365798363026,
1.11690264325927));
#60537=CARTESIAN_POINT('Ctrl Pts',(2.32429331732944,-0.476572486717228,
1.12106599940257));
#60538=CARTESIAN_POINT('Ctrl Pts',(2.35711028523803,-0.290656993342265,
1.13291324646778));
#60539=CARTESIAN_POINT('Ctrl Pts',(2.36904694510039,-0.167540627655701,
1.14041529987787));
#60540=CARTESIAN_POINT('Ctrl Pts',(2.37331650557341,0.0623029918453421,
1.15457924796031));
#60541=CARTESIAN_POINT('Ctrl Pts',(2.36813512602746,0.168658437822752,1.16119618343337));
#60542=CARTESIAN_POINT('Ctrl Pts',(2.35114024660654,0.314619171190187,1.17062268103334));
#60543=CARTESIAN_POINT('Ctrl Pts',(2.34541175956555,0.354808470624256,1.17325394703149));
#60544=CARTESIAN_POINT('Ctrl Pts',(2.33547819809848,0.413647013762072,1.17716896028009));
#60545=CARTESIAN_POINT('Ctrl Pts',(2.33207430500875,0.43242533077708,1.17842788247742));
#60546=CARTESIAN_POINT('Ctrl Pts',(2.32561513168213,0.465761225338047,1.18068058186839));
#60547=CARTESIAN_POINT('Ctrl Pts',(2.32264878815785,0.480335142972431,1.18167152057143));
#60548=CARTESIAN_POINT('Ctrl Pts',(2.31608532724853,0.51109866029067,1.1837766253785));
#60549=CARTESIAN_POINT('Ctrl Pts',(2.31245509137365,0.527280295558261,1.18489178941482));
#60550=CARTESIAN_POINT('Ctrl Pts',(2.30224575422273,0.570653281422498,1.18790272057808));
#60551=CARTESIAN_POINT('Ctrl Pts',(2.29535492624418,0.597767787649016,1.18980823700607));
#60552=CARTESIAN_POINT('Ctrl Pts',(2.25236548060049,0.755204805825151,1.20101305092277));
#60553=CARTESIAN_POINT('Ctrl Pts',(2.20565929593438,0.882349537132457,1.2106493263401));
#60554=CARTESIAN_POINT('Ctrl Pts',(2.10602163479816,1.09538605110796,1.22771497423976));
#60555=CARTESIAN_POINT('Ctrl Pts',(2.05797104977608,1.18319599497077,1.23504329626426));
#60556=CARTESIAN_POINT('Ctrl Pts',(1.97546824325865,1.31365059042779,1.2462162935932));
#60557=CARTESIAN_POINT('Ctrl Pts',(1.94484207762595,1.35858112456882,1.25011999086455));
#60558=CARTESIAN_POINT('Ctrl Pts',(1.89271151206976,1.42967954289466,1.25634602099076));
#60559=CARTESIAN_POINT('Ctrl Pts',(1.87214417518171,1.45650847356269,1.25870722562996));
#60560=CARTESIAN_POINT('Ctrl Pts',(1.84321257030297,1.49262218317863,1.26189214982886));
#60561=CARTESIAN_POINT('Ctrl Pts',(1.8353391612079,1.50229282810518,1.26274567825644));
#60562=CARTESIAN_POINT('Ctrl Pts',(1.82192727040874,1.51850337839297,1.26417689962928));
#60563=CARTESIAN_POINT('Ctrl Pts',(1.81642902016666,1.52507610068707,1.26475733239305));
#60564=CARTESIAN_POINT('Ctrl Pts',(1.80571843012323,1.53773966336289,1.26587568955951));
#60565=CARTESIAN_POINT('Ctrl Pts',(1.80051070095198,1.54383403954897,1.26641395052481));
#60566=CARTESIAN_POINT('Ctrl Pts',(1.78609781030232,1.56052868218542,1.26788894907222));
#60567=CARTESIAN_POINT('Ctrl Pts',(1.77682909768598,1.5710740074874,1.2688212190783));
#60568=CARTESIAN_POINT('Ctrl Pts',(1.73881299221089,1.61355940269632,1.27258253134564));
#60569=CARTESIAN_POINT('Ctrl Pts',(1.70929187990182,1.64479979659607,1.27536077511873));
#60570=CARTESIAN_POINT('Ctrl Pts',(1.56896881864915,1.78543388897563,1.28802358061695));
#60571=CARTESIAN_POINT('Ctrl Pts',(1.44840802975891,1.88455828856604,1.29742458676366));
#60572=CARTESIAN_POINT('Ctrl Pts',(1.25095296966123,2.01668462593621,1.31208166062832));
#60573=CARTESIAN_POINT('Ctrl Pts',(1.18060613597337,2.05865681985602,1.31717442538939));
#60574=CARTESIAN_POINT('Ctrl Pts',(1.07598602026902,2.11394952103229,1.32469497210036));
#60575=CARTESIAN_POINT('Ctrl Pts',(1.043350237628,2.13024612847815,1.32703343007177));
#60576=CARTESIAN_POINT('Ctrl Pts',(0.983582086034664,2.15838826618867,1.33131285083499));
#60577=CARTESIAN_POINT('Ctrl Pts',(0.956578760293498,2.17049086109374,1.33324513966153));
#60578=CARTESIAN_POINT('Ctrl Pts',(0.913771316919989,2.18872269142306,1.3363102914883));
#60579=CARTESIAN_POINT('Ctrl Pts',(0.898115292716805,2.19519337094388,1.33743170823019));
#60580=CARTESIAN_POINT('Ctrl Pts',(0.86861530878883,2.20701739560162,1.33954616141698));
#60581=CARTESIAN_POINT('Ctrl Pts',(0.854787737307872,2.2124096018377,1.34053784776935));
#60582=CARTESIAN_POINT('Ctrl Pts',(0.823542505097351,2.22425736656804,1.34278044063124));
#60583=CARTESIAN_POINT('Ctrl Pts',(0.806097950028428,2.23063873178006,1.34403371803809));
#60584=CARTESIAN_POINT('Ctrl Pts',(0.760906815053217,2.24657069964286,1.34728432434011));
#60585=CARTESIAN_POINT('Ctrl Pts',(0.733055415140581,2.25581220761512,1.34929148513945));
#60586=CARTESIAN_POINT('Ctrl Pts',(0.501028944814056,2.32805139670054,1.36605033321133));
#60587=CARTESIAN_POINT('Ctrl Pts',(0.289399634212843,2.36369736878585,1.38170565954516));
#60588=CARTESIAN_POINT('Ctrl Pts',(0.0129065280083569,2.37255274745297,
1.40179246940914));
#60589=CARTESIAN_POINT('Ctrl Pts',(-0.0501686818238375,2.37205758837739,
1.40633980092114));
#60590=CARTESIAN_POINT('Ctrl Pts',(-0.138549892540939,2.36783624402563,
1.41260575429781));
#60591=CARTESIAN_POINT('Ctrl Pts',(-0.163927051732747,2.36621482211109,
1.41439254081993));
#60592=CARTESIAN_POINT('Ctrl Pts',(-0.208595446698214,2.36263871595097,
1.41751047450307));
#60593=CARTESIAN_POINT('Ctrl Pts',(-0.22789769611826,2.3608550277577,1.41884884466261));
#60594=CARTESIAN_POINT('Ctrl Pts',(-0.257166003484129,2.35778807188474,
1.42086249922082));
#60595=CARTESIAN_POINT('Ctrl Pts',(-0.267148829524415,2.35667784334923,
1.42154652871749));
#60596=CARTESIAN_POINT('Ctrl Pts',(-0.285414330981306,2.35452891131814,
1.42279262155435));
#60597=CARTESIAN_POINT('Ctrl Pts',(-0.293698756828221,2.35350988501504,
1.42335569120835));
#60598=CARTESIAN_POINT('Ctrl Pts',(-0.312684798195064,2.35107269199345,
1.42464141640278));
#60599=CARTESIAN_POINT('Ctrl Pts',(-0.323382300967351,2.34962517960746,
1.42536245910796));
#60600=CARTESIAN_POINT('Ctrl Pts',(-0.356296458515065,2.34494241295582,
1.42757156306101));
#60601=CARTESIAN_POINT('Ctrl Pts',(-0.378478072361685,2.3414646107761,1.42904710907445));
#60602=CARTESIAN_POINT('Ctrl Pts',(-0.527857820217949,2.315865337619,1.43891493182303));
#60603=CARTESIAN_POINT('Ctrl Pts',(-0.653131419620313,2.28370178563684,
1.44685848978369));
#60604=CARTESIAN_POINT('Ctrl Pts',(-0.83701416943505,2.22010958420151,1.45881150154125));
#60605=CARTESIAN_POINT('Ctrl Pts',(-0.897939740785599,2.19617470235712,
1.46282173611685));
#60606=CARTESIAN_POINT('Ctrl Pts',(-1.02650860820612,2.13942035309998,1.47151402142603));
#60607=CARTESIAN_POINT('Ctrl Pts',(-1.0937363537981,2.10584399320494,1.47620317707526));
#60608=CARTESIAN_POINT('Ctrl Pts',(-1.18938284589454,2.05225708376759,1.48318523328244));
#60609=CARTESIAN_POINT('Ctrl Pts',(-1.21913757012021,2.03472211830085,1.48540315433815));
#60610=CARTESIAN_POINT('Ctrl Pts',(-1.27260704927299,2.00161770177533,1.48948198991082));
#60611=CARTESIAN_POINT('Ctrl Pts',(-1.29644581715873,1.9862603703108,1.49133545102009));
#60612=CARTESIAN_POINT('Ctrl Pts',(-1.33385653720017,1.96119934133804,1.4943035706306));
#60613=CARTESIAN_POINT('Ctrl Pts',(-1.34761178097542,1.95177318929354,1.49540798514837));
#60614=CARTESIAN_POINT('Ctrl Pts',(-1.37344587871876,1.93366638762244,1.49750780499589));
#60615=CARTESIAN_POINT('Ctrl Pts',(-1.38554474548066,1.92501558994655,1.49850205205797));
#60616=CARTESIAN_POINT('Ctrl Pts',(-1.41289086437254,1.9050715113429,1.50077455982046));
#60617=CARTESIAN_POINT('Ctrl Pts',(-1.4280854046399,1.89370802899853,1.50205546394941));
#60618=CARTESIAN_POINT('Ctrl Pts',(-1.46752713953218,1.8634662349006,1.5054293972987));
#60619=CARTESIAN_POINT('Ctrl Pts',(-1.49154597110368,1.84429736715957,1.50753355964401));
#60620=CARTESIAN_POINT('Ctrl Pts',(-1.6430602872611,1.71848151000432,1.52113441313658));
#60621=CARTESIAN_POINT('Ctrl Pts',(-1.75939799465173,1.59916427142744,1.53314498467794));
#60622=CARTESIAN_POINT('Ctrl Pts',(-1.92099104389118,1.39426563647308,1.552170670839));
#60623=CARTESIAN_POINT('Ctrl Pts',(-1.9751774817936,1.31638098276282,1.55908778748221));
#60624=CARTESIAN_POINT('Ctrl Pts',(-2.04147834108255,1.20773309595234,1.56816851417481));
#60625=CARTESIAN_POINT('Ctrl Pts',(-2.05782718896163,1.17966118857975,1.5704664715147));
#60626=CARTESIAN_POINT('Ctrl Pts',(-2.08492124358308,1.13086070089689,1.57436877392988));
#60627=CARTESIAN_POINT('Ctrl Pts',(-2.09594634355981,1.11029344871243,1.5759859582585));
#60628=CARTESIAN_POINT('Ctrl Pts',(-2.11163009397244,1.07996904804094,1.57832694160497));
#60629=CARTESIAN_POINT('Ctrl Pts',(-2.11652806775114,1.07033814666915,1.57906411690521));
#60630=CARTESIAN_POINT('Ctrl Pts',(-2.12473609464031,1.05392199683107,1.58030955096247));
#60631=CARTESIAN_POINT('Ctrl Pts',(-2.128079791182,1.04715397890926,1.5808198210157));
#60632=CARTESIAN_POINT('Ctrl Pts',(-2.13563697569309,1.03167167948198,1.58197975587104));
#60633=CARTESIAN_POINT('Ctrl Pts',(-2.13982949879235,1.02294744269284,1.58262814843581));
#60634=CARTESIAN_POINT('Ctrl Pts',(-2.15131280325997,0.99867224798369,1.5844185112618));
#60635=CARTESIAN_POINT('Ctrl Pts',(-2.15848842343937,0.98306703929463,1.58555383592393));
#60636=CARTESIAN_POINT('Ctrl Pts',(-2.20845847513104,0.871208900056178,
1.5935907474126));
#60637=CARTESIAN_POINT('Ctrl Pts',(-2.24497356370835,0.772264898072949,
1.60017195110047));
#60638=CARTESIAN_POINT('Ctrl Pts',(-2.2794488463323,0.655424946887912,1.60769393027819));
#60639=CARTESIAN_POINT('Ctrl Pts',(-2.28394189547846,0.63959231471769,1.60870797867424));
#60640=CARTESIAN_POINT('Ctrl Pts',(-2.31658584853866,0.519828833390991,
1.61634705046536));
#60641=CARTESIAN_POINT('Ctrl Pts',(-2.3377939046557,0.414138771475803,1.62291648441333));
#60642=CARTESIAN_POINT('Ctrl Pts',(-2.35759003868515,0.262677186163501,
1.63244055125887));
#60643=CARTESIAN_POINT('Ctrl Pts',(-2.36215595308437,0.2178267288989,1.63527322863562));
#60644=CARTESIAN_POINT('Ctrl Pts',(-2.3654410189124,0.172878132066172,1.63813797379334));
#60645=CARTESIAN_POINT('Origin',(0.,0.,-1.84858989190501));
#60646=CARTESIAN_POINT('',(-2.36906969114779,0.173130678776567,2.83701751404115));
#60647=CARTESIAN_POINT('',(-2.36544104518992,0.172877772518167,2.63906222572513));
#60648=CARTESIAN_POINT('',(-2.36544101854889,0.172878137039864,-1.84858989190501));
#60649=CARTESIAN_POINT('',(-2.37214954248261,-0.00208751672060286,1.84858989190502));
#60650=CARTESIAN_POINT('Ctrl Pts',(-2.37214954248261,-0.00208751672060286,
1.84858989190502));
#60651=CARTESIAN_POINT('Ctrl Pts',(-2.37368814589582,-0.171375740131997,
1.85995808893514));
#60652=CARTESIAN_POINT('Ctrl Pts',(-2.28019409230745,-1.12323247312203,
1.92399124963194));
#60653=CARTESIAN_POINT('Ctrl Pts',(-0.995855715555496,-2.61553061219188,
2.04068937399542));
#60654=CARTESIAN_POINT('Ctrl Pts',(1.64637781974439,-2.26322161422709,2.19868426499547));
#60655=CARTESIAN_POINT('Ctrl Pts',(2.79508756969503,0.142186649832604,2.35667915599553));
#60656=CARTESIAN_POINT('Ctrl Pts',(1.40821242874264,2.41860884498944,2.51467404699558));
#60657=CARTESIAN_POINT('Ctrl Pts',(-1.25613315819632,2.50097199645567,2.67266893799564));
#60658=CARTESIAN_POINT('Ctrl Pts',(-2.29312995726813,1.01405513820569,2.78011676034415));
#60659=CARTESIAN_POINT('Ctrl Pts',(-2.36688836699276,0.204481261054058,
2.83489961902599));
#60660=CARTESIAN_POINT('Ctrl Pts',(-2.36906969114779,0.173130678776576,
2.83701751404115));
#60661=CARTESIAN_POINT('Ctrl Pts',(-2.37174906936557,-0.00210106248464756,
1.84835957816189));
#60662=CARTESIAN_POINT('Ctrl Pts',(-2.3718008254975,0.0563229770868639,
1.84477173666528));
#60663=CARTESIAN_POINT('Ctrl Pts',(-2.36969378183979,0.114688971414575,
1.8411930390963));
#60664=CARTESIAN_POINT('Ctrl Pts',(-2.36544098584031,0.172878584581292,
1.83759047784057));
#60665=CARTESIAN_POINT('Ctrl Pts',(-2.3654410189124,0.172878132066172,1.63813797379334));
#60666=CARTESIAN_POINT('Ctrl Pts',(-2.36650722285482,0.158289574740896,
1.63906775807807));
#60667=CARTESIAN_POINT('Ctrl Pts',(-2.36743850206663,0.143690677903543,
1.64000089714618));
#60668=CARTESIAN_POINT('Ctrl Pts',(-2.37057162816117,0.0862085864060536,
1.6436872167648));
#60669=CARTESIAN_POINT('Ctrl Pts',(-2.37174370262375,0.043280608190179,
1.64646696461456));
#60670=CARTESIAN_POINT('Ctrl Pts',(-2.37175279409662,-0.0189531630133541,
1.65054751451175));
#60671=CARTESIAN_POINT('Ctrl Pts',(-2.37152004312492,-0.0382516358593104,
1.65181990760461));
#60672=CARTESIAN_POINT('Ctrl Pts',(-2.37068903727249,-0.0724921348320239,
1.65409095565325));
#60673=CARTESIAN_POINT('Ctrl Pts',(-2.37018493560669,-0.0874355465879592,
1.65508666046218));
#60674=CARTESIAN_POINT('Ctrl Pts',(-2.36883482135379,-0.118685505063106,
1.65717890899175));
#60675=CARTESIAN_POINT('Ctrl Pts',(-2.36796164018241,-0.134990028426079,
1.65827624007328));
#60676=CARTESIAN_POINT('Ctrl Pts',(-2.36521514840107,-0.177960411516417,
1.66118392719267));
#60677=CARTESIAN_POINT('Ctrl Pts',(-2.36305929083378,-0.204605214837943,
1.66300288021788));
#60678=CARTESIAN_POINT('Ctrl Pts',(-2.34930136124216,-0.345063581175934,
1.67267964128663));
#60679=CARTESIAN_POINT('Ctrl Pts',(-2.32992773745585,-0.457947168149107,
1.68077369546693));
#60680=CARTESIAN_POINT('Ctrl Pts',(-2.28206810369801,-0.651621110046698,
1.69516658157102));
#60681=CARTESIAN_POINT('Ctrl Pts',(-2.25721196628489,-0.733101716672578,
1.70138214880325));
#60682=CARTESIAN_POINT('Ctrl Pts',(-2.18816697038893,-0.922304390653416,
1.7160585732042));
#60683=CARTESIAN_POINT('Ctrl Pts',(-2.14031895910505,-1.02847493746381,
1.72449265393572));
#60684=CARTESIAN_POINT('Ctrl Pts',(-2.0766287312908,-1.14591009468153,1.7337645618215));
#60685=CARTESIAN_POINT('Ctrl Pts',(-2.06822208430992,-1.16101433479644,
1.73495578440575));
#60686=CARTESIAN_POINT('Ctrl Pts',(-2.05483921263766,-1.18445263069519,
1.7368006808796));
#60687=CARTESIAN_POINT('Ctrl Pts',(-2.04997588534783,-1.19284999139944,
1.73746092872973));
#60688=CARTESIAN_POINT('Ctrl Pts',(-2.04123949529479,-1.20772361065788,
1.73862875053818));
#60689=CARTESIAN_POINT('Ctrl Pts',(-2.03738700580321,-1.21421134394877,
1.73913755885768));
#60690=CARTESIAN_POINT('Ctrl Pts',(-2.02796060001715,-1.22991457094225,
1.74036781969376));
#60691=CARTESIAN_POINT('Ctrl Pts',(-2.02235478740453,-1.23911063751104,
1.74108723303817));
#60692=CARTESIAN_POINT('Ctrl Pts',(-2.0045078157739,-1.26794397522642,1.74334061983464));
#60693=CARTESIAN_POINT('Ctrl Pts',(-1.9920413936179,-1.2874411405809,1.74486103753852));
#60694=CARTESIAN_POINT('Ctrl Pts',(-1.92276550832126,-1.39237074713954,
1.75304329595376));
#60695=CARTESIAN_POINT('Ctrl Pts',(-1.86073758110891,-1.47424009859307,
1.75942883148912));
#60696=CARTESIAN_POINT('Ctrl Pts',(-1.66497211251407,-1.70050282960164,
1.77787529660315));
#60697=CARTESIAN_POINT('Ctrl Pts',(-1.51838104454189,-1.83258123097054,
1.78977095423047));
#60698=CARTESIAN_POINT('Ctrl Pts',(-1.33211247178348,-1.96255160862391,
1.80446468675414));
#60699=CARTESIAN_POINT('Ctrl Pts',(-1.30670912094453,-1.97955641251372,
1.80645862279762));
#60700=CARTESIAN_POINT('Ctrl Pts',(-1.2664079672809,-2.00541988919985,1.80961065409293));
#60701=CARTESIAN_POINT('Ctrl Pts',(-1.25172909603453,-2.01461468160752,
1.8107564278356));
#60702=CARTESIAN_POINT('Ctrl Pts',(-1.22444052572031,-2.03129477310934,
1.81288298982044));
#60703=CARTESIAN_POINT('Ctrl Pts',(-1.21185950215961,-2.03882554107477,
1.81386207170541));
#60704=CARTESIAN_POINT('Ctrl Pts',(-1.18368629670252,-2.0553366038865,1.81605204221856));
#60705=CARTESIAN_POINT('Ctrl Pts',(-1.16806025376419,-2.06425701336986,
1.8172649941684));
#60706=CARTESIAN_POINT('Ctrl Pts',(-1.12195538575618,-2.0898857017594,1.8208397329011));
#60707=CARTESIAN_POINT('Ctrl Pts',(-1.09121010184416,-2.10610218851039,
1.82321846071209));
#60708=CARTESIAN_POINT('Ctrl Pts',(-1.01989030276269,-2.14173864684127,
1.82872758292421));
#60709=CARTESIAN_POINT('Ctrl Pts',(-0.979098407183258,-2.16069121512166,
1.83187231751021));
#60710=CARTESIAN_POINT('Ctrl Pts',(-0.830576121562144,-2.22462750021829,
1.84329896870486));
#60711=CARTESIAN_POINT('Ctrl Pts',(-0.720106475424665,-2.26280045639512,
1.8517651200716));
#60712=CARTESIAN_POINT('Ctrl Pts',(-0.480166277638578,-2.32635594391503,
1.86985963073218));
#60713=CARTESIAN_POINT('Ctrl Pts',(-0.350453921239645,-2.34939985246926,
1.87946992782941));
#60714=CARTESIAN_POINT('Ctrl Pts',(-0.197163516641058,-2.36364705789476,
1.89022514801687));
#60715=CARTESIAN_POINT('Ctrl Pts',(-0.174807133522279,-2.36540555132379,
1.89177852776345));
#60716=CARTESIAN_POINT('Ctrl Pts',(-0.14166168391293,-2.36754016407954,
1.89405589825042));
#60717=CARTESIAN_POINT('Ctrl Pts',(-0.130890296634255,-2.36816008806694,
1.8947919753747));
#60718=CARTESIAN_POINT('Ctrl Pts',(-0.111781702529406,-2.36912906623916,
1.89609024697721));
#60719=CARTESIAN_POINT('Ctrl Pts',(-0.103446432340889,-2.36950765438207,
1.89665399116552));
#60720=CARTESIAN_POINT('Ctrl Pts',(-0.0850765978253238,-2.37024489128089,
1.89789071701065));
#60721=CARTESIAN_POINT('Ctrl Pts',(-0.0750415913657593,-2.37058381855894,
1.89856262722164));
#60722=CARTESIAN_POINT('Ctrl Pts',(-0.0456270833055152,-2.37139030922434,
1.90052212175037));
#60723=CARTESIAN_POINT('Ctrl Pts',(-0.0262431140405828,-2.37168404029352,
1.90180069868994));
#60724=CARTESIAN_POINT('Ctrl Pts',(0.0739099002708013,-2.37197359425699,
1.90835119281824));
#60725=CARTESIAN_POINT('Ctrl Pts',(0.154644763099063,-2.36808131734941,
1.91344549821364));
#60726=CARTESIAN_POINT('Ctrl Pts',(0.409343641714807,-2.34271680135929,
1.92935658329961));
#60727=CARTESIAN_POINT('Ctrl Pts',(0.581191867306626,-2.30610086432765,
1.93989315444686));
#60728=CARTESIAN_POINT('Ctrl Pts',(0.808024438819154,-2.23077775345193,
1.95497703000433));
#60729=CARTESIAN_POINT('Ctrl Pts',(0.867764560154263,-2.20822473082563,
1.95906254299357));
#60730=CARTESIAN_POINT('Ctrl Pts',(0.947927506989698,-2.17420614907816,
1.96474296683036));
#60731=CARTESIAN_POINT('Ctrl Pts',(0.969200816938654,-2.16480683929959,
1.96626990901411));
#60732=CARTESIAN_POINT('Ctrl Pts',(1.00309067814366,-2.14923342531369,1.96873561568744));
#60733=CARTESIAN_POINT('Ctrl Pts',(1.01579693047782,-2.14325728901133,1.96966766686124));
#60734=CARTESIAN_POINT('Ctrl Pts',(1.04205032239121,-2.13062362216693,1.97160966886287));
#60735=CARTESIAN_POINT('Ctrl Pts',(1.05558843459342,-2.12394890064327,1.97262017396673));
#60736=CARTESIAN_POINT('Ctrl Pts',(1.08741410856206,-2.10787839111442,1.97501769598573));
#60737=CARTESIAN_POINT('Ctrl Pts',(1.10564477550843,-2.0983732603837,1.97640843997294));
#60738=CARTESIAN_POINT('Ctrl Pts',(1.16717112620376,-2.06527017601494,1.98116279699018));
#60739=CARTESIAN_POINT('Ctrl Pts',(1.20985108058,-2.04056097312134,1.98456471940501));
#60740=CARTESIAN_POINT('Ctrl Pts',(1.31329521226092,-1.97628635806193,1.99307606533235));
#60741=CARTESIAN_POINT('Ctrl Pts',(1.37307170333304,-1.93523243100975,1.99823270050377));
#60742=CARTESIAN_POINT('Ctrl Pts',(1.54550823622632,-1.80478933377107,2.01380375854382));
#60743=CARTESIAN_POINT('Ctrl Pts',(1.65201948031217,-1.70783183530549,2.0243887758945));
#60744=CARTESIAN_POINT('Ctrl Pts',(1.79376765309942,-1.55305205325193,2.03950710441214));
#60745=CARTESIAN_POINT('Ctrl Pts',(1.83638420011413,-1.50242064882401,2.0442122215492));
#60746=CARTESIAN_POINT('Ctrl Pts',(1.88668385765034,-1.43731755481127,2.0499105828646));
#60747=CARTESIAN_POINT('Ctrl Pts',(1.89640611804759,-1.42446537436496,2.05101924858662));
#60748=CARTESIAN_POINT('Ctrl Pts',(1.91156143615865,-1.40400084024771,2.05275779948194));
#60749=CARTESIAN_POINT('Ctrl Pts',(1.91708155730352,-1.39645400704104,2.05339327428123));
#60750=CARTESIAN_POINT('Ctrl Pts',(1.92752700819558,-1.38199483596361,2.05459973613502));
#60751=CARTESIAN_POINT('Ctrl Pts',(1.93246002570753,-1.37508848628665,2.05517120318125));
#60752=CARTESIAN_POINT('Ctrl Pts',(1.9442632199243,-1.35837475369387,2.05654298993827));
#60753=CARTESIAN_POINT('Ctrl Pts',(1.95109650770349,-1.34854138698825,2.05734088021646));
#60754=CARTESIAN_POINT('Ctrl Pts',(1.97497264494,-1.31362128471925,2.0601436685427));
#60755=CARTESIAN_POINT('Ctrl Pts',(1.9916092857163,-1.28825870336095,2.06212395566854));
#60756=CARTESIAN_POINT('Ctrl Pts',(2.03252255310066,-1.22319852539074,2.06708400758758));
#60757=CARTESIAN_POINT('Ctrl Pts',(2.05612665688058,-1.18309181836247,2.07003186619664));
#60758=CARTESIAN_POINT('Ctrl Pts',(2.18308825035769,-0.95207454479456,2.08654820420345));
#60759=CARTESIAN_POINT('Ctrl Pts',(2.26102693710006,-0.748387278041042,
2.09946127208388));
#60760=CARTESIAN_POINT('Ctrl Pts',(2.32064384756769,-0.491883416028774,
2.1162702325225));
#60761=CARTESIAN_POINT('Ctrl Pts',(2.32979376655162,-0.446539721317087,
2.11925645290524));
#60762=CARTESIAN_POINT('Ctrl Pts',(2.3407538491598,-0.382641990822375,2.12350009450854));
#60763=CARTESIAN_POINT('Ctrl Pts',(2.3436803195018,-0.364288352075148,2.12472304457366));
#60764=CARTESIAN_POINT('Ctrl Pts',(2.34840882212246,-0.332213098388674,
2.12686823929053));
#60765=CARTESIAN_POINT('Ctrl Pts',(2.35030704136993,-0.318506414750984,
2.12778745934583));
#60766=CARTESIAN_POINT('Ctrl Pts',(2.35404628870528,-0.289649834210623,
2.12972835949216));
#60767=CARTESIAN_POINT('Ctrl Pts',(2.35586124224451,-0.274497257825233,
2.13075080354843));
#60768=CARTESIAN_POINT('Ctrl Pts',(2.35988206230597,-0.237944381955068,
2.13322565482779));
#60769=CARTESIAN_POINT('Ctrl Pts',(2.36194319240294,-0.216529860221301,
2.13468246550038));
#60770=CARTESIAN_POINT('Ctrl Pts',(2.36829912274163,-0.139521672987643,
2.1399476304263));
#60771=CARTESIAN_POINT('Ctrl Pts',(2.37092421625406,-0.083812353207781,
2.14380637099085));
#60772=CARTESIAN_POINT('Ctrl Pts',(2.37261213971251,0.0588174204132735,
2.15381835638895));
#60773=CARTESIAN_POINT('Ctrl Pts',(2.36886503509941,0.145683725439771,2.16004402054196));
#60774=CARTESIAN_POINT('Ctrl Pts',(2.34795669888371,0.3582749801262,2.17552368244949));
#60775=CARTESIAN_POINT('Ctrl Pts',(2.32546121546305,0.48321001142874,2.18483933680214));
#60776=CARTESIAN_POINT('Ctrl Pts',(2.2776057435873,0.664369024038535,2.19830362552081));
#60777=CARTESIAN_POINT('Ctrl Pts',(2.25987701094352,0.722378953942853,2.20260550700941));
#60778=CARTESIAN_POINT('Ctrl Pts',(2.23477184592509,0.794506321767673,2.2078921405661));
#60779=CARTESIAN_POINT('Ctrl Pts',(2.22945314942921,0.809310932877813,2.20897386102416));
#60780=CARTESIAN_POINT('Ctrl Pts',(2.22076778582128,0.83275108506334,2.21067994120251));
#60781=CARTESIAN_POINT('Ctrl Pts',(2.21749723010272,0.84142139860191,2.21130955714423));
#60782=CARTESIAN_POINT('Ctrl Pts',(2.2111215323019,0.858028118825069,2.21251240726086));
#60783=CARTESIAN_POINT('Ctrl Pts',(2.20802433273991,0.865967223137882,2.2130860509396));
#60784=CARTESIAN_POINT('Ctrl Pts',(2.20039719867509,0.885211014543394,2.21447346106541));
#60785=CARTESIAN_POINT('Ctrl Pts',(2.19582277882416,0.896498026716529,2.21528465316774));
#60786=CARTESIAN_POINT('Ctrl Pts',(2.17903014924088,0.937032733036599,2.21819034212709));
#60787=CARTESIAN_POINT('Ctrl Pts',(2.16631228801756,0.966071445361223,2.22025777556173));
#60788=CARTESIAN_POINT('Ctrl Pts',(2.06267174775505,1.19036666658164,2.23618113030257));
#60789=CARTESIAN_POINT('Ctrl Pts',(1.94610863667187,1.37268773231333,2.24893413652057));
#60790=CARTESIAN_POINT('Ctrl Pts',(1.75338574569002,1.59923739335471,2.26752828031237));
#60791=CARTESIAN_POINT('Ctrl Pts',(1.69705640283385,1.65889097788463,2.27273353050838));
#60792=CARTESIAN_POINT('Ctrl Pts',(1.61937051417628,1.73305605138435,2.27972164372801));
#60793=CARTESIAN_POINT('Ctrl Pts',(1.60070509083984,1.75031062132554,2.28138713359509));
#60794=CARTESIAN_POINT('Ctrl Pts',(1.56980699861919,1.77796559605334,2.28412474896665));
#60795=CARTESIAN_POINT('Ctrl Pts',(1.55773936931983,1.78854793331922,2.28518928346335));
#60796=CARTESIAN_POINT('Ctrl Pts',(1.53414733249378,1.80881636095374,2.28726203110273));
#60797=CARTESIAN_POINT('Ctrl Pts',(1.52263625611515,1.8185168350131,2.288269589531));
#60798=CARTESIAN_POINT('Ctrl Pts',(1.495382159341,1.8410438889784,2.29064679455069));
#60799=CARTESIAN_POINT('Ctrl Pts',(1.47956541345178,1.85377899084149,2.29201999202037));
#60800=CARTESIAN_POINT('Ctrl Pts',(1.42604878679015,1.89574752987011,2.29664633392032));
#60801=CARTESIAN_POINT('Ctrl Pts',(1.38763292796508,1.92404473386648,2.29993503479337));
#60802=CARTESIAN_POINT('Ctrl Pts',(1.29150721130187,1.99047444130965,2.30809188003879));
#60803=CARTESIAN_POINT('Ctrl Pts',(1.23293486661149,2.02727638982289,2.31300218648632));
#60804=CARTESIAN_POINT('Ctrl Pts',(1.09118004450687,2.10792590973622,2.3247264753537));
#60805=CARTESIAN_POINT('Ctrl Pts',(1.00683175670646,2.14949152870335,2.33158314192042));
#60806=CARTESIAN_POINT('Ctrl Pts',(0.818738021908449,2.22867581720257,2.34645711017889));
#60807=CARTESIAN_POINT('Ctrl Pts',(0.714367718196973,2.26429043566019,2.35445456779312));
#60808=CARTESIAN_POINT('Ctrl Pts',(0.585672881320951,2.29841547776209,2.36375910320478));
#60809=CARTESIAN_POINT('Ctrl Pts',(0.563368915810369,2.30398393948334,2.36535172390611));
#60810=CARTESIAN_POINT('Ctrl Pts',(0.530528557705808,2.31167750424403,2.36766415938219));
#60811=CARTESIAN_POINT('Ctrl Pts',(0.520053811472902,2.31405649854322,2.36839690676218));
#60812=CARTESIAN_POINT('Ctrl Pts',(0.501417289955651,2.31815623452871,2.3696916096472));
#60813=CARTESIAN_POINT('Ctrl Pts',(0.493262176902826,2.31990518298289,2.3702550812083));
#60814=CARTESIAN_POINT('Ctrl Pts',(0.475233376679526,2.32367227708012,2.37149396182267));
#60815=CARTESIAN_POINT('Ctrl Pts',(0.465355895043343,2.32567055141762,2.37216827167205));
#60816=CARTESIAN_POINT('Ctrl Pts',(0.436263396578076,2.33136336952561,2.37414210426682));
#60817=CARTESIAN_POINT('Ctrl Pts',(0.417014519108134,2.33488326538684,2.37543241850249));
#60818=CARTESIAN_POINT('Ctrl Pts',(0.267001230920364,2.36040063644657,2.3853823207734));
#60819=CARTESIAN_POINT('Ctrl Pts',(0.134625913696415,2.3716378619941,2.39354585699655));
#60820=CARTESIAN_POINT('Ctrl Pts',(-0.164800082457489,2.37188912922675,
2.4119421846848));
#60821=CARTESIAN_POINT('Ctrl Pts',(-0.331121029983698,2.35443594925894,
2.42213921139802));
#60822=CARTESIAN_POINT('Ctrl Pts',(-0.524251091600474,2.31328794722317,
2.43487672094202));
#60823=CARTESIAN_POINT('Ctrl Pts',(-0.554145508291139,2.30630937928264,
2.43687307521349));
#60824=CARTESIAN_POINT('Ctrl Pts',(-0.602275439247987,2.29408412975374,
2.44013195577816));
#60825=CARTESIAN_POINT('Ctrl Pts',(-0.620598743577357,2.28919524379991,
2.4413832258896));
#60826=CARTESIAN_POINT('Ctrl Pts',(-0.653183564977096,2.28008124337408,
2.44362831775515));
#60827=CARTESIAN_POINT('Ctrl Pts',(-0.667467826403133,2.27594066918248,
2.44461939185791));
#60828=CARTESIAN_POINT('Ctrl Pts',(-0.697688281726195,2.26687171097754,
2.44673126621278));
#60829=CARTESIAN_POINT('Ctrl Pts',(-0.713613249026269,2.26190901650747,
2.4478531258937));
#60830=CARTESIAN_POINT('Ctrl Pts',(-0.756489667696547,2.24804958588336,
2.45089864073422));
#60831=CARTESIAN_POINT('Ctrl Pts',(-0.783335211578066,2.23883661401164,
2.45283241264343));
#60832=CARTESIAN_POINT('Ctrl Pts',(-0.842502914985661,2.21733674538441,
2.45715631128878));
#60833=CARTESIAN_POINT('Ctrl Pts',(-0.874734247176489,2.20482044436274,
2.45955342125923));
#60834=CARTESIAN_POINT('Ctrl Pts',(-0.976205886801671,2.1628410583344,2.46723480880692));
#60835=CARTESIAN_POINT('Ctrl Pts',(-1.04431852684647,2.13078774389948,2.47259532172554));
#60836=CARTESIAN_POINT('Ctrl Pts',(-1.22934198965628,2.03271261063227,2.48769677888344));
#60837=CARTESIAN_POINT('Ctrl Pts',(-1.34234470561332,1.95992633849734,2.49756488809204));
#60838=CARTESIAN_POINT('Ctrl Pts',(-1.50456002505023,1.8348009886683,2.51234834003741));
#60839=CARTESIAN_POINT('Ctrl Pts',(-1.55858274656376,1.78913870953042,2.51738707575922));
#60840=CARTESIAN_POINT('Ctrl Pts',(-1.62249603759713,1.73002085921584,2.52341950897839));
#60841=CARTESIAN_POINT('Ctrl Pts',(-1.63438801055534,1.71879068913576,2.52454510010271));
#60842=CARTESIAN_POINT('Ctrl Pts',(-1.65293207110211,1.70091211854387,2.52630403641596));
#60843=CARTESIAN_POINT('Ctrl Pts',(-1.65966216411146,1.69434588420771,2.52694318444354));
#60844=CARTESIAN_POINT('Ctrl Pts',(-1.67237924130797,1.68178995366011,2.52815210284693));
#60845=CARTESIAN_POINT('Ctrl Pts',(-1.67837323685405,1.67580817963298,2.52872238208247));
#60846=CARTESIAN_POINT('Ctrl Pts',(-1.68438613384638,1.66974292027718,2.52929506774057));
#60847=CARTESIAN_POINT('Ctrl Pts',(-1.68443694764035,1.66969165929934,2.52929990743776));
#60848=CARTESIAN_POINT('Ctrl Pts',(-1.68453737238546,1.66959034152202,2.52930947235767));
#60849=CARTESIAN_POINT('Ctrl Pts',(-1.68458698344294,1.66954028483338,2.52931419758844));
#60850=CARTESIAN_POINT('Ctrl Pts',(-1.68468505886197,1.66944131963004,2.52932353891723));
#60851=CARTESIAN_POINT('Ctrl Pts',(-1.684733523341,1.66939241119992,2.52932815502448));
#60852=CARTESIAN_POINT('Ctrl Pts',(-1.68482935847505,1.66929568975979,2.52933728313654));
#60853=CARTESIAN_POINT('Ctrl Pts',(-1.68487672922794,1.66924787684041,2.52934179514882));
#60854=CARTESIAN_POINT('Ctrl Pts',(-1.6849704267261,1.6691532967022,2.52935071981064));
#60855=CARTESIAN_POINT('Ctrl Pts',(-1.68501675354766,1.66910652958314,2.52935513246572));
#60856=CARTESIAN_POINT('Ctrl Pts',(-1.69275121881801,1.66129790453169,2.53009185080793));
#60857=CARTESIAN_POINT('Ctrl Pts',(-1.70038582126558,1.65348283530524,2.53082009581914));
#60858=CARTESIAN_POINT('Ctrl Pts',(-1.72620911450056,1.62668111522474,2.53328806396711));
#60859=CARTESIAN_POINT('Ctrl Pts',(-1.74413670366934,1.60744413708869,2.53500956635476));
#60860=CARTESIAN_POINT('Ctrl Pts',(-1.78797017729644,1.55881219237146,2.53925135948999));
#60861=CARTESIAN_POINT('Ctrl Pts',(-1.81347524889252,1.52906529142509,2.54174919284464));
#60862=CARTESIAN_POINT('Ctrl Pts',(-1.92441892772621,1.39298701020566,2.55282155417023));
#60863=CARTESIAN_POINT('Ctrl Pts',(-2.00133024481161,1.280032310735,2.56108727189952));
#60864=CARTESIAN_POINT('Ctrl Pts',(-2.12884680834715,1.05290190120611,2.57714961082586));
#60865=CARTESIAN_POINT('Ctrl Pts',(-2.18099497152325,0.940131094760641,
2.58489645022722));
#60866=CARTESIAN_POINT('Ctrl Pts',(-2.23368168852974,0.797889780500425,
2.59474186846515));
#60867=CARTESIAN_POINT('Ctrl Pts',(-2.24282780723674,0.771806525001884,
2.59654950174099));
#60868=CARTESIAN_POINT('Ctrl Pts',(-2.25670967017767,0.729885280115304,
2.59946136659405));
#60869=CARTESIAN_POINT('Ctrl Pts',(-2.26173945592868,0.7141468113005,2.6005560299086));
#60870=CARTESIAN_POINT('Ctrl Pts',(-2.27099276224718,0.68411407480358,2.60264831038471));
#60871=CARTESIAN_POINT('Ctrl Pts',(-2.27524679299409,0.669829983843014,
2.60364488571619));
#60872=CARTESIAN_POINT('Ctrl Pts',(-2.28468512286114,0.637010493029739,
2.60593841808241));
#60873=CARTESIAN_POINT('Ctrl Pts',(-2.28977893222255,0.618450388397305,
2.60723820241515));
#60874=CARTESIAN_POINT('Ctrl Pts',(-2.29995844813261,0.579508761910597,
2.6099717508555));
#60875=CARTESIAN_POINT('Ctrl Pts',(-2.30500036937791,0.559117623483894,
2.61140677763455));
#60876=CARTESIAN_POINT('Ctrl Pts',(-2.3178181405796,0.504155383295277,2.61528529455615));
#60877=CARTESIAN_POINT('Ctrl Pts',(-2.32509093595485,0.469473639692089,
2.61774388493411));
#60878=CARTESIAN_POINT('Ctrl Pts',(-2.34772955812159,0.34803193996765,2.62639308156394));
#60879=CARTESIAN_POINT('Ctrl Pts',(-2.35902693891148,0.260640299986158,
2.63269147581119));
#60880=CARTESIAN_POINT('Ctrl Pts',(-2.36544104518992,0.172877772518167,
2.63906222572513));
#60881=CARTESIAN_POINT('Origin',(0.,0.,-1.84858989190501));
#60882=CARTESIAN_POINT('',(-2.36544101854889,0.172878137039867,3.83707348408299));
#60883=CARTESIAN_POINT('',(-2.36544101877862,0.172878133896551,3.6418462952528));
#60884=CARTESIAN_POINT('',(-2.36544101854889,0.172878137039864,-1.84858989190501));
#60885=CARTESIAN_POINT('',(-2.37174955725825,0.00144918780827443,2.84858993475468));
#60886=CARTESIAN_POINT('Ctrl Pts',(-2.37174955725825,0.00144918780827443,
2.84858993475469));
#60887=CARTESIAN_POINT('Ctrl Pts',(-2.37179726134704,-0.0766236132632544,
2.85385139941758));
#60888=CARTESIAN_POINT('Ctrl Pts',(-2.36798576321773,-0.154846589518332,
2.85911286408048));
#60889=CARTESIAN_POINT('Ctrl Pts',(-2.36029698198233,-0.232800814743257,
2.86437432874338));
#60890=CARTESIAN_POINT('Ctrl Pts',(-2.35261882788851,-0.310647294596898,
2.86962852120952));
#60891=CARTESIAN_POINT('Ctrl Pts',(-2.34107408131574,-0.388225285324987,
2.87488271367567));
#60892=CARTESIAN_POINT('Ctrl Pts',(-2.32569668339652,-0.465116113823676,
2.88013690614181));
#60893=CARTESIAN_POINT('Ctrl Pts',(-2.31033102347183,-0.541948249419353,
2.88538708793705));
#60894=CARTESIAN_POINT('Ctrl Pts',(-2.29113860801431,-0.618093792558647,
2.89063726973229));
#60895=CARTESIAN_POINT('Ctrl Pts',(-2.26820501046763,-0.693140745440315,
2.89588745152753));
#60896=CARTESIAN_POINT('Ctrl Pts',(-2.24528134677732,-0.768155191182627,
2.90113535916792));
#60897=CARTESIAN_POINT('Ctrl Pts',(-2.21861985678342,-0.842071530751637,
2.90638326680832));
#60898=CARTESIAN_POINT('Ctrl Pts',(-2.18835647317101,-0.914491120148553,
2.91163117444872));
#60899=CARTESIAN_POINT('Ctrl Pts',(-2.15809620728109,-0.986903248906358,
2.91687854145162));
#60900=CARTESIAN_POINT('Ctrl Pts',(-2.12423497147806,-1.05781848976263,
2.92212590845453));
#60901=CARTESIAN_POINT('Ctrl Pts',(-2.08695690071309,-1.12685800217509,
2.92737327545744));
#60902=CARTESIAN_POINT('Ctrl Pts',(-2.04964530915196,-1.19595959557442,
2.93262536094271));
#60903=CARTESIAN_POINT('Ctrl Pts',(-2.00891097447246,-1.26318166641551,
2.93787744642799));
#60904=CARTESIAN_POINT('Ctrl Pts',(-1.9649837094817,-1.32817057788958,2.94312953191326));
#60905=CARTESIAN_POINT('Ctrl Pts',(-1.92103736272031,-1.39318772020167,
2.94838389887658));
#60906=CARTESIAN_POINT('Ctrl Pts',(-1.87389561400849,-1.45596938633539,
2.9536382658399));
#60907=CARTESIAN_POINT('Ctrl Pts',(-1.82382969244265,-1.51619369325444,
2.95889263280322));
#60908=CARTESIAN_POINT('Ctrl Pts',(-1.77367591830687,-1.57652367804719,
2.96415621980338));
#60909=CARTESIAN_POINT('Ctrl Pts',(-1.72058804887877,-1.63428698509946,
2.96941980680354));
#60910=CARTESIAN_POINT('Ctrl Pts',(-1.66487510562834,-1.68919772234012,
2.9746833938037));
#60911=CARTESIAN_POINT('Ctrl Pts',(-1.61556737720283,-1.73779547290835,
2.97934183586771));
#60912=CARTESIAN_POINT('Ctrl Pts',(-1.56420417740737,-1.7841592771669,2.98400027793172));
#60913=CARTESIAN_POINT('Ctrl Pts',(-1.51101990214086,-1.82811840913936,
2.98865871999573));
#60914=CARTESIAN_POINT('Ctrl Pts',(-1.45010266434992,-1.87846917319566,
2.99399449681185));
#60915=CARTESIAN_POINT('Ctrl Pts',(-1.38655261703524,-1.92586544674143,
2.99933027362796));
#60916=CARTESIAN_POINT('Ctrl Pts',(-1.32068805983314,-1.97002058646964,
3.00466605044407));
#60917=CARTESIAN_POINT('Ctrl Pts',(-1.25491766702395,-2.01411259904565,
3.00999419887542));
#60918=CARTESIAN_POINT('Ctrl Pts',(-1.18683972146185,-2.05497242184816,
3.01532234730677));
#60919=CARTESIAN_POINT('Ctrl Pts',(-1.1168056515261,-2.0923535072304,3.02065049573812));
#60920=CARTESIAN_POINT('Ctrl Pts',(-1.04685189699581,-2.12969172380563,
3.02597253382343));
#60921=CARTESIAN_POINT('Ctrl Pts',(-0.974946887030453,-2.16355891193964,
3.03129457190874));
#60922=CARTESIAN_POINT('Ctrl Pts',(-0.90146981626064,-2.19375254595203,
3.03661660999406));
#60923=CARTESIAN_POINT('Ctrl Pts',(-0.828038758435314,-2.22392727205218,
3.04193531530303));
#60924=CARTESIAN_POINT('Ctrl Pts',(-0.753038025698316,-2.25043283296074,
3.047254020612));
#60925=CARTESIAN_POINT('Ctrl Pts',(-0.676869037026495,-2.27311380472136,
3.05257272592098));
#60926=CARTESIAN_POINT('Ctrl Pts',(-0.600724117037506,-2.29578760950859,
3.05788975056918));
#60927=CARTESIAN_POINT('Ctrl Pts',(-0.523412122448103,-2.31463909170633,
3.06320677521738));
#60928=CARTESIAN_POINT('Ctrl Pts',(-0.445350561000367,-2.32956239244985,
3.06852379986559));
#60929=CARTESIAN_POINT('Ctrl Pts',(-0.367289449785087,-2.34448560712086,
3.07384079384701));
#60930=CARTESIAN_POINT('Ctrl Pts',(-0.288479240262441,-2.35548059896049,
3.07915778782843));
#60931=CARTESIAN_POINT('Ctrl Pts',(-0.209347124003659,-2.36249271833193,
3.08447478180984));
#60932=CARTESIAN_POINT('Ctrl Pts',(-0.130136702035626,-2.36951177659249,
3.08979703725784));
#60933=CARTESIAN_POINT('Ctrl Pts',(-0.0506042042954726,-2.37254004843377,
3.09511929270583));
#60934=CARTESIAN_POINT('Ctrl Pts',(0.0288191732936541,-2.37157490241204,
3.10044154815383));
#60935=CARTESIAN_POINT('Ctrl Pts',(0.108281098580519,-2.37060928796201,
3.10576638672912));
#60936=CARTESIAN_POINT('Ctrl Pts',(0.187633330540198,-2.36564642374603,
3.1110912253044));
#60937=CARTESIAN_POINT('Ctrl Pts',(0.266448342489727,-2.35673573895855,
3.11641606387969));
#60938=CARTESIAN_POINT('Ctrl Pts',(0.345403638790127,-2.34780919387236,
3.12175038023725));
#60939=CARTESIAN_POINT('Ctrl Pts',(0.42381934167684,-2.33492086440187,3.12708469659481));
#60940=CARTESIAN_POINT('Ctrl Pts',(0.501276921251674,-2.31817158785118,
3.13241901295237));
#60941=CARTESIAN_POINT('Ctrl Pts',(0.570175316519782,-2.30327313268928,
3.13716387896684));
#60942=CARTESIAN_POINT('Ctrl Pts',(0.63831559260771,-2.28532066239902,3.14190874498132));
#60943=CARTESIAN_POINT('Ctrl Pts',(0.705415006637884,-2.2644177465543,3.1466536109958));
#60944=CARTESIAN_POINT('Ctrl Pts',(0.780870772090863,-2.24091164686538,
3.15198938780203));
#60945=CARTESIAN_POINT('Ctrl Pts',(0.855290743765986,-2.21358614523013,
3.15732516460827));
#60946=CARTESIAN_POINT('Ctrl Pts',(0.928260929205188,-2.18255119294167,
3.1626609414145));
#60947=CARTESIAN_POINT('Ctrl Pts',(1.00112679155559,-2.15156061031,3.16798908983506));
#60948=CARTESIAN_POINT('Ctrl Pts',(1.07254655687529,-2.11687129091511,3.17331723825561));
#60949=CARTESIAN_POINT('Ctrl Pts',(1.14212171099343,-2.0786428408405,3.17864538667617));
#60950=CARTESIAN_POINT('Ctrl Pts',(1.21161707597577,-2.04045823134421,3.18396742474939));
#60951=CARTESIAN_POINT('Ctrl Pts',(1.27927162561687,-1.99874278130691,3.1892894628226));
#60952=CARTESIAN_POINT('Ctrl Pts',(1.3447085425351,-1.95370340587642,3.19461150089582));
#60953=CARTESIAN_POINT('Ctrl Pts',(1.41010448141865,-1.9086922350921,3.1999302061919));
#60954=CARTESIAN_POINT('Ctrl Pts',(1.47328515965246,-1.86036153533037,3.20524891148798));
#60955=CARTESIAN_POINT('Ctrl Pts',(1.5339010641881,-1.80896257224483,3.21056761678406));
#60956=CARTESIAN_POINT('Ctrl Pts',(1.59449781466011,-1.7575798507549,3.2158846414186));
#60957=CARTESIAN_POINT('Ctrl Pts',(1.65253104419497,-1.70313109381767,3.22120166605313));
#60958=CARTESIAN_POINT('Ctrl Pts',(1.70768395978545,-1.64590812501533,3.22651869068767));
#60959=CARTESIAN_POINT('Ctrl Pts',(1.76283655726462,-1.58868548626397,3.23183568465464));
#60960=CARTESIAN_POINT('Ctrl Pts',(1.81510855012025,-1.52868900545532,3.23715267862161));
#60961=CARTESIAN_POINT('Ctrl Pts',(1.86422074216089,-1.46624659829003,3.24246967258858));
#60962=CARTESIAN_POINT('Ctrl Pts',(1.9133815334861,-1.40374240084032,3.24779192802102));
#60963=CARTESIAN_POINT('Ctrl Pts',(1.95937598834536,-1.33878781111464,3.25311418345347));
#60964=CARTESIAN_POINT('Ctrl Pts',(2.00196628826689,-1.27174252234597,3.25843643888592));
#60965=CARTESIAN_POINT('Ctrl Pts',(2.04457725915028,-1.20466469352454,3.26376127744502));
#60966=CARTESIAN_POINT('Ctrl Pts',(2.08378055264218,-1.13549455186852,3.26908611600412));
#60967=CARTESIAN_POINT('Ctrl Pts',(2.11938395655237,-1.0646171646223,3.27441095456322));
#60968=CARTESIAN_POINT('Ctrl Pts',(2.15505073163808,-0.993613621366983,
3.27974527090371));
#60969=CARTESIAN_POINT('Ctrl Pts',(2.18710462542536,-0.920897190148557,
3.2850795872442));
#60970=CARTESIAN_POINT('Ctrl Pts',(2.21540139658963,-0.846873493792748,
3.29041390358468));
#60971=CARTESIAN_POINT('Ctrl Pts',(2.24057133078837,-0.78102953033815,3.29515876972174));
#60972=CARTESIAN_POINT('Ctrl Pts',(2.26276924267427,-0.714151720879358,
3.2999036358588));
#60973=CARTESIAN_POINT('Ctrl Pts',(2.28192737613385,-0.646533458183634,
3.30464850199585));
#60974=CARTESIAN_POINT('Ctrl Pts',(2.30347140343113,-0.570494229185414,
3.30998427887591));
#60975=CARTESIAN_POINT('Ctrl Pts',(2.32125066165164,-0.493235486043965,
3.31532005575597));
#60976=CARTESIAN_POINT('Ctrl Pts',(2.33513102189741,-0.415164031525341,
3.32065583263602));
#60977=CARTESIAN_POINT('Ctrl Pts',(2.34899153784952,-0.337204193192593,
3.3259839811317));
#60978=CARTESIAN_POINT('Ctrl Pts',(2.35896414468065,-0.258434408031037,
3.33131212962738));
#60979=CARTESIAN_POINT('Ctrl Pts',(2.36496475756639,-0.179275648008737,
3.33664027812306));
#60980=CARTESIAN_POINT('Ctrl Pts',(2.3709584889211,-0.100207667624079,3.34196231627303));
#60981=CARTESIAN_POINT('Ctrl Pts',(2.37298924354505,-0.0207520632132589,
3.347284354423));
#60982=CARTESIAN_POINT('Ctrl Pts',(2.3710244140385,0.0586625138686694,3.35260639257297));
#60983=CARTESIAN_POINT('Ctrl Pts',(2.36906081495098,0.138027359813093,3.35792509794676));
#60984=CARTESIAN_POINT('Ctrl Pts',(2.36310660992711,0.217350762769891,3.36324380332054));
#60985=CARTESIAN_POINT('Ctrl Pts',(2.35318125524889,0.296202704993171,3.36856250869433));
#60986=CARTESIAN_POINT('Ctrl Pts',(2.34325903688908,0.375029730746759,3.3738795334074));
#60987=CARTESIAN_POINT('Ctrl Pts',(2.3293682192789,0.453385127608195,3.37919655812048));
#60988=CARTESIAN_POINT('Ctrl Pts',(2.31158010531648,0.530844119497464,3.38451358283356));
#60989=CARTESIAN_POINT('Ctrl Pts',(2.29379209394997,0.608302664629148,3.38983057687981));
#60990=CARTESIAN_POINT('Ctrl Pts',(2.2721069371148,0.684864359270751,3.39514757092607));
#60991=CARTESIAN_POINT('Ctrl Pts',(2.24664670893548,0.760116193571344,3.40046456497232));
#60992=CARTESIAN_POINT('Ctrl Pts',(2.22116128642164,0.835442493814362,3.40578682048464));
#60993=CARTESIAN_POINT('Ctrl Pts',(2.19189348108999,0.909455900312832,3.41110907599696));
#60994=CARTESIAN_POINT('Ctrl Pts',(2.15901459074628,0.981760693572873,3.41643133150928));
#60995=CARTESIAN_POINT('Ctrl Pts',(2.126119742816,1.05410057956219,3.42175617014871));
#60996=CARTESIAN_POINT('Ctrl Pts',(2.0896105335621,1.12472978403073,3.42708100878814));
#60997=CARTESIAN_POINT('Ctrl Pts',(2.04970443203159,1.1932769183262,3.43240584742757));
#60998=CARTESIAN_POINT('Ctrl Pts',(2.00972730087455,1.26194606096529,3.43774016384823));
#60999=CARTESIAN_POINT('Ctrl Pts',(1.96634145294465,1.32852533584444,3.44307448026888));
#61000=CARTESIAN_POINT('Ctrl Pts',(1.91980778510332,1.39267229840932,3.44840879668954));
#61001=CARTESIAN_POINT('Ctrl Pts',(1.87841616625029,1.44973091313356,3.453153662125));
#61002=CARTESIAN_POINT('Ctrl Pts',(1.83453471518382,1.50486534392455,3.45789852756045));
#61003=CARTESIAN_POINT('Ctrl Pts',(1.78837212794992,1.5578585283882,3.46264339299591));
#61004=CARTESIAN_POINT('Ctrl Pts',(1.73646058963283,1.61745132616385,3.46797916983645));
#61005=CARTESIAN_POINT('Ctrl Pts',(1.68147054569493,1.67455745878579,3.47331494667699));
#61006=CARTESIAN_POINT('Ctrl Pts',(1.62366940683842,1.72884230622604,3.47865072351753));
#61007=CARTESIAN_POINT('Ctrl Pts',(1.56595090437147,1.78304954440306,3.48397887197319));
#61008=CARTESIAN_POINT('Ctrl Pts',(1.50542962686771,1.8344431900713,3.48930702042885));
#61009=CARTESIAN_POINT('Ctrl Pts',(1.44241219702958,1.88272279328644,3.49463516888451));
#61010=CARTESIAN_POINT('Ctrl Pts',(1.37946703588314,1.93094702922037,3.49995720699389));
#61011=CARTESIAN_POINT('Ctrl Pts',(1.31403178093854,1.976064036589,3.50527924510327));
#61012=CARTESIAN_POINT('Ctrl Pts',(1.24644761482377,2.01781228215118,3.51060128321265));
#61013=CARTESIAN_POINT('Ctrl Pts',(1.17890577139001,2.0595343840501,3.51591998854552));
#61014=CARTESIAN_POINT('Ctrl Pts',(1.10921808509587,2.09789166630804,3.5212386938784));
#61015=CARTESIAN_POINT('Ctrl Pts',(1.0377553316376,2.13266545293859,3.52655739921127));
#61016=CARTESIAN_POINT('Ctrl Pts',(0.966315159738883,2.16742825137884,3.53187442388316));
#61017=CARTESIAN_POINT('Ctrl Pts',(0.893101455105723,2.19860959829671,3.53719144855505));
#61018=CARTESIAN_POINT('Ctrl Pts',(0.818508933576427,2.22603710394854,3.54250847322694));
#61019=CARTESIAN_POINT('Ctrl Pts',(0.743916842274842,2.25346445140658,3.5478254672318));
#61020=CARTESIAN_POINT('Ctrl Pts',(0.667946389649167,2.27713784052501,3.55314246123665));
#61021=CARTESIAN_POINT('Ctrl Pts',(0.591010179673689,2.29693383231256,3.55845945524151));
#61022=CARTESIAN_POINT('Ctrl Pts',(0.513997836970756,2.31674941335267,3.5637817107124));
#61023=CARTESIAN_POINT('Ctrl Pts',(0.436018282280889,2.33267981610995,3.56910396618329));
#61024=CARTESIAN_POINT('Ctrl Pts',(0.357496535587641,2.34465227476119,3.57442622165418));
#61025=CARTESIAN_POINT('Ctrl Pts',(0.278936678802386,2.3566305441785,3.57975106025209));
#61026=CARTESIAN_POINT('Ctrl Pts',(0.199834571975749,2.36464699539121,3.58507589885001));
#61027=CARTESIAN_POINT('Ctrl Pts',(0.120620086702649,2.36868082636387,3.59040073744792));
#61028=CARTESIAN_POINT('Ctrl Pts',(0.0412646060595808,2.37272183722906,
3.59573505382739));
#61029=CARTESIAN_POINT('Ctrl Pts',(-0.0382031836249495,2.37276606394699,
3.60106937020687));
#61030=CARTESIAN_POINT('Ctrl Pts',(-0.117353921861988,2.36884489140248,
3.60640368658634));
#61031=CARTESIAN_POINT('Ctrl Pts',(-0.187758375674292,2.36535701475787,
3.61114855238954));
#61032=CARTESIAN_POINT('Ctrl Pts',(-0.25791180239772,2.35873246204575,3.61589341819275));
#61033=CARTESIAN_POINT('Ctrl Pts',(-0.327518373976074,2.34902741091033,
3.62063828399595));
#61034=CARTESIAN_POINT('Ctrl Pts',(-0.405793534570179,2.33811372246147,
3.62597406083887));
#61035=CARTESIAN_POINT('Ctrl Pts',(-0.483668247821571,2.32326298659204,
3.63130983768179));
#61036=CARTESIAN_POINT('Ctrl Pts',(-0.56071614705779,2.30451631908491,3.63664561452472));
#61037=CARTESIAN_POINT('Ctrl Pts',(-0.63765389344232,2.28579645307278,3.64197376298269));
#61038=CARTESIAN_POINT('Ctrl Pts',(-0.71376672234596,2.26319182685123,3.64730191144066));
#61039=CARTESIAN_POINT('Ctrl Pts',(-0.788635458630563,2.23679506792432,
3.65263005989863));
#61040=CARTESIAN_POINT('Ctrl Pts',(-0.863418335086616,2.2104285809281,3.6579520980102));
#61041=CARTESIAN_POINT('Ctrl Pts',(-0.936959515113458,2.18027875856735,
3.66327413612177));
#61042=CARTESIAN_POINT('Ctrl Pts',(-1.00885353244335,2.14648843755949,3.66859617423334));
#61043=CARTESIAN_POINT('Ctrl Pts',(-1.08070252816821,2.11271927678919,3.67391487956832));
#61044=CARTESIAN_POINT('Ctrl Pts',(-1.15090598621153,2.07531434119648,3.6792335849033));
#61045=CARTESIAN_POINT('Ctrl Pts',(-1.21907816342561,2.03446467011813,3.68455229023828));
#61046=CARTESIAN_POINT('Ctrl Pts',(-1.28722879887042,1.99362790715309,3.68986931491221));
#61047=CARTESIAN_POINT('Ctrl Pts',(-1.35334902700049,1.94934881074585,3.69518633958615));
#61048=CARTESIAN_POINT('Ctrl Pts',(-1.41707878848044,1.90186376213934,3.70050336426008));
#61049=CARTESIAN_POINT('Ctrl Pts',(-1.48080818238509,1.8543789874132,3.70582035826691));
#61050=CARTESIAN_POINT('Ctrl Pts',(-1.5421467626551,1.80368857806275,3.71113735227374));
#61051=CARTESIAN_POINT('Ctrl Pts',(-1.60076569226688,1.75007064456305,3.71645434628057));
#61052=CARTESIAN_POINT('Ctrl Pts',(-1.65944262862038,1.69639965308975,3.72177660175328));
#61053=CARTESIAN_POINT('Ctrl Pts',(-1.71539419253147,1.63979566751615,3.72709885722599));
#61054=CARTESIAN_POINT('Ctrl Pts',(-1.76832720191574,1.58057488575039,3.7324211126987));
#61055=CARTESIAN_POINT('Ctrl Pts',(-1.82128590204025,1.52132536150921,3.73774595129836));
#61056=CARTESIAN_POINT('Ctrl Pts',(-1.871222834753,1.45945687557879,3.74307078989801));
#61057=CARTESIAN_POINT('Ctrl Pts',(-1.91788568716399,1.3953180832597,3.74839562849767));
#61058=CARTESIAN_POINT('Ctrl Pts',(-1.96463159567272,1.33106512908532,3.75372994487874));
#61059=CARTESIAN_POINT('Ctrl Pts',(-2.00809152353448,1.26453418719018,3.75906426125981));
#61060=CARTESIAN_POINT('Ctrl Pts',(-2.04805714423203,1.19610200085951,3.76439857764088));
#61061=CARTESIAN_POINT('Ctrl Pts',(-2.08360649914073,1.13523168190572,3.76914344342592));
#61062=CARTESIAN_POINT('Ctrl Pts',(-2.11639168839733,1.0728576543847,3.77388830921096));
#61063=CARTESIAN_POINT('Ctrl Pts',(-2.14629811463882,1.00925837405387,3.77863317499601));
#61064=CARTESIAN_POINT('Ctrl Pts',(-2.18263941226135,0.931974637226914,
3.7843989785822));
#61065=CARTESIAN_POINT('Ctrl Pts',(-2.21484794111681,0.85262973882922,3.79016478216839));
#61066=CARTESIAN_POINT('Ctrl Pts',(-2.24270515369829,0.771668099687384,
3.79593058575458));
#61067=CARTESIAN_POINT('Ctrl Pts',(-2.27049771914493,0.690894345029207,
3.80168300886773));
#61068=CARTESIAN_POINT('Ctrl Pts',(-2.29395896027847,0.608511644250268,
3.80743543198088));
#61069=CARTESIAN_POINT('Ctrl Pts',(-2.31291772532025,0.524985388748469,
3.81318785509404));
#61070=CARTESIAN_POINT('Ctrl Pts',(-2.33181254437535,0.441740858813186,
3.81892087586896));
#61071=CARTESIAN_POINT('Ctrl Pts',(-2.34623506616155,0.357360794564243,
3.82465389664388));
#61072=CARTESIAN_POINT('Ctrl Pts',(-2.35606389049652,0.27232518502411,3.8303869174188));
#61073=CARTESIAN_POINT('Ctrl Pts',(-2.35988509236819,0.239265459948207,
3.83261577297353));
#61074=CARTESIAN_POINT('Ctrl Pts',(-2.36301250100132,0.206106832811691,
3.83484462852826));
#61075=CARTESIAN_POINT('Ctrl Pts',(-2.36544101854889,0.172878137039867,
3.83707348408299));
#61076=CARTESIAN_POINT('Ctrl Pts',(-2.36906969114779,0.173130678776576,
2.83701751404115));
#61077=CARTESIAN_POINT('Ctrl Pts',(-2.37304267803412,0.116029833869745,
2.8408749733291));
#61078=CARTESIAN_POINT('Ctrl Pts',(-2.37479248963291,0.0587544673927994,
2.84473243261706));
#61079=CARTESIAN_POINT('Ctrl Pts',(-2.37437841508221,0.00145143062880148,
2.84858989190502));
#61080=CARTESIAN_POINT('',(-2.37174914026029,-0.00201944907760664,2.65179578499715));
#61081=CARTESIAN_POINT('Ctrl Pts',(-2.36544104518992,0.172877772518167,
2.63906222572513));
#61082=CARTESIAN_POINT('Ctrl Pts',(-2.36969278946239,0.114702275059686,
2.64328523019093));
#61083=CARTESIAN_POINT('Ctrl Pts',(-2.37179885119879,0.0563637395522385,
2.6475390334268));
#61084=CARTESIAN_POINT('Ctrl Pts',(-2.3717491402603,-0.00201944906437184,
2.65179578499619));
#61085=CARTESIAN_POINT('Ctrl Pts',(-2.37174913936198,-0.00202050382956093,
2.65179586189972));
#61086=CARTESIAN_POINT('Ctrl Pts',(-2.37166453571845,-0.101331683442273,
2.65903669660693));
#61087=CARTESIAN_POINT('Ctrl Pts',(-2.36534239168155,-0.200547931638166,
2.66627265898347));
#61088=CARTESIAN_POINT('Ctrl Pts',(-2.34848290809305,-0.333177612601596,
2.67575133944222));
#61089=CARTESIAN_POINT('Ctrl Pts',(-2.34340804703312,-0.36717611268781,
2.6781632165284));
#61090=CARTESIAN_POINT('Ctrl Pts',(-2.33568000408453,-0.412219996206787,
2.68132484123119));
#61091=CARTESIAN_POINT('Ctrl Pts',(-2.33368430366111,-0.423372164611656,
2.68210483314665));
#61092=CARTESIAN_POINT('Ctrl Pts',(-2.33007339056013,-0.442748563509511,
2.68345470913304));
#61093=CARTESIAN_POINT('Ctrl Pts',(-2.32849437259453,-0.4509792212025,2.68402642878467));
#61094=CARTESIAN_POINT('Ctrl Pts',(-2.325242245973,-0.467458439313042,2.68516751588963));
#61095=CARTESIAN_POINT('Ctrl Pts',(-2.32356879468021,-0.475706800675879,
2.68573683866824));
#61096=CARTESIAN_POINT('Ctrl Pts',(-2.31989725724312,-0.493321898956267,
2.68694862933164));
#61097=CARTESIAN_POINT('Ctrl Pts',(-2.31788631035481,-0.502685627807307,
2.68759038368554));
#61098=CARTESIAN_POINT('Ctrl Pts',(-2.31220975293191,-0.528359308527758,
2.6893440006925));
#61099=CARTESIAN_POINT('Ctrl Pts',(-2.30842826483674,-0.544643447591906,
2.69044965248019));
#61100=CARTESIAN_POINT('Ctrl Pts',(-2.28536479591067,-0.639402644780134,
2.69685211272984));
#61101=CARTESIAN_POINT('Ctrl Pts',(-2.26225242380764,-0.716899442474599,
2.70196271518307));
#61102=CARTESIAN_POINT('Ctrl Pts',(-2.19733986671101,-0.899851464508593,
2.71404999186243));
#61103=CARTESIAN_POINT('Ctrl Pts',(-2.15185054296296,-1.00378074622129,
2.72094008662029));
#61104=CARTESIAN_POINT('Ctrl Pts',(-2.04284984697178,-1.21101896549969,
2.73538850854864));
#61105=CARTESIAN_POINT('Ctrl Pts',(-1.9785088706946,-1.31350667611797,2.74294251414993));
#61106=CARTESIAN_POINT('Ctrl Pts',(-1.89047562978078,-1.43249399692652,
2.75254888714955));
#61107=CARTESIAN_POINT('Ctrl Pts',(-1.87393209068782,-1.45406862974567,
2.75432655394988));
#61108=CARTESIAN_POINT('Ctrl Pts',(-1.84665564650964,-1.48840138863509,
2.75721695251851));
#61109=CARTESIAN_POINT('Ctrl Pts',(-1.8361524018056,-1.50133943671476,2.75832069538014));
#61110=CARTESIAN_POINT('Ctrl Pts',(-1.8160173654448,-1.52561471568281,2.76041996748123));
#61111=CARTESIAN_POINT('Ctrl Pts',(-1.80641351121026,-1.53697415127627,
2.76141434622753));
#61112=CARTESIAN_POINT('Ctrl Pts',(-1.78430657918546,-1.56262879548297,
2.76368817914601));
#61113=CARTESIAN_POINT('Ctrl Pts',(-1.77173751121983,-1.57686552258463,
2.76497028855934));
#61114=CARTESIAN_POINT('Ctrl Pts',(-1.73834562075071,-1.61378455068332,
2.76834964052941));
#61115=CARTESIAN_POINT('Ctrl Pts',(-1.71725027135635,-1.63621435832771,
2.77045807458388));
#61116=CARTESIAN_POINT('Ctrl Pts',(-1.58060609254344,-1.77594858184031,
2.78395602370275));
#61117=CARTESIAN_POINT('Ctrl Pts',(-1.45356019928084,-1.88134368605657,
2.79584863206657));
#61118=CARTESIAN_POINT('Ctrl Pts',(-1.2058179797959,-2.04669431722735,2.81756344679459));
#61119=CARTESIAN_POINT('Ctrl Pts',(-1.08893579591564,-2.11120345832247,
2.82729705161046));
#61120=CARTESIAN_POINT('Ctrl Pts',(-0.948629568679176,-2.17387111707438,
2.83800288245232));
#61121=CARTESIAN_POINT('Ctrl Pts',(-0.929907749476828,-2.1819453105832,
2.83941201723572));
#61122=CARTESIAN_POINT('Ctrl Pts',(-0.901627251860468,-2.19371175379784,
2.84150918321944));
#61123=CARTESIAN_POINT('Ctrl Pts',(-0.892145509892006,-2.1975848923158,
2.84220706046038));
#61124=CARTESIAN_POINT('Ctrl Pts',(-0.874904986726808,-2.20449739237499,
2.84346612342719));
#61125=CARTESIAN_POINT('Ctrl Pts',(-0.867155050661275,-2.20755738583396,
2.84402846474413));
#61126=CARTESIAN_POINT('Ctrl Pts',(-0.849557506330287,-2.21439864687001,
2.8452972231283));
#61127=CARTESIAN_POINT('Ctrl Pts',(-0.839700636960674,-2.21815512860845,
2.8460021995197));
#61128=CARTESIAN_POINT('Ctrl Pts',(-0.809246984323049,-2.22952901128098,
2.84816375918392));
#61129=CARTESIAN_POINT('Ctrl Pts',(-0.788568558226539,-2.23692646416329,
2.84960830611528));
#61130=CARTESIAN_POINT('Ctrl Pts',(-0.629834987532405,-2.29123663097842,
2.86054242576756));
#61131=CARTESIAN_POINT('Ctrl Pts',(-0.487802681198767,-2.32562191554701,
2.86945081499974));
#61132=CARTESIAN_POINT('Ctrl Pts',(-0.185556086462792,-2.36986208987159,
2.88820972579896));
#61133=CARTESIAN_POINT('Ctrl Pts',(-0.0257068585975406,-2.37697456937508,
2.8980371786083));
#61134=CARTESIAN_POINT('Ctrl Pts',(0.162007784731706,-2.36638101001443,
2.91023067338174));
#61135=CARTESIAN_POINT('Ctrl Pts',(0.190347867848262,-2.36427011674935,
2.9120880442439));
#61136=CARTESIAN_POINT('Ctrl Pts',(0.235259078202485,-2.36011222500127,
2.91506095313287));
#61137=CARTESIAN_POINT('Ctrl Pts',(0.25185885337257,-2.35839853349126,2.91616618794845));
#61138=CARTESIAN_POINT('Ctrl Pts',(0.283214153234367,-2.35482673446843,
2.91826664366234));
#61139=CARTESIAN_POINT('Ctrl Pts',(0.29797304011469,-2.35300472932154,2.91926069643645));
#61140=CARTESIAN_POINT('Ctrl Pts',(0.331499227975257,-2.3485453945005,2.92153146857095));
#61141=CARTESIAN_POINT('Ctrl Pts',(0.350253812158593,-2.34582169813812,
2.92281081636011));
#61142=CARTESIAN_POINT('Ctrl Pts',(0.39925165192219,-2.33810515132208,2.92617785743884));
#61143=CARTESIAN_POINT('Ctrl Pts',(0.429433456606923,-2.33275038018007,
2.92827660984285));
#61144=CARTESIAN_POINT('Ctrl Pts',(0.624031994540121,-2.2943208159619,2.94197405122998));
#61145=CARTESIAN_POINT('Ctrl Pts',(0.784624612047842,-2.24447534336406,
2.95409702900155));
#61146=CARTESIAN_POINT('Ctrl Pts',(1.05843989599386,-2.12648399221279,2.97583526038778));
#61147=CARTESIAN_POINT('Ctrl Pts',(1.1738338386256,-2.06503019974873,2.98535973460226));
#61148=CARTESIAN_POINT('Ctrl Pts',(1.30071312692411,-1.98337033561466,2.99587157269382));
#61149=CARTESIAN_POINT('Ctrl Pts',(1.3176905062577,-1.9721319238037,2.99727869131485));
#61150=CARTESIAN_POINT('Ctrl Pts',(1.34298384387888,-1.95491617169873,2.99937347463077));
#61151=CARTESIAN_POINT('Ctrl Pts',(1.351408756389,-1.94910164592195,3.00007095353421));
#61152=CARTESIAN_POINT('Ctrl Pts',(1.36662289829965,-1.93845540195784,3.00132962642542));
#61153=CARTESIAN_POINT('Ctrl Pts',(1.37342451441274,-1.93364231427944,3.00189197182804));
#61154=CARTESIAN_POINT('Ctrl Pts',(1.38878412204666,-1.92265132524841,3.00316114727992));
#61155=CARTESIAN_POINT('Ctrl Pts',(1.39732638564255,-1.91645204442879,3.00386653217528));
#61156=CARTESIAN_POINT('Ctrl Pts',(1.42353998628357,-1.89715989004291,3.00603066029356));
#61157=CARTESIAN_POINT('Ctrl Pts',(1.44107138510319,-1.88387767321635,3.00747732587617));
#61158=CARTESIAN_POINT('Ctrl Pts',(1.57255892680883,-1.78134966314566,3.01834376197554));
#61159=CARTESIAN_POINT('Ctrl Pts',(1.67833030230401,-1.68207215486069,3.02719118274639));
#61160=CARTESIAN_POINT('Ctrl Pts',(1.88102388917087,-1.45353674525177,3.04595007909564));
#61161=CARTESIAN_POINT('Ctrl Pts',(1.97514295908593,-1.3228082725533,3.05583942088915));
#61162=CARTESIAN_POINT('Ctrl Pts',(2.06948631094064,-1.15897813553268,3.06810070947339));
#61163=CARTESIAN_POINT('Ctrl Pts',(2.08320923435577,-1.13412657359018,3.06995617130182));
#61164=CARTESIAN_POINT('Ctrl Pts',(2.10428269235227,-1.09429003822757,3.07292673732268));
#61165=CARTESIAN_POINT('Ctrl Pts',(2.11192707352632,-1.07946299128262,3.07403156693486));
#61166=CARTESIAN_POINT('Ctrl Pts',(2.12608954213736,-1.05126709186429,3.07613169967825));
#61167=CARTESIAN_POINT('Ctrl Pts',(2.13263955064154,-1.03791510709839,3.07712583946221));
#61168=CARTESIAN_POINT('Ctrl Pts',(2.14725422183462,-1.00740107335586,3.07939743601935));
#61169=CARTESIAN_POINT('Ctrl Pts',(2.15523941853019,-0.990202317078247,
3.08067752845397));
#61170=CARTESIAN_POINT('Ctrl Pts',(2.17560613224354,-0.944922125510865,
3.08404788834286));
#61171=CARTESIAN_POINT('Ctrl Pts',(2.18764998694002,-0.916693650963465,
3.08614925053638));
#61172=CARTESIAN_POINT('Ctrl Pts',(2.26166578770966,-0.733442301421913,
3.09979731541105));
#61173=CARTESIAN_POINT('Ctrl Pts',(2.30765989744538,-0.572500818307961,
3.11186297917274));
#61174=CARTESIAN_POINT('Ctrl Pts',(2.35904897518861,-0.278295532692503,
3.13363767897881));
#61175=CARTESIAN_POINT('Ctrl Pts',(2.37086724139451,-0.146818167714574,
3.14325649730304));
#61176=CARTESIAN_POINT('Ctrl Pts',(2.37182913393468,0.00497294922744031,
3.15382687299924));
#61177=CARTESIAN_POINT('Ctrl Pts',(2.37170284630969,0.0249768833519108,
3.15520892442808));
#61178=CARTESIAN_POINT('Ctrl Pts',(2.37113071400462,0.0551410130007561,
3.1572740696992));
#61179=CARTESIAN_POINT('Ctrl Pts',(2.37087259952802,0.0653032963990511,
3.15796658518657));
#61180=CARTESIAN_POINT('Ctrl Pts',(2.37028393970051,0.0837948958401544,
3.15922045115297));
#61181=CARTESIAN_POINT('Ctrl Pts',(2.36997482015665,0.0921243492102253,
3.15978290072399));
#61182=CARTESIAN_POINT('Ctrl Pts',(2.36917134274281,0.111077975085575,3.16105750119646));
#61183=CARTESIAN_POINT('Ctrl Pts',(2.36864943261805,0.121700632243204,3.16176814951743));
#61184=CARTESIAN_POINT('Ctrl Pts',(2.36680530349489,0.154704048760214,3.16396552482737));
#61185=CARTESIAN_POINT('Ctrl Pts',(2.36523715385412,0.177070555720267,3.16543963335945));
#61186=CARTESIAN_POINT('Ctrl Pts',(2.35150418927784,0.339827858317348,3.17607853896595));
#61187=CARTESIAN_POINT('Ctrl Pts',(2.32716438876703,0.478927133189543,3.18470459370553));
#61188=CARTESIAN_POINT('Ctrl Pts',(2.2479750258018,0.773846644428364,3.20345668953966));
#61189=CARTESIAN_POINT('Ctrl Pts',(2.18894875000501,0.927752632783989,3.21356258072216));
#61190=CARTESIAN_POINT('Ctrl Pts',(2.10176293994524,1.09935423735365,3.22604993979178));
#61191=CARTESIAN_POINT('Ctrl Pts',(2.0885951057883,1.12416972540307,3.22788648813877));
#61192=CARTESIAN_POINT('Ctrl Pts',(2.06694085704888,1.16328403187454,3.23083384157158));
#61193=CARTESIAN_POINT('Ctrl Pts',(2.05873923588458,1.17773807809033,3.23193465391899));
#61194=CARTESIAN_POINT('Ctrl Pts',(2.04290556004708,1.20497156127583,3.23403162470707));
#61195=CARTESIAN_POINT('Ctrl Pts',(2.03530374886283,1.21776772147098,3.2350266674232));
#61196=CARTESIAN_POINT('Ctrl Pts',(2.01768799607393,1.24679465369323,3.23730663709432));
#61197=CARTESIAN_POINT('Ctrl Pts',(2.00759782214453,1.26297771398559,3.23859427303348));
#61198=CARTESIAN_POINT('Ctrl Pts',(1.98055987773673,1.30519952862996,3.24199832377279));
#61199=CARTESIAN_POINT('Ctrl Pts',(1.96329420080058,1.33102928724237,3.24412619804061));
#61200=CARTESIAN_POINT('Ctrl Pts',(1.85625475913446,1.48454668379774,3.25705502584972));
#61201=CARTESIAN_POINT('Ctrl Pts',(1.75457638646392,1.60343600905729,3.26830255431575));
#61202=CARTESIAN_POINT('Ctrl Pts',(1.5401057842388,1.80919968824234,3.28996226398094));
#61203=CARTESIAN_POINT('Ctrl Pts',(1.42969920166433,1.89765552071005,3.30029993218363));
#61204=CARTESIAN_POINT('Ctrl Pts',(1.2950196791271,1.98709362431834,3.31156470294395));
#61205=CARTESIAN_POINT('Ctrl Pts',(1.27782155411741,1.99819648344215,3.31297961613056));
#61206=CARTESIAN_POINT('Ctrl Pts',(1.25179156430458,2.01452753091751,3.31508360477274));
#61207=CARTESIAN_POINT('Ctrl Pts',(1.24306650281883,2.0199230115549,3.31578261789045));
#61208=CARTESIAN_POINT('Ctrl Pts',(1.22719193146805,2.02959785280089,3.3170427924258));
#61209=CARTESIAN_POINT('Ctrl Pts',(1.22005466474621,2.03389628563111,3.31760512136554));
#61210=CARTESIAN_POINT('Ctrl Pts',(1.20384546618367,2.04354227760208,3.31887268921134));
#61211=CARTESIAN_POINT('Ctrl Pts',(1.19476042414047,2.04886712261145,3.31957650018949));
#61212=CARTESIAN_POINT('Ctrl Pts',(1.16670220549042,2.0650622630127,3.32173074617748));
#61213=CARTESIAN_POINT('Ctrl Pts',(1.14761332809395,2.07573117669822,3.32316926201546));
#61214=CARTESIAN_POINT('Ctrl Pts',(0.999959514516119,2.15559630259737,3.33411135948907));
#61215=CARTESIAN_POINT('Ctrl Pts',(0.865382772913855,2.21306088995876,3.34303140298237));
#61216=CARTESIAN_POINT('Ctrl Pts',(0.578911483076773,2.30522248790353,3.36151177117991));
#61217=CARTESIAN_POINT('Ctrl Pts',(0.427189429310361,2.33809554939542,3.37104601028774));
#61218=CARTESIAN_POINT('Ctrl Pts',(0.242538495689467,2.3595202049885,3.38307070299426));
#61219=CARTESIAN_POINT('Ctrl Pts',(0.211655769213763,2.36249067973927,3.38509442718464));
#61220=CARTESIAN_POINT('Ctrl Pts',(0.163539723890257,2.36616776072085,3.38827136197865));
#61221=CARTESIAN_POINT('Ctrl Pts',(0.146341258491917,2.36729367067556,3.38941164375629));
#61222=CARTESIAN_POINT('Ctrl Pts',(0.114346405112707,2.36903825177073,3.39154244233865));
#61223=CARTESIAN_POINT('Ctrl Pts',(0.0995534574451802,2.3697059798536,3.39253139279111));
#61224=CARTESIAN_POINT('Ctrl Pts',(0.0666083012848616,2.37088404162967,
3.39474270413428));
#61225=CARTESIAN_POINT('Ctrl Pts',(0.0484546893818588,2.37132450673931,
3.39596716048946));
#61226=CARTESIAN_POINT('Ctrl Pts',(0.00235233804396185,2.37191349537953,
3.39909264994207));
#61227=CARTESIAN_POINT('Ctrl Pts',(-0.0255966113182181,2.37177652030432,
3.40100229129329));
#61228=CARTESIAN_POINT('Ctrl Pts',(-0.249432814631122,2.36672275643254,
3.41642052159575));
#61229=CARTESIAN_POINT('Ctrl Pts',(-0.443993706923091,2.3380405970847,3.43067946292181));
#61230=CARTESIAN_POINT('Ctrl Pts',(-0.732052942945985,2.2582979636334,3.45245168288398));
#61231=CARTESIAN_POINT('Ctrl Pts',(-0.829452489929389,2.22437042359602,
3.45991648798485));
#61232=CARTESIAN_POINT('Ctrl Pts',(-0.945693140785667,2.1751781375895,3.46873928221864));
#61233=CARTESIAN_POINT('Ctrl Pts',(-0.966909089703273,2.1658306392081,3.47034570740838));
#61234=CARTESIAN_POINT('Ctrl Pts',(-0.997783078708247,2.15168379109401,
3.4726742153637));
#61235=CARTESIAN_POINT('Ctrl Pts',(-1.00755016112144,2.14712759123717,3.47340947806434));
#61236=CARTESIAN_POINT('Ctrl Pts',(-1.0241030810991,2.13926807345349,3.47465282699743));
#61237=CARTESIAN_POINT('Ctrl Pts',(-1.03090464680746,2.1359987420046,3.47516290530994));
#61238=CARTESIAN_POINT('Ctrl Pts',(-1.04641282702203,2.12845303962702,3.47632400736059));
#61239=CARTESIAN_POINT('Ctrl Pts',(-1.0551089413061,2.12415566206872,3.47697374399987));
#61240=CARTESIAN_POINT('Ctrl Pts',(-1.07920848677103,2.112061822259,3.47877128973083));
#61241=CARTESIAN_POINT('Ctrl Pts',(-1.09455388052996,2.10415017137319,3.47991236933233));
#61242=CARTESIAN_POINT('Ctrl Pts',(-1.21170642635877,2.04212112591012,3.48860725875878));
#61243=CARTESIAN_POINT('Ctrl Pts',(-1.30954532108287,1.98080519080484,3.49577605428415));
#61244=CARTESIAN_POINT('Ctrl Pts',(-1.47464001851495,1.8597385624952,3.50838902616582));
#61245=CARTESIAN_POINT('Ctrl Pts',(-1.54368698249952,1.8028369606035,3.51384799308044));
#61246=CARTESIAN_POINT('Ctrl Pts',(-1.66380590988287,1.69187546378425,3.52396621626858));
#61247=CARTESIAN_POINT('Ctrl Pts',(-1.71586372671038,1.63905556964233,3.52859646960668));
#61248=CARTESIAN_POINT('Ctrl Pts',(-1.79880521309339,1.54661112068368,3.53650843350266));
#61249=CARTESIAN_POINT('Ctrl Pts',(-1.83105878846296,1.50828687827062,3.53973800000726));
#61250=CARTESIAN_POINT('Ctrl Pts',(-1.87488154557976,1.45273703382052,3.54436915877928));
#61251=CARTESIAN_POINT('Ctrl Pts',(-1.88747634768317,1.43633516010049,3.54573063422613));
#61252=CARTESIAN_POINT('Ctrl Pts',(-1.90890230195197,1.40766419983463,3.54810160937212));
#61253=CARTESIAN_POINT('Ctrl Pts',(-1.91783373911453,1.39547132869362,3.5491071812765));
#61254=CARTESIAN_POINT('Ctrl Pts',(-1.93593151511913,1.37026297948856,3.55118108078306));
#61255=CARTESIAN_POINT('Ctrl Pts',(-1.9450845494038,1.35723893944155,3.55224984412771));
#61256=CARTESIAN_POINT('Ctrl Pts',(-1.96815724513777,1.32369554359574,3.55499608475645));
#61257=CARTESIAN_POINT('Ctrl Pts',(-1.98188720607198,1.30304867751405,3.55668049550362));
#61258=CARTESIAN_POINT('Ctrl Pts',(-2.03744874723032,1.21658619620018,3.56371224121628));
#61259=CARTESIAN_POINT('Ctrl Pts',(-2.0763412523535,1.14894910766037,3.5691631557414));
#61260=CARTESIAN_POINT('Ctrl Pts',(-2.19383857373315,0.919094233418538,
3.58752407035314));
#61261=CARTESIAN_POINT('Ctrl Pts',(-2.2572960728765,0.749843854805076,3.60083851056522));
#61262=CARTESIAN_POINT('Ctrl Pts',(-2.31162296755825,0.532471099831156,
3.6169654277794));
#61263=CARTESIAN_POINT('Ctrl Pts',(-2.32108540255774,0.489580652901819,
3.62009898901766));
#61264=CARTESIAN_POINT('Ctrl Pts',(-2.33483045129457,0.417865870720783,
3.62523409357893));
#61265=CARTESIAN_POINT('Ctrl Pts',(-2.33978264259073,0.389181826825073,
3.62726054756144));
#61266=CARTESIAN_POINT('Ctrl Pts',(-2.34599674811093,0.348763839767802,
3.63007101161806));
#61267=CARTESIAN_POINT('Ctrl Pts',(-2.34770086165767,0.337101819498761,
3.63087669578817));
#61268=CARTESIAN_POINT('Ctrl Pts',(-2.35047841630775,0.317050153393801,
3.63225245957036));
#61269=CARTESIAN_POINT('Ctrl Pts',(-2.35159402653814,0.308666695474465,
3.6328247911001));
#61270=CARTESIAN_POINT('Ctrl Pts',(-2.35385932033755,0.290918165297765,
3.63403024016599));
#61271=CARTESIAN_POINT('Ctrl Pts',(-2.35499799602778,0.281551993777993,
3.6346627613146));
#61272=CARTESIAN_POINT('Ctrl Pts',(-2.3579749418256,0.255782471514389,3.63639373260987));
#61273=CARTESIAN_POINT('Ctrl Pts',(-2.35969796028263,0.239365980109384,
3.63748609457126));
#61274=CARTESIAN_POINT('Ctrl Pts',(-2.36282343523366,0.206261639698165,
3.63967045633817));
#61275=CARTESIAN_POINT('Ctrl Pts',(-2.36422065732617,0.189575983256105,
3.64076204671802));
#61276=CARTESIAN_POINT('Ctrl Pts',(-2.36544101877862,0.172878133896551,
3.6418462952528));
#61277=CARTESIAN_POINT('Origin',(0.,0.,-1.84858989190501));
#61278=CARTESIAN_POINT('',(-2.36544099470095,0.17287846334401,4.83774038296924));
#61279=CARTESIAN_POINT('',(-2.36544101871062,0.172878134827039,4.63810474394384));
#61280=CARTESIAN_POINT('',(-2.36544101854889,0.172878137039864,-1.84858989190501));
#61281=CARTESIAN_POINT('',(-2.37174988974127,0.00072227238077198,3.84873773164287));
#61282=CARTESIAN_POINT('Ctrl Pts',(-2.36544099470095,0.17287846334401,4.83774038296924));
#61283=CARTESIAN_POINT('Ctrl Pts',(-2.35845789403178,0.268426007401591,
4.83181080292367));
#61284=CARTESIAN_POINT('Ctrl Pts',(-2.34568866385242,0.36351075498014,4.82580135690754));
#61285=CARTESIAN_POINT('Ctrl Pts',(-2.3212245766169,0.487922993545994,4.81762457349267));
#61286=CARTESIAN_POINT('Ctrl Pts',(-2.3146727700282,0.518114090840626,4.81561589105462));
#61287=CARTESIAN_POINT('Ctrl Pts',(-2.30323476294297,0.566262842874677,
4.8123685283912));
#61288=CARTESIAN_POINT('Ctrl Pts',(-2.29872352692894,0.584306507532516,
4.81114161496601));
#61289=CARTESIAN_POINT('Ctrl Pts',(-2.2902983252808,0.616396136938661,4.80894087874079));
#61290=CARTESIAN_POINT('Ctrl Pts',(-2.28646612701277,0.630462727196739,
4.80796970529589));
#61291=CARTESIAN_POINT('Ctrl Pts',(-2.27813325548061,0.659974020912009,
4.80591813255358));
#61292=CARTESIAN_POINT('Ctrl Pts',(-2.27360465954054,0.675410000111424,
4.80483687897286));
#61293=CARTESIAN_POINT('Ctrl Pts',(-2.26114186226874,0.716343916098403,
4.80194716149905));
#61294=CARTESIAN_POINT('Ctrl Pts',(-2.25293365914112,0.741755319964089,
4.80012995772897));
#61295=CARTESIAN_POINT('Ctrl Pts',(-2.20495541253557,0.882139200335281,
4.78995695452051));
#61296=CARTESIAN_POINT('Ctrl Pts',(-2.15681995077656,0.994040958670789,
4.7813307000172));
#61297=CARTESIAN_POINT('Ctrl Pts',(-2.07968406714421,1.14108999831635,4.76932471665483));
#61298=CARTESIAN_POINT('Ctrl Pts',(-2.05794337717007,1.1798479103429,4.76609389117295));
#61299=CARTESIAN_POINT('Ctrl Pts',(-1.96198624137587,1.34018417860742,4.75247721082198));
#61300=CARTESIAN_POINT('Ctrl Pts',(-1.87797948599761,1.45556974013896,4.74203532983824));
#61301=CARTESIAN_POINT('Ctrl Pts',(-1.76969488421872,1.57919516943305,4.73056032611397));
#61302=CARTESIAN_POINT('Ctrl Pts',(-1.75504178266853,1.59546413041297,4.72904433915943));
#61303=CARTESIAN_POINT('Ctrl Pts',(-1.73299980593201,1.6192655540833,4.72682058500436));
#61304=CARTESIAN_POINT('Ctrl Pts',(-1.72578304381654,1.62695487282724,4.72610124638695));
#61305=CARTESIAN_POINT('Ctrl Pts',(-1.71289563352824,1.64050391429979,4.72483247642879));
#61306=CARTESIAN_POINT('Ctrl Pts',(-1.70724576759697,1.64638283513615,4.72428155819449));
#61307=CARTESIAN_POINT('Ctrl Pts',(-1.69474901234744,1.65925272050383,4.72307466066358));
#61308=CARTESIAN_POINT('Ctrl Pts',(-1.68788907825854,1.66623055826905,4.72241968954665));
#61309=CARTESIAN_POINT('Ctrl Pts',(-1.66773234870903,1.68648149715284,4.72051631798583));
#61310=CARTESIAN_POINT('Ctrl Pts',(-1.65432043859211,1.6996396580964,4.7192763805575));
#61311=CARTESIAN_POINT('Ctrl Pts',(-1.62302745897077,1.72961917868486,4.71643972880632));
#61312=CARTESIAN_POINT('Ctrl Pts',(-1.60503852439135,1.74632530506812,4.71485032134242));
#61313=CARTESIAN_POINT('Ctrl Pts',(-1.54207755816471,1.80300152926619,4.70941422412766));
#61314=CARTESIAN_POINT('Ctrl Pts',(-1.49584391310177,1.84154002401672,4.70563968335683));
#61315=CARTESIAN_POINT('Ctrl Pts',(-1.33032824362677,1.96915589106222,4.69266465441261));
#61316=CARTESIAN_POINT('Ctrl Pts',(-1.20417405850344,2.04873471784786,4.68367366123366));
#61317=CARTESIAN_POINT('Ctrl Pts',(-0.997149374780716,2.15355901505117,
4.66917485786519));
#61318=CARTESIAN_POINT('Ctrl Pts',(-0.920986004189636,2.18721418513263,
4.66389425793215));
#61319=CARTESIAN_POINT('Ctrl Pts',(-0.819666053969448,2.22575392393162,
4.65684065919758));
#61320=CARTESIAN_POINT('Ctrl Pts',(-0.795974413765612,2.23433605887255,
4.65518957553623));
#61321=CARTESIAN_POINT('Ctrl Pts',(-0.757244906739538,2.24767140747357,
4.65248539432111));
#61322=CARTESIAN_POINT('Ctrl Pts',(-0.742288066988935,2.25265510237962,
4.65143985887729));
#61323=CARTESIAN_POINT('Ctrl Pts',(-0.713311807731035,2.26199022530392,
4.64941143401917));
#61324=CARTESIAN_POINT('Ctrl Pts',(-0.699299456547478,2.26636134982266,
4.6484292378752));
#61325=CARTESIAN_POINT('Ctrl Pts',(-0.66646102967369,2.27627169782476,4.64612398009258));
#61326=CARTESIAN_POINT('Ctrl Pts',(-0.647605222470179,2.28170782143175,
4.64479766855683));
#61327=CARTESIAN_POINT('Ctrl Pts',(-0.585148346867495,2.29887757887209,
4.64039465720854));
#61328=CARTESIAN_POINT('Ctrl Pts',(-0.541281944014829,2.30959955213128,
4.63728630136688));
#61329=CARTESIAN_POINT('Ctrl Pts',(-0.43421692983303,2.33255113885727,4.62965689799795));
#61330=CARTESIAN_POINT('Ctrl Pts',(-0.370777175498944,2.34347226418801,
4.62509998918338));
#61331=CARTESIAN_POINT('Ctrl Pts',(-0.208562413869567,2.36464586969637,
4.61337272413455));
#61332=CARTESIAN_POINT('Ctrl Pts',(-0.10944417106953,2.37130096920578,4.60613354795731));
#61333=CARTESIAN_POINT('Ctrl Pts',(0.0159847305790551,2.37184075278795,
4.59698800652647));
#61334=CARTESIAN_POINT('Ctrl Pts',(0.0421764701777665,2.37151960445827,
4.59507948702687));
#61335=CARTESIAN_POINT('Ctrl Pts',(0.165502411761317,2.36796367281134,4.5861100154732));
#61336=CARTESIAN_POINT('Ctrl Pts',(0.262394352952177,2.35919400419603,4.57910899415974));
#61337=CARTESIAN_POINT('Ctrl Pts',(0.375150272313595,2.34195315826303,4.57119626828872));
#61338=CARTESIAN_POINT('Ctrl Pts',(0.391789525015507,2.33922707971141,4.57003476787374));
#61339=CARTESIAN_POINT('Ctrl Pts',(0.417738144042488,2.33469115576377,4.56823452908552));
#61340=CARTESIAN_POINT('Ctrl Pts',(0.427067751631594,2.33300259174809,4.56758951938854));
#61341=CARTESIAN_POINT('Ctrl Pts',(0.443633123965498,2.32990172694089,4.56644856285664));
#61342=CARTESIAN_POINT('Ctrl Pts',(0.450872536074295,2.32851161995794,4.56595143382581));
#61343=CARTESIAN_POINT('Ctrl Pts',(0.468406170674319,2.32505998503571,4.56475089698214));
#61344=CARTESIAN_POINT('Ctrl Pts',(0.478693345768431,2.32296383221399,4.56404942396354));
#61345=CARTESIAN_POINT('Ctrl Pts',(0.510921991991115,2.31617361652859,4.56185990680654));
#61346=CARTESIAN_POINT('Ctrl Pts',(0.532811705332697,2.31123630968462,4.56038462934856));
#61347=CARTESIAN_POINT('Ctrl Pts',(0.649570798466337,2.28315378937986,4.55256300541919));
#61348=CARTESIAN_POINT('Ctrl Pts',(0.743022769986403,2.25447440445754,4.54646917062328));
#61349=CARTESIAN_POINT('Ctrl Pts',(0.999996153721674,2.1578886009422,4.52952392502141));
#61350=CARTESIAN_POINT('Ctrl Pts',(1.15805291858275,2.07735061850423,4.51883506625677));
#61351=CARTESIAN_POINT('Ctrl Pts',(1.3448213058204,1.95418810934944,4.50456151357855));
#61352=CARTESIAN_POINT('Ctrl Pts',(1.38317938631754,1.92722853683288,4.5015357655861));
#61353=CARTESIAN_POINT('Ctrl Pts',(1.4354836397085,1.88810092727864,4.49726046696396));
#61354=CARTESIAN_POINT('Ctrl Pts',(1.4501258829477,1.87687860121356,4.49604668584982));
#61355=CARTESIAN_POINT('Ctrl Pts',(1.47532735031823,1.8570923664218,4.493927011705));
#61356=CARTESIAN_POINT('Ctrl Pts',(1.48594675019473,1.84860625625839,4.49302417787153));
#61357=CARTESIAN_POINT('Ctrl Pts',(1.50801167414376,1.83066089605524,4.4911275910862));
#61358=CARTESIAN_POINT('Ctrl Pts',(1.51944245696827,1.82118453994611,4.49013318180053));
#61359=CARTESIAN_POINT('Ctrl Pts',(1.54655385162029,1.7982757124639,4.48774558136999));
#61360=CARTESIAN_POINT('Ctrl Pts',(1.56214928487663,1.78474477708923,4.48634844001489));
#61361=CARTESIAN_POINT('Ctrl Pts',(1.61616741925779,1.73662701245878,4.48142377068412));
#61362=CARTESIAN_POINT('Ctrl Pts',(1.65363186088829,1.70099131893692,4.4778533197269));
#61363=CARTESIAN_POINT('Ctrl Pts',(1.74466797548432,1.60854726663301,4.46877142174846));
#61364=CARTESIAN_POINT('Ctrl Pts',(1.79665242060521,1.55026732056716,4.46320305573679));
#61365=CARTESIAN_POINT('Ctrl Pts',(1.90321196875481,1.41823067705923,4.45095103701813));
#61366=CARTESIAN_POINT('Ctrl Pts',(1.95657638519192,1.34365245889521,4.44425093270349));
#61367=CARTESIAN_POINT('Ctrl Pts',(2.06315775429619,1.17483885456498,4.42971264681733));
#61368=CARTESIAN_POINT('Ctrl Pts',(2.11452414790608,1.07965690774899,4.42190065623915));
#61369=CARTESIAN_POINT('Ctrl Pts',(2.16624008016026,0.965861972001209,4.41322864503305));
#61370=CARTESIAN_POINT('Ctrl Pts',(2.17308845319953,0.950353644228385,4.41206068155645));
#61371=CARTESIAN_POINT('Ctrl Pts',(2.18351497952661,0.926040319995402,4.410252626388));
#61372=CARTESIAN_POINT('Ctrl Pts',(2.18720733988164,0.917285342893548,4.40960617908199));
#61373=CARTESIAN_POINT('Ctrl Pts',(2.19366958342968,0.901701788512333,4.40846399769113));
#61374=CARTESIAN_POINT('Ctrl Pts',(2.19646030406429,0.894882389807685,4.40796706626231));
#61375=CARTESIAN_POINT('Ctrl Pts',(2.20313895757089,0.87834297525935,4.40676869411586));
#61376=CARTESIAN_POINT('Ctrl Pts',(2.20699437960985,0.868610077744394,4.40606916853241));
#61377=CARTESIAN_POINT('Ctrl Pts',(2.21885229884336,0.838086400145388,4.40389211388469));
#61378=CARTESIAN_POINT('Ctrl Pts',(2.22662666443721,0.817207514879115,4.40242714575856));
#61379=CARTESIAN_POINT('Ctrl Pts',(2.26637032313686,0.705691345979062,4.39471478986543));
#61380=CARTESIAN_POINT('Ctrl Pts',(2.29310583908683,0.613273512243121,4.38871220791078));
#61381=CARTESIAN_POINT('Ctrl Pts',(2.35190250016047,0.351347744039928,4.37213475522055));
#61382=CARTESIAN_POINT('Ctrl Pts',(2.37120780076013,0.179614940895584,4.36172154529799));
#61383=CARTESIAN_POINT('Ctrl Pts',(2.37189757378398,-0.0442382673390364,
4.3474844876419));
#61384=CARTESIAN_POINT('Ctrl Pts',(2.37037593223402,-0.0957729588965799,
4.3441651283401));
#61385=CARTESIAN_POINT('Ctrl Pts',(2.36586265613288,-0.168345491211155,
4.33941043632361));
#61386=CARTESIAN_POINT('Ctrl Pts',(2.36426566607077,-0.189457448937834,
4.33801769942444));
#61387=CARTESIAN_POINT('Ctrl Pts',(2.36107292456982,-0.225281150232464,
4.33563685937602));
#61388=CARTESIAN_POINT('Ctrl Pts',(2.35962171899245,-0.240004746497715,
4.33465327321344));
#61389=CARTESIAN_POINT('Ctrl Pts',(2.35639571671077,-0.269869746572138,
4.33264746229202));
#61390=CARTESIAN_POINT('Ctrl Pts',(2.35461249657588,-0.285009519575753,
4.33162502017097));
#61391=CARTESIAN_POINT('Ctrl Pts',(2.34981001686762,-0.322655494175157,
4.32906816008474));
#61392=CARTESIAN_POINT('Ctrl Pts',(2.34661330435842,-0.345137105172466,
4.32752829690175));
#61393=CARTESIAN_POINT('Ctrl Pts',(2.33262165099824,-0.434327955169522,
4.32136573094173));
#61394=CARTESIAN_POINT('Ctrl Pts',(2.31930156868292,-0.500602861913786,
4.31666584621332));
#61395=CARTESIAN_POINT('Ctrl Pts',(2.27466302471612,-0.682177886188146,
4.30344862022022));
#61396=CARTESIAN_POINT('Ctrl Pts',(2.23743948392025,-0.795812691469167,
4.29477952852381));
#61397=CARTESIAN_POINT('Ctrl Pts',(2.14255598133254,-1.02531973278421,4.2766692049156));
#61398=CARTESIAN_POINT('Ctrl Pts',(2.08364740383289,-1.14028333751504,4.26725119025549));
#61399=CARTESIAN_POINT('Ctrl Pts',(2.00377091230396,-1.26909839936587,4.25666283393892));
#61400=CARTESIAN_POINT('Ctrl Pts',(1.99158892105191,-1.28813131236185,4.2550977695728));
#61401=CARTESIAN_POINT('Ctrl Pts',(1.97333490729165,-1.31577286588697,4.25282716542868));
#61402=CARTESIAN_POINT('Ctrl Pts',(1.96747500355845,-1.32451916249002,4.25210905594809));
#61403=CARTESIAN_POINT('Ctrl Pts',(1.9569741758644,-1.33996888048981,4.25084159771245));
#61404=CARTESIAN_POINT('Ctrl Pts',(1.95235669777415,-1.34668773548087,4.25029077432447));
#61405=CARTESIAN_POINT('Ctrl Pts',(1.94211313216427,-1.36142963676411,4.24908306791377));
#61406=CARTESIAN_POINT('Ctrl Pts',(1.93647188904811,-1.36944174954849,4.24842720308254));
#61407=CARTESIAN_POINT('Ctrl Pts',(1.91983115396502,-1.39276770858054,4.2465185352256));
#61408=CARTESIAN_POINT('Ctrl Pts',(1.90869822401609,-1.40798604173824,4.24527426702636));
#61409=CARTESIAN_POINT('Ctrl Pts',(1.88258756946727,-1.44279946160086,4.24242604634609));
#61410=CARTESIAN_POINT('Ctrl Pts',(1.86748313310406,-1.46229719687333,4.24082948511135));
#61411=CARTESIAN_POINT('Ctrl Pts',(1.81422139748642,-1.52887907505249,4.23535892285664));
#61412=CARTESIAN_POINT('Ctrl Pts',(1.77456366399939,-1.57473657679957,4.23155805754317));
#61413=CARTESIAN_POINT('Ctrl Pts',(1.63120539536901,-1.72820351593248,4.21852356336183));
#61414=CARTESIAN_POINT('Ctrl Pts',(1.51913434336749,-1.82749832796879,4.20949822421794));
#61415=CARTESIAN_POINT('Ctrl Pts',(1.33209471739352,-1.96404548753282,4.19502204936909));
#61416=CARTESIAN_POINT('Ctrl Pts',(1.26325618140182,-2.00901286902285,4.18980526248348));
#61417=CARTESIAN_POINT('Ctrl Pts',(1.17052819686494,-2.06293284123708,4.18282489399736));
#61418=CARTESIAN_POINT('Ctrl Pts',(1.14863003527273,-2.07520532272388,4.1811799296383));
#61419=CARTESIAN_POINT('Ctrl Pts',(1.11268643216556,-2.09460613681363,4.17848324347907));
#61420=CARTESIAN_POINT('Ctrl Pts',(1.09875715505498,-2.10194639772447,4.17743900321718));
#61421=CARTESIAN_POINT('Ctrl Pts',(1.07169605474444,-2.1158641994673,4.17541132145039));
#61422=CARTESIAN_POINT('Ctrl Pts',(1.0585741576185,-2.12245953568389,4.17442855622038));
#61423=CARTESIAN_POINT('Ctrl Pts',(1.02773161935617,-2.13760447173287,4.17211921938208));
#61424=CARTESIAN_POINT('Ctrl Pts',(1.00996438650176,-2.14605616348765,4.17078936336591));
#61425=CARTESIAN_POINT('Ctrl Pts',(0.950800729540961,-2.17330229040582,
4.16636140601271));
#61426=CARTESIAN_POINT('Ctrl Pts',(0.908971334312819,-2.19112653675992,
4.16323115098714));
#61427=CARTESIAN_POINT('Ctrl Pts',(0.80618083444961,-2.23147745306819,4.15553523603898));
#61428=CARTESIAN_POINT('Ctrl Pts',(0.744758537213033,-2.25272116811427,
4.15093287237395));
#61429=CARTESIAN_POINT('Ctrl Pts',(0.58827374188585,-2.29974386013181,4.1392150810796));
#61430=CARTESIAN_POINT('Ctrl Pts',(0.492333892617951,-2.32217423507779,
4.13203464139189));
#61431=CARTESIAN_POINT('Ctrl Pts',(0.370267598890551,-2.34280679262582,
4.12300822057258));
#61432=CARTESIAN_POINT('Ctrl Pts',(0.34518477999019,-2.34663359917616,4.12115949797622));
#61433=CARTESIAN_POINT('Ctrl Pts',(0.223203318384627,-2.3632457835402,4.11220871919175));
#61434=CARTESIAN_POINT('Ctrl Pts',(0.125627582437506,-2.3704371448102,4.10516657274025));
#61435=CARTESIAN_POINT('Ctrl Pts',(0.0110075317138,-2.37178445840316,4.09721476815244));
#61436=CARTESIAN_POINT('Ctrl Pts',(-0.00586423581657563,-2.37180276029429,
4.09605251703333));
#61437=CARTESIAN_POINT('Ctrl Pts',(-0.0322181906673156,-2.37155012245268,
4.09425137018612));
#61438=CARTESIAN_POINT('Ctrl Pts',(-0.0417006121300469,-2.37140234078195,
4.09360619336722));
#61439=CARTESIAN_POINT('Ctrl Pts',(-0.0585517794148577,-2.37103860980113,
4.09246509497976));
#61440=CARTESIAN_POINT('Ctrl Pts',(-0.0659205130694228,-2.37084518435683,
4.09196798945262));
#61441=CARTESIAN_POINT('Ctrl Pts',(-0.0837782321403945,-2.37029310615626,
4.09076770661422));
#61442=CARTESIAN_POINT('Ctrl Pts',(-0.0942659001028998,-2.36989918596927,
4.09006646179363));
#61443=CARTESIAN_POINT('Ctrl Pts',(-0.127147659085825,-2.36844550974648,
4.08787840735119));
#61444=CARTESIAN_POINT('Ctrl Pts',(-0.149530292015629,-2.36713781604501,
4.08640434017427));
#61445=CARTESIAN_POINT('Ctrl Pts',(-0.269102929512568,-2.35844896950068,
4.078595610074));
#61446=CARTESIAN_POINT('Ctrl Pts',(-0.365797296301814,-2.34539857523862,
4.07251254326013));
#61447=CARTESIAN_POINT('Ctrl Pts',(-0.63436775037423,-2.29213044491303,
4.05561104291321));
#61448=CARTESIAN_POINT('Ctrl Pts',(-0.802936027419543,-2.2386547026024,
4.04495508880096));
#61449=CARTESIAN_POINT('Ctrl Pts',(-1.00733947850798,-2.14772280654071,
4.03068723882586));
#61450=CARTESIAN_POINT('Ctrl Pts',(-1.05006934938803,-2.12715771904762,
4.02762774263896));
#61451=CARTESIAN_POINT('Ctrl Pts',(-1.10859749909969,-2.09679586015655,
4.02331273995464));
#61452=CARTESIAN_POINT('Ctrl Pts',(-1.12494197748666,-2.08807251064354,
4.02209391797285));
#61453=CARTESIAN_POINT('Ctrl Pts',(-1.15311563121957,-2.07260891407359,
4.019967950112));
#61454=CARTESIAN_POINT('Ctrl Pts',(-1.16499222382804,-2.06595655208449,
4.01906390952175));
#61455=CARTESIAN_POINT('Ctrl Pts',(-1.18968797524339,-2.05184321203258,
4.01716725282294));
#61456=CARTESIAN_POINT('Ctrl Pts',(-1.20249569141502,-2.04436350492416,
4.01617399996849));
#61457=CARTESIAN_POINT('Ctrl Pts',(-1.23288414477396,-2.02623228280788,
4.01379383632225));
#61458=CARTESIAN_POINT('Ctrl Pts',(-1.25039796334513,-2.01547152443161,
4.01240303903997));
#61459=CARTESIAN_POINT('Ctrl Pts',(-1.31093871659444,-1.97718153296033,
4.00752720830551));
#61460=CARTESIAN_POINT('Ctrl Pts',(-1.35321182773701,-1.94849280155184,
4.00400038419033));
#61461=CARTESIAN_POINT('Ctrl Pts',(-1.45656370327992,-1.87336675142013,
3.99506029683457));
#61462=CARTESIAN_POINT('Ctrl Pts',(-1.51637462466789,-1.82529091446302,
3.98959242311701));
#61463=CARTESIAN_POINT('Ctrl Pts',(-1.64030347625462,-1.71537657887789,
3.97763838214814));
#61464=CARTESIAN_POINT('Ctrl Pts',(-1.70348390795264,-1.65265056421737,
3.97113763530534));
#61465=CARTESIAN_POINT('Ctrl Pts',(-1.83846496284148,-1.50265614753404,
3.9564353808969));
#61466=CARTESIAN_POINT('Ctrl Pts',(-1.90786819837947,-1.41349689189942,
3.94826156076083));
#61467=CARTESIAN_POINT('Ctrl Pts',(-1.98011516267886,-1.30561496058001,
3.93925310703173));
#61468=CARTESIAN_POINT('Ctrl Pts',(-1.98941357740214,-1.29140239340679,
3.93808297256903));
#61469=CARTESIAN_POINT('Ctrl Pts',(-2.003678704858,-1.26907845261888,3.93627229254215));
#61470=CARTESIAN_POINT('Ctrl Pts',(-2.00875044729849,-1.26103533635753,
3.93562536294709));
#61471=CARTESIAN_POINT('Ctrl Pts',(-2.01766586928946,-1.24670637304252,
3.93448276834022));
#61472=CARTESIAN_POINT('Ctrl Pts',(-2.02152869395997,-1.24043302215224,
3.93398590090995));
#61473=CARTESIAN_POINT('Ctrl Pts',(-2.03080444394315,-1.22521049286998,
3.93278824481496));
#61474=CARTESIAN_POINT('Ctrl Pts',(-2.03618749146496,-1.21624337662611,
3.93208936476674));
#61475=CARTESIAN_POINT('Ctrl Pts',(-2.05282351834494,-1.18811093072897,
3.92991643108976));
#61476=CARTESIAN_POINT('Ctrl Pts',(-2.06386692145194,-1.16882222690597,
3.92845487073881));
#61477=CARTESIAN_POINT('Ctrl Pts',(-2.12096811369601,-1.06575424811521,
3.92077835534359));
#61478=CARTESIAN_POINT('Ctrl Pts',(-2.16220483257843,-0.97939376186528,
3.91480570476036));
#61479=CARTESIAN_POINT('Ctrl Pts',(-2.25591523234802,-0.748148465755502,
3.89939502201402));
#61480=CARTESIAN_POINT('Ctrl Pts',(-2.29969200259628,-0.600245810281099,
3.89007972928553));
#61481=CARTESIAN_POINT('Ctrl Pts',(-2.34134467674219,-0.384275792330606,
3.87621504777191));
#61482=CARTESIAN_POINT('Ctrl Pts',(-2.35113892366926,-0.318915889244687,
3.87199024757244));
#61483=CARTESIAN_POINT('Ctrl Pts',(-2.36066405767634,-0.230215841739212,
3.86617158441218));
#61484=CARTESIAN_POINT('Ctrl Pts',(-2.36279885865572,-0.207160853132173,
3.86465161021022));
#61485=CARTESIAN_POINT('Ctrl Pts',(-2.36566705718336,-0.170317259552894,
3.86220880151603));
#61486=CARTESIAN_POINT('Ctrl Pts',(-2.36661819953601,-0.156546729317892,
3.86129272594805));
#61487=CARTESIAN_POINT('Ctrl Pts',(-2.36828596455728,-0.128891209416927,
3.85944644787649));
#61488=CARTESIAN_POINT('Ctrl Pts',(-2.36900080342762,-0.115006665483295,
3.85851622788222));
#61489=CARTESIAN_POINT('Ctrl Pts',(-2.37030257836427,-0.0845006092579927,
3.85646484375004));
#61490=CARTESIAN_POINT('Ctrl Pts',(-2.37083682662562,-0.0678777079366085,
3.85534209807801));
#61491=CARTESIAN_POINT('Ctrl Pts',(-2.37157155047331,-0.0338846715542729,
3.85303559976754));
#61492=CARTESIAN_POINT('Ctrl Pts',(-2.37175610092984,-0.0165153028660104,
3.85185143007632));
#61493=CARTESIAN_POINT('Ctrl Pts',(-2.37174984622549,0.000854066367404124,
3.85066146066936));
#61494=CARTESIAN_POINT('Ctrl Pts',(-2.36544101854889,0.172878137039867,
3.83707348408299));
#61495=CARTESIAN_POINT('Ctrl Pts',(-2.36962370299618,0.115647688304842,
3.84091228667815));
#61496=CARTESIAN_POINT('Ctrl Pts',(-2.37173262894057,0.0582092763231678,
3.84475108927331));
#61497=CARTESIAN_POINT('Ctrl Pts',(-2.37174989308549,0.000712143930775687,
3.84858989186847));
#61498=CARTESIAN_POINT('Ctrl Pts',(-2.36544101877862,0.172878133896551,
3.6418462952528));
#61499=CARTESIAN_POINT('Ctrl Pts',(-2.36960373216792,0.115920942269559,
3.64554472073481));
#61500=CARTESIAN_POINT('Ctrl Pts',(-2.37170862035855,0.0588218952681139,
3.6491579191629));
#61501=CARTESIAN_POINT('Ctrl Pts',(-2.37182237577473,-0.100556551570478,
3.6591144445237));
#61502=CARTESIAN_POINT('Ctrl Pts',(-2.36528314127671,-0.202707173211117,
3.66535159178271));
#61503=CARTESIAN_POINT('Ctrl Pts',(-2.33431192864043,-0.442249481340446,
3.68020778777026));
#61504=CARTESIAN_POINT('Ctrl Pts',(-2.30432302065855,-0.578519835038019,
3.68885420376579));
#61505=CARTESIAN_POINT('Ctrl Pts',(-2.25419661921153,-0.737951563018058,
3.69969918411873));
#61506=CARTESIAN_POINT('Ctrl Pts',(-2.24536920043085,-0.764389924131961,
3.70152169769104));
#61507=CARTESIAN_POINT('Ctrl Pts',(-2.23055360967836,-0.806289830611636,
3.70445182595685));
#61508=CARTESIAN_POINT('Ctrl Pts',(-2.22486552183372,-0.821855268976713,
3.705549654916));
#61509=CARTESIAN_POINT('Ctrl Pts',(-2.21375673553023,-0.851293714938383,
3.70764432718616));
#61510=CARTESIAN_POINT('Ctrl Pts',(-2.20836754204316,-0.865177817128302,
3.70864009047137));
#61511=CARTESIAN_POINT('Ctrl Pts',(-2.19574904883458,-0.896800465124892,
3.71092652551209));
#61512=CARTESIAN_POINT('Ctrl Pts',(-2.18843497853554,-0.914503836771113,
3.71221996270711));
#61513=CARTESIAN_POINT('Ctrl Pts',(-2.16482515182747,-0.969744637267543,
3.71629927681385));
#61514=CARTESIAN_POINT('Ctrl Pts',(-2.14777261681502,-1.00694837526237,
3.71911015748796));
#61515=CARTESIAN_POINT('Ctrl Pts',(-2.07892292666634,-1.14744386373356,
3.72997687826846));
#61516=CARTESIAN_POINT('Ctrl Pts',(-2.02057178792455,-1.24732964837458,
3.73824448739884));
#61517=CARTESIAN_POINT('Ctrl Pts',(-1.87647698814062,-1.45717708624776,
3.75672085480706));
#61518=CARTESIAN_POINT('Ctrl Pts',(-1.78784244632585,-1.56465722476262,
3.766951691505));
#61519=CARTESIAN_POINT('Ctrl Pts',(-1.65961926930181,-1.69492623233866,
3.77996216420211));
#61520=CARTESIAN_POINT('Ctrl Pts',(-1.62807903049174,-1.7252449938275,3.78303824535418));
#61521=CARTESIAN_POINT('Ctrl Pts',(-1.58526480940449,-1.76418057721875,
3.78703365527381));
#61522=CARTESIAN_POINT('Ctrl Pts',(-1.57472854975662,-1.77359173537276,
3.78800303914029));
#61523=CARTESIAN_POINT('Ctrl Pts',(-1.55740601791513,-1.78878843222804,
3.78957347697477));
#61524=CARTESIAN_POINT('Ctrl Pts',(-1.55067027790634,-1.79463067390134,
3.79017848176432));
#61525=CARTESIAN_POINT('Ctrl Pts',(-1.53726889079682,-1.80612257680302,
3.79137078963198));
#61526=CARTESIAN_POINT('Ctrl Pts',(-1.53060468937429,-1.81177363228175,
3.79195818021095));
#61527=CARTESIAN_POINT('Ctrl Pts',(-1.51372287944996,-1.82592930503251,
3.79343276296195));
#61528=CARTESIAN_POINT('Ctrl Pts',(-1.50346453024742,-1.83438524011886,
3.7943165606353));
#61529=CARTESIAN_POINT('Ctrl Pts',(-1.46191181147329,-1.86805430750717,
3.79785010427348));
#61530=CARTESIAN_POINT('Ctrl Pts',(-1.4300481238227,-1.89255801807241,3.80045509588657));
#61531=CARTESIAN_POINT('Ctrl Pts',(-1.34059995990195,-1.9577953576976,3.80753269189188));
#61532=CARTESIAN_POINT('Ctrl Pts',(-1.28179600352902,-1.99679024544941,
3.81192823862155));
#61533=CARTESIAN_POINT('Ctrl Pts',(-1.07608650476142,-2.12036494675952,
3.82675526953262));
#61534=CARTESIAN_POINT('Ctrl Pts',(-0.921911437537798,-2.19179988184697,
3.83699808164418));
#61535=CARTESIAN_POINT('Ctrl Pts',(-0.710339041339512,-2.26352119270964,
3.85118257011784));
#61536=CARTESIAN_POINT('Ctrl Pts',(-0.658662532730912,-2.279094716536,3.85465268105317));
#61537=CARTESIAN_POINT('Ctrl Pts',(-0.585369056277798,-2.29848189356178,
3.85960692999845));
#61538=CARTESIAN_POINT('Ctrl Pts',(-0.564159647413503,-2.30377945719161,
3.86104426684483));
#61539=CARTESIAN_POINT('Ctrl Pts',(-0.528110413886234,-2.31225597060964,
3.86349499251605));
#61540=CARTESIAN_POINT('Ctrl Pts',(-0.513307533194915,-2.31558710509237,
3.86450351509957));
#61541=CARTESIAN_POINT('Ctrl Pts',(-0.483264784661054,-2.32204548200769,
3.86655522940651));
#61542=CARTESIAN_POINT('Ctrl Pts',(-0.468024093897173,-2.32516526303998,
3.86759860130792));
#61543=CARTESIAN_POINT('Ctrl Pts',(-0.430136834202159,-2.33253322675051,
3.87019915988852));
#61544=CARTESIAN_POINT('Ctrl Pts',(-0.4074573698885,-2.33660167281496,3.8717618857363));
#61545=CARTESIAN_POINT('Ctrl Pts',(-0.317823210964544,-2.3513364247715,
3.87796378307435));
#61546=CARTESIAN_POINT('Ctrl Pts',(-0.250489025047789,-2.35945931665607,
3.8826802032051));
#61547=CARTESIAN_POINT('Ctrl Pts',(-0.0638319271176766,-2.37389694802061,
3.89591650184541));
#61548=CARTESIAN_POINT('Ctrl Pts',(0.0557555377632189,-2.37409927154267,
3.9045867423562));
#61549=CARTESIAN_POINT('Ctrl Pts',(0.301957369246828,-2.35590059003178,
3.92258574050193));
#61550=CARTESIAN_POINT('Ctrl Pts',(0.42812431333008,-2.33627077933483,3.93189051339065));
#61551=CARTESIAN_POINT('Ctrl Pts',(0.574359523544318,-2.30126759588808,
3.94239742209559));
#61552=CARTESIAN_POINT('Ctrl Pts',(0.596530656273767,-2.29562032605396,
3.94398230327808));
#61553=CARTESIAN_POINT('Ctrl Pts',(0.628967189899483,-2.28685663518021,
3.94628571041083));
#61554=CARTESIAN_POINT('Ctrl Pts',(0.639297966425779,-2.28399017445573,
3.9470170316191));
#61555=CARTESIAN_POINT('Ctrl Pts',(0.65762959210004,-2.27876960789954,3.94831022000159));
#61556=CARTESIAN_POINT('Ctrl Pts',(0.665637873394858,-2.27644324211311,
3.94887358871724));
#61557=CARTESIAN_POINT('Ctrl Pts',(0.683312070433236,-2.27120773122983,
3.95011344532317));
#61558=CARTESIAN_POINT('Ctrl Pts',(0.692971842172196,-2.26827907877277,
3.95078882181577));
#61559=CARTESIAN_POINT('Ctrl Pts',(0.72137837333316,-2.25946837272362,3.9527690331935));
#61560=CARTESIAN_POINT('Ctrl Pts',(0.740071599563027,-2.25341478056034,
3.95406456951641));
#61561=CARTESIAN_POINT('Ctrl Pts',(0.858913919426857,-2.21329058306258,
3.96226538897946));
#61562=CARTESIAN_POINT('Ctrl Pts',(0.956776237648073,-2.17278001089318,
3.9688591417187));
#61563=CARTESIAN_POINT('Ctrl Pts',(1.21914071544413,-2.04299434809594,3.98691472218457));
#61564=CARTESIAN_POINT('Ctrl Pts',(1.37626784177599,-1.94062144287982,3.99822060707618));
#61565=CARTESIAN_POINT('Ctrl Pts',(1.54907314261894,-1.79639349247608,4.01268839277248));
#61566=CARTESIAN_POINT('Ctrl Pts',(1.57780231699497,-1.77121336080525,4.01516826308633));
#61567=CARTESIAN_POINT('Ctrl Pts',(1.61963773597091,-1.73272031031374,4.01890103934084));
#61568=CARTESIAN_POINT('Ctrl Pts',(1.6332159220035,-1.7199278441055,4.02013245013286));
#61569=CARTESIAN_POINT('Ctrl Pts',(1.65732373511459,-1.6966721535124,4.02235581977527));
#61570=CARTESIAN_POINT('Ctrl Pts',(1.6679088150969,-1.68626763210078,4.0233452399468));
#61571=CARTESIAN_POINT('Ctrl Pts',(1.69031696490801,-1.66382430484322,4.02546871441459));
#61572=CARTESIAN_POINT('Ctrl Pts',(1.7021105580445,-1.65175736179064,4.02660397093101));
#61573=CARTESIAN_POINT('Ctrl Pts',(1.73402365170021,-1.61839985202185,4.02972545169917));
#61574=CARTESIAN_POINT('Ctrl Pts',(1.75387848902808,-1.59686136516933,4.03172267533304));
#61575=CARTESIAN_POINT('Ctrl Pts',(1.87376773244004,-1.46187201748468,4.04413458710343));
#61576=CARTESIAN_POINT('Ctrl Pts',(1.96314144056444,-1.33945373199465,4.05497540280774));
#61577=CARTESIAN_POINT('Ctrl Pts',(2.11847212772815,-1.07740949034975,4.07714530327044));
#61578=CARTESIAN_POINT('Ctrl Pts',(2.18371769189735,-0.93814673163701,4.0884232732239));
#61579=CARTESIAN_POINT('Ctrl Pts',(2.24222617527117,-0.773355684348227,
4.10062182614449));
#61580=CARTESIAN_POINT('Ctrl Pts',(2.24912206391935,-0.753065240368606,
4.10210440717391));
#61581=CARTESIAN_POINT('Ctrl Pts',(2.2589692899577,-0.722748178192925,4.10428808619995));
#61582=CARTESIAN_POINT('Ctrl Pts',(2.26213069229004,-0.712791640886172,
4.10500022173271));
#61583=CARTESIAN_POINT('Ctrl Pts',(2.26769476123474,-0.694858205213966,
4.10627350452493));
#61584=CARTESIAN_POINT('Ctrl Pts',(2.27012128503816,-0.686889228627869,
4.10683595607547));
#61585=CARTESIAN_POINT('Ctrl Pts',(2.2754649100563,-0.669002514741316,4.10809094143575));
#61586=CARTESIAN_POINT('Ctrl Pts',(2.27835920849477,-0.659078332658007,
4.10878218577872));
#61587=CARTESIAN_POINT('Ctrl Pts',(2.28690057009943,-0.629062315652003,
4.11085850311069));
#61588=CARTESIAN_POINT('Ctrl Pts',(2.29234758987992,-0.608913962599894,
4.11223286994105));
#61589=CARTESIAN_POINT('Ctrl Pts',(2.30448160260397,-0.561558011167402,
4.11542360382502));
#61590=CARTESIAN_POINT('Ctrl Pts',(2.31095400754689,-0.534298206414138,
4.11723001445656));
#61591=CARTESIAN_POINT('Ctrl Pts',(2.33269242551105,-0.434941757797497,
4.12372555979368));
#61592=CARTESIAN_POINT('Ctrl Pts',(2.34508027030422,-0.362254482681901,
4.12831043431692));
#61593=CARTESIAN_POINT('Ctrl Pts',(2.37615340116676,-0.109237659319397,
4.14404250816702));
#61594=CARTESIAN_POINT('Ctrl Pts',(2.37755541494182,0.0725530699381401,
4.15500091254152));
#61595=CARTESIAN_POINT('Ctrl Pts',(2.35368716776626,0.295272103271014,4.1693400533406));
#61596=CARTESIAN_POINT('Ctrl Pts',(2.34797753559637,0.337683332490251,4.17210908079347));
#61597=CARTESIAN_POINT('Ctrl Pts',(2.33798897570018,0.399235158617621,4.17619598556813));
#61598=CARTESIAN_POINT('Ctrl Pts',(2.33461475566494,0.418515313216202,4.1774859431454));
#61599=CARTESIAN_POINT('Ctrl Pts',(2.32823503460333,0.452487008944127,4.1797772538756));
#61600=CARTESIAN_POINT('Ctrl Pts',(2.32532807168639,0.467196116464522,4.18077547506145));
#61601=CARTESIAN_POINT('Ctrl Pts',(2.31898938680194,0.49774381159621,4.18286180723362));
#61602=CARTESIAN_POINT('Ctrl Pts',(2.31553441070921,0.513576721242177,4.18395060376919));
#61603=CARTESIAN_POINT('Ctrl Pts',(2.30608096832637,0.554862531998601,4.18680985523015));
#61604=CARTESIAN_POINT('Ctrl Pts',(2.29982346335846,0.580253225161831,4.188588392458));
#61605=CARTESIAN_POINT('Ctrl Pts',(2.26660510211341,0.706050544341082,4.1975038301838));
#61606=CARTESIAN_POINT('Ctrl Pts',(2.23348616480765,0.80469891273897,4.20483346058679));
#61607=CARTESIAN_POINT('Ctrl Pts',(2.15832209104737,0.987760876724163,4.2190595290515));
#61608=CARTESIAN_POINT('Ctrl Pts',(2.11750370050633,1.07247487818202,4.22591631181305));
#61609=CARTESIAN_POINT('Ctrl Pts',(2.01815769334302,1.25074684114226,4.24079050600832));
#61610=CARTESIAN_POINT('Ctrl Pts',(1.95790302393165,1.34311148162399,4.24878807269437));
#61611=CARTESIAN_POINT('Ctrl Pts',(1.87757276406196,1.44929187799698,4.25809270484753));
#61612=CARTESIAN_POINT('Ctrl Pts',(1.86343792138482,1.46742142600187,4.25968532571127));
#61613=CARTESIAN_POINT('Ctrl Pts',(1.84231438009874,1.49371722793525,4.26199775483745));
#61614=CARTESIAN_POINT('Ctrl Pts',(1.83553068430216,1.50204545545152,4.26273049597324));
#61615=CARTESIAN_POINT('Ctrl Pts',(1.8233793143044,1.51675822108982,4.2640251875543));
#61616=CARTESIAN_POINT('Ctrl Pts',(1.81803426817176,1.52316086861205,4.26458865403766));
#61617=CARTESIAN_POINT('Ctrl Pts',(1.80615655186901,1.53723717164261,4.26582752360302));
#61618=CARTESIAN_POINT('Ctrl Pts',(1.79960864862018,1.54489751529094,4.26650182749112));
#61619=CARTESIAN_POINT('Ctrl Pts',(1.78020423330311,1.56730781413396,4.26847562822554));
#61620=CARTESIAN_POINT('Ctrl Pts',(1.76721343980189,1.5819410908333,4.26976591697229));
#61621=CARTESIAN_POINT('Ctrl Pts',(1.66502024174839,1.6942248627772,4.27969344865641));
#61622=CARTESIAN_POINT('Ctrl Pts',(1.56795969961087,1.78443326465879,4.28783723443293));
#61623=CARTESIAN_POINT('Ctrl Pts',(1.33234479367039,1.96926387833958,4.30623615426188));
#61624=CARTESIAN_POINT('Ctrl Pts',(1.19029418389439,2.05823596475885,4.31645481621377));
#61625=CARTESIAN_POINT('Ctrl Pts',(1.01250670250646,2.14498704125831,4.3292156858405));
#61626=CARTESIAN_POINT('Ctrl Pts',(0.984678062614286,2.1579036601609,4.33121089777562));
#61627=CARTESIAN_POINT('Ctrl Pts',(0.939259284668015,2.17792320782464,4.33446828650197));
#61628=CARTESIAN_POINT('Ctrl Pts',(0.921820239631107,2.18536150659485,4.33571922441971));
#61629=CARTESIAN_POINT('Ctrl Pts',(0.890545985524313,2.19826001148066,4.33796395122685));
#61630=CARTESIAN_POINT('Ctrl Pts',(0.876744913067595,2.20380071031838,4.33895499597927));
#61631=CARTESIAN_POINT('Ctrl Pts',(0.847352914695435,2.21528089271755,4.34106705365825));
#61632=CARTESIAN_POINT('Ctrl Pts',(0.831749661643027,2.22118636581461,4.34218912831756));
#61633=CARTESIAN_POINT('Ctrl Pts',(0.78942388685468,2.23669718737106,4.3452358535863));
#61634=CARTESIAN_POINT('Ctrl Pts',(0.76258976112885,2.24598778206482,4.3471706347175));
#61635=CARTESIAN_POINT('Ctrl Pts',(0.58370959232814,2.3043450348951,4.36009444920802));
#61636=CARTESIAN_POINT('Ctrl Pts',(0.427232053849851,2.33841366935678,4.37156607975096));
#61637=CARTESIAN_POINT('Ctrl Pts',(0.123641458017868,2.37301105248853,4.39382105527679));
#61638=CARTESIAN_POINT('Ctrl Pts',(-0.0224902270683318,2.37612490106955,
4.40452075403554));
#61639=CARTESIAN_POINT('Ctrl Pts',(-0.189818035341091,2.36424321649236,
4.41622888168404));
#61640=CARTESIAN_POINT('Ctrl Pts',(-0.211623299379721,2.36239127502634,
4.41774346910772));
#61641=CARTESIAN_POINT('Ctrl Pts',(-0.243882774834674,2.35920117881856,
4.41996470345987));
#61642=CARTESIAN_POINT('Ctrl Pts',(-0.254358038094077,2.35809478371122,
4.42068292560049));
#61643=CARTESIAN_POINT('Ctrl Pts',(-0.273105517132446,2.35598829745526,
4.42196243634705));
#61644=CARTESIAN_POINT('Ctrl Pts',(-0.281380188187089,2.35501436874272,
4.42252509212732));
#61645=CARTESIAN_POINT('Ctrl Pts',(-0.299828667998173,2.3527443564465,4.42377489344016));
#61646=CARTESIAN_POINT('Ctrl Pts',(-0.309999365756123,2.35142587377134,
4.42446080884023));
#61647=CARTESIAN_POINT('Ctrl Pts',(-0.34042932692158,2.34728020230701,4.42650457728493));
#61648=CARTESIAN_POINT('Ctrl Pts',(-0.360661489414601,2.34425677625829,
4.42785221174127));
#61649=CARTESIAN_POINT('Ctrl Pts',(-0.518866454472196,2.31851840323123,
4.43831981837334));
#61650=CARTESIAN_POINT('Ctrl Pts',(-0.654643601409779,2.28390067787529,
4.44689431564035));
#61651=CARTESIAN_POINT('Ctrl Pts',(-0.934854572738278,2.18539308545424,
4.46513509942551));
#61652=CARTESIAN_POINT('Ctrl Pts',(-1.07755166740775,2.11867208953042,4.47477547046208));
#61653=CARTESIAN_POINT('Ctrl Pts',(-1.23942986016123,2.02237152506852,4.4869191703135));
#61654=CARTESIAN_POINT('Ctrl Pts',(-1.26594506163832,2.00588033573256,4.48894897991668));
#61655=CARTESIAN_POINT('Ctrl Pts',(-1.30815575669471,1.97845697060891,4.49225156112831));
#61656=CARTESIAN_POINT('Ctrl Pts',(-1.32405857191477,1.96784967193015,4.49351256481133));
#61657=CARTESIAN_POINT('Ctrl Pts',(-1.35163394769947,1.94897109673667,4.49572963594782));
#61658=CARTESIAN_POINT('Ctrl Pts',(-1.36336327075376,1.94078418205506,4.49668252559138));
#61659=CARTESIAN_POINT('Ctrl Pts',(-1.38790595311149,1.92332143263944,4.4986976435483));
#61660=CARTESIAN_POINT('Ctrl Pts',(-1.40070195983474,1.91402253563031,4.49976071468466));
#61661=CARTESIAN_POINT('Ctrl Pts',(-1.42685422316272,1.89461490461995,4.50195962318708));
#61662=CARTESIAN_POINT('Ctrl Pts',(-1.44019829076275,1.88449130258461,4.5030959933871));
#61663=CARTESIAN_POINT('Ctrl Pts',(-1.49956907625671,1.83845019765496,4.50821787184103));
#61664=CARTESIAN_POINT('Ctrl Pts',(-1.54436394055369,1.80098460680724,4.5122630007033));
#61665=CARTESIAN_POINT('Ctrl Pts',(-1.65701062699657,1.69947399305766,4.52292423399785));
#61666=CARTESIAN_POINT('Ctrl Pts',(-1.72254385661214,1.63301430173476,4.52962570077938));
#61667=CARTESIAN_POINT('Ctrl Pts',(-1.87795491040315,1.45561588080458,4.5467508536347));
#61668=CARTESIAN_POINT('Ctrl Pts',(-1.96205789598359,1.34009836122726,4.55724541564508));
#61669=CARTESIAN_POINT('Ctrl Pts',(-2.05540245718138,1.18408420749316,4.57014498711645));
#61670=CARTESIAN_POINT('Ctrl Pts',(-2.0746930028049,1.1499495800197,4.57289450358811));
#61671=CARTESIAN_POINT('Ctrl Pts',(-2.09951373352872,1.10336958265515,4.57653488918519));
#61672=CARTESIAN_POINT('Ctrl Pts',(-2.10579496058023,1.09133402715711,4.57746569521676));
#61673=CARTESIAN_POINT('Ctrl Pts',(-2.11557888794184,1.07218787397129,4.57893017838993));
#61674=CARTESIAN_POINT('Ctrl Pts',(-2.11914976800319,1.06511273280841,4.57946787428792));
#61675=CARTESIAN_POINT('Ctrl Pts',(-2.1265442834618,1.05027725437029,4.58058787513904));
#61676=CARTESIAN_POINT('Ctrl Pts',(-2.130361031667,1.04251368274627,4.58116972030882));
#61677=CARTESIAN_POINT('Ctrl Pts',(-2.13974951608967,1.02314987841658,4.58261078683348));
#61678=CARTESIAN_POINT('Ctrl Pts',(-2.14526958637589,1.01152463412428,4.58346693222359));
#61679=CARTESIAN_POINT('Ctrl Pts',(-2.16617979731744,0.966546615213636,
4.58674694458278));
#61680=CARTESIAN_POINT('Ctrl Pts',(-2.18088983625737,0.932881099418687,
4.58913376975468));
#61681=CARTESIAN_POINT('Ctrl Pts',(-2.21810468336384,0.842013421677471,
4.59543075903007));
#61682=CARTESIAN_POINT('Ctrl Pts',(-2.23917887005602,0.784253772634774,
4.59928297783405));
#61683=CARTESIAN_POINT('Ctrl Pts',(-2.31566055517881,0.546296231661375,
4.61479023688534));
#61684=CARTESIAN_POINT('Ctrl Pts',(-2.35171383526137,0.360703176060175,
4.62611511055786));
#61685=CARTESIAN_POINT('Ctrl Pts',(-2.36544101871061,0.17287813482709,4.63810474394384));
#61686=CARTESIAN_POINT('Origin',(0.,0.,-1.84858989190501));
#61687=CARTESIAN_POINT('',(-2.36544101854819,0.172878137049535,5.83485941057446));
#61688=CARTESIAN_POINT('',(-2.36449584214975,0.172800370348396,5.63966122007073));
#61689=CARTESIAN_POINT('',(-2.36544101854889,0.172878137039864,-1.84858989190501));
#61690=CARTESIAN_POINT('Ctrl Pts',(-2.36544101854819,0.172878137049535,
5.83485941057446));
#61691=CARTESIAN_POINT('Ctrl Pts',(-2.3652981630827,0.174832786628508,5.83472426691884));
#61692=CARTESIAN_POINT('Ctrl Pts',(-2.36515288377511,0.176787273442486,
5.83458923813668));
#61693=CARTESIAN_POINT('Ctrl Pts',(-2.36428940002551,0.18821239004539,5.833800530386));
#61694=CARTESIAN_POINT('Ctrl Pts',(-2.36351672128189,0.197678998633314,
5.83314949174867));
#61695=CARTESIAN_POINT('Ctrl Pts',(-2.36201461348199,0.214812316023825,
5.83197596993832));
#61696=CARTESIAN_POINT('Ctrl Pts',(-2.36130467689932,0.222480544027811,
5.83145247919523));
#61697=CARTESIAN_POINT('Ctrl Pts',(-2.35976308180321,0.238292396343194,
5.83037680667898));
#61698=CARTESIAN_POINT('Ctrl Pts',(-2.35892662326193,0.246435097312728,
5.82982496239602));
#61699=CARTESIAN_POINT('Ctrl Pts',(-2.35689706009234,0.265234398327371,
5.82855557255112));
#61700=CARTESIAN_POINT('Ctrl Pts',(-2.35567382524878,0.27588743699874,5.82783968257873));
#61701=CARTESIAN_POINT('Ctrl Pts',(-2.35144113758588,0.310666609810523,
5.82551266801943));
#61702=CARTESIAN_POINT('Ctrl Pts',(-2.34813285296849,0.334755704981761,
5.82391691158141));
#61703=CARTESIAN_POINT('Ctrl Pts',(-2.333313581828,0.431589597217501,5.81755143098955));
#61704=CARTESIAN_POINT('Ctrl Pts',(-2.31878680031268,0.503836880407571,
5.81291382130682));
#61705=CARTESIAN_POINT('Ctrl Pts',(-2.27547228552324,0.677074775104708,
5.80181754294908));
#61706=CARTESIAN_POINT('Ctrl Pts',(-2.24329946016118,0.777054009232324,
5.79543025349959));
#61707=CARTESIAN_POINT('Ctrl Pts',(-2.17357425332955,0.952815698519893,
5.78377520704926));
#61708=CARTESIAN_POINT('Ctrl Pts',(-2.13839541039005,1.02934265702245,5.77854518477113));
#61709=CARTESIAN_POINT('Ctrl Pts',(-2.07390923761444,1.15197982358111,5.76974385018016));
#61710=CARTESIAN_POINT('Ctrl Pts',(-2.046945456575,1.19923752065692,5.76624346743483));
#61711=CARTESIAN_POINT('Ctrl Pts',(-2.00733491089914,1.26342676080899,5.76131037827371));
#61712=CARTESIAN_POINT('Ctrl Pts',(-1.99604985044595,1.28118131912445,5.75992630082692));
#61713=CARTESIAN_POINT('Ctrl Pts',(-1.97636083657577,1.31126598132529,5.75754592825429));
#61714=CARTESIAN_POINT('Ctrl Pts',(-1.96807383953829,1.32367139997946,5.75655396937008));
#61715=CARTESIAN_POINT('Ctrl Pts',(-1.95205588501542,1.34716688659854,5.75465482810676));
#61716=CARTESIAN_POINT('Ctrl Pts',(-1.944346040109,1.35827068802221,5.75374846317746));
#61717=CARTESIAN_POINT('Ctrl Pts',(-1.92408916587008,1.38691894726582,5.75138654882944));
#61718=CARTESIAN_POINT('Ctrl Pts',(-1.91139721180828,1.40435890365694,5.74992555067283));
#61719=CARTESIAN_POINT('Ctrl Pts',(-1.86603712327907,1.46493386236972,5.74476744932677));
#61720=CARTESIAN_POINT('Ctrl Pts',(-1.83213455788877,1.50711907949305,5.74102339401878));
#61721=CARTESIAN_POINT('Ctrl Pts',(-1.68596654338915,1.67677020325248,5.72531277353773));
#61722=CARTESIAN_POINT('Ctrl Pts',(-1.56162420310305,1.79314147399814,5.71288703647184));
#61723=CARTESIAN_POINT('Ctrl Pts',(-1.36929726689747,1.93784654386613,5.69537099228855));
#61724=CARTESIAN_POINT('Ctrl Pts',(-1.31075967405018,1.97791166165294,5.69023947562557));
#61725=CARTESIAN_POINT('Ctrl Pts',(-1.22738382822378,2.02964722521763,5.68327588209299));
#61726=CARTESIAN_POINT('Ctrl Pts',(-1.20400945848729,2.04359983326879,5.68135951949691));
#61727=CARTESIAN_POINT('Ctrl Pts',(-1.16276246966077,2.06726751150561,5.67804631629346));
#61728=CARTESIAN_POINT('Ctrl Pts',(-1.14499572833956,2.0771606522856,5.67664083845206));
#61729=CARTESIAN_POINT('Ctrl Pts',(-1.11822052172634,2.09162206115305,5.67455730604109));
#61730=CARTESIAN_POINT('Ctrl Pts',(-1.10930706651258,2.09636299896061,5.67386935512712));
#61731=CARTESIAN_POINT('Ctrl Pts',(-1.09315269787907,2.10482338860201,5.6726330888083));
#61732=CARTESIAN_POINT('Ctrl Pts',(-1.08592268450922,2.10856260193877,5.67208360288256));
#61733=CARTESIAN_POINT('Ctrl Pts',(-1.06960093446685,2.11689765311899,5.67085165395637));
#61734=CARTESIAN_POINT('Ctrl Pts',(-1.06049870366577,2.12147221094061,5.67017048638989));
#61735=CARTESIAN_POINT('Ctrl Pts',(-1.03272227467651,2.13520851693974,5.66810873788662));
#61736=CARTESIAN_POINT('Ctrl Pts',(-1.01395621266517,2.14418366234985,5.66673889412827));
#61737=CARTESIAN_POINT('Ctrl Pts',(-0.851983897161047,2.21904713208814,
5.65509187739822));
#61738=CARTESIAN_POINT('Ctrl Pts',(-0.702636285996771,2.27076264096107,
5.64550775631935));
#61739=CARTESIAN_POINT('Ctrl Pts',(-0.40193321266248,2.34234450758117,5.62652227180799));
#61740=CARTESIAN_POINT('Ctrl Pts',(-0.25162267459038,2.36321942364835,5.61716492363531));
#61741=CARTESIAN_POINT('Ctrl Pts',(-0.0728094653995724,2.37079251387567,
5.60554912862823));
#61742=CARTESIAN_POINT('Ctrl Pts',(-0.0452433520591043,2.37147871573019,
5.60374591454108));
#61743=CARTESIAN_POINT('Ctrl Pts',(-0.00140084380394981,2.37180540508297,
5.60085510525446));
#61744=CARTESIAN_POINT('Ctrl Pts',(0.0148712176391393,2.37175919241675,
5.59977718294867));
#61745=CARTESIAN_POINT('Ctrl Pts',(0.0456792490888016,2.37135464671611,
5.59772627023614));
#61746=CARTESIAN_POINT('Ctrl Pts',(0.0602149690143406,2.37103007061824,
5.59675436961611));
#61747=CARTESIAN_POINT('Ctrl Pts',(0.0933088821955444,2.36998658625858,
5.59453151179002));
#61748=CARTESIAN_POINT('Ctrl Pts',(0.111863264907208,2.36918330712374,5.5932780044235));
#61749=CARTESIAN_POINT('Ctrl Pts',(0.160457345085561,2.36650741247831,5.58997526291353));
#61750=CARTESIAN_POINT('Ctrl Pts',(0.190473364226601,2.3642807886782,5.58791530968564));
#61751=CARTESIAN_POINT('Ctrl Pts',(0.429685760111566,2.34195099634652,5.57133338897994));
#61752=CARTESIAN_POINT('Ctrl Pts',(0.635377674367417,2.29469504398765,5.55594167216778));
#61753=CARTESIAN_POINT('Ctrl Pts',(0.893047341279078,2.19815840643455,5.53594574169321));
#61754=CARTESIAN_POINT('Ctrl Pts',(0.953032197343802,2.17282411141126,5.53124676581123));
#61755=CARTESIAN_POINT('Ctrl Pts',(1.03523985700263,2.1340436610381,5.5248064050044));
#61756=CARTESIAN_POINT('Ctrl Pts',(1.05839727220288,2.12265381994892,5.52299224255321));
#61757=CARTESIAN_POINT('Ctrl Pts',(1.09873925563241,2.10198743731354,5.51983745033577));
#61758=CARTESIAN_POINT('Ctrl Pts',(1.11600350124328,2.09287251990842,5.51848921491388));
#61759=CARTESIAN_POINT('Ctrl Pts',(1.14188058911878,2.07879904341009,5.5164733282726));
#61760=CARTESIAN_POINT('Ctrl Pts',(1.15057756203222,2.07399807746633,5.51579667111589));
#61761=CARTESIAN_POINT('Ctrl Pts',(1.16634931940817,2.06516189535902,5.51457148536338));
#61762=CARTESIAN_POINT('Ctrl Pts',(1.17343365954732,2.0611447886668,5.51402190231649));
#61763=CARTESIAN_POINT('Ctrl Pts',(1.1894858889286,2.05193293743101,5.51277822630914));
#61764=CARTESIAN_POINT('Ctrl Pts',(1.19844056514836,2.04671582820594,5.51208555200552));
#61765=CARTESIAN_POINT('Ctrl Pts',(1.22605519974177,2.03038381224104,5.50995198202931));
#61766=CARTESIAN_POINT('Ctrl Pts',(1.24459748956698,2.0190708129608,5.50852294264353));
#61767=CARTESIAN_POINT('Ctrl Pts',(1.38679911980856,1.9296074011854,5.49757035896489));
#61768=CARTESIAN_POINT('Ctrl Pts',(1.50316085553991,1.84041176953142,5.48863532489169));
#61769=CARTESIAN_POINT('Ctrl Pts',(1.72821612349001,1.63222258639811,5.46981310634935));
#61770=CARTESIAN_POINT('Ctrl Pts',(1.83451215049238,1.51176656786397,5.4599490771709));
#61771=CARTESIAN_POINT('Ctrl Pts',(1.944252560164,1.3586291946268,5.4477290081568));
#61772=CARTESIAN_POINT('Ctrl Pts',(1.96024849047158,1.33544638728331,5.44588799831982));
#61773=CARTESIAN_POINT('Ctrl Pts',(1.98489798545891,1.29832466371339,5.44295079437928));
#61774=CARTESIAN_POINT('Ctrl Pts',(1.99382659044595,1.28457092050305,5.44186483033838));
#61775=CARTESIAN_POINT('Ctrl Pts',(2.01039006568428,1.25846756746148,5.43980742768117));
#61776=CARTESIAN_POINT('Ctrl Pts',(2.01805558247382,1.24613822854737,5.43883717110611));
#61777=CARTESIAN_POINT('Ctrl Pts',(2.03515929948378,1.21805660100813,5.4366302663616));
#61778=CARTESIAN_POINT('Ctrl Pts',(2.04452862363098,1.2022636699432,5.43539120548939));
#61779=CARTESIAN_POINT('Ctrl Pts',(2.06840828539195,1.16092561098876,5.43215256908947));
#61780=CARTESIAN_POINT('Ctrl Pts',(2.0826286711716,1.13521750978203,5.43014294213169));
#61781=CARTESIAN_POINT('Ctrl Pts',(2.18152427802634,0.948315562040573,5.41555916008675));
#61782=CARTESIAN_POINT('Ctrl Pts',(2.24785087046105,0.778134607647297,5.40235055184386));
#61783=CARTESIAN_POINT('Ctrl Pts',(2.32458491401091,0.485762832607977,5.38030984705614));
#61784=CARTESIAN_POINT('Ctrl Pts',(2.34622556603806,0.367276497671959,5.37156367947194));
#61785=CARTESIAN_POINT('Ctrl Pts',(2.36082076241201,0.228261731792622,5.36183539373392));
#61786=CARTESIAN_POINT('Ctrl Pts',(2.3626172586553,0.208848845309161,5.36048904969874));
#61787=CARTESIAN_POINT('Ctrl Pts',(2.36496716956883,0.179518584567353,5.35847540310722));
#61788=CARTESIAN_POINT('Ctrl Pts',(2.36569794845537,0.16961680606868,5.35779912341425));
#61789=CARTESIAN_POINT('Ctrl Pts',(2.36691497295297,0.151584642381062,5.3565743011276));
#61790=CARTESIAN_POINT('Ctrl Pts',(2.36742153652131,0.143456145451489,5.35602470798875));
#61791=CARTESIAN_POINT('Ctrl Pts',(2.36847789615951,0.124972175922791,5.35478060972845));
#61792=CARTESIAN_POINT('Ctrl Pts',(2.36900166236205,0.114615544500593,5.35408752760864));
#61793=CARTESIAN_POINT('Ctrl Pts',(2.37041365644713,0.0825245981244625,
5.35195138467514));
#61794=CARTESIAN_POINT('Ctrl Pts',(2.37107085863046,0.0607805612814262,
5.35052022127107));
#61795=CARTESIAN_POINT('Ctrl Pts',(2.37383034879061,-0.106885211152354,
5.33958861474284));
#61796=CARTESIAN_POINT('Ctrl Pts',(2.36275974514105,-0.252730697895482,
5.33067358259826));
#61797=CARTESIAN_POINT('Ctrl Pts',(2.31146507372993,-0.555126139779607,
5.3118433003837));
#61798=CARTESIAN_POINT('Ctrl Pts',(2.26854638195518,-0.710439670629666,
5.30195077076225));
#61799=CARTESIAN_POINT('Ctrl Pts',(2.20007801831038,-0.886364708090971,
5.28970476914955));
#61800=CARTESIAN_POINT('Ctrl Pts',(2.18943622845295,-0.912334684508902,
5.28787015368775));
#61801=CARTESIAN_POINT('Ctrl Pts',(2.17185904416167,-0.953149800327596,
5.28494079845569));
#61802=CARTESIAN_POINT('Ctrl Pts',(2.16522613825512,-0.968122924715021,
5.28385619355425));
#61803=CARTESIAN_POINT('Ctrl Pts',(2.15242015739865,-0.996241133839447,
5.28179990791864));
#61804=CARTESIAN_POINT('Ctrl Pts',(2.14628034848585,-1.00940060455088,5.28082939376168));
#61805=CARTESIAN_POINT('Ctrl Pts',(2.13208893729212,-1.03910214861662,5.27861989222144));
#61806=CARTESIAN_POINT('Ctrl Pts',(2.12396500553494,-1.05560841898881,5.277378469678));
#61807=CARTESIAN_POINT('Ctrl Pts',(2.10231856712259,-1.09832811564316,5.2741293841941));
#61808=CARTESIAN_POINT('Ctrl Pts',(2.08849798705697,-1.12438606845454,5.27211156236119));
#61809=CARTESIAN_POINT('Ctrl Pts',(1.98648720663364,-1.30834908178088,5.25760195107445));
#61810=CARTESIAN_POINT('Ctrl Pts',(1.88098923744897,-1.45594131183394,5.24448543434291));
#61811=CARTESIAN_POINT('Ctrl Pts',(1.67734628204884,-1.6813164779206,5.22233620840792));
#61812=CARTESIAN_POINT('Ctrl Pts',(1.58793661111369,-1.76600658334652,5.21339144794867));
#61813=CARTESIAN_POINT('Ctrl Pts',(1.478003763277,-1.85500507579957,5.20356061779455));
#61814=CARTESIAN_POINT('Ctrl Pts',(1.46351787916972,-1.86645504227541,5.20228682431552));
#61815=CARTESIAN_POINT('Ctrl Pts',(1.44120525051743,-1.88367192775855,5.20035933772398));
#61816=CARTESIAN_POINT('Ctrl Pts',(1.43347469438542,-1.88956154026869,5.19969774223817));
#61817=CARTESIAN_POINT('Ctrl Pts',(1.41918679323507,-1.90030878944935,5.19848666369345));
#61818=CARTESIAN_POINT('Ctrl Pts',(1.41264047963194,-1.90518018257248,5.19793628361086));
#61819=CARTESIAN_POINT('Ctrl Pts',(1.39764765189411,-1.91621722445493,5.1966858609638));
#61820=CARTESIAN_POINT('Ctrl Pts',(1.38918536357089,-1.92236090419131,5.19598729516338));
#61821=CARTESIAN_POINT('Ctrl Pts',(1.36212866676027,-1.94173228346285,5.19377558464823));
#61822=CARTESIAN_POINT('Ctrl Pts',(1.34338323805886,-1.95474815109517,5.19227577796469));
#61823=CARTESIAN_POINT('Ctrl Pts',(1.22223227320997,-2.03630306585041,5.18276828875893));
#61824=CARTESIAN_POINT('Ctrl Pts',(1.11479213393869,-2.09705218913936,5.17516855675224));
#61825=CARTESIAN_POINT('Ctrl Pts',(0.945379235625385,-2.17612370770374,
5.16368088096112));
#61826=CARTESIAN_POINT('Ctrl Pts',(0.886591354429019,-2.20072986871388,
5.15977966306666));
#61827=CARTESIAN_POINT('Ctrl Pts',(0.751620642816595,-2.25093602605472,
5.15089184486527));
#61828=CARTESIAN_POINT('Ctrl Pts',(0.674988086665912,-2.27509038153553,
5.14589223014156));
#61829=CARTESIAN_POINT('Ctrl Pts',(0.546276860842511,-2.30858340583356,
5.1374346946491));
#61830=CARTESIAN_POINT('Ctrl Pts',(0.494846738765258,-2.32015124687534,
5.13404036366586));
#61831=CARTESIAN_POINT('Ctrl Pts',(0.422648284155725,-2.33388065400993,
5.12923221876156));
#61832=CARTESIAN_POINT('Ctrl Pts',(0.402170081182587,-2.3374964513562,5.12786372808805));
#61833=CARTESIAN_POINT('Ctrl Pts',(0.366966882564049,-2.34323592901909,
5.12550187172242));
#61834=CARTESIAN_POINT('Ctrl Pts',(0.352264361810375,-2.34549123092685,
5.1245126707273));
#61835=CARTESIAN_POINT('Ctrl Pts',(0.324116109565076,-2.34953842011654,
5.12261309467419));
#61836=CARTESIAN_POINT('Ctrl Pts',(0.310674273850211,-2.35135355116424,
5.12170348714916));
#61837=CARTESIAN_POINT('Ctrl Pts',(0.275558193711459,-2.35578911827115,
5.11932032703938));
#61838=CARTESIAN_POINT('Ctrl Pts',(0.253862449704423,-2.35822570795184,
5.11784112932851));
#61839=CARTESIAN_POINT('Ctrl Pts',(0.176527516144385,-2.36583143911257,
5.11254270950452));
#61840=CARTESIAN_POINT('Ctrl Pts',(0.120746687765224,-2.3693331786405,5.10867306486535));
#61841=CARTESIAN_POINT('Ctrl Pts',(-0.103178546333948,-2.37546272277441,
5.09293911122627));
#61842=CARTESIAN_POINT('Ctrl Pts',(-0.271250090448635,-2.36217655614269,
5.08063398237339));
#61843=CARTESIAN_POINT('Ctrl Pts',(-0.529518501311077,-2.31382120385999,
5.06151362631611));
#61844=CARTESIAN_POINT('Ctrl Pts',(-0.621443989771581,-2.290844658127,5.05467638259956));
#61845=CARTESIAN_POINT('Ctrl Pts',(-0.732862488046355,-2.25579257394576,
5.04652125382848));
#61846=CARTESIAN_POINT('Ctrl Pts',(-0.753874397545816,-2.24885771949728,
5.04498944050483));
#61847=CARTESIAN_POINT('Ctrl Pts',(-0.784654115750265,-2.2382191514835,
5.04275763140437));
#61848=CARTESIAN_POINT('Ctrl Pts',(-0.794498746923263,-2.23474356533645,
5.04204564603436));
#61849=CARTESIAN_POINT('Ctrl Pts',(-0.811249105518429,-2.22870527387681,
5.04083774844552));
#61850=CARTESIAN_POINT('Ctrl Pts',(-0.818166239288852,-2.22617526694883,
5.04033998914812));
#61851=CARTESIAN_POINT('Ctrl Pts',(-0.833998536931158,-2.22030069161058,
5.0392031457014));
#61852=CARTESIAN_POINT('Ctrl Pts',(-0.842905466013555,-2.21693461878631,
5.03856532685785));
#61853=CARTESIAN_POINT('Ctrl Pts',(-0.867696864975055,-2.20739453531885,
5.0367942713596));
#61854=CARTESIAN_POINT('Ctrl Pts',(-0.883535786400458,-2.20110268703148,
5.03566764365087));
#61855=CARTESIAN_POINT('Ctrl Pts',(-1.00668284353969,-2.15064025459855,
5.02693608509348));
#61856=CARTESIAN_POINT('Ctrl Pts',(-1.11070066680025,-2.09881276778849,
5.01972333614952));
#61857=CARTESIAN_POINT('Ctrl Pts',(-1.28769825776428,-1.9937619301061,5.00704677436244));
#61858=CARTESIAN_POINT('Ctrl Pts',(-1.36221653708385,-1.94360989732643,
5.00156804588226));
#61859=CARTESIAN_POINT('Ctrl Pts',(-1.49280769753586,-1.84451249259589,
4.99142566107865));
#61860=CARTESIAN_POINT('Ctrl Pts',(-1.54976213834342,-1.79692438871535,
4.98679178318952));
#61861=CARTESIAN_POINT('Ctrl Pts',(-1.62949049096849,-1.72369380374607,
4.97989462267737));
#61862=CARTESIAN_POINT('Ctrl Pts',(-1.65408978781575,-1.70010187651077,
4.97770498499979));
#61863=CARTESIAN_POINT('Ctrl Pts',(-1.69792110029346,-1.65621348917713,
4.97368083338071));
#61864=CARTESIAN_POINT('Ctrl Pts',(-1.71731905625329,-1.63609117639608,
4.97185363526228));
#61865=CARTESIAN_POINT('Ctrl Pts',(-1.74749507321233,-1.60366031706711,
4.9689333846657));
#61866=CARTESIAN_POINT('Ctrl Pts',(-1.75850954035204,-1.59157457179876,
4.96785035710913));
#61867=CARTESIAN_POINT('Ctrl Pts',(-1.77907049449402,-1.56853983762533,
4.96579535782261));
#61868=CARTESIAN_POINT('Ctrl Pts',(-1.78864311734304,-1.55761510951789,
4.96482453466022));
#61869=CARTESIAN_POINT('Ctrl Pts',(-1.81013736893641,-1.53262542620302,
4.96261197007417));
#61870=CARTESIAN_POINT('Ctrl Pts',(-1.82199642763213,-1.51850814161053,
4.96136776704467));
#61871=CARTESIAN_POINT('Ctrl Pts',(-1.85248378237576,-1.48134398854073,
4.95810636426919));
#61872=CARTESIAN_POINT('Ctrl Pts',(-1.8708463669378,-1.45808432931162,4.95607887827389));
#61873=CARTESIAN_POINT('Ctrl Pts',(-1.99725136090337,-1.29164882871519,
4.94166095743455));
#61874=CARTESIAN_POINT('Ctrl Pts',(-2.08916325645431,-1.13698900617608,
4.92865761031279));
#61875=CARTESIAN_POINT('Ctrl Pts',(-2.21370757501617,-0.860293800848927,
4.90653067278365));
#61876=CARTESIAN_POINT('Ctrl Pts',(-2.25569782886252,-0.743263297334418,
4.89749655228345));
#61877=CARTESIAN_POINT('Ctrl Pts',(-2.29319862305957,-0.605623952511441,
4.88758085445317));
#61878=CARTESIAN_POINT('Ctrl Pts',(-2.29785288088542,-0.587718033360064,
4.88630450918909));
#61879=CARTESIAN_POINT('Ctrl Pts',(-2.30463369035238,-0.560317949411029,
4.884373984422));
#61880=CARTESIAN_POINT('Ctrl Pts',(-2.30691202010398,-0.550862588145834,
4.88371186573602));
#61881=CARTESIAN_POINT('Ctrl Pts',(-2.31099467408976,-0.533449391215215,
4.88250031183981));
#61882=CARTESIAN_POINT('Ctrl Pts',(-2.31281613072446,-0.525496132773104,
4.88194997407838));
#61883=CARTESIAN_POINT('Ctrl Pts',(-2.31687624121119,-0.507337844474354,
4.88070023853457));
#61884=CARTESIAN_POINT('Ctrl Pts',(-2.31908855145077,-0.497127253536078,
4.88000231090401));
#61885=CARTESIAN_POINT('Ctrl Pts',(-2.3257420416033,-0.465407731117818,
4.87784813625195));
#61886=CARTESIAN_POINT('Ctrl Pts',(-2.32995213459907,-0.443850801518335,
4.87640399157544));
#61887=CARTESIAN_POINT('Ctrl Pts',(-2.35894128111667,-0.283617131047518,
4.86579545824992));
#61888=CARTESIAN_POINT('Ctrl Pts',(-2.37162363284765,-0.143018943548074,
4.85717261551335));
#61889=CARTESIAN_POINT('Ctrl Pts',(-2.37180106459394,0.0563113734359232,
4.84493532920882));
#61890=CARTESIAN_POINT('Ctrl Pts',(-2.36969438103518,0.114680731789333,
4.84135207295172));
#61891=CARTESIAN_POINT('Ctrl Pts',(-2.36544099470095,0.17287846334401,4.83774038296924));
#61892=CARTESIAN_POINT('',(-2.36824990783039,0.000427589681932447,4.65128666940576));
#61893=CARTESIAN_POINT('Ctrl Pts',(-2.36544101871061,0.172878134827089,
4.63810474394384));
#61894=CARTESIAN_POINT('Ctrl Pts',(-2.36696574558802,0.152015742357601,
4.63943647498258));
#61895=CARTESIAN_POINT('Ctrl Pts',(-2.36821501678678,0.131125760271669,
4.64077559292494));
#61896=CARTESIAN_POINT('Ctrl Pts',(-2.37023193297686,0.0877694335960402,
4.64356885572076));
#61897=CARTESIAN_POINT('Ctrl Pts',(-2.37095701087706,0.0653122499247474,
4.64502343606539));
#61898=CARTESIAN_POINT('Ctrl Pts',(-2.37161918842369,0.0286655714961145,
4.64741167205354));
#61899=CARTESIAN_POINT('Ctrl Pts',(-2.37174821222471,0.01448071021935,4.64833964750865));
#61900=CARTESIAN_POINT('Ctrl Pts',(-2.37174998154971,0.000295836006343133,
4.64927143992648));
#61901=CARTESIAN_POINT('Ctrl Pts',(-2.36803551809634,0.000435659979227676,
4.65141010809499));
#61902=CARTESIAN_POINT('Ctrl Pts',(-2.36733685507668,-0.420470574046625,
4.67955118317444));
#61903=CARTESIAN_POINT('Ctrl Pts',(-2.06020439223756,-1.62937224150312,
4.76031262862425));
#61904=CARTESIAN_POINT('Ctrl Pts',(-0.135586668767159,-2.79462423533096,
4.89369444444444));
#61905=CARTESIAN_POINT('Ctrl Pts',(2.2650598786042,-1.64250178316317,5.05155555555556));
#61906=CARTESIAN_POINT('Ctrl Pts',(2.61412853009539,0.997316594419356,5.20941666666666));
#61907=CARTESIAN_POINT('Ctrl Pts',(0.595450368366912,2.73381550588105,5.36727777777778));
#61908=CARTESIAN_POINT('Ctrl Pts',(-1.72846737744239,2.061848728322,5.51069262891245));
#61909=CARTESIAN_POINT('Ctrl Pts',(-2.31767164028317,0.740184958633683,
5.60148710967678));
#61910=CARTESIAN_POINT('Ctrl Pts',(-2.36449584214975,0.172800370348396,
5.63966122007073));
#61911=CARTESIAN_POINT('Origin',(0.,0.,-1.84858989190501));
#61912=CARTESIAN_POINT('',(-2.36285989125428,0.172707701180992,6.83708460818679));
#61913=CARTESIAN_POINT('',(-2.36544101887183,0.172878132621275,6.64182320144908));
#61914=CARTESIAN_POINT('',(-2.36544101854889,0.172878137039864,-1.84858989190501));
#61915=CARTESIAN_POINT('',(-2.37459233302104,0.00130583459664112,5.84859123935915));
#61916=CARTESIAN_POINT('Ctrl Pts',(-2.37459233302104,0.00130583459664112,
5.84859123935915));
#61917=CARTESIAN_POINT('Ctrl Pts',(-2.36985292963545,-0.701523551850097,
5.89591470923835));
#61918=CARTESIAN_POINT('Ctrl Pts',(-1.66848328383473,-2.19471928883836,
5.99590314278425));
#61919=CARTESIAN_POINT('Ctrl Pts',(0.864288593995119,-2.66190468356086,
6.14855653999681));
#61920=CARTESIAN_POINT('Ctrl Pts',(2.70163876039796,-0.730670463607777,
6.30655143099686));
#61921=CARTESIAN_POINT('Ctrl Pts',(2.08817696449889,1.86339697407977,6.46454632199692));
#61922=CARTESIAN_POINT('Ctrl Pts',(-0.419590302218696,2.76706980330411,
6.62254121299697));
#61923=CARTESIAN_POINT('Ctrl Pts',(-2.09145531965774,1.50441074284138,6.74672064172692));
#61924=CARTESIAN_POINT('Ctrl Pts',(-2.34427764227796,0.453694740318712,
6.8182351067902));
#61925=CARTESIAN_POINT('Ctrl Pts',(-2.36285989125428,0.172707701180992,
6.83708460818679));
#61926=CARTESIAN_POINT('Ctrl Pts',(-2.37174969264697,0.00120744731113393,
5.84695890962807));
#61927=CARTESIAN_POINT('Ctrl Pts',(-2.37173086567736,0.0381886546764642,
5.84431029447727));
#61928=CARTESIAN_POINT('Ctrl Pts',(-2.37084710102938,0.0751666995482175,
5.84168447192852));
#61929=CARTESIAN_POINT('Ctrl Pts',(-2.36813959604457,0.132380889107501,
5.83767047856927));
#61930=CARTESIAN_POINT('Ctrl Pts',(-2.36692025046112,0.152638239149765,
5.83625878866294));
#61931=CARTESIAN_POINT('Ctrl Pts',(-2.36544101854819,0.172878137049535,
5.83485941057446));
#61932=CARTESIAN_POINT('',(-2.37251493491373,-0.00202804545912198,5.65140963369938));
#61933=CARTESIAN_POINT('Ctrl Pts',(-2.36449584214975,0.172800370348396,
5.63966122007073));
#61934=CARTESIAN_POINT('Ctrl Pts',(-2.36929936025563,0.114594527340226,
5.64357735794695));
#61935=CARTESIAN_POINT('Ctrl Pts',(-2.37198857858181,0.056265582705663,
5.64749349582317));
#61936=CARTESIAN_POINT('Ctrl Pts',(-2.37251493491373,-0.00202804545912198,
5.65140963369939));
#61937=CARTESIAN_POINT('Ctrl Pts',(-2.37174915472122,-0.00200239336298696,
5.65184980432678));
#61938=CARTESIAN_POINT('Ctrl Pts',(-2.37166794312654,-0.0981940481058294,
5.65886281514045));
#61939=CARTESIAN_POINT('Ctrl Pts',(-2.36573489179878,-0.194299783852276,
5.66586596605852));
#61940=CARTESIAN_POINT('Ctrl Pts',(-2.3497986979236,-0.323751847410071,
5.67511270209506));
#61941=CARTESIAN_POINT('Ctrl Pts',(-2.34488253083876,-0.357624627038201,
5.67751425362095));
#61942=CARTESIAN_POINT('Ctrl Pts',(-2.33735999376333,-0.402585872055809,
5.68066812323276));
#61943=CARTESIAN_POINT('Ctrl Pts',(-2.33540477226843,-0.413777339585329,
5.68145035057679));
#61944=CARTESIAN_POINT('Ctrl Pts',(-2.33186555464311,-0.43321071317438,
5.68280325624251));
#61945=CARTESIAN_POINT('Ctrl Pts',(-2.33031810765848,-0.441458955457005,
5.68337578586718));
#61946=CARTESIAN_POINT('Ctrl Pts',(-2.32713019967211,-0.457967259067173,
5.68451803759382));
#61947=CARTESIAN_POINT('Ctrl Pts',(-2.32548946222107,-0.466227140607921,
5.68508771958931));
#61948=CARTESIAN_POINT('Ctrl Pts',(-2.32189257884279,-0.483843228240834,
5.68629862105365));
#61949=CARTESIAN_POINT('Ctrl Pts',(-2.31992383518342,-0.493196536974783,
5.6869391423792));
#61950=CARTESIAN_POINT('Ctrl Pts',(-2.3143744281283,-0.518792542470743,
5.68868600205301));
#61951=CARTESIAN_POINT('Ctrl Pts',(-2.31067929090371,-0.535010231847836,
5.68978620766974));
#61952=CARTESIAN_POINT('Ctrl Pts',(-2.28839528053491,-0.628272489029095,
5.69608199438093));
#61953=CARTESIAN_POINT('Ctrl Pts',(-2.26612256851991,-0.704393706809874,
5.70109852589671));
#61954=CARTESIAN_POINT('Ctrl Pts',(-2.20294805643682,-0.885995548806609,
5.71307902927118));
#61955=CARTESIAN_POINT('Ctrl Pts',(-2.15823755304937,-0.989939599355856,
5.71995216633633));
#61956=CARTESIAN_POINT('Ctrl Pts',(-2.05095933236282,-1.1971835582713,5.73434570236838));
#61957=CARTESIAN_POINT('Ctrl Pts',(-1.9875847909272,-1.29968620325887,5.74186106462762));
#61958=CARTESIAN_POINT('Ctrl Pts',(-1.89989583690999,-1.42000316492679,
5.75151037429319));
#61959=CARTESIAN_POINT('Ctrl Pts',(-1.88266547412633,-1.44276948252377,
5.75337524915367));
#61960=CARTESIAN_POINT('Ctrl Pts',(-1.85455393447574,-1.47855174696766,
5.75637277602015));
#61961=CARTESIAN_POINT('Ctrl Pts',(-1.84393649331933,-1.49177201614181,
5.75749516343398));
#61962=CARTESIAN_POINT('Ctrl Pts',(-1.82376738348017,-1.5163411846726,5.7596099266484));
#61963=CARTESIAN_POINT('Ctrl Pts',(-1.81424918020712,-1.52771658121852,
5.76060093619527));
#61964=CARTESIAN_POINT('Ctrl Pts',(-1.79259963651647,-1.55310271869043,
5.76283993916535));
#61965=CARTESIAN_POINT('Ctrl Pts',(-1.78040962704136,-1.56706191266333,
5.76409027952431));
#61966=CARTESIAN_POINT('Ctrl Pts',(-1.74858607135156,-1.60265348425514,
5.7673289357105));
#61967=CARTESIAN_POINT('Ctrl Pts',(-1.7287146750491,-1.62406800395068,5.7693269732948));
#61968=CARTESIAN_POINT('Ctrl Pts',(-1.58063178415813,-1.77785277088925,
5.78404817766247));
#61969=CARTESIAN_POINT('Ctrl Pts',(-1.43779618794092,-1.89522429238506,
5.79742202102943));
#61970=CARTESIAN_POINT('Ctrl Pts',(-1.18456463126363,-2.05807213279846,
5.81936802902516));
#61971=CARTESIAN_POINT('Ctrl Pts',(-1.08172724905443,-2.11393611482528,
5.82785934724171));
#61972=CARTESIAN_POINT('Ctrl Pts',(-0.956752551750246,-2.17030673506258,
5.83740901699846));
#61973=CARTESIAN_POINT('Ctrl Pts',(-0.938217684610245,-2.17838344028346,
5.83880613460741));
#61974=CARTESIAN_POINT('Ctrl Pts',(-0.910171579756127,-2.1901803489787,
5.84088910000979));
#61975=CARTESIAN_POINT('Ctrl Pts',(-0.900736422135724,-2.19407752212689,
5.84158460455654));
#61976=CARTESIAN_POINT('Ctrl Pts',(-0.883553561026318,-2.20104534553064,
5.84284135633981));
#61977=CARTESIAN_POINT('Ctrl Pts',(-0.8758146192241,-2.2041361722323,5.84340373421265));
#61978=CARTESIAN_POINT('Ctrl Pts',(-0.85820768060397,-2.21106076408846,
5.84467502784564));
#61979=CARTESIAN_POINT('Ctrl Pts',(-0.848330143529769,-2.21486931977632,
5.84538247591548));
#61980=CARTESIAN_POINT('Ctrl Pts',(-0.817698653911014,-2.22644515083145,
5.84755959837781));
#61981=CARTESIAN_POINT('Ctrl Pts',(-0.796860432302053,-2.23398805618294,
5.84901698517874));
#61982=CARTESIAN_POINT('Ctrl Pts',(-0.641225565782021,-2.28786898746856,
5.85974823718837));
#61983=CARTESIAN_POINT('Ctrl Pts',(-0.502584568826552,-2.3222691889155,
5.86846862559448));
#61984=CARTESIAN_POINT('Ctrl Pts',(-0.200484376636533,-2.36888287304801,
5.88723970182822));
#61985=CARTESIAN_POINT('Ctrl Pts',(-0.0371763193537273,-2.37705895602669,
5.89726972323087));
#61986=CARTESIAN_POINT('Ctrl Pts',(0.153769447917697,-2.36692730583829,
5.90967436473727));
#61987=CARTESIAN_POINT('Ctrl Pts',(0.181840008248037,-2.36493636650573,
5.91151400393899));
#61988=CARTESIAN_POINT('Ctrl Pts',(0.226431364426487,-2.36097510024288,
5.91446515068847));
#61989=CARTESIAN_POINT('Ctrl Pts',(0.242978858837109,-2.35932953134603,
5.91556661966193));
#61990=CARTESIAN_POINT('Ctrl Pts',(0.27429980513601,-2.35588181959543,5.91766410185168));
#61991=CARTESIAN_POINT('Ctrl Pts',(0.289076325572834,-2.35411435402693,
5.91865899152265));
#61992=CARTESIAN_POINT('Ctrl Pts',(0.322730659542994,-2.34976722015807,
5.9209375659714));
#61993=CARTESIAN_POINT('Ctrl Pts',(0.34159577959488,-2.34709892303891,5.9222239475366));
#61994=CARTESIAN_POINT('Ctrl Pts',(0.391070384778924,-2.3394920985684,5.92562238761362));
#61995=CARTESIAN_POINT('Ctrl Pts',(0.421617885048203,-2.33418026909222,
5.92774584447236));
#61996=CARTESIAN_POINT('Ctrl Pts',(0.607481495457014,-2.29809345997478,
5.94082479006268));
#61997=CARTESIAN_POINT('Ctrl Pts',(0.759473790852414,-2.25243224387335,
5.95224128414857));
#61998=CARTESIAN_POINT('Ctrl Pts',(1.03485026984828,-2.13864274578075,5.97395822250262));
#61999=CARTESIAN_POINT('Ctrl Pts',(1.15898801540537,-2.07399653816928,5.98417970654474));
#62000=CARTESIAN_POINT('Ctrl Pts',(1.29364213274884,-1.98798671299195,5.99530717374739));
#62001=CARTESIAN_POINT('Ctrl Pts',(1.31042462640827,-1.97696446678553,5.99669444299449));
#62002=CARTESIAN_POINT('Ctrl Pts',(1.33550313641406,-1.96003394582676,5.99876576210146));
#62003=CARTESIAN_POINT('Ctrl Pts',(1.34390390814573,-1.95428349821039,5.99945931474755));
#62004=CARTESIAN_POINT('Ctrl Pts',(1.35911474806026,-1.94372699455734,6.00071417881865));
#62005=CARTESIAN_POINT('Ctrl Pts',(1.36593669637092,-1.9389390072561,6.00127660029417));
#62006=CARTESIAN_POINT('Ctrl Pts',(1.38139228425708,-1.92796943935018,6.00255003912493));
#62007=CARTESIAN_POINT('Ctrl Pts',(1.39000980042788,-1.92176574208364,6.00325956611506));
#62008=CARTESIAN_POINT('Ctrl Pts',(1.41661840509883,-1.90233774513479,6.00544983191101));
#62009=CARTESIAN_POINT('Ctrl Pts',(1.43446521057047,-1.88891668667636,6.00691806890733));
#62010=CARTESIAN_POINT('Ctrl Pts',(1.56440607940641,-1.78829526939246,6.01762398864826));
#62011=CARTESIAN_POINT('Ctrl Pts',(1.66867043826281,-1.69142422172829,6.02631362159911));
#62012=CARTESIAN_POINT('Ctrl Pts',(1.87255311146014,-1.46467491947559,6.04503903001394));
#62013=CARTESIAN_POINT('Ctrl Pts',(1.96867757303984,-1.33267691942787,6.05505415970181));
#62014=CARTESIAN_POINT('Ctrl Pts',(2.06478852906705,-1.16732727622128,6.06745799708827));
#62015=CARTESIAN_POINT('Ctrl Pts',(2.07861790555876,-1.14252007918357,6.06931428010355));
#62016=CARTESIAN_POINT('Ctrl Pts',(2.09985899735469,-1.10275501329495,6.07228585413338));
#62017=CARTESIAN_POINT('Ctrl Pts',(2.10756427569611,-1.08795644593969,6.07339085826053));
#62018=CARTESIAN_POINT('Ctrl Pts',(2.12184112361499,-1.05981577237725,6.07549113037718));
#62019=CARTESIAN_POINT('Ctrl Pts',(2.12844460552388,-1.04649069242988,6.07648523296498));
#62020=CARTESIAN_POINT('Ctrl Pts',(2.14317976182847,-1.01604032845627,6.07875647537248));
#62021=CARTESIAN_POINT('Ctrl Pts',(2.15123221052809,-0.99887806118754,6.08003624774184));
#62022=CARTESIAN_POINT('Ctrl Pts',(2.17177274193197,-0.953699134860895,
6.08340518033409));
#62023=CARTESIAN_POINT('Ctrl Pts',(2.18392422570758,-0.925534282549245,
6.0855054199611));
#62024=CARTESIAN_POINT('Ctrl Pts',(2.25880126029705,-0.742292049572722,
6.09917507062049));
#62025=CARTESIAN_POINT('Ctrl Pts',(2.30550651396125,-0.581207258801752,
6.11126576478187));
#62026=CARTESIAN_POINT('Ctrl Pts',(2.35139354153301,-0.324017641551093,
6.13031318824199));
#62027=CARTESIAN_POINT('Ctrl Pts',(2.36239035490912,-0.230548353423396,
6.13717293743749));
#62028=CARTESIAN_POINT('Ctrl Pts',(2.36967215289794,-0.104390336391882,
6.14618724693443));
#62029=CARTESIAN_POINT('Ctrl Pts',(2.37087512005553,-0.072075158327642,
6.14847441463289));
#62030=CARTESIAN_POINT('Ctrl Pts',(2.37180665194257,-0.0164930959482848,
6.15236043475196));
#62031=CARTESIAN_POINT('Ctrl Pts',(2.3718543744367,0.00676331707411645,
6.15397199079599));
#62032=CARTESIAN_POINT('Ctrl Pts',(2.37142346659216,0.0408073455603119,
6.15630647100209));
#62033=CARTESIAN_POINT('Ctrl Pts',(2.3712132637851,0.0515961845427436,6.1570426674515));
#62034=CARTESIAN_POINT('Ctrl Pts',(2.37073089880731,0.0699288182410932,
6.15828705818149));
#62035=CARTESIAN_POINT('Ctrl Pts',(2.3704963484424,0.0774732345676194,6.15879725358695));
#62036=CARTESIAN_POINT('Ctrl Pts',(2.36987840497654,0.0947012026120704,
6.15995788123622));
#62037=CARTESIAN_POINT('Ctrl Pts',(2.36947167751313,0.10438366663914,6.16060703320101));
#62038=CARTESIAN_POINT('Ctrl Pts',(2.36817728492117,0.131267123853438,6.16240135066376));
#62039=CARTESIAN_POINT('Ctrl Pts',(2.36716156245559,0.148461744861513,6.16353982541141));
#62040=CARTESIAN_POINT('Ctrl Pts',(2.35805772577831,0.278495139973572,6.17209036885216));
#62041=CARTESIAN_POINT('Ctrl Pts',(2.34209176644544,0.3906515282706,6.17913186592397));
#62042=CARTESIAN_POINT('Ctrl Pts',(2.31562194557889,0.513068438372429,6.18685153373076));
#62043=CARTESIAN_POINT('Ctrl Pts',(2.31297660886462,0.524865150709604,6.18759574457694));
#62044=CARTESIAN_POINT('Ctrl Pts',(2.2814148673633,0.660738504601893,6.19617569045349));
#62045=CARTESIAN_POINT('Ctrl Pts',(2.24263809764807,0.782305326129489,6.20394463107483));
#62046=CARTESIAN_POINT('Ctrl Pts',(2.16761985853045,0.965173117035017,6.21638260139341));
#62047=CARTESIAN_POINT('Ctrl Pts',(2.13807902265709,1.0289565946446,6.22087010455547));
#62048=CARTESIAN_POINT('Ctrl Pts',(2.09502335796077,1.11203368889986,6.22697333188627));
#62049=CARTESIAN_POINT('Ctrl Pts',(2.08398942813815,1.13257661834035,6.22850421071076));
#62050=CARTESIAN_POINT('Ctrl Pts',(2.06506507766063,1.16659677877985,6.23107774091571));
#62051=CARTESIAN_POINT('Ctrl Pts',(2.05734106109059,1.18016505542708,6.23211451179386));
#62052=CARTESIAN_POINT('Ctrl Pts',(2.04186932841817,1.20672971922513,6.23416540886358));
#62053=CARTESIAN_POINT('Ctrl Pts',(2.03413008477298,1.21973019546412,6.23517919624074));
#62054=CARTESIAN_POINT('Ctrl Pts',(2.01502784637667,1.25113088968851,6.23765300620252));
#62055=CARTESIAN_POINT('Ctrl Pts',(2.0035367252948,1.26945116565578,6.23911760440889));
#62056=CARTESIAN_POINT('Ctrl Pts',(1.96320934194487,1.33183331897786,6.24417993860481));
#62057=CARTESIAN_POINT('Ctrl Pts',(1.93315896656321,1.37508784267071,6.24782152875939));
#62058=CARTESIAN_POINT('Ctrl Pts',(1.79963732491798,1.5542432063077,6.26348319573832));
#62059=CARTESIAN_POINT('Ctrl Pts',(1.68309694255494,1.67974274988152,6.27597317026033));
#62060=CARTESIAN_POINT('Ctrl Pts',(1.50057186855107,1.83807146027089,6.29355498997769));
#62061=CARTESIAN_POINT('Ctrl Pts',(1.44496712732386,1.88209825588017,6.29868542273145));
#62062=CARTESIAN_POINT('Ctrl Pts',(1.36528505362854,1.93957290831984,6.30565854747292));
#62063=CARTESIAN_POINT('Ctrl Pts',(1.34282320786524,1.95519111906169,6.30758471133477));
#62064=CARTESIAN_POINT('Ctrl Pts',(1.30306828536725,1.98182520638829,6.31091900388936));
#62065=CARTESIAN_POINT('Ctrl Pts',(1.28589350464133,1.99301180865828,6.31233574800345));
#62066=CARTESIAN_POINT('Ctrl Pts',(1.25990330910869,2.00946436907164,6.31444189797018));
#62067=CARTESIAN_POINT('Ctrl Pts',(1.25119570016981,2.01489769678574,6.31514127058831));
#62068=CARTESIAN_POINT('Ctrl Pts',(1.2353559568882,2.02463901429807,6.31640179781952));
#62069=CARTESIAN_POINT('Ctrl Pts',(1.22823617740633,2.02896608544545,6.31696412372678));
#62070=CARTESIAN_POINT('Ctrl Pts',(1.21207089210003,2.0386743195224,6.3182313186339));
#62071=CARTESIAN_POINT('Ctrl Pts',(1.20301222255233,2.04403288411482,6.31893476371194));
#62072=CARTESIAN_POINT('Ctrl Pts',(1.17504981067659,2.06032348065511,6.32108671648624));
#62073=CARTESIAN_POINT('Ctrl Pts',(1.15602992510676,2.07105523750016,6.32252334163217));
#62074=CARTESIAN_POINT('Ctrl Pts',(1.00841092271245,2.15168017927849,6.33348752082668));
#62075=CARTESIAN_POINT('Ctrl Pts',(0.873721809573873,2.20980584028212,6.34242836118869));
#62076=CARTESIAN_POINT('Ctrl Pts',(0.583487503549271,2.30433726137325,6.36117352513113));
#62077=CARTESIAN_POINT('Ctrl Pts',(0.427917875657047,2.33822706952737,6.37095396050662));
#62078=CARTESIAN_POINT('Ctrl Pts',(0.241681792298568,2.35957801538512,6.38310849996914));
#62079=CARTESIAN_POINT('Ctrl Pts',(0.213169196996673,2.36232454992421,6.38498030710498));
#62080=CARTESIAN_POINT('Ctrl Pts',(0.167929800115494,2.36585665908776,6.38797093359657));
#62081=CARTESIAN_POINT('Ctrl Pts',(0.151231834886828,2.36698269054815,6.3890792321497));
#62082=CARTESIAN_POINT('Ctrl Pts',(0.119684918883122,2.36877489069326,6.39118215537347));
#62083=CARTESIAN_POINT('Ctrl Pts',(0.104838835965593,2.36947837381484,6.39217557597353));
#62084=CARTESIAN_POINT('Ctrl Pts',(0.0711297031559081,2.37075826548578,
6.39444023879082));
#62085=CARTESIAN_POINT('Ctrl Pts',(0.0522646125744744,2.37124915666286,
6.39571405572123));
#62086=CARTESIAN_POINT('Ctrl Pts',(0.00302386918786248,2.37194257433258,
6.39905648113215));
#62087=CARTESIAN_POINT('Ctrl Pts',(-0.0273525361268728,2.37178675520128,
6.40113588612477));
#62088=CARTESIAN_POINT('Ctrl Pts',(-0.26650507321228,2.36596526740108,6.41765082735151));
#62089=CARTESIAN_POINT('Ctrl Pts',(-0.473676394463343,2.33332678581228,
6.43294090165484));
#62090=CARTESIAN_POINT('Ctrl Pts',(-0.758236246628948,2.24900496389794,
6.45450603596177));
#62091=CARTESIAN_POINT('Ctrl Pts',(-0.841179760054879,2.21931636515862,
6.46084645882629));
#62092=CARTESIAN_POINT('Ctrl Pts',(-0.942183816947739,2.17668419956558,
6.46849574397388));
#62093=CARTESIAN_POINT('Ctrl Pts',(-0.961965353313174,2.16801457315593,
6.46999015892612));
#62094=CARTESIAN_POINT('Ctrl Pts',(-0.991165323829755,2.15473876830929,
6.47218773379054));
#62095=CARTESIAN_POINT('Ctrl Pts',(-1.00067548523696,2.15033868086364,6.47290212873397));
#62096=CARTESIAN_POINT('Ctrl Pts',(-1.01769368528513,2.14232747856053,6.47417771323426));
#62097=CARTESIAN_POINT('Ctrl Pts',(-1.02521216477358,2.13873969559181,6.47474023046216));
#62098=CARTESIAN_POINT('Ctrl Pts',(-1.04199003476132,2.13062456835668,6.47599324657539));
#62099=CARTESIAN_POINT('Ctrl Pts',(-1.05123896914347,2.1260764152266,6.47668247835339));
#62100=CARTESIAN_POINT('Ctrl Pts',(-1.07898516150538,2.11220692658176,6.4787464694199));
#62101=CARTESIAN_POINT('Ctrl Pts',(-1.09739080255681,2.10270315940521,6.48011070850734));
#62102=CARTESIAN_POINT('Ctrl Pts',(-1.25726881501884,2.01747877350479,6.49193834297783));
#62103=CARTESIAN_POINT('Ctrl Pts',(-1.39086250400372,1.92781262917818,6.50168438669642));
#62104=CARTESIAN_POINT('Ctrl Pts',(-1.61100020577519,1.74517466684006,6.51926163015064));
#62105=CARTESIAN_POINT('Ctrl Pts',(-1.70108575256117,1.65748577807768,6.52701750948861));
#62106=CARTESIAN_POINT('Ctrl Pts',(-1.81110409040156,1.53193206389676,6.53771988382237));
#62107=CARTESIAN_POINT('Ctrl Pts',(-1.83758098174724,1.50006989261944,6.54040385598605));
#62108=CARTESIAN_POINT('Ctrl Pts',(-1.87511626406298,1.45241433384362,6.54438308900106));
#62109=CARTESIAN_POINT('Ctrl Pts',(-1.88683895878102,1.43715243057007,6.54565235426911));
#62110=CARTESIAN_POINT('Ctrl Pts',(-1.90730849595032,1.40982072915163,6.54791744813605));
#62111=CARTESIAN_POINT('Ctrl Pts',(-1.9161298147236,1.39780782050987,6.54891033929669));
#62112=CARTESIAN_POINT('Ctrl Pts',(-1.93449125404957,1.37230269361937,6.55101326012844));
#62113=CARTESIAN_POINT('Ctrl Pts',(-1.94400472687026,1.35879236572654,6.55212422997065));
#62114=CARTESIAN_POINT('Ctrl Pts',(-1.96905512816116,1.32241603864394,6.55510826510037));
#62115=CARTESIAN_POINT('Ctrl Pts',(-1.98433434223131,1.2993765367708,6.5569907555173));
#62116=CARTESIAN_POINT('Ctrl Pts',(-2.06610586074821,1.17126647757892,6.56742170154033));
#62117=CARTESIAN_POINT('Ctrl Pts',(-2.12464894754521,1.06137495115133,6.57625134991567));
#62118=CARTESIAN_POINT('Ctrl Pts',(-2.24341076832004,0.788819037881383,
6.59776737571126));
#62119=CARTESIAN_POINT('Ctrl Pts',(-2.29495825635376,0.623134794124575,
6.61056644981406));
#62120=CARTESIAN_POINT('Ctrl Pts',(-2.33347219714566,0.42534408358896,6.62472907394182));
#62121=CARTESIAN_POINT('Ctrl Pts',(-2.3384144303431,0.397275990065826,6.62671227495847));
#62122=CARTESIAN_POINT('Ctrl Pts',(-2.34466907916963,0.357577416564442,
6.62947372682879));
#62123=CARTESIAN_POINT('Ctrl Pts',(-2.34640297078246,0.346017069639293,
6.63027269063599));
#62124=CARTESIAN_POINT('Ctrl Pts',(-2.3492418767404,0.326085794439408,6.63164074259073));
#62125=CARTESIAN_POINT('Ctrl Pts',(-2.35038777459285,0.317721039527598,
6.63221201510996));
#62126=CARTESIAN_POINT('Ctrl Pts',(-2.35272563345256,0.299950068680857,
6.63341943561299));
#62127=CARTESIAN_POINT('Ctrl Pts',(-2.35390589037828,0.290542625114165,
6.63405494874092));
#62128=CARTESIAN_POINT('Ctrl Pts',(-2.35701148363441,0.264526858563489,
6.63580294536797));
#62129=CARTESIAN_POINT('Ctrl Pts',(-2.35881771050953,0.247904497812455,
6.63690914094991));
#62130=CARTESIAN_POINT('Ctrl Pts',(-2.36235291397937,0.211821625798301,
6.63929002479679));
#62131=CARTESIAN_POINT('Ctrl Pts',(-2.36401731734834,0.192358224933772,
6.64056147713844));
#62132=CARTESIAN_POINT('Ctrl Pts',(-2.36544101887183,0.172878132621275,
6.64182320144908));
#62133=CARTESIAN_POINT('Origin',(0.,0.,-1.84858989190501));
#62134=CARTESIAN_POINT('',(-2.36544101854889,0.172878137039867,7.83684641963031));
#62135=CARTESIAN_POINT('',(-2.36544101891311,0.172878132056353,7.63807246982441));
#62136=CARTESIAN_POINT('',(-2.36544101854889,0.172878137039864,-1.84858989190501));
#62137=CARTESIAN_POINT('',(-2.37167361653571,0.000854563641824859,6.84858987464153));
#62138=CARTESIAN_POINT('Ctrl Pts',(-2.37174984612948,0.000854332948242326,
6.84858989190503));
#62139=CARTESIAN_POINT('Ctrl Pts',(-2.37177915559275,-0.0805129081841288,
6.85402314595505));
#62140=CARTESIAN_POINT('Ctrl Pts',(-2.36761694184918,-0.161853312165533,
6.85945640000507));
#62141=CARTESIAN_POINT('Ctrl Pts',(-2.35929771545254,-0.242718669163329,
6.86488965405509));
#62142=CARTESIAN_POINT('Ctrl Pts',(-2.35097324343856,-0.323635015123228,
6.87032633399717));
#62143=CARTESIAN_POINT('Ctrl Pts',(-2.33848658967688,-0.404075282207293,
6.87576301393926));
#62144=CARTESIAN_POINT('Ctrl Pts',(-2.32192384517465,-0.483598717646512,
6.88119969388134));
#62145=CARTESIAN_POINT('Ctrl Pts',(-2.30533317653517,-0.563256226477143,
6.88664553985245));
#62146=CARTESIAN_POINT('Ctrl Pts',(-2.28465278577067,-0.641993387252711,
6.89209138582357));
#62147=CARTESIAN_POINT('Ctrl Pts',(-2.26001938753787,-0.71938197812632,
6.89753723179468));
#62148=CARTESIAN_POINT('Ctrl Pts',(-2.23536311814162,-0.796842421332077,
6.90298813402447));
#62149=CARTESIAN_POINT('Ctrl Pts',(-2.20674668417494,-0.87295139022043,
6.90843903625425));
#62150=CARTESIAN_POINT('Ctrl Pts',(-2.17435507022211,-0.947300422832917,
6.91388993848403));
#62151=CARTESIAN_POINT('Ctrl Pts',(-2.14189739854026,-1.0218010788951,6.91935195699296));
#62152=CARTESIAN_POINT('Ctrl Pts',(-2.10564936477121,-1.09453423738812,
6.92481397550188));
#62153=CARTESIAN_POINT('Ctrl Pts',(-2.06584201697569,-1.16511579827835,
6.9302759940108));
#62154=CARTESIAN_POINT('Ctrl Pts',(-2.04578778886831,-1.20067352318729,
6.93302766100623));
#62155=CARTESIAN_POINT('Ctrl Pts',(-2.02483090688869,-1.2356856397051,6.93577932800166));
#62156=CARTESIAN_POINT('Ctrl Pts',(-2.00300491013283,-1.27010605560473,
6.93853099499709));
#62157=CARTESIAN_POINT('Ctrl Pts',(-1.96068196612791,-1.33685092645943,
6.94386677184479));
#62158=CARTESIAN_POINT('Ctrl Pts',(-1.91494048268382,-1.40160223551842,
6.94920254869248));
#62159=CARTESIAN_POINT('Ctrl Pts',(-1.8659943053119,-1.46398883706248,6.95453832554018));
#62160=CARTESIAN_POINT('Ctrl Pts',(-1.81711810468153,-1.52628624653219,
6.95986647400304));
#62161=CARTESIAN_POINT('Ctrl Pts',(-1.76504659571131,-1.5862252973756,6.96519462246589));
#62162=CARTESIAN_POINT('Ctrl Pts',(-1.71003754383265,-1.64346270453053,
6.97052277092875));
#62163=CARTESIAN_POINT('Ctrl Pts',(-1.65509157659909,-1.70063447155181,
6.97584480904534));
#62164=CARTESIAN_POINT('Ctrl Pts',(-1.59721508397275,-1.75511041634507,
6.98116684716193));
#62165=CARTESIAN_POINT('Ctrl Pts',(-1.53670586889553,-1.80658050886254,
6.98648888527852));
#62166=CARTESIAN_POINT('Ctrl Pts',(-1.47623454601038,-1.85801836968392,
6.9918075906186));
#62167=CARTESIAN_POINT('Ctrl Pts',(-1.41313412880433,-1.90645381215827,
6.99712629595868));
#62168=CARTESIAN_POINT('Ctrl Pts',(-1.34773814248875,-1.95161470628323,
7.00244500129877));
#62169=CARTESIAN_POINT('Ctrl Pts',(-1.28236282069116,-1.99676132998944,
7.00776202597787));
#62170=CARTESIAN_POINT('Ctrl Pts',(-1.21469375514147,-2.038635194455,7.01307905065698));
#62171=CARTESIAN_POINT('Ctrl Pts',(-1.14509512266201,-2.07700631259409,
7.01839607533609));
#62172=CARTESIAN_POINT('Ctrl Pts',(-1.07549689160726,-2.1153772094197,7.02371306934814));
#62173=CARTESIAN_POINT('Ctrl Pts',(-1.00396952630723,-2.15024517542969,
7.02903006336019));
#62174=CARTESIAN_POINT('Ctrl Pts',(-0.930902274650232,-2.18142591383504,
7.03434705737224));
#62175=CARTESIAN_POINT('Ctrl Pts',(-0.857762718819599,-2.21263750734267,
7.03966931285026));
#62176=CARTESIAN_POINT('Ctrl Pts',(-0.783080664326686,-2.24015440096073,
7.04499156832829));
#62177=CARTESIAN_POINT('Ctrl Pts',(-0.707265280633499,-2.26384051675696,
7.05031382380631));
#62178=CARTESIAN_POINT('Ctrl Pts',(-0.63141310036695,-2.2875381284773,7.05563866241132));
#62179=CARTESIAN_POINT('Ctrl Pts',(-0.554426948833437,-2.30740114141282,
7.06096350101634));
#62180=CARTESIAN_POINT('Ctrl Pts',(-0.47672863410306,-2.32334411397155,
7.06628833962136));
#62181=CARTESIAN_POINT('Ctrl Pts',(-0.398892022665602,-2.33931546373013,
7.07162265600781));
#62182=CARTESIAN_POINT('Ctrl Pts',(-0.320341178971256,-2.35135276097182,
7.07695697239425));
#62183=CARTESIAN_POINT('Ctrl Pts',(-0.241505282084628,-2.35942223038294,
7.08229128878071));
#62184=CARTESIAN_POINT('Ctrl Pts',(-0.171380880188349,-2.366600010283,7.08703615451951));
#62185=CARTESIAN_POINT('Ctrl Pts',(-0.101031231045985,-2.37063915759974,
7.09178102025832));
#62186=CARTESIAN_POINT('Ctrl Pts',(-0.0307572526518399,-2.37155055900339,
7.09652588599712));
#62187=CARTESIAN_POINT('Ctrl Pts',(0.0482684326998375,-2.3725754635584,
7.10186166284482));
#62188=CARTESIAN_POINT('Ctrl Pts',(0.127492451646572,-2.36964798094668,
7.10719743969251));
#62189=CARTESIAN_POINT('Ctrl Pts',(0.206487116023799,-2.36274440712832,
7.11253321654021));
#62190=CARTESIAN_POINT('Ctrl Pts',(0.285368844324812,-2.35585070312263,
7.11786136500305));
#62191=CARTESIAN_POINT('Ctrl Pts',(0.36402140683267,-2.34499223760633,7.1231895134659));
#62192=CARTESIAN_POINT('Ctrl Pts',(0.442016450198779,-2.3301973135882,7.12851766192875));
#62193=CARTESIAN_POINT('Ctrl Pts',(0.519922048474432,-2.31541935646002,
7.13383970004534));
#62194=CARTESIAN_POINT('Ctrl Pts',(0.597171168623043,-2.29671399904263,
7.13916173816193));
#62195=CARTESIAN_POINT('Ctrl Pts',(0.673341431373987,-2.27416124742623,
7.14448377627852));
#62196=CARTESIAN_POINT('Ctrl Pts',(0.749463994642761,-2.25162261883547,
7.1498024816186));
#62197=CARTESIAN_POINT('Ctrl Pts',(0.824508593977999,-2.2252415110142,7.15512118695869));
#62198=CARTESIAN_POINT('Ctrl Pts',(0.898065072388576,-2.19514855721787,
7.16043989229877));
#62199=CARTESIAN_POINT('Ctrl Pts',(0.971598307642224,-2.16506511251255,
7.16575691697788));
#62200=CARTESIAN_POINT('Ctrl Pts',(1.0436439229545,-2.13127232819516,7.17107394165699));
#62201=CARTESIAN_POINT('Ctrl Pts',(1.11381030777835,-2.09394953635151,7.17639096633609));
#62202=CARTESIAN_POINT('Ctrl Pts',(1.18397628790289,-2.05662695977488,7.18170796034815));
#62203=CARTESIAN_POINT('Ctrl Pts',(1.25226264659941,-2.01577463724099,7.1870249543602));
#62204=CARTESIAN_POINT('Ctrl Pts',(1.31830234006142,-1.97161786426493,7.19234194837225));
#62205=CARTESIAN_POINT('Ctrl Pts',(1.38440738353117,-1.92741739566726,7.19766420385028));
#62206=CARTESIAN_POINT('Ctrl Pts',(1.44826093106839,-1.87990620577915,7.2029864593283));
#62207=CARTESIAN_POINT('Ctrl Pts',(1.50952543709459,-1.82935262244992,7.20830871480632));
#62208=CARTESIAN_POINT('Ctrl Pts',(1.57081967750687,-1.77877450322115,7.21363355341134));
#62209=CARTESIAN_POINT('Ctrl Pts',(1.62952202715037,-1.72515136495837,7.21895839201636));
#62210=CARTESIAN_POINT('Ctrl Pts',(1.68533044290944,-1.66878978924928,7.22428323062138));
#62211=CARTESIAN_POINT('Ctrl Pts',(1.74123819312836,-1.61232789450045,7.22961754700782));
#62212=CARTESIAN_POINT('Ctrl Pts',(1.79424140472672,-1.55311817291498,7.23495186339427));
#62213=CARTESIAN_POINT('Ctrl Pts',(1.84407727797157,-1.49150161091732,7.24028617978072));
#62214=CARTESIAN_POINT('Ctrl Pts',(1.88840620606527,-1.43669377936282,7.24503104551954));
#62215=CARTESIAN_POINT('Ctrl Pts',(1.9302295762927,-1.37998228539239,7.24977591125837));
#62216=CARTESIAN_POINT('Ctrl Pts',(1.96939207837337,-1.32162509969363,7.25452077699719));
#62217=CARTESIAN_POINT('Ctrl Pts',(2.01343175903073,-1.25600028805771,7.25985655384489));
#62218=CARTESIAN_POINT('Ctrl Pts',(2.05426964762353,-1.18804970168938,7.26519233069258));
#62219=CARTESIAN_POINT('Ctrl Pts',(2.09165219387575,-1.11811858152647,7.27052810754028));
#62220=CARTESIAN_POINT('Ctrl Pts',(2.12898129552994,-1.0482874395882,7.27585625600314));
#62221=CARTESIAN_POINT('Ctrl Pts',(2.16286464673432,-0.976481796539616,
7.281184404466));
#62222=CARTESIAN_POINT('Ctrl Pts',(2.19309189019156,-0.903075868172765,
7.28651255292887));
#62223=CARTESIAN_POINT('Ctrl Pts',(2.2232844689007,-0.829754122077439,7.29183459104546));
#62224=CARTESIAN_POINT('Ctrl Pts',(2.24982909504344,-0.754836168402808,
7.29715662916205));
#62225=CARTESIAN_POINT('Ctrl Pts',(2.27256197755904,-0.678719471249317,
7.30247866727864));
#62226=CARTESIAN_POINT('Ctrl Pts',(2.2952806242471,-0.602650440034032,7.30779737261873));
#62227=CARTESIAN_POINT('Ctrl Pts',(2.31419213185353,-0.525384602697456,
7.31311607795882));
#62228=CARTESIAN_POINT('Ctrl Pts',(2.32918178861309,-0.447336850810598,
7.3184347832989));
#62229=CARTESIAN_POINT('Ctrl Pts',(2.34416670878176,-0.369313761280986,
7.32375180797801));
#62230=CARTESIAN_POINT('Ctrl Pts',(2.35523215095679,-0.290509707152289,
7.32906883265711));
#62231=CARTESIAN_POINT('Ctrl Pts',(2.36231432332553,-0.211350657228775,
7.33438585733622));
#62232=CARTESIAN_POINT('Ctrl Pts',(2.36939645484637,-0.132192063871593,
7.33970285134828));
#62233=CARTESIAN_POINT('Ctrl Pts',(2.37249532201,-0.0526789450624656,7.34501984536034));
#62234=CARTESIAN_POINT('Ctrl Pts',(2.37159905164703,0.0267581899038842,
7.35033683937239));
#62235=CARTESIAN_POINT('Ctrl Pts',(2.37070189437389,0.106273932403163,7.35565909485041));
#62236=CARTESIAN_POINT('Ctrl Pts',(2.36580170807694,0.185713071823991,7.36098135032843));
#62237=CARTESIAN_POINT('Ctrl Pts',(2.35693877807661,0.264646290166226,7.36630360580646));
#62238=CARTESIAN_POINT('Ctrl Pts',(2.34807154650266,0.343617818305553,7.37162844441148));
#62239=CARTESIAN_POINT('Ctrl Pts',(2.33523781536877,0.422082473762712,7.3769532830165));
#62240=CARTESIAN_POINT('Ctrl Pts',(2.31852930720246,0.499619769568116,7.38227812162152));
#62241=CARTESIAN_POINT('Ctrl Pts',(2.30179105924491,0.577295075479918,7.38761243800797));
#62242=CARTESIAN_POINT('Ctrl Pts',(2.28116437588896,0.654039270724346,7.39294675439442));
#62243=CARTESIAN_POINT('Ctrl Pts',(2.25679123749161,0.729445935543599,7.39828107078087));
#62244=CARTESIAN_POINT('Ctrl Pts',(2.23511137057895,0.796520041100205,7.40302593651966));
#62245=CARTESIAN_POINT('Ctrl Pts',(2.21046807638914,0.86253591719785,7.40777080225845));
#62246=CARTESIAN_POINT('Ctrl Pts',(2.18299254324694,0.927222529185008,7.41251566799724));
#62247=CARTESIAN_POINT('Ctrl Pts',(2.15209529099812,0.999965014557204,7.41785144484493));
#62248=CARTESIAN_POINT('Ctrl Pts',(2.11750065082667,1.07129681815087,7.42318722169263));
#62249=CARTESIAN_POINT('Ctrl Pts',(2.07935922038889,1.14081694196908,7.42852299854032));
#62250=CARTESIAN_POINT('Ctrl Pts',(2.04127231950099,1.21023767515052,7.43385114700318));
#62251=CARTESIAN_POINT('Ctrl Pts',(1.99964892199597,1.27785146547898,7.43917929546604));
#62252=CARTESIAN_POINT('Ctrl Pts',(1.95468749383537,1.34327765705516,7.44450744392889));
#62253=CARTESIAN_POINT('Ctrl Pts',(1.90977762765667,1.40862881756041,7.44982948204548));
#62254=CARTESIAN_POINT('Ctrl Pts',(1.8615376021355,1.47179698119973,7.45515152016207));
#62255=CARTESIAN_POINT('Ctrl Pts',(1.81021079871614,1.53242778841662,7.46047355827866));
#62256=CARTESIAN_POINT('Ctrl Pts',(1.75891613726213,1.59302062729779,7.46579226361875));
#62257=CARTESIAN_POINT('Ctrl Pts',(1.70453883648867,1.65107890749843,7.47111096895883));
#62258=CARTESIAN_POINT('Ctrl Pts',(1.64736369149876,1.7062798511474,7.47642967429891));
#62259=CARTESIAN_POINT('Ctrl Pts',(1.59020661331815,1.76146335181617,7.48174669897802));
#62260=CARTESIAN_POINT('Ctrl Pts',(1.53025378309257,1.81379098414925,7.48706372365712));
#62261=CARTESIAN_POINT('Ctrl Pts',(1.4678270969674,1.86297656343505,7.49238074833623));
#62262=CARTESIAN_POINT('Ctrl Pts',(1.40540077090118,1.91216185903273,7.49769774234828));
#62263=CARTESIAN_POINT('Ctrl Pts',(1.34050098582996,1.95820484914146,7.50301473636034));
#62264=CARTESIAN_POINT('Ctrl Pts',(1.27348181005652,2.00086035043807,7.50833173037239));
#62265=CARTESIAN_POINT('Ctrl Pts',(1.20639631502228,2.04355806176312,7.51365398585042));
#62266=CARTESIAN_POINT('Ctrl Pts',(1.13718763582058,2.08286133670076,7.51897624132844));
#62267=CARTESIAN_POINT('Ctrl Pts',(1.06623734353874,2.11856932615939,7.52429849680646));
#62268=CARTESIAN_POINT('Ctrl Pts',(0.995252615928549,2.15429464629141,7.52962333541147));
#62269=CARTESIAN_POINT('Ctrl Pts',(0.92252501993645,2.18642101539873,7.53494817401649));
#62270=CARTESIAN_POINT('Ctrl Pts',(0.84845683695102,2.21479548905335,7.5402730126215));
#62271=CARTESIAN_POINT('Ctrl Pts',(0.774256818598921,2.24322046697293,7.54560732900795));
#62272=CARTESIAN_POINT('Ctrl Pts',(0.698711891547283,2.26788006078031,7.5509416453944));
#62273=CARTESIAN_POINT('Ctrl Pts',(0.622240017692211,2.2886711041306,7.55627596178086));
#62274=CARTESIAN_POINT('Ctrl Pts',(0.554218410432574,2.30716470333247,7.56102082751967));
#62275=CARTESIAN_POINT('Ctrl Pts',(0.485463801873102,2.3225981620295,7.56576569325849));
#62276=CARTESIAN_POINT('Ctrl Pts',(0.416274870466302,2.33493325273299,7.5705105589973));
#62277=CARTESIAN_POINT('Ctrl Pts',(0.338469360544844,2.34880451801486,7.575846335845));
#62278=CARTESIAN_POINT('Ctrl Pts',(0.259824980161947,2.3588083556142,7.5811821126927));
#62279=CARTESIAN_POINT('Ctrl Pts',(0.180759859107338,2.36485177883002,7.5865178895404));
#62280=CARTESIAN_POINT('Ctrl Pts',(0.101807774858563,2.37088656196222,7.59184603800324));
#62281=CARTESIAN_POINT('Ctrl Pts',(0.022436607384243,2.37297214010521,7.59717418646609));
#62282=CARTESIAN_POINT('Ctrl Pts',(-0.0569263939879318,2.37106673212028,
7.60250233492894));
#62283=CARTESIAN_POINT('Ctrl Pts',(-0.13619838148887,2.36916350926638,7.60782437304554));
#62284=CARTESIAN_POINT('Ctrl Pts',(-0.215461755963201,2.36327840716033,
7.61314641116213));
#62285=CARTESIAN_POINT('Ctrl Pts',(-0.294286748773025,2.35342163073186,
7.61846844927873));
#62286=CARTESIAN_POINT('Ctrl Pts',(-0.373062379650736,2.34357102683207,
7.62378715461882));
#62287=CARTESIAN_POINT('Ctrl Pts',(-0.451399710594871,2.32975374345857,
7.62910585995891));
#62288=CARTESIAN_POINT('Ctrl Pts',(-0.528872793658224,2.31203192681852,
7.63442456529899));
#62289=CARTESIAN_POINT('Ctrl Pts',(-0.606321395954214,2.29431571010625,
7.6397415899781));
#62290=CARTESIAN_POINT('Ctrl Pts',(-0.682905836808822,2.27269751460741,
7.6450586146572));
#62291=CARTESIAN_POINT('Ctrl Pts',(-0.758210542632892,2.24729055432099,
7.6503756393363));
#62292=CARTESIAN_POINT('Ctrl Pts',(-0.833514814121615,2.22188374057443,
7.65569263334838));
#62293=CARTESIAN_POINT('Ctrl Pts',(-0.907538922285617,2.19268835650416,
7.66100962736044));
#62294=CARTESIAN_POINT('Ctrl Pts',(-0.979884053079207,2.15986696465802,
7.66632662137252));
#62295=CARTESIAN_POINT('Ctrl Pts',(-1.05230077346679,2.12701309419044,7.67164887685054));
#62296=CARTESIAN_POINT('Ctrl Pts',(-1.12303477064667,2.09052624257737,7.67697113232857));
#62297=CARTESIAN_POINT('Ctrl Pts',(-1.19170933285217,2.0506162314029,7.68229338780659));
#62298=CARTESIAN_POINT('Ctrl Pts',(-1.26041722587316,2.01068685012725,7.68761822641161));
#62299=CARTESIAN_POINT('Ctrl Pts',(-1.3270632999103,1.9673312550298,7.69294306501663));
#62300=CARTESIAN_POINT('Ctrl Pts',(-1.39129964730741,1.92080278891465,7.69826790362165));
#62301=CARTESIAN_POINT('Ctrl Pts',(-1.45565033020007,1.87419150589837,7.7036022200081));
#62302=CARTESIAN_POINT('Ctrl Pts',(-1.51758235103075,1.82439636190014,7.70893653639454));
#62303=CARTESIAN_POINT('Ctrl Pts',(-1.57678092364827,1.77171103211526,7.71427085278099));
#62304=CARTESIAN_POINT('Ctrl Pts',(-1.62943795758635,1.72484751706995,7.71901571851978));
#62305=CARTESIAN_POINT('Ctrl Pts',(-1.67993261919358,1.67569797999556,7.72376058425856));
#62306=CARTESIAN_POINT('Ctrl Pts',(-1.72806968829886,1.62449167892072,7.72850544999735));
#62307=CARTESIAN_POINT('Ctrl Pts',(-1.78152787162293,1.56762498800901,7.73377481739396));
#62308=CARTESIAN_POINT('Ctrl Pts',(-1.83228762165757,1.50799773269415,7.73904418479058));
#62309=CARTESIAN_POINT('Ctrl Pts',(-1.88004585703971,1.44589959469108,7.74431355218719));
#62310=CARTESIAN_POINT('Ctrl Pts',(-1.92774098637691,1.38388351097364,7.7495759568279));
#62311=CARTESIAN_POINT('Ctrl Pts',(-1.97244217725324,1.31940339730663,7.7548383614686));
#62312=CARTESIAN_POINT('Ctrl Pts',(-2.01388372529189,1.25278505878083,7.7601007661093));
#62313=CARTESIAN_POINT('Ctrl Pts',(-2.05528415322878,1.1862328218605,7.76535794916383));
#62314=CARTESIAN_POINT('Ctrl Pts',(-2.0934311035362,1.11754697568823,7.77061513221836));
#62315=CARTESIAN_POINT('Ctrl Pts',(-2.12810067786589,1.04708431721937,7.77587231527289));
#62316=CARTESIAN_POINT('Ctrl Pts',(-2.16275317801482,0.976656360421645,
7.78112690925342));
#62317=CARTESIAN_POINT('Ctrl Pts',(-2.19393148153228,0.90445375435945,7.78638150323394));
#62318=CARTESIAN_POINT('Ctrl Pts',(-2.22145711368449,0.830858805430019,
7.79163609721447));
#62319=CARTESIAN_POINT('Ctrl Pts',(-2.24897367615864,0.757288105988838,
7.79688895980966));
#62320=CARTESIAN_POINT('Ctrl Pts',(-2.27283979226548,0.682326426055847,
7.80214182240485));
#62321=CARTESIAN_POINT('Ctrl Pts',(-2.29292544290108,0.606375276373366,
7.80739468500005));
#62322=CARTESIAN_POINT('Ctrl Pts',(-2.31302103634047,0.530386529333843,
7.81265014786859));
#62323=CARTESIAN_POINT('Ctrl Pts',(-2.32933230031485,0.453407798864271,
7.81790561073714));
#62324=CARTESIAN_POINT('Ctrl Pts',(-2.34177963671045,0.375853955131875,
7.82316107360568));
#62325=CARTESIAN_POINT('Ctrl Pts',(-2.35258402000454,0.308536624983187,
7.82772285561389));
#62326=CARTESIAN_POINT('Ctrl Pts',(-2.3604779488569,0.240786368979323,7.8322846376221));
#62327=CARTESIAN_POINT('Ctrl Pts',(-2.36544101854889,0.172878137039867,
7.83684641963031));
#62328=CARTESIAN_POINT('Ctrl Pts',(-2.36285989125428,0.172707701180992,
6.83708460818679));
#62329=CARTESIAN_POINT('Ctrl Pts',(-2.3666403501721,0.115542394696668,6.84091943817652));
#62330=CARTESIAN_POINT('Ctrl Pts',(-2.36843179856191,0.0582097310194607,
6.84475426816626));
#62331=CARTESIAN_POINT('Ctrl Pts',(-2.36824492703387,0.000864939883196495,
6.848589098156));
#62332=CARTESIAN_POINT('Ctrl Pts',(-2.36544101887183,0.172878132621275,
6.64182320144908));
#62333=CARTESIAN_POINT('Ctrl Pts',(-2.3696028942636,0.115932406647306,6.6455115724124));
#62334=CARTESIAN_POINT('Ctrl Pts',(-2.3717078335312,0.0588440556893744,
6.649117014029));
#62335=CARTESIAN_POINT('Ctrl Pts',(-2.37182241343598,-0.0987107308918925,
6.6589457848745));
#62336=CARTESIAN_POINT('Ctrl Pts',(-2.36551574960962,-0.199052636883313,
6.66507245937646));
#62337=CARTESIAN_POINT('Ctrl Pts',(-2.33549906223717,-0.435498516360033,
6.6797348662378));
#62338=CARTESIAN_POINT('Ctrl Pts',(-2.30623659196225,-0.570509188646735,
6.68830004755357));
#62339=CARTESIAN_POINT('Ctrl Pts',(-2.25715959474339,-0.728838943472387,
6.69905632790079));
#62340=CARTESIAN_POINT('Ctrl Pts',(-2.24843486114649,-0.755325235666134,
6.70087968329226));
#62341=CARTESIAN_POINT('Ctrl Pts',(-2.2337829333825,-0.797299564727317,
6.7038108446944));
#62342=CARTESIAN_POINT('Ctrl Pts',(-2.22815662326822,-0.812890415955453,
6.70490885260466));
#62343=CARTESIAN_POINT('Ctrl Pts',(-2.21716565087573,-0.842375410527281,
6.70700366143278));
#62344=CARTESIAN_POINT('Ctrl Pts',(-2.21183260335262,-0.856280545869361,
6.70799938017444));
#62345=CARTESIAN_POINT('Ctrl Pts',(-2.19934361038919,-0.887948448863229,
6.7102854209587));
#62346=CARTESIAN_POINT('Ctrl Pts',(-2.19210285774203,-0.905676425964556,
6.71157850500284));
#62347=CARTESIAN_POINT('Ctrl Pts',(-2.16872901781536,-0.960981125305863,
6.71565551079747));
#62348=CARTESIAN_POINT('Ctrl Pts',(-2.1518390454007,-0.998227751475453,
6.71846439584239));
#62349=CARTESIAN_POINT('Ctrl Pts',(-2.0838998956203,-1.13830449049972,6.72927701819808));
#62350=CARTESIAN_POINT('Ctrl Pts',(-2.02637815012396,-1.23780500804915,
6.73748938227872));
#62351=CARTESIAN_POINT('Ctrl Pts',(-1.88448336932091,-1.44668425086851,
6.75581480762632));
#62352=CARTESIAN_POINT('Ctrl Pts',(-1.79729884355684,-1.55367030911945,
6.76594959572496));
#62353=CARTESIAN_POINT('Ctrl Pts',(-1.66966416242216,-1.68507682140923,
6.77900317946093));
#62354=CARTESIAN_POINT('Ctrl Pts',(-1.63707618817158,-1.71675405646577,
6.78220163287787));
#62355=CARTESIAN_POINT('Ctrl Pts',(-1.59304679130593,-1.75715821104158,
6.78632873058291));
#62356=CARTESIAN_POINT('Ctrl Pts',(-1.58240993682746,-1.76674329627262,
6.78731148563113));
#62357=CARTESIAN_POINT('Ctrl Pts',(-1.56497805070622,-1.78216778236279,
6.7888980762533));
#62358=CARTESIAN_POINT('Ctrl Pts',(-1.55823577411518,-1.78806587759391,
6.78950601099475));
#62359=CARTESIAN_POINT('Ctrl Pts',(-1.54487658720046,-1.79961944690007,
6.79069906659249));
#62360=CARTESIAN_POINT('Ctrl Pts',(-1.53826169253364,-1.80527692966612,
6.79128431618931));
#62361=CARTESIAN_POINT('Ctrl Pts',(-1.52158884797871,-1.81937843692709,
6.79274613828125));
#62362=CARTESIAN_POINT('Ctrl Pts',(-1.51149144480041,-1.82777573864787,
6.79361943816486));
#62363=CARTESIAN_POINT('Ctrl Pts',(-1.47125703817624,-1.86067441761021,
6.79705441129358));
#62364=CARTESIAN_POINT('Ctrl Pts',(-1.44058811093905,-1.88451926582055,
6.79957442141113));
#62365=CARTESIAN_POINT('Ctrl Pts',(-1.3555449256559,-1.94734958384348,6.80634203326719));
#62366=CARTESIAN_POINT('Ctrl Pts',(-1.30008328969004,-1.98480656522978,
6.81052051454161));
#62367=CARTESIAN_POINT('Ctrl Pts',(-1.10981909712928,-2.1019027092626,6.82434498460179));
#62368=CARTESIAN_POINT('Ctrl Pts',(-0.968741844165485,-2.17053725949386,
6.83380780514352));
#62369=CARTESIAN_POINT('Ctrl Pts',(-0.758149723052398,-2.24833952044726,
6.84794352022592));
#62370=CARTESIAN_POINT('Ctrl Pts',(-0.693388028410569,-2.26914815654295,
6.8522872965909));
#62371=CARTESIAN_POINT('Ctrl Pts',(-0.604934630307132,-2.29342880016947,
6.85826705130769));
#62372=CARTESIAN_POINT('Ctrl Pts',(-0.581950793738913,-2.29936834284573,
6.85982488139079));
#62373=CARTESIAN_POINT('Ctrl Pts',(-0.543625745317512,-2.30866098842447,
6.86243112964569));
#62374=CARTESIAN_POINT('Ctrl Pts',(-0.528333121618525,-2.31220859854863,
6.86347333685002));
#62375=CARTESIAN_POINT('Ctrl Pts',(-0.498124045824823,-2.31890121876107,
6.86553707858791));
#62376=CARTESIAN_POINT('Ctrl Pts',(-0.483210246131083,-2.32205475106376,
6.86655828832828));
#62377=CARTESIAN_POINT('Ctrl Pts',(-0.44727151231933,-2.32929280336112,
6.86902534493162));
#62378=CARTESIAN_POINT('Ctrl Pts',(-0.426219949576982,-2.33323665160871,
6.87047552616544));
#62379=CARTESIAN_POINT('Ctrl Pts',(-0.350850603343726,-2.3463024998168,
6.87568710122809));
#62380=CARTESIAN_POINT('Ctrl Pts',(-0.29627569461842,-2.3538163539585,6.87949752965821));
#62381=CARTESIAN_POINT('Ctrl Pts',(-0.156647771769953,-2.3681075898587,
6.88934496853297));
#62382=CARTESIAN_POINT('Ctrl Pts',(-0.0714042844503148,-2.37220805810313,
6.89545131762471));
#62383=CARTESIAN_POINT('Ctrl Pts',(0.0938088628072688,-2.37124202659616,
6.90741669484149));
#62384=CARTESIAN_POINT('Ctrl Pts',(0.173673970260044,-2.36673313615369,
6.91325942787623));
#62385=CARTESIAN_POINT('Ctrl Pts',(0.359484437566331,-2.34678607061269,
6.92686391936632));
#62386=CARTESIAN_POINT('Ctrl Pts',(0.464930602485518,-2.32819210286688,
6.93459460465086));
#62387=CARTESIAN_POINT('Ctrl Pts',(0.585450773473143,-2.29842133445283,
6.94320921632534));
#62388=CARTESIAN_POINT('Ctrl Pts',(0.602085472828304,-2.29411995423426,
6.94439310884151));
#62389=CARTESIAN_POINT('Ctrl Pts',(0.628018514899812,-2.28711270642982,
6.94622919340903));
#62390=CARTESIAN_POINT('Ctrl Pts',(0.637349143619226,-2.28453011894731,
6.94688786126991));
#62391=CARTESIAN_POINT('Ctrl Pts',(0.653927657307026,-2.27983194138786,
6.94805437885535));
#62392=CARTESIAN_POINT('Ctrl Pts',(0.661181370154349,-2.27773884806067,
6.94856344561814));
#62393=CARTESIAN_POINT('Ctrl Pts',(0.678792133937286,-2.27256596069434,
6.94979628319067));
#62394=CARTESIAN_POINT('Ctrl Pts',(0.689138306711379,-2.26944998010988,
6.9505179912615));
#62395=CARTESIAN_POINT('Ctrl Pts',(0.721757411035039,-2.25938236855589,
6.95278628826473));
#62396=CARTESIAN_POINT('Ctrl Pts',(0.743950017063917,-2.25217248865375,
6.95431906506496));
#62397=CARTESIAN_POINT('Ctrl Pts',(0.796770387086757,-2.23414632356999,
6.95795013535149));
#62398=CARTESIAN_POINT('Ctrl Pts',(0.827290014210964,-2.22302593013655,
6.96003428440339));
#62399=CARTESIAN_POINT('Ctrl Pts',(0.945934746429238,-2.17701346200874,
6.96811683093034));
#62400=CARTESIAN_POINT('Ctrl Pts',(1.03216932058011,-2.13747728404483,6.9739510531906));
#62401=CARTESIAN_POINT('Ctrl Pts',(1.26242978010615,-2.01471497116616,6.98998226599722));
#62402=CARTESIAN_POINT('Ctrl Pts',(1.4004118987679,-1.92136528535204,7.00014274218385));
#62403=CARTESIAN_POINT('Ctrl Pts',(1.55100694858399,-1.79458061730114,7.01284075786388));
#62404=CARTESIAN_POINT('Ctrl Pts',(1.5741243849488,-1.77433774417279,7.01483898618652));
#62405=CARTESIAN_POINT('Ctrl Pts',(1.61086944380141,-1.74087841552257,7.01810031701388));
#62406=CARTESIAN_POINT('Ctrl Pts',(1.62474351091385,-1.72793706828704,7.0193521349625));
#62407=CARTESIAN_POINT('Ctrl Pts',(1.64921414687152,-1.704556238788,7.02159783301899));
#62408=CARTESIAN_POINT('Ctrl Pts',(1.65987069285566,-1.6941807871086,7.02258895972179));
#62409=CARTESIAN_POINT('Ctrl Pts',(1.68226652790765,-1.67196155944354,7.02470054566282));
#62410=CARTESIAN_POINT('Ctrl Pts',(1.69397985287178,-1.66009287719607,7.02582206058283));
#62411=CARTESIAN_POINT('Ctrl Pts',(1.72527231413255,-1.62770933203581,7.02886562047749));
#62412=CARTESIAN_POINT('Ctrl Pts',(1.74460973630826,-1.60696576684072,7.03079775985279));
#62413=CARTESIAN_POINT('Ctrl Pts',(1.87108150618424,-1.46632357893424,7.04378872692781));
#62414=CARTESIAN_POINT('Ctrl Pts',(1.96613768300477,-1.33616463509958,7.05533702008942));
#62415=CARTESIAN_POINT('Ctrl Pts',(2.12034581783549,-1.0725075358376,7.07758578855422));
#62416=CARTESIAN_POINT('Ctrl Pts',(2.18182507985484,-0.941161387785913,
7.0881991744085));
#62417=CARTESIAN_POINT('Ctrl Pts',(2.23841745355933,-0.78432733609461,7.09983793475331));
#62418=CARTESIAN_POINT('Ctrl Pts',(2.2455967817933,-0.763529465914965,7.1013608786973));
#62419=CARTESIAN_POINT('Ctrl Pts',(2.25579114984286,-0.732608882176843,
7.10359190384237));
#62420=CARTESIAN_POINT('Ctrl Pts',(2.25902943875635,-0.722561756086708,
7.10431170247714));
#62421=CARTESIAN_POINT('Ctrl Pts',(2.26470373884189,-0.704545574605662,
7.10559284019789));
#62422=CARTESIAN_POINT('Ctrl Pts',(2.26716494702284,-0.696584955734328,
7.10615556269561));
#62423=CARTESIAN_POINT('Ctrl Pts',(2.27255588861011,-0.678817022944849,
7.10740408249667));
#62424=CARTESIAN_POINT('Ctrl Pts',(2.27546414251413,-0.669003559961076,
7.10808866458126));
#62425=CARTESIAN_POINT('Ctrl Pts',(2.28396520799075,-0.639621135265913,
7.11012433346575));
#62426=CARTESIAN_POINT('Ctrl Pts',(2.28936992662831,-0.61999812442002,7.11146532127249));
#62427=CARTESIAN_POINT('Ctrl Pts',(2.32739653088577,-0.474651097669245,
7.12127826543412));
#62428=CARTESIAN_POINT('Ctrl Pts',(2.34989833898823,-0.346489452995756,
7.12928008233079));
#62429=CARTESIAN_POINT('Ctrl Pts',(2.37720545198774,-0.0494414544196821,
7.14760929545741));
#62430=CARTESIAN_POINT('Ctrl Pts',(2.37471928981639,0.119378172044436,7.15789767836298));
#62431=CARTESIAN_POINT('Ctrl Pts',(2.35068326201323,0.316896903420457,7.1707336660732));
#62432=CARTESIAN_POINT('Ctrl Pts',(2.34639679030516,0.347213785266757,7.17272495750371));
#62433=CARTESIAN_POINT('Ctrl Pts',(2.33851055651111,0.396137861007947,7.17597722197912));
#62434=CARTESIAN_POINT('Ctrl Pts',(2.33527246206423,0.414800339368095,7.17722701539976));
#62435=CARTESIAN_POINT('Ctrl Pts',(2.32909389986666,0.448041047810954,7.17947048015268));
#62436=CARTESIAN_POINT('Ctrl Pts',(2.32623916086342,0.462634331164522,7.18046141939979));
#62437=CARTESIAN_POINT('Ctrl Pts',(2.31988861408223,0.493551988515321,7.18257409584109));
#62438=CARTESIAN_POINT('Ctrl Pts',(2.31635730883444,0.509868159939565,7.18369690267167));
#62439=CARTESIAN_POINT('Ctrl Pts',(2.30634384967794,0.553881982349753,7.18674776940844));
#62440=CARTESIAN_POINT('Ctrl Pts',(2.29953533989399,0.581501765347872,7.18868600717747));
#62441=CARTESIAN_POINT('Ctrl Pts',(2.25081620746351,0.764879642677311,7.20171904912304));
#62442=CARTESIAN_POINT('Ctrl Pts',(2.19361389118331,0.916108566889364,7.21330647354243));
#62443=CARTESIAN_POINT('Ctrl Pts',(2.05720142096442,1.18904290086975,7.23553349990947));
#62444=CARTESIAN_POINT('Ctrl Pts',(1.98129183426437,1.31163636877934,7.24608424605006));
#62445=CARTESIAN_POINT('Ctrl Pts',(1.88143878534284,1.44425572347289,7.25767378523139));
#62446=CARTESIAN_POINT('Ctrl Pts',(1.86789863484344,1.4617254441259,7.25920382494491));
#62447=CARTESIAN_POINT('Ctrl Pts',(1.84752129772089,1.48727097199259,7.2614431590431));
#62448=CARTESIAN_POINT('Ctrl Pts',(1.84087154258191,1.49549385288059,7.26216429222363));
#62449=CARTESIAN_POINT('Ctrl Pts',(1.82888380371679,1.51011639737894,7.26344681150377));
#62450=CARTESIAN_POINT('Ctrl Pts',(1.82356685908338,1.51653269592234,7.26400959474538));
#62451=CARTESIAN_POINT('Ctrl Pts',(1.81165494779065,1.53075432965639,7.26525704861679));
#62452=CARTESIAN_POINT('Ctrl Pts',(1.80504325576535,1.53854519660589,7.26594051651285));
#62453=CARTESIAN_POINT('Ctrl Pts',(1.78516852306887,1.56166005310812,7.2679694303066));
#62454=CARTESIAN_POINT('Ctrl Pts',(1.7717588243932,1.57685747988189,7.26930487642771));
#62455=CARTESIAN_POINT('Ctrl Pts',(1.67651827873663,1.68204599781137,7.27857420177716));
#62456=CARTESIAN_POINT('Ctrl Pts',(1.58805513640682,1.76580880417996,7.28609653806636));
#62457=CARTESIAN_POINT('Ctrl Pts',(1.35522057316574,1.95455429770869,7.30452970151637));
#62458=CARTESIAN_POINT('Ctrl Pts',(1.20472447806156,2.05074054312495,7.31537289045612));
#62459=CARTESIAN_POINT('Ctrl Pts',(1.01802605995908,2.14236235361175,7.32879829177989));
#62460=CARTESIAN_POINT('Ctrl Pts',(0.990916385407184,2.15503552248849,7.33074558170127));
#62461=CARTESIAN_POINT('Ctrl Pts',(0.946451114429461,2.17480563504929,7.33394029118139));
#62462=CARTESIAN_POINT('Ctrl Pts',(0.929237882064308,2.18221588932124,7.33517718633303));
#62463=CARTESIAN_POINT('Ctrl Pts',(0.898230569055258,2.1951310740017,7.33740651521236));
#62464=CARTESIAN_POINT('Ctrl Pts',(0.884469043556387,2.20071194872723,7.33839635258057));
#62465=CARTESIAN_POINT('Ctrl Pts',(0.855012935228019,2.21233672179498,7.34051642941176));
#62466=CARTESIAN_POINT('Ctrl Pts',(0.839304728604938,2.21834362477832,7.34164783037931));
#62467=CARTESIAN_POINT('Ctrl Pts',(0.796311002216604,2.23426264372641,7.34474740083008));
#62468=CARTESIAN_POINT('Ctrl Pts',(0.768906020756085,2.24384138840245,7.34672631188091));
#62469=CARTESIAN_POINT('Ctrl Pts',(0.589652009753747,2.3028258492445,7.35969626420056));
#62470=CARTESIAN_POINT('Ctrl Pts',(0.433345000726604,2.33728291154694,7.37116771494721));
#62471=CARTESIAN_POINT('Ctrl Pts',(0.131213378561963,2.37252530053532,7.39332478450898));
#62472=CARTESIAN_POINT('Ctrl Pts',(-0.0136061789618504,2.37611337086567,
7.40392620990931));
#62473=CARTESIAN_POINT('Ctrl Pts',(-0.179829903316131,2.36502517623719,
7.41555551566093));
#62474=CARTESIAN_POINT('Ctrl Pts',(-0.201779121588205,2.36325372100239,
7.41707976194162));
#62475=CARTESIAN_POINT('Ctrl Pts',(-0.234213596287553,2.36018083023182,
7.41931231241066));
#62476=CARTESIAN_POINT('Ctrl Pts',(-0.244719247619747,2.35911467726927,
7.42003235626606));
#62477=CARTESIAN_POINT('Ctrl Pts',(-0.263501796326132,2.35708173308941,
7.42131374755409));
#62478=CARTESIAN_POINT('Ctrl Pts',(-0.27178108341004,2.35614145203311,7.42187648092241));
#62479=CARTESIAN_POINT('Ctrl Pts',(-0.290215911158583,2.35394933627779,
7.42312480357085));
#62480=CARTESIAN_POINT('Ctrl Pts',(-0.300368469263164,2.35267540156487,
7.42380917993586));
#62481=CARTESIAN_POINT('Ctrl Pts',(-0.330673815942261,2.34867333812875,
7.42584360067606));
#62482=CARTESIAN_POINT('Ctrl Pts',(-0.350800678673438,2.3457516008146,7.4271835644265));
#62483=CARTESIAN_POINT('Ctrl Pts',(-0.497668738454781,2.32249867215093,
7.43689602851683));
#62484=CARTESIAN_POINT('Ctrl Pts',(-0.622627905629938,2.29216434121425,
7.44480949288075));
#62485=CARTESIAN_POINT('Ctrl Pts',(-0.905971725192098,2.19848255461361,
7.46314905448098));
#62486=CARTESIAN_POINT('Ctrl Pts',(-1.06118657362328,2.1279064789699,7.47353213792594));
#62487=CARTESIAN_POINT('Ctrl Pts',(-1.2338205645033,2.02578845683034,7.48647204132157));
#62488=CARTESIAN_POINT('Ctrl Pts',(-1.25982027544244,2.00972256693065,7.48845981518635));
#62489=CARTESIAN_POINT('Ctrl Pts',(-1.30140558394444,1.98290184534547,7.49170748152236));
#62490=CARTESIAN_POINT('Ctrl Pts',(-1.31718603580137,1.97245459647306,7.49295624740771));
#62491=CARTESIAN_POINT('Ctrl Pts',(-1.34458946251215,1.95383700182474,7.49515459183675));
#62492=CARTESIAN_POINT('Ctrl Pts',(-1.35626734123795,1.94574888838764,7.49610107924194));
#62493=CARTESIAN_POINT('Ctrl Pts',(-1.38102182846849,1.92827277290675,7.49812857621854));
#62494=CARTESIAN_POINT('Ctrl Pts',(-1.39407686900362,1.91885560657373,7.49921065641467));
#62495=CARTESIAN_POINT('Ctrl Pts',(-1.42066314855186,1.89926324663761,7.50144123238396));
#62496=CARTESIAN_POINT('Ctrl Pts',(-1.43418329336556,1.88907461927215,7.50259020258912));
#62497=CARTESIAN_POINT('Ctrl Pts',(-1.49569639889367,1.84167805341126,7.50788628647372));
#62498=CARTESIAN_POINT('Ctrl Pts',(-1.54235459523769,1.80278310986801,7.51209819253961));
#62499=CARTESIAN_POINT('Ctrl Pts',(-1.66120912669775,1.69571040312451,7.52336172220979));
#62500=CARTESIAN_POINT('Ctrl Pts',(-1.73070257644153,1.62471986270786,7.53051189332773));
#62501=CARTESIAN_POINT('Ctrl Pts',(-1.90003827368715,1.42850765006668,7.54936016177648));
#62502=CARTESIAN_POINT('Ctrl Pts',(-1.99202732439295,1.29715600336247,7.56113686158805));
#62503=CARTESIAN_POINT('Ctrl Pts',(-2.08023707081611,1.1394048306588,7.57373487372417));
#62504=CARTESIAN_POINT('Ctrl Pts',(-2.09013782533608,1.12113941259399,7.57517132401714));
#62505=CARTESIAN_POINT('Ctrl Pts',(-2.10459530074865,1.09361014734234,7.57730071914553));
#62506=CARTESIAN_POINT('Ctrl Pts',(-2.10933334190351,1.08444335811109,7.5780039462687));
#62507=CARTESIAN_POINT('Ctrl Pts',(-2.11778819313102,1.06782050400462,7.5792682793152));
#62508=CARTESIAN_POINT('Ctrl Pts',(-2.12152567489906,1.0603755352024,7.57983059687707));
#62509=CARTESIAN_POINT('Ctrl Pts',(-2.12987011299709,1.04353289006254,7.58109389960709));
#62510=CARTESIAN_POINT('Ctrl Pts',(-2.13445417226877,1.03412426119809,7.58179350300568));
#62511=CARTESIAN_POINT('Ctrl Pts',(-2.14827750379485,1.0052687961514,7.58392146781022));
#62512=CARTESIAN_POINT('Ctrl Pts',(-2.15731468306736,0.98572563264348,7.58533832636668));
#62513=CARTESIAN_POINT('Ctrl Pts',(-2.20169701805067,0.886212377915345,
7.59244386638894));
#62514=CARTESIAN_POINT('Ctrl Pts',(-2.2328705999432,0.80444654839222,7.59793024137301));
#62515=CARTESIAN_POINT('Ctrl Pts',(-2.31627508780185,0.54312473178222,7.614921824028));
#62516=CARTESIAN_POINT('Ctrl Pts',(-2.35183113479429,0.359098203816666,
7.62616644971573));
#62517=CARTESIAN_POINT('Ctrl Pts',(-2.36544101891311,0.172878132056388,
7.63807246982441));
#62518=CARTESIAN_POINT('Origin',(0.,0.,-1.84858989190501));
#62519=CARTESIAN_POINT('',(-2.36544101854848,0.172878137045581,8.83481520889907));
#62520=CARTESIAN_POINT('',(-2.36544103037033,0.172877975290513,8.63916402106918));
#62521=CARTESIAN_POINT('',(-2.36544101854889,0.172878137039864,-1.84858989190501));
#62522=CARTESIAN_POINT('',(-2.37174905777015,-0.00211411125499902,7.84858989190503));
#62523=CARTESIAN_POINT('Ctrl Pts',(-2.36544101854848,0.172878137045581,
8.83481520889907));
#62524=CARTESIAN_POINT('Ctrl Pts',(-2.36522450343307,0.175840650084406,
8.83461214175899));
#62525=CARTESIAN_POINT('Ctrl Pts',(-2.3650024209695,0.178802782450663,8.83440935971078));
#62526=CARTESIAN_POINT('Ctrl Pts',(-2.36410014521746,0.190541481262514,
8.83360679734256));
#62527=CARTESIAN_POINT('Ctrl Pts',(-2.3633766456752,0.199314800527096,8.83300929497062));
#62528=CARTESIAN_POINT('Ctrl Pts',(-2.36186181322496,0.216514337868644,
8.83184274600605));
#62529=CARTESIAN_POINT('Ctrl Pts',(-2.36107420171444,0.224940660154587,
8.83127352558446));
#62530=CARTESIAN_POINT('Ctrl Pts',(-2.3590011093727,0.245908015463755,8.82986243955776));
#62531=CARTESIAN_POINT('Ctrl Pts',(-2.35766068704253,0.25844358802887,8.82902354076649));
#62532=CARTESIAN_POINT('Ctrl Pts',(-2.35210421230338,0.306760246587437,
8.82580633671276));
#62533=CARTESIAN_POINT('Ctrl Pts',(-2.34717280660752,0.342456162550787,
8.82346384134261));
#62534=CARTESIAN_POINT('Ctrl Pts',(-2.33185541045421,0.437329024720731,
8.81729671325565));
#62535=CARTESIAN_POINT('Ctrl Pts',(-2.32003109877927,0.496248920226127,
8.81352787248409));
#62536=CARTESIAN_POINT('Ctrl Pts',(-2.27120500380131,0.699241929876785,
8.80056570211307));
#62537=CARTESIAN_POINT('Ctrl Pts',(-2.22290870527848,0.840231695052893,
8.79158212610435));
#62538=CARTESIAN_POINT('Ctrl Pts',(-2.12739746066221,1.05182749343225,8.77707835176978));
#62539=CARTESIAN_POINT('Ctrl Pts',(-2.08908072762203,1.1260108944087,8.77178389100937));
#62540=CARTESIAN_POINT('Ctrl Pts',(-2.03420015004174,1.21978020202948,8.76471440933066));
#62541=CARTESIAN_POINT('Ctrl Pts',(-2.02111635563053,1.2413390310197,8.76306202687768));
#62542=CARTESIAN_POINT('Ctrl Pts',(-1.99929622471128,1.27603344259689,8.76035625467828));
#62543=CARTESIAN_POINT('Ctrl Pts',(-1.99076800753314,1.28929804965762,8.75931044418509));
#62544=CARTESIAN_POINT('Ctrl Pts',(-1.97404845384651,1.31474186374438,8.7572818596292));
#62545=CARTESIAN_POINT('Ctrl Pts',(-1.96587507144712,1.32693204549555,8.7562997824317));
#62546=CARTESIAN_POINT('Ctrl Pts',(-1.94651621994868,1.35523331184055,8.75399538133016));
#62547=CARTESIAN_POINT('Ctrl Pts',(-1.93524313552712,1.37128286311329,8.75266981477617));
#62548=CARTESIAN_POINT('Ctrl Pts',(-1.89740250655503,1.42376071119182,8.74827203217096));
#62549=CARTESIAN_POINT('Ctrl Pts',(-1.86999666409134,1.45956940107746,8.74516826388431));
#62550=CARTESIAN_POINT('Ctrl Pts',(-1.80111860798629,1.54443980171655,8.73755276639764));
#62551=CARTESIAN_POINT('Ctrl Pts',(-1.75864311121558,1.59263798907632,8.7330053506173));
#62552=CARTESIAN_POINT('Ctrl Pts',(-1.64557086036521,1.7108992094521,8.72127702110117));
#62553=CARTESIAN_POINT('Ctrl Pts',(-1.57242868832636,1.77835471967077,8.71402651703346));
#62554=CARTESIAN_POINT('Ctrl Pts',(-1.47481048283427,1.85764021923475,8.70485691316441));
#62555=CARTESIAN_POINT('Ctrl Pts',(-1.45406980998814,1.87391946285739,8.7029358044755));
#62556=CARTESIAN_POINT('Ctrl Pts',(-1.3557057095739,1.94850838306494,8.69396148001873));
#62557=CARTESIAN_POINT('Ctrl Pts',(-1.27481196478586,2.00236896616912,8.68696818903353));
#62558=CARTESIAN_POINT('Ctrl Pts',(-1.17625706659223,2.05958771732764,8.67906281579098));
#62559=CARTESIAN_POINT('Ctrl Pts',(-1.1615877440449,2.06789656535271,8.67790146167291));
#62560=CARTESIAN_POINT('Ctrl Pts',(-1.13853212877622,2.08063272412531,8.67610139985186));
#62561=CARTESIAN_POINT('Ctrl Pts',(-1.13020609757778,2.0851671697375,8.67545642272779));
#62562=CARTESIAN_POINT('Ctrl Pts',(-1.11535786594808,2.09313860933563,8.6743154938278));
#62563=CARTESIAN_POINT('Ctrl Pts',(-1.10884673773102,2.09659517347276,8.67381836019959));
#62564=CARTESIAN_POINT('Ctrl Pts',(-1.09302327933246,2.10490104278499,8.67261777377626));
#62565=CARTESIAN_POINT('Ctrl Pts',(-1.08369472387583,2.10971894925435,8.67191625622493));
#62566=CARTESIAN_POINT('Ctrl Pts',(-1.0543273968431,2.12464006572886,8.66972645354584));
#62567=CARTESIAN_POINT('Ctrl Pts',(-1.03417637749854,2.13452125256227,8.66825093983201));
#62568=CARTESIAN_POINT('Ctrl Pts',(-0.925577947587826,2.18587416356705,
8.66042679686366));
#62569=CARTESIAN_POINT('Ctrl Pts',(-0.834762813857075,2.22214213612493,
8.6543308583523));
#62570=CARTESIAN_POINT('Ctrl Pts',(-0.573882021064348,2.30806681387092,
8.63737705458315));
#62571=CARTESIAN_POINT('Ctrl Pts',(-0.400148476741573,2.34443827029624,
8.62668175452108));
#62572=CARTESIAN_POINT('Ctrl Pts',(-0.177424114017925,2.36556684892325,
8.61240698104738));
#62573=CARTESIAN_POINT('Ctrl Pts',(-0.130741758282932,2.36860548953888,
8.60938773498955));
#62574=CARTESIAN_POINT('Ctrl Pts',(-0.0655818506414271,2.3709147658194,
8.60512013221767));
#62575=CARTESIAN_POINT('Ctrl Pts',(-0.0471547398900403,2.37135282172969,
8.60390737059215));
#62576=CARTESIAN_POINT('Ctrl Pts',(-0.0151360867046855,2.37174063545921,
8.60178896826439));
#62577=CARTESIAN_POINT('Ctrl Pts',(-0.00154644273461836,2.37178842618969,
8.60088637745654));
#62578=CARTESIAN_POINT('Ctrl Pts',(0.0268937806436004,2.3716440182913,8.59898979918228));
#62579=CARTESIAN_POINT('Ctrl Pts',(0.0417436014420987,2.37142912176135,
8.59799515139003));
#62580=CARTESIAN_POINT('Ctrl Pts',(0.0772498838415376,2.37058169782121,
8.5956060241282));
#62581=CARTESIAN_POINT('Ctrl Pts',(0.0979017153081718,2.36981862981113,
8.59420758135082));
#62582=CARTESIAN_POINT('Ctrl Pts',(0.170298611195169,2.36619569516256,8.58927283794836));
#62583=CARTESIAN_POINT('Ctrl Pts',(0.221954290254871,2.36191008797139,8.585693378759));
#62584=CARTESIAN_POINT('Ctrl Pts',(0.351239397644735,2.34690553736394,8.57658206813842));
#62585=CARTESIAN_POINT('Ctrl Pts',(0.428551784349948,2.3340257277654,8.5709928118362));
#62586=CARTESIAN_POINT('Ctrl Pts',(0.593272769837011,2.29812381549023,8.55881752016145));
#62587=CARTESIAN_POINT('Ctrl Pts',(0.68029485049825,2.27388294270118,8.55221817955544));
#62588=CARTESIAN_POINT('Ctrl Pts',(0.868812085910096,2.20957647639467,8.53771182038727));
#62589=CARTESIAN_POINT('Ctrl Pts',(0.969370758663379,2.1673458932066,8.52983184972568));
#62590=CARTESIAN_POINT('Ctrl Pts',(1.08182285689192,2.11072140477582,8.52109675662066));
#62591=CARTESIAN_POINT('Ctrl Pts',(1.09688488749237,2.10293345747359,8.51992856855779));
#62592=CARTESIAN_POINT('Ctrl Pts',(1.12025595959787,2.09052982246708,8.5181202418336));
#62593=CARTESIAN_POINT('Ctrl Pts',(1.1286226299633,2.08602476510235,8.51747374462084));
#62594=CARTESIAN_POINT('Ctrl Pts',(1.14342870561117,2.07793723441988,8.51633152052423));
#62595=CARTESIAN_POINT('Ctrl Pts',(1.14987859225252,2.07437498546742,8.51583459577112));
#62596=CARTESIAN_POINT('Ctrl Pts',(1.16545109200853,2.06567939893509,8.5146362979563));
#62597=CARTESIAN_POINT('Ctrl Pts',(1.17455646312786,2.0605156520165,8.51393683935252));
#62598=CARTESIAN_POINT('Ctrl Pts',(1.20292762902248,2.0441769034375,8.51176021252081));
#62599=CARTESIAN_POINT('Ctrl Pts',(1.22207102978549,2.03279034292229,8.51029559819831));
#62600=CARTESIAN_POINT('Ctrl Pts',(1.32290721839901,1.97087318452317,8.50258696973562));
#62601=CARTESIAN_POINT('Ctrl Pts',(1.4016428748682,1.91567897537897,8.49658750066281));
#62602=CARTESIAN_POINT('Ctrl Pts',(1.61153487136253,1.74865468825113,8.48002248623198));
#62603=CARTESIAN_POINT('Ctrl Pts',(1.73416844896571,1.62711248166638,8.46961856041105));
#62604=CARTESIAN_POINT('Ctrl Pts',(1.87511476060403,1.45320853084984,8.45538332487945));
#62605=CARTESIAN_POINT('Ctrl Pts',(1.9063404750766,1.41199709021595,8.45205471097492));
#62606=CARTESIAN_POINT('Ctrl Pts',(1.94843710648818,1.35249411567479,8.44728870621528));
#62607=CARTESIAN_POINT('Ctrl Pts',(1.96044804945538,1.33502467718915,8.44589418158319));
#62608=CARTESIAN_POINT('Ctrl Pts',(1.98044361621967,1.30509010653594,8.44351121409396));
#62609=CARTESIAN_POINT('Ctrl Pts',(1.98854880600868,1.29270674656078,8.44252730817855));
#62610=CARTESIAN_POINT('Ctrl Pts',(2.00476255860354,1.26742152898944,8.44052164388082));
#62611=CARTESIAN_POINT('Ctrl Pts',(2.01286372749634,1.25451578089376,8.43949967509763));
#62612=CARTESIAN_POINT('Ctrl Pts',(2.03270896549492,1.22221374523139,8.43694556304038));
#62613=CARTESIAN_POINT('Ctrl Pts',(2.04430009125479,1.20272575962581,8.43540799964329));
#62614=CARTESIAN_POINT('Ctrl Pts',(2.08917208247737,1.12476004464512,8.42926788902468));
#62615=CARTESIAN_POINT('Ctrl Pts',(2.12023466188495,1.06504863671246,8.42458887911569));
#62616=CARTESIAN_POINT('Ctrl Pts',(2.19888708545887,0.896737495981399,8.41145862750961));
#62617=CARTESIAN_POINT('Ctrl Pts',(2.24093685424168,0.785773114316431,8.40285823962442));
#62618=CARTESIAN_POINT('Ctrl Pts',(2.3114478150972,0.547165774077421,8.38471499241365));
#62619=CARTESIAN_POINT('Ctrl Pts',(2.33801974314791,0.419345989834354,8.3751934093175));
#62620=CARTESIAN_POINT('Ctrl Pts',(2.35671102505075,0.267617134542715,8.36451461947616));
#62621=CARTESIAN_POINT('Ctrl Pts',(2.35914726529833,0.245214310936882,8.36295398526356));
#62622=CARTESIAN_POINT('Ctrl Pts',(2.36225172205368,0.212309792661528,8.36068854443314));
#62623=CARTESIAN_POINT('Ctrl Pts',(2.36316986619369,0.201833694850995,8.35997124610218));
#62624=CARTESIAN_POINT('Ctrl Pts',(2.36467600348764,0.183226396494269,8.35870465200194));
#62625=CARTESIAN_POINT('Ctrl Pts',(2.36529179137303,0.175097864132252,8.35815388969546));
#62626=CARTESIAN_POINT('Ctrl Pts',(2.3665561245411,0.157182576707728,8.35694564274529));
#62627=CARTESIAN_POINT('Ctrl Pts',(2.3671858875695,0.147394827700926,8.35628918294804));
#62628=CARTESIAN_POINT('Ctrl Pts',(2.36885140783511,0.118736026631401,8.35437698533906));
#62629=CARTESIAN_POINT('Ctrl Pts',(2.36972237578679,0.0998556597063659,
8.35312983037368));
#62630=CARTESIAN_POINT('Ctrl Pts',(2.37121207371819,0.0562432340600832,
8.35027389255599));
#62631=CARTESIAN_POINT('Ctrl Pts',(2.37166974445286,0.0315075437582258,
8.34867255753801));
#62632=CARTESIAN_POINT('Ctrl Pts',(2.37191411308031,-0.0541249708904168,
8.34317893529605));
#62633=CARTESIAN_POINT('Ctrl Pts',(2.36974272322408,-0.115006467625612,
8.339360447559));
#62634=CARTESIAN_POINT('Ctrl Pts',(2.35050445200808,-0.373927493967537,
8.32324840626464));
#62635=CARTESIAN_POINT('Ctrl Pts',(2.3109305833944,-0.569466351606306,8.31132645191904));
#62636=CARTESIAN_POINT('Ctrl Pts',(2.23338867465496,-0.799441032081753,
8.29580891030043));
#62637=CARTESIAN_POINT('Ctrl Pts',(2.21818702988349,-0.840700213819528,
8.29296653520742));
#62638=CARTESIAN_POINT('Ctrl Pts',(2.19516774341166,-0.898198042199665,
8.28890975906897));
#62639=CARTESIAN_POINT('Ctrl Pts',(2.18829782121302,-0.914808046156683,
8.28772638639143));
#62640=CARTESIAN_POINT('Ctrl Pts',(2.17541718153855,-0.944975145147703,
8.28555528996647));
#62641=CARTESIAN_POINT('Ctrl Pts',(2.16946679310329,-0.958557121662552,
8.28456962007275));
#62642=CARTESIAN_POINT('Ctrl Pts',(2.15715898200056,-0.985948417582597,
8.28256467815422));
#62643=CARTESIAN_POINT('Ctrl Pts',(2.15079537093093,-0.999754174651041,
8.28154523335808));
#62644=CARTESIAN_POINT('Ctrl Pts',(2.1346863681327,-1.0338366733664,8.27900581621406));
#62645=CARTESIAN_POINT('Ctrl Pts',(2.12478452997909,-1.05403738008532,8.27748055742196));
#62646=CARTESIAN_POINT('Ctrl Pts',(2.08482351369028,-1.13270971422044,8.27145896364283));
#62647=CARTESIAN_POINT('Ctrl Pts',(2.05262829280513,-1.19005715929661,8.266889900931));
#62648=CARTESIAN_POINT('Ctrl Pts',(1.95828903181032,-1.3428559664986,8.25420939913357));
#62649=CARTESIAN_POINT('Ctrl Pts',(1.89159161789649,-1.43528201554369,8.24596182080934));
#62650=CARTESIAN_POINT('Ctrl Pts',(1.73036274840799,-1.62785226054613,8.22765312878666));
#62651=CARTESIAN_POINT('Ctrl Pts',(1.63321534326675,-1.72530352243292,8.2175994000662));
#62652=CARTESIAN_POINT('Ctrl Pts',(1.51114707343403,-1.82814884274172,8.206453115561));
#62653=CARTESIAN_POINT('Ctrl Pts',(1.49392007381084,-1.84225312325041,8.20491158833296));
#62654=CARTESIAN_POINT('Ctrl Pts',(1.46830603961633,-1.86262850934513,8.20266843586979));
#62655=CARTESIAN_POINT('Ctrl Pts',(1.46007256951136,-1.86908953554275,8.20195465282239));
#62656=CARTESIAN_POINT('Ctrl Pts',(1.44535259522795,-1.88048407107331,8.20069178935787));
#62657=CARTESIAN_POINT('Ctrl Pts',(1.43888312655781,-1.8854388933468,8.20014127753173));
#62658=CARTESIAN_POINT('Ctrl Pts',(1.42453876318168,-1.89630808618116,8.19893062469174));
#62659=CARTESIAN_POINT('Ctrl Pts',(1.4166524543515,-1.90220684409439,8.19827153781574));
#62660=CARTESIAN_POINT('Ctrl Pts',(1.39336614327712,-1.91939926654922,8.19634371691687));
#62661=CARTESIAN_POINT('Ctrl Pts',(1.37786579882295,-1.93055656492797,8.19508377983455));
#62662=CARTESIAN_POINT('Ctrl Pts',(1.34170524456011,-1.95592787613369,8.1921936176166));
#62663=CARTESIAN_POINT('Ctrl Pts',(1.32095072354095,-1.97000408928778,8.19057109414517));
#62664=CARTESIAN_POINT('Ctrl Pts',(1.24794922003068,-2.01784290332449,8.18497452303515));
#62665=CARTESIAN_POINT('Ctrl Pts',(1.19459769589462,-2.04987917258099,8.18107727318176));
#62666=CARTESIAN_POINT('Ctrl Pts',(0.955018527770854,-2.18120589196073,
8.16413441409012));
#62667=CARTESIAN_POINT('Ctrl Pts',(0.757300459264175,-2.25747941330803,
8.15148606117072));
#62668=CARTESIAN_POINT('Ctrl Pts',(0.517978059911723,-2.31476302733993,
8.13563367842031));
#62669=CARTESIAN_POINT('Ctrl Pts',(0.483679640576045,-2.32217203166779,
8.13335229361054));
#62670=CARTESIAN_POINT('Ctrl Pts',(0.431516783128349,-2.33223429212277,
8.12986190819428));
#62671=CARTESIAN_POINT('Ctrl Pts',(0.413764709319992,-2.3354490495559,8.12867047352132));
#62672=CARTESIAN_POINT('Ctrl Pts',(0.381691025755587,-2.34088017555615,
8.12651056788367));
#62673=CARTESIAN_POINT('Ctrl Pts',(0.367382370088271,-2.3431684134538,8.12554439898229));
#62674=CARTESIAN_POINT('Ctrl Pts',(0.336626289043042,-2.34779828480732,
8.12346165910674));
#62675=CARTESIAN_POINT('Ctrl Pts',(0.320173509679108,-2.35009849670347,
8.12234384871914));
#62676=CARTESIAN_POINT('Ctrl Pts',(0.274756070910216,-2.35596238905125,
8.11924742589648));
#62677=CARTESIAN_POINT('Ctrl Pts',(0.245748532917796,-2.35916451419739,
8.11725774251436));
#62678=CARTESIAN_POINT('Ctrl Pts',(0.0591210187654135,-2.37628699024479,
8.10437404035668));
#62679=CARTESIAN_POINT('Ctrl Pts',(-0.09947168399798,-2.37493659998389,
8.09300851852358));
#62680=CARTESIAN_POINT('Ctrl Pts',(-0.402375771350924,-2.34195616925058,
8.07081159269121));
#62681=CARTESIAN_POINT('Ctrl Pts',(-0.546258892797123,-2.31263334205272,
8.06005903640391));
#62682=CARTESIAN_POINT('Ctrl Pts',(-0.707295762208248,-2.26393499483603,
8.04831837123785));
#62683=CARTESIAN_POINT('Ctrl Pts',(-0.727980609219806,-2.25736866081363,
8.04681653139063));
#62684=CARTESIAN_POINT('Ctrl Pts',(-0.758403439035173,-2.24724934285205,
8.04461977516528));
#62685=CARTESIAN_POINT('Ctrl Pts',(-0.768212282890147,-2.2439151685677,
8.04391338172618));
#62686=CARTESIAN_POINT('Ctrl Pts',(-0.785692470000997,-2.23784533158747,
8.04265828092084));
#62687=CARTESIAN_POINT('Ctrl Pts',(-0.793371903728572,-2.23513431673883,
8.04210821624337));
#62688=CARTESIAN_POINT('Ctrl Pts',(-0.810390599576168,-2.22902756390045,
8.04089215288714));
#62689=CARTESIAN_POINT('Ctrl Pts',(-0.81972262433329,-2.22561264206116,
8.0402272724433));
#62690=CARTESIAN_POINT('Ctrl Pts',(-0.847337384001219,-2.21531015901738,
8.03826477397155));
#62691=CARTESIAN_POINT('Ctrl Pts',(-0.865557295347477,-2.20825505127425,
8.03697643716299));
#62692=CARTESIAN_POINT('Ctrl Pts',(-0.907659460200483,-2.19135108834415,
8.03400991573589));
#62693=CARTESIAN_POINT('Ctrl Pts',(-0.931472478570623,-2.18133546810302,
8.0323400160753));
#62694=CARTESIAN_POINT('Ctrl Pts',(-1.01478852177506,-2.14467994504452,
8.02650964257522));
#62695=CARTESIAN_POINT('Ctrl Pts',(-1.07335540150549,-2.115976641658,8.02243298681323));
#62696=CARTESIAN_POINT('Ctrl Pts',(-1.31506949936308,-1.98489157082227,
8.00540628000545));
#62697=CARTESIAN_POINT('Ctrl Pts',(-1.48537359650764,-1.86087721654588,
7.99281027195385));
#62698=CARTESIAN_POINT('Ctrl Pts',(-1.65900313125208,-1.69523420656825,
7.97732462592896));
#62699=CARTESIAN_POINT('Ctrl Pts',(-1.68045690164503,-1.673969795345,7.97535959163726));
#62700=CARTESIAN_POINT('Ctrl Pts',(-1.71445780075216,-1.63895655077891,
7.9721560204747));
#62701=CARTESIAN_POINT('Ctrl Pts',(-1.72725982599742,-1.62545919262608,
7.9709284486055));
#62702=CARTESIAN_POINT('Ctrl Pts',(-1.74978451575416,-1.6011444974019,7.96872915234497));
#62703=CARTESIAN_POINT('Ctrl Pts',(-1.75956904977996,-1.59038558099717,
7.96776010198917));
#62704=CARTESIAN_POINT('Ctrl Pts',(-1.78007875157388,-1.56741248460543,
7.96569912445809));
#62705=CARTESIAN_POINT('Ctrl Pts',(-1.79077849484654,-1.55517671617345,
7.96460621675112));
#62706=CARTESIAN_POINT('Ctrl Pts',(-1.81852355427765,-1.52278265416788,
7.96172462349407));
#62707=CARTESIAN_POINT('Ctrl Pts',(-1.83535914732937,-1.50244854579761,
7.9599276204616));
#62708=CARTESIAN_POINT('Ctrl Pts',(-1.92021413417696,-1.39640539046586,
7.95061261952489));
#62709=CARTESIAN_POINT('Ctrl Pts',(-1.98257335796383,-1.3063564356396,7.9428795273893));
#62710=CARTESIAN_POINT('Ctrl Pts',(-2.09630194528895,-1.1151270540726,7.92684681226009));
#62711=CARTESIAN_POINT('Ctrl Pts',(-2.14708599253335,-1.01390836739786,
7.91855684364855));
#62712=CARTESIAN_POINT('Ctrl Pts',(-2.22648796364629,-0.822666879990042,
7.90351253933223));
#62713=CARTESIAN_POINT('Ctrl Pts',(-2.257337138877,-0.733799932419877,7.89675096671677));
#62714=CARTESIAN_POINT('Ctrl Pts',(-2.2873862596507,-0.627171368670858,
7.88906692167713));
#62715=CARTESIAN_POINT('Ctrl Pts',(-2.29176786362082,-0.610966386429781,
7.88791063045272));
#62716=CARTESIAN_POINT('Ctrl Pts',(-2.29835036979,-0.585553766115996,7.88611669392574));
#62717=CARTESIAN_POINT('Ctrl Pts',(-2.30066872901587,-0.576377517269646,
7.88547284490305));
#62718=CARTESIAN_POINT('Ctrl Pts',(-2.30469573223073,-0.560026811119789,
7.88433286964282));
#62719=CARTESIAN_POINT('Ctrl Pts',(-2.30642587166939,-0.55285816260873,
7.88383557346393));
#62720=CARTESIAN_POINT('Ctrl Pts',(-2.31054363709618,-0.535440838022192,
7.88263325517533));
#62721=CARTESIAN_POINT('Ctrl Pts',(-2.31289653340099,-0.525184183039262,
7.88193018399214));
#62722=CARTESIAN_POINT('Ctrl Pts',(-2.3177110549547,-0.503536813787723,
7.88045605554141));
#62723=CARTESIAN_POINT('Ctrl Pts',(-2.32015715841289,-0.49214289625118,
7.87968582548661));
#62724=CARTESIAN_POINT('Ctrl Pts',(-2.32931266135115,-0.447910621972815,
7.87671600705543));
#62725=CARTESIAN_POINT('Ctrl Pts',(-2.33541000664873,-0.414947895937856,
7.87454605676779));
#62726=CARTESIAN_POINT('Ctrl Pts',(-2.36128728269817,-0.256321997131525,
7.86426222955652));
#62727=CARTESIAN_POINT('Ctrl Pts',(-2.3716359730428,-0.12932670716072,7.85649532889853));
#62728=CARTESIAN_POINT('Ctrl Pts',(-2.37174906289902,-0.00210834949801023,
7.84868373744261));
#62729=CARTESIAN_POINT('Ctrl Pts',(-2.36544101854889,0.172878137039867,
7.83684641963031));
#62730=CARTESIAN_POINT('Ctrl Pts',(-2.36969985652205,0.114605701869349,
7.84076091038855));
#62731=CARTESIAN_POINT('Ctrl Pts',(-2.37180105257304,0.0562170784915722,
7.84467540114679));
#62732=CARTESIAN_POINT('Ctrl Pts',(-2.37174905777015,-0.00211411125499902,
7.84858989190503));
#62733=CARTESIAN_POINT('',(-2.37174998736518,0.000244812681607679,7.64926189700123));
#62734=CARTESIAN_POINT('Ctrl Pts',(-2.36544101891311,0.172878132056386,
7.63807246982441));
#62735=CARTESIAN_POINT('Ctrl Pts',(-2.36683982265571,0.153738708748238,
7.63929615294632));
#62736=CARTESIAN_POINT('Ctrl Pts',(-2.36800678971193,0.134576069779931,
7.64052614156132));
#62737=CARTESIAN_POINT('Ctrl Pts',(-2.37008903249588,0.0918295100026025,
7.64328254293788));
#62738=CARTESIAN_POINT('Ctrl Pts',(-2.37088519743952,0.0682495467476106,
7.64481159244682));
#62739=CARTESIAN_POINT('Ctrl Pts',(-2.37160827875137,0.0298577568740206,
7.64731723586861));
#62740=CARTESIAN_POINT('Ctrl Pts',(-2.37174845903576,0.0150512976496863,
7.6482874755401));
#62741=CARTESIAN_POINT('Ctrl Pts',(-2.37174998736518,0.000244812681607679,
7.64926189700123));
#62742=CARTESIAN_POINT('Ctrl Pts',(-2.37174998746501,0.000243843695986532,
7.64926196077062));
#62743=CARTESIAN_POINT('Ctrl Pts',(-2.37175104793131,-0.0100708004041009,
7.64994077228303));
#62744=CARTESIAN_POINT('Ctrl Pts',(-2.37168482144786,-0.0203852376566066,
7.65062159798491));
#62745=CARTESIAN_POINT('Ctrl Pts',(-2.37138670818907,-0.0434151458843365,
7.65214645450117));
#62746=CARTESIAN_POINT('Ctrl Pts',(-2.37111982763709,-0.0561297343481302,
7.65299152717104));
#62747=CARTESIAN_POINT('Ctrl Pts',(-2.37031804331917,-0.0837414902881062,
7.65483402903007));
#62748=CARTESIAN_POINT('Ctrl Pts',(-2.36974492408593,-0.0986369157752481,
7.65583259857848));
#62749=CARTESIAN_POINT('Ctrl Pts',(-2.36804869582846,-0.134033476588653,
7.65821696919595));
#62750=CARTESIAN_POINT('Ctrl Pts',(-2.36679972368118,-0.154527088572115,
7.65960658558108));
#62751=CARTESIAN_POINT('Ctrl Pts',(-2.36170347148804,-0.223407056852555,
7.66430918087067));
#62752=CARTESIAN_POINT('Ctrl Pts',(-2.35663721639544,-0.271688137133943,
7.66765901622017));
#62753=CARTESIAN_POINT('Ctrl Pts',(-2.34370905362379,-0.366699345244975,
7.67436090788512));
#62754=CARTESIAN_POINT('Ctrl Pts',(-2.33592084255079,-0.413417317870091,
7.6777094133968));
#62755=CARTESIAN_POINT('Ctrl Pts',(-2.30104722842467,-0.589863052739477,
7.69054991057742));
#62756=CARTESIAN_POINT('Ctrl Pts',(-2.26450673015186,-0.717468680115592,
7.70025457385694));
#62757=CARTESIAN_POINT('Ctrl Pts',(-2.1931890865448,-0.905438696381539,
7.71487583134441));
#62758=CARTESIAN_POINT('Ctrl Pts',(-2.16610180842508,-0.968453254887932,
7.71983270889984));
#62759=CARTESIAN_POINT('Ctrl Pts',(-2.12468236338812,-1.05434380345765,
7.72659638762268));
#62760=CARTESIAN_POINT('Ctrl Pts',(-2.112635098113,-1.07828060889541,7.7284820391519));
#62761=CARTESIAN_POINT('Ctrl Pts',(-2.09081062957852,-1.11987319050323,
7.73175360898754));
#62762=CARTESIAN_POINT('Ctrl Pts',(-2.08120906876835,-1.13761765559537,
7.73314772895018));
#62763=CARTESIAN_POINT('Ctrl Pts',(-2.06641387352654,-1.16414595118647,
7.73522715033727));
#62764=CARTESIAN_POINT('Ctrl Pts',(-2.06138834858849,-1.17302181491389,
7.73592206153771));
#62765=CARTESIAN_POINT('Ctrl Pts',(-2.05215282107977,-1.18909054021136,
7.73717823822132));
#62766=CARTESIAN_POINT('Ctrl Pts',(-2.04796205438064,-1.19629383613383,
7.73774062808807));
#62767=CARTESIAN_POINT('Ctrl Pts',(-2.03835675822992,-1.2126054823266,7.73901256824784));
#62768=CARTESIAN_POINT('Ctrl Pts',(-2.03291907270906,-1.22169979291215,
7.73972064400058));
#62769=CARTESIAN_POINT('Ctrl Pts',(-2.01589510681606,-1.2497432827057,7.74190172958407));
#62770=CARTESIAN_POINT('Ctrl Pts',(-2.00410309549641,-1.26856699586418,
7.74336238742602));
#62771=CARTESIAN_POINT('Ctrl Pts',(-1.91444306773753,-1.40732077547722,
7.75412574517736));
#62772=CARTESIAN_POINT('Ctrl Pts',(-1.82612578710931,-1.52017084870762,
7.7628717943006));
#62773=CARTESIAN_POINT('Ctrl Pts',(-1.61705746750953,-1.74259640166611,
7.78161731740108));
#62774=CARTESIAN_POINT('Ctrl Pts',(-1.49412683980813,-1.84907908301282,
7.79159582261825));
#62775=CARTESIAN_POINT('Ctrl Pts',(-1.33810842607101,-1.95843458488203,
7.80395352541111));
#62776=CARTESIAN_POINT('Ctrl Pts',(-1.31462784998292,-1.97427295204799,
7.8058047879604));
#62777=CARTESIAN_POINT('Ctrl Pts',(-1.27688742162115,-1.99875821068158,
7.80877020031037));
#62778=CARTESIAN_POINT('Ctrl Pts',(-1.26280983825666,-2.0076820368439,7.80987413839438));
#62779=CARTESIAN_POINT('Ctrl Pts',(-1.23599335115478,-2.02428746740166,
7.81197356307449));
#62780=CARTESIAN_POINT('Ctrl Pts',(-1.22327390427851,-2.03199907794294,
7.81296789685022));
#62781=CARTESIAN_POINT('Ctrl Pts',(-1.19415622648995,-2.04928022137772,
7.81524131996426));
#62782=CARTESIAN_POINT('Ctrl Pts',(-1.17771410983524,-2.05877341116072,
7.81652306098004));
#62783=CARTESIAN_POINT('Ctrl Pts',(-1.13432883227761,-2.08313298667806,
7.81990077277483));
#62784=CARTESIAN_POINT('Ctrl Pts',(-1.10720796216833,-2.09767378692851,
7.82200791740675));
#62785=CARTESIAN_POINT('Ctrl Pts',(-0.931416305383729,-2.18756520041128,
7.83564376912977));
#62786=CARTESIAN_POINT('Ctrl Pts',(-0.775458739050126,-2.24758166178981,
7.84768929423007));
#62787=CARTESIAN_POINT('Ctrl Pts',(-0.52341126050802,-2.31519740855457,
7.86671529496087));
#62788=CARTESIAN_POINT('Ctrl Pts',(-0.430909845994576,-2.33418439900242,
7.87359865419005));
#62789=CARTESIAN_POINT('Ctrl Pts',(-0.305455623747408,-2.35222113461249,
7.88264031079023));
#62790=CARTESIAN_POINT('Ctrl Pts',(-0.273299043263232,-2.35617385753945,
7.88493191582932));
#62791=CARTESIAN_POINT('Ctrl Pts',(-0.217903690123094,-2.36183367887303,
7.88882464079312));
#62792=CARTESIAN_POINT('Ctrl Pts',(-0.194702647581203,-2.36385941287312,
7.8904385189752));
#62793=CARTESIAN_POINT('Ctrl Pts',(-0.160706206545447,-2.36632376122687,
7.89277570137009));
#62794=CARTESIAN_POINT('Ctrl Pts',(-0.149932454659455,-2.36703081899685,
7.89351231976217));
#62795=CARTESIAN_POINT('Ctrl Pts',(-0.131618332410639,-2.36810718917024,
7.89475718163007));
#62796=CARTESIAN_POINT('Ctrl Pts',(-0.124080539978081,-2.36851410599818,
7.89526743031774));
#62797=CARTESIAN_POINT('Ctrl Pts',(-0.106865646805108,-2.36936101668786,
7.89642784542258));
#62798=CARTESIAN_POINT('Ctrl Pts',(-0.0971876511047162,-2.36977772429777,
7.89707673462868));
#62799=CARTESIAN_POINT('Ctrl Pts',(-0.0703134833379145,-2.37076993867694,
7.89886960189225));
#62800=CARTESIAN_POINT('Ctrl Pts',(-0.053112798728508,-2.37121765352606,
7.90000690656921));
#62801=CARTESIAN_POINT('Ctrl Pts',(0.075658706849736,-2.37316747054677,
7.90845500545173));
#62802=CARTESIAN_POINT('Ctrl Pts',(0.187220952049796,-2.36698180242157,
7.91540543526459));
#62803=CARTESIAN_POINT('Ctrl Pts',(0.385550877352111,-2.34186813535702,
7.92773142044119));
#62804=CARTESIAN_POINT('Ctrl Pts',(0.472468110367663,-2.32589117207989,
7.93312277505396));
#62805=CARTESIAN_POINT('Ctrl Pts',(0.633251191678771,-2.28694982202508,
7.94334614415156));
#62806=CARTESIAN_POINT('Ctrl Pts',(0.707275425986675,-2.26515048701398,
7.94815594274821));
#62807=CARTESIAN_POINT('Ctrl Pts',(0.828707032653938,-2.2228566493564,7.95633965407458));
#62808=CARTESIAN_POINT('Ctrl Pts',(0.876744479901385,-2.20435150165048,
7.95965629790721));
#62809=CARTESIAN_POINT('Ctrl Pts',(0.943378917228261,-2.17615962116963,
7.96439064099154));
#62810=CARTESIAN_POINT('Ctrl Pts',(0.962509498593233,-2.16776610774485,
7.96576568239927));
#62811=CARTESIAN_POINT('Ctrl Pts',(0.995318013290381,-2.1528515130751,7.96815258762281));
#62812=CARTESIAN_POINT('Ctrl Pts',(1.00904913808842,-2.14644995374487,7.96916037439106));
#62813=CARTESIAN_POINT('Ctrl Pts',(1.03531649933598,-2.13389615334149,7.97110570974525));
#62814=CARTESIAN_POINT('Ctrl Pts',(1.04786161372329,-2.12776386642913,7.97204254258729));
#62815=CARTESIAN_POINT('Ctrl Pts',(1.08077060550112,-2.11131571515383,7.97452101023074));
#62816=CARTESIAN_POINT('Ctrl Pts',(1.10104054891598,-2.10081622181181,7.97606892068383));
#62817=CARTESIAN_POINT('Ctrl Pts',(1.174635342519,-2.06133767887945,7.98176936904308));
#62818=CARTESIAN_POINT('Ctrl Pts',(1.22699016722261,-2.03060956797838,7.98598193802389));
#62819=CARTESIAN_POINT('Ctrl Pts',(1.42857460566665,-1.90165173056859,8.00284243729954));
#62820=CARTESIAN_POINT('Ctrl Pts',(1.56767509570022,-1.78871026071855,8.01597479239079));
#62821=CARTESIAN_POINT('Ctrl Pts',(1.73367315373764,-1.61956393454659,8.03315698938038));
#62822=CARTESIAN_POINT('Ctrl Pts',(1.77303497408888,-1.57637488109569,8.03736062896923));
#62823=CARTESIAN_POINT('Ctrl Pts',(1.83369206723989,-1.5046699923059,8.04400220543952));
#62824=CARTESIAN_POINT('Ctrl Pts',(1.85601014446657,-1.47705282584351,8.04648499509374));
#62825=CARTESIAN_POINT('Ctrl Pts',(1.88546471992215,-1.43888232631621,8.04980495012984));
#62826=CARTESIAN_POINT('Ctrl Pts',(1.89314756706856,-1.4287588551893,8.0506751111582));
#62827=CARTESIAN_POINT('Ctrl Pts',(1.90590417313046,-1.41166626262207,8.0521263706434));
#62828=CARTESIAN_POINT('Ctrl Pts',(1.91102191345115,-1.40473044014356,8.0527103737348));
#62829=CARTESIAN_POINT('Ctrl Pts',(1.92145332455339,-1.39043073807732,8.05390418486546));
#62830=CARTESIAN_POINT('Ctrl Pts',(1.9267626932921,-1.38306400663559,8.05451371437129));
#62831=CARTESIAN_POINT('Ctrl Pts',(1.94065974795882,-1.36354654600783,8.05611472685101));
#62832=CARTESIAN_POINT('Ctrl Pts',(1.94917579079016,-1.35134496143176,8.05710155675881));
#62833=CARTESIAN_POINT('Ctrl Pts',(1.98629388330938,-1.29708203477689,8.06143234451782));
#62834=CARTESIAN_POINT('Ctrl Pts',(2.01365552263569,-1.25418398747864,8.06470418220121));
#62835=CARTESIAN_POINT('Ctrl Pts',(2.11677153463526,-1.08043060282398,8.07750325440686));
#62836=CARTESIAN_POINT('Ctrl Pts',(2.18132326108089,-0.943338418588722,
8.0866329687639));
#62837=CARTESIAN_POINT('Ctrl Pts',(2.25896486338486,-0.72695815522344,8.10083109307866));
#62838=CARTESIAN_POINT('Ctrl Pts',(2.28183747897087,-0.651618582400698,
8.10573437923005));
#62839=CARTESIAN_POINT('Ctrl Pts',(2.31357889990477,-0.524664984486468,
8.11405891259849));
#62840=CARTESIAN_POINT('Ctrl Pts',(2.32456049313992,-0.473643915337655,
8.11742011879281));
#62841=CARTESIAN_POINT('Ctrl Pts',(2.33758877497483,-0.401643683845031,
8.12220718185949));
#62842=CARTESIAN_POINT('Ctrl Pts',(2.34105275907137,-0.38093419735971,8.12358904942655));
#62843=CARTESIAN_POINT('Ctrl Pts',(2.34654477234757,-0.345189477301149,
8.12598399626081));
#62844=CARTESIAN_POINT('Ctrl Pts',(2.34870437684061,-0.330175523164932,
8.12699292296573));
#62845=CARTESIAN_POINT('Ctrl Pts',(2.35257208377099,-0.301325385395171,
8.12893777833687));
#62846=CARTESIAN_POINT('Ctrl Pts',(2.35430250346827,-0.287492791581175,
8.12987296774164));
#62847=CARTESIAN_POINT('Ctrl Pts',(2.35852961179169,-0.251100187496578,
8.13234088113243));
#62848=CARTESIAN_POINT('Ctrl Pts',(2.3608245166847,-0.228518650783053,8.13387977929147));
#62849=CARTESIAN_POINT('Ctrl Pts',(2.36798421088701,-0.146361263384634,
8.13950789423378));
#62850=CARTESIAN_POINT('Ctrl Pts',(2.37092018767185,-0.0866442644387087,
8.14365517117644));
#62851=CARTESIAN_POINT('Ctrl Pts',(2.37363386820713,0.152742235553974,8.16051305208115));
#62852=CARTESIAN_POINT('Ctrl Pts',(2.3552549731757,0.332003595872032,8.17371929308276));
#62853=CARTESIAN_POINT('Ctrl Pts',(2.30430581762809,0.564623405310789,8.19098502197735));
#62854=CARTESIAN_POINT('Ctrl Pts',(2.28966766152932,0.621327399653343,8.19519813350487));
#62855=CARTESIAN_POINT('Ctrl Pts',(2.26279028055774,0.711507028324684,8.20185273378364));
#62856=CARTESIAN_POINT('Ctrl Pts',(2.25186977110335,0.745348887392009,8.20433927125092));
#62857=CARTESIAN_POINT('Ctrl Pts',(2.23601586026846,0.790944250913351,8.20766335722722));
#62858=CARTESIAN_POINT('Ctrl Pts',(2.23174332786445,0.802920588793549,8.2085340031808));
#62859=CARTESIAN_POINT('Ctrl Pts',(2.22441278644027,0.822958159861634,8.20998583848492));
#62860=CARTESIAN_POINT('Ctrl Pts',(2.22140680512468,0.83103802107498,8.21056993743034));
#62861=CARTESIAN_POINT('Ctrl Pts',(2.21514495737823,0.847592646330202,8.21176370141507));
#62862=CARTESIAN_POINT('Ctrl Pts',(2.21188438689456,0.856065384304466,8.21237309002592));
#62863=CARTESIAN_POINT('Ctrl Pts',(2.20315538768663,0.878365232877269,8.21397330748037));
#62864=CARTESIAN_POINT('Ctrl Pts',(2.19760534318609,0.892160259078836,8.21495949156517));
#62865=CARTESIAN_POINT('Ctrl Pts',(2.17253914976547,0.952810526192658,8.21928260919121));
#62866=CARTESIAN_POINT('Ctrl Pts',(2.15165015710305,0.999087931669876,8.22254773850242));
#62867=CARTESIAN_POINT('Ctrl Pts',(2.06267822881898,1.1804355062056,8.23534464334201));
#62868=CARTESIAN_POINT('Ctrl Pts',(1.98322852628405,1.30953450504377,8.24447781274483));
#62869=CARTESIAN_POINT('Ctrl Pts',(1.84454225789204,1.49300403029087,8.25868192825093));
#62870=CARTESIAN_POINT('Ctrl Pts',(1.79396941336661,1.55340579437019,8.26358777893927));
#62871=CARTESIAN_POINT('Ctrl Pts',(1.71631535254533,1.63729227873551,8.27085941053797));
#62872=CARTESIAN_POINT('Ctrl Pts',(1.69155767902533,1.66285802770128,8.27314262891968));
#62873=CARTESIAN_POINT('Ctrl Pts',(1.64557935119972,1.70824738362576,8.27733015674813));
#62874=CARTESIAN_POINT('Ctrl Pts',(1.62455175200325,1.72825692872703,8.27922636046222));
#62875=CARTESIAN_POINT('Ctrl Pts',(1.59076988728,1.75924188943857,8.28224692581897));
#62876=CARTESIAN_POINT('Ctrl Pts',(1.57825654192364,1.77047652441155,8.28336039453712));
#62877=CARTESIAN_POINT('Ctrl Pts',(1.55447008533641,1.79137973218446,8.28546757197581));
#62878=CARTESIAN_POINT('Ctrl Pts',(1.54322352293435,1.80107738098956,8.28646001654407));
#62879=CARTESIAN_POINT('Ctrl Pts',(1.51757882069618,1.82277366612269,8.28871481616));
#62880=CARTESIAN_POINT('Ctrl Pts',(1.50312817914012,1.8347084120912,8.28997965882692));
#62881=CARTESIAN_POINT('Ctrl Pts',(1.46523747993118,1.86525411996823,8.29328228312747));
#62882=CARTESIAN_POINT('Ctrl Pts',(1.44158449807153,1.88359438296152,8.29533044290969));
#62883=CARTESIAN_POINT('Ctrl Pts',(1.24839831843216,2.02761846612328,8.31195815579918));
#62884=CARTESIAN_POINT('Ctrl Pts',(1.06315109295959,2.13058917605791,8.32741447140575));
#62885=CARTESIAN_POINT('Ctrl Pts',(0.80702706284224,2.23114931548736,8.34740251456449));
#62886=CARTESIAN_POINT('Ctrl Pts',(0.746334343286624,2.25217806002468,8.35203582257617));
#62887=CARTESIAN_POINT('Ctrl Pts',(0.660238702723952,2.27814491495189,8.35840649756832));
#62888=CARTESIAN_POINT('Ctrl Pts',(0.635497476423738,2.28517011850271,8.36021429525033));
#62889=CARTESIAN_POINT('Ctrl Pts',(0.591754601202301,2.29682536779215,8.36336484504061));
#62890=CARTESIAN_POINT('Ctrl Pts',(0.572801079892815,2.30162535223692,8.36471502984957));
#62891=CARTESIAN_POINT('Ctrl Pts',(0.543994135296906,2.30854281483105,8.36674241938423));
#62892=CARTESIAN_POINT('Ctrl Pts',(0.53418352674584,2.31083264564142,8.36742855669106));
#62893=CARTESIAN_POINT('Ctrl Pts',(0.516224045974578,2.31490396453901,8.3686763633121));
#62894=CARTESIAN_POINT('Ctrl Pts',(0.508080183135024,2.31670502272567,8.36923906401294));
#62895=CARTESIAN_POINT('Ctrl Pts',(0.48942298130101,2.32072804592323,8.37052115535057));
#62896=CARTESIAN_POINT('Ctrl Pts',(0.478903861111284,2.32292157004819,8.3712389656026));
#62897=CARTESIAN_POINT('Ctrl Pts',(0.445815240669384,2.32958712914599,8.37348210010128));
#62898=CARTESIAN_POINT('Ctrl Pts',(0.423194598073375,2.33380244413997,8.37499404197863));
#62899=CARTESIAN_POINT('Ctrl Pts',(0.290843859099948,2.35647804493942,8.3837337524287));
#62900=CARTESIAN_POINT('Ctrl Pts',(0.179972709486823,2.36752920512794,8.39063323555376));
#62901=CARTESIAN_POINT('Ctrl Pts',(-0.0265363382539642,2.37351554953665,
8.40335013819423));
#62902=CARTESIAN_POINT('Ctrl Pts',(-0.121874997163298,2.37053293151438,
8.40916897789272));
#62903=CARTESIAN_POINT('Ctrl Pts',(-0.318069480469154,2.35252564811557,
8.42139720165957));
#62904=CARTESIAN_POINT('Ctrl Pts',(-0.418650117422634,2.3367228257694,8.42780831070464));
#62905=CARTESIAN_POINT('Ctrl Pts',(-0.543279363520799,2.30883564606645,
8.43611221546574));
#62906=CARTESIAN_POINT('Ctrl Pts',(-0.568564297047864,2.30273946887195,
8.43781551918868));
#62907=CARTESIAN_POINT('Ctrl Pts',(-0.609403473070009,2.29217955545606,
8.44059942945652));
#62908=CARTESIAN_POINT('Ctrl Pts',(-0.625021689852114,2.28797018621753,
8.44167193645631));
#62909=CARTESIAN_POINT('Ctrl Pts',(-0.655041812495071,2.27954894897275,
8.44374918634264));
#62910=CARTESIAN_POINT('Ctrl Pts',(-0.669449242239081,2.27535950595442,
8.44475316704247));
#62911=CARTESIAN_POINT('Ctrl Pts',(-0.702623583775113,2.26537060332344,
8.44708171946393));
#62912=CARTESIAN_POINT('Ctrl Pts',(-0.721359913133924,2.25947421023918,
8.4484093576213));
#62913=CARTESIAN_POINT('Ctrl Pts',(-0.78273816590162,2.23931700455241,8.45280100880603));
#62914=CARTESIAN_POINT('Ctrl Pts',(-0.825045717980147,2.22407706187215,
8.45589626532447));
#62915=CARTESIAN_POINT('Ctrl Pts',(-1.0339909561512,2.14202898626124,8.47153540447672));
#62916=CARTESIAN_POINT('Ctrl Pts',(-1.19307743526602,2.05766179960348,8.48464331104332));
#62917=CARTESIAN_POINT('Ctrl Pts',(-1.40150453032509,1.91477077908679,8.50303971272681));
#62918=CARTESIAN_POINT('Ctrl Pts',(-1.45996445986056,1.87057936132581,8.50834565794288));
#62919=CARTESIAN_POINT('Ctrl Pts',(-1.53774925555721,1.80590814140734,8.51552966696886));
#62920=CARTESIAN_POINT('Ctrl Pts',(-1.55889438197209,1.78768717527148,8.51749594556425));
#62921=CARTESIAN_POINT('Ctrl Pts',(-1.5952364426701,1.75523554765958,8.52089217870456));
#62922=CARTESIAN_POINT('Ctrl Pts',(-1.6105765616182,1.74117039595729,8.52233116748917));
#62923=CARTESIAN_POINT('Ctrl Pts',(-1.63324840008679,1.71982683546863,8.5244635545474));
#62924=CARTESIAN_POINT('Ctrl Pts',(-1.64072048606587,1.7126999086007,8.52516727606303));
#62925=CARTESIAN_POINT('Ctrl Pts',(-1.65413634948671,1.69973538982177,8.52643210028336));
#62926=CARTESIAN_POINT('Ctrl Pts',(-1.66009611935743,1.69391509167485,8.52699441978956));
#62927=CARTESIAN_POINT('Ctrl Pts',(-1.67346887482924,1.68071691872532,8.52825723663176));
#62928=CARTESIAN_POINT('Ctrl Pts',(-1.68086385122312,1.67332129603862,8.5289563575037));
#62929=CARTESIAN_POINT('Ctrl Pts',(-1.70330488962462,1.65057940950423,8.53108132074057));
#62930=CARTESIAN_POINT('Ctrl Pts',(-1.71819196493604,1.63507687407473,8.53249570733397));
#62931=CARTESIAN_POINT('Ctrl Pts',(-1.8370517548105,1.50788682375964,8.54384847515719));
#62932=CARTESIAN_POINT('Ctrl Pts',(-1.93024923217312,1.38659022980856,8.55314549380267));
#62933=CARTESIAN_POINT('Ctrl Pts',(-2.09167677948846,1.12834593644778,8.57185183086385));
#62934=CARTESIAN_POINT('Ctrl Pts',(-2.15962830449452,0.992105902265263,
8.58122612207079));
#62935=CARTESIAN_POINT('Ctrl Pts',(-2.22459448335393,0.822944109772677,
8.59296753734976));
#62936=CARTESIAN_POINT('Ctrl Pts',(-2.23459680753082,0.79538330969721,8.59488245600698));
#62937=CARTESIAN_POINT('Ctrl Pts',(-2.24954824514856,0.751675220080702,
8.59792598459038));
#62938=CARTESIAN_POINT('Ctrl Pts',(-2.2548403984496,0.735647807567967,8.59904341237464));
#62939=CARTESIAN_POINT('Ctrl Pts',(-2.26446374840526,0.705423468798896,
8.60115392024307));
#62940=CARTESIAN_POINT('Ctrl Pts',(-2.26883363597871,0.691239649774912,
8.60214569062537));
#62941=CARTESIAN_POINT('Ctrl Pts',(-2.27839272861406,0.659145155211388,
8.60439329619397));
#62942=CARTESIAN_POINT('Ctrl Pts',(-2.28350435452909,0.641212593606924,
8.60565155513117));
#62943=CARTESIAN_POINT('Ctrl Pts',(-2.29618263350691,0.594659326431703,
8.60892508674917));
#62944=CARTESIAN_POINT('Ctrl Pts',(-2.30342562779406,0.565954629436567,
8.61095043661536));
#62945=CARTESIAN_POINT('Ctrl Pts',(-2.33800615071406,0.417226160865794,
8.62148371565086));
#62946=CARTESIAN_POINT('Ctrl Pts',(-2.35648357902692,0.2954402791331,8.63025421109628));
#62947=CARTESIAN_POINT('Ctrl Pts',(-2.36544103037033,0.172877975290479,
8.63916402106918));
#62948=CARTESIAN_POINT('Origin',(0.,0.,-1.84858989190501));
#62949=CARTESIAN_POINT('',(-2.36544098814976,0.172878552981809,9.83847008213854));
#62950=CARTESIAN_POINT('',(-2.36544101901418,0.172878130673515,9.64179857564526));
#62951=CARTESIAN_POINT('',(-2.36544101854889,0.172878137039864,-1.84858989190501));
#62952=CARTESIAN_POINT('Ctrl Pts',(-2.36544098814985,0.172878552980627,
9.83847008213863));
#62953=CARTESIAN_POINT('Ctrl Pts',(-2.35148711096064,0.36380491416238,9.82484861518335));
#62954=CARTESIAN_POINT('Ctrl Pts',(-2.31445237025283,0.55253567477952,9.8106434709485));
#62955=CARTESIAN_POINT('Ctrl Pts',(-2.23794170651039,0.787307871903176,
9.7929557917114));
#62956=CARTESIAN_POINT('Ctrl Pts',(-2.21903757596194,0.839112664346452,
9.78905776136071));
#62957=CARTESIAN_POINT('Ctrl Pts',(-2.1928766108117,0.903715870097693,9.78424123912396));
#62958=CARTESIAN_POINT('Ctrl Pts',(-2.18728531968704,0.917165830621656,
9.78324098386449));
#62959=CARTESIAN_POINT('Ctrl Pts',(-2.17808512853153,0.938734328061768,
9.78164198851849));
#62960=CARTESIAN_POINT('Ctrl Pts',(-2.17455400606125,0.946885339958971,
9.78103887316123));
#62961=CARTESIAN_POINT('Ctrl Pts',(-2.16762966264957,0.962626001179744,
9.77987670827261));
#62962=CARTESIAN_POINT('Ctrl Pts',(-2.16424221786804,0.970217912399061,
9.77931735336366));
#62963=CARTESIAN_POINT('Ctrl Pts',(-2.15656846452531,0.987176080711072,
9.77807022063541));
#62964=CARTESIAN_POINT('Ctrl Pts',(-2.15226086240516,0.996532661901697,
9.77738370216783));
#62965=CARTESIAN_POINT('Ctrl Pts',(-2.13699632842712,1.02912819213788,9.77499659573381));
#62966=CARTESIAN_POINT('Ctrl Pts',(-2.125722433982,1.05221785109319,9.77331371025024));
#62967=CARTESIAN_POINT('Ctrl Pts',(-2.0439129998954,1.21308467798131,9.76161433437499));
#62968=CARTESIAN_POINT('Ctrl Pts',(-1.96040531853024,1.34386673884254,9.7522175609079));
#62969=CARTESIAN_POINT('Ctrl Pts',(-1.80428914859166,1.54250058301034,9.73669321773066));
#62970=CARTESIAN_POINT('Ctrl Pts',(-1.73914371988262,1.615594176294,9.73065469331309));
#62971=CARTESIAN_POINT('Ctrl Pts',(-1.64093522793271,1.71294110253295,9.72190171273114));
#62972=CARTESIAN_POINT('Ctrl Pts',(-1.61147184054409,1.74068775928852,9.71931623468367));
#62973=CARTESIAN_POINT('Ctrl Pts',(-1.56432940170174,1.78286032489152,9.71522843926986));
#62974=CARTESIAN_POINT('Ctrl Pts',(-1.54712688814872,1.79780859689002,9.71374654372105));
#62975=CARTESIAN_POINT('Ctrl Pts',(-1.51557579985745,1.82443696347632,9.71104395242591));
#62976=CARTESIAN_POINT('Ctrl Pts',(-1.50130075098538,1.83620158540842,9.70982670402882));
#62977=CARTESIAN_POINT('Ctrl Pts',(-1.48667747145421,1.84796867741251,9.70858477716191));
#62978=CARTESIAN_POINT('Ctrl Pts',(-1.48646503961248,1.84813955718636,9.70856673680146));
#62979=CARTESIAN_POINT('Ctrl Pts',(-1.48602988534387,1.8484894708987,9.70852978435111));
#62980=CARTESIAN_POINT('Ctrl Pts',(-1.48580716002368,1.84866850121398,9.7085108721204));
#62981=CARTESIAN_POINT('Ctrl Pts',(-1.48534938349809,1.84903633342807,9.70847200343065));
#62982=CARTESIAN_POINT('Ctrl Pts',(-1.48511432864625,1.84922513076281,9.70845204679392));
#62983=CARTESIAN_POINT('Ctrl Pts',(-1.48462944364324,1.8496144409547,9.70841088174035));
#62984=CARTESIAN_POINT('Ctrl Pts',(-1.48437960886694,1.84981494801519,9.70838967309801));
#62985=CARTESIAN_POINT('Ctrl Pts',(-1.48386216936193,1.85023005123698,9.70834575033391));
#62986=CARTESIAN_POINT('Ctrl Pts',(-1.48359455869878,1.85044463996172,9.70832303592245));
#62987=CARTESIAN_POINT('Ctrl Pts',(-1.48303784424433,1.85089085368922,9.70827578626848));
#62988=CARTESIAN_POINT('Ctrl Pts',(-1.4827487327451,1.85112246901003,9.70825125064959));
#62989=CARTESIAN_POINT('Ctrl Pts',(-1.48214430274669,1.85160646236075,9.70819995940289));
#62990=CARTESIAN_POINT('Ctrl Pts',(-1.48182897404411,1.85185882758476,9.70817320327594));
#62991=CARTESIAN_POINT('Ctrl Pts',(-1.48116601963447,1.85238912836158,9.70811695541674));
#62992=CARTESIAN_POINT('Ctrl Pts',(-1.48081838015965,1.85266704660413,9.70808746301048));
#62993=CARTESIAN_POINT('Ctrl Pts',(-1.48008275391455,1.85325479915633,9.70802506119342));
#62994=CARTESIAN_POINT('Ctrl Pts',(-1.47969474808779,1.85356460947873,9.70799215084859));
#62995=CARTESIAN_POINT('Ctrl Pts',(-1.47886746035172,1.85422474714124,9.7079219883459));
#62996=CARTESIAN_POINT('Ctrl Pts',(-1.47842815125135,1.854575040214,9.70788473485352));
#62997=CARTESIAN_POINT('Ctrl Pts',(-1.46712066230866,1.86358475192356,9.70692597145883));
#62998=CARTESIAN_POINT('Ctrl Pts',(-1.45617691199566,1.87214848568603,9.70600075008007));
#62999=CARTESIAN_POINT('Ctrl Pts',(-1.43267453005572,1.89020888890415,9.70401911832907));
#63000=CARTESIAN_POINT('Ctrl Pts',(-1.42009537486021,1.89967761964359,9.70296168208276));
#63001=CARTESIAN_POINT('Ctrl Pts',(-1.38722006069915,1.92391491023237,9.70020575582528));
#63002=CARTESIAN_POINT('Ctrl Pts',(-1.36678251426728,1.93848743973094,9.69849991446179));
#63003=CARTESIAN_POINT('Ctrl Pts',(-1.2771135363642,2.00030084697416,9.69104482019084));
#63004=CARTESIAN_POINT('Ctrl Pts',(-1.20564389511275,2.04417279079857,9.68517408335815));
#63005=CARTESIAN_POINT('Ctrl Pts',(-1.00131563043175,2.15515313382224,9.6685890935545));
#63006=CARTESIAN_POINT('Ctrl Pts',(-0.864240406150317,2.21368475219605,
9.65766246877988));
#63007=CARTESIAN_POINT('Ctrl Pts',(-0.665480470696995,2.27726387852573,
9.64252253836906));
#63008=CARTESIAN_POINT('Ctrl Pts',(-0.607680832715585,2.29336432617498,
9.63820291478292));
#63009=CARTESIAN_POINT('Ctrl Pts',(-0.525497889041362,2.31293107984241,
9.63222641491523));
#63010=CARTESIAN_POINT('Ctrl Pts',(-0.501578594032632,2.31823580053441,
9.63050644420239));
#63011=CARTESIAN_POINT('Ctrl Pts',(-0.45920639861616,2.32694637196008,9.62749864111949));
#63012=CARTESIAN_POINT('Ctrl Pts',(-0.440787490615252,2.33050560544254,
9.62620410026929));
#63013=CARTESIAN_POINT('Ctrl Pts',(-0.412705011742257,2.33558734839377,
9.62425192786481));
#63014=CARTESIAN_POINT('Ctrl Pts',(-0.403071534776486,2.33726914048361,
9.62358609255653));
#63015=CARTESIAN_POINT('Ctrl Pts',(-0.385386426734616,2.34024397373358,
9.62237112969533));
#63016=CARTESIAN_POINT('Ctrl Pts',(-0.377338384388984,2.34155510330733,
9.62182106045599));
#63017=CARTESIAN_POINT('Ctrl Pts',(-0.35885921704808,2.34446784730728,9.62056440624811));
#63018=CARTESIAN_POINT('Ctrl Pts',(-0.34842399171355,2.3460413801096,9.61985937110377));
#63019=CARTESIAN_POINT('Ctrl Pts',(-0.316270310105425,2.35067057685119,
9.6177001515864));
#63020=CARTESIAN_POINT('Ctrl Pts',(-0.29451900707349,2.35349478591801,9.6162579564743));
#63021=CARTESIAN_POINT('Ctrl Pts',(-0.131703921679352,2.37234213629051,
9.60557945547388));
#63022=CARTESIAN_POINT('Ctrl Pts',(0.0105232603289849,2.37597412133972,
9.5968935442722));
#63023=CARTESIAN_POINT('Ctrl Pts',(0.196983066990513,2.36398102361645,9.58542279486496));
#63024=CARTESIAN_POINT('Ctrl Pts',(0.241638704094815,2.35983458609864,9.58267045296649));
#63025=CARTESIAN_POINT('Ctrl Pts',(0.366532928588348,2.34465533006828,9.57490731471129));
#63026=CARTESIAN_POINT('Ctrl Pts',(0.446358526545137,2.3307761850153,9.56986758619594));
#63027=CARTESIAN_POINT('Ctrl Pts',(0.576998983451227,2.3011039576171,9.56135003850568));
#63028=CARTESIAN_POINT('Ctrl Pts',(0.62827298326351,2.28763625862558,9.5579370272949));
#63029=CARTESIAN_POINT('Ctrl Pts',(0.699015558183576,2.2664971932997,9.55310685203236));
#63030=CARTESIAN_POINT('Ctrl Pts',(0.718901041158526,2.26026846317124,9.55173558474785));
#63031=CARTESIAN_POINT('Ctrl Pts',(0.752843381958993,2.24914347841472,9.54937043530725));
#63032=CARTESIAN_POINT('Ctrl Pts',(0.766941178466973,2.24437535987474,9.54838074829018));
#63033=CARTESIAN_POINT('Ctrl Pts',(0.795498563013189,2.23441627798508,9.54636057078262));
#63034=CARTESIAN_POINT('Ctrl Pts',(0.809954431395487,2.22921687305942,9.54532984388606));
#63035=CARTESIAN_POINT('Ctrl Pts',(0.84618993467659,2.21578490818336,9.54272522441529));
#63036=CARTESIAN_POINT('Ctrl Pts',(0.867900338501009,2.20737153663911,9.54114544548773));
#63037=CARTESIAN_POINT('Ctrl Pts',(0.951315592386749,2.17362502927501,9.53499894183274));
#63038=CARTESIAN_POINT('Ctrl Pts',(1.01205998159402,2.1460149655055,9.5303579142361));
#63039=CARTESIAN_POINT('Ctrl Pts',(1.21268036011542,2.04441400655871,9.51445905386734));
#63040=CARTESIAN_POINT('Ctrl Pts',(1.34628882035849,1.95900952645719,9.50286599063631));
#63041=CARTESIAN_POINT('Ctrl Pts',(1.52344307442583,1.81903598766663,9.48644729432043));
#63042=CARTESIAN_POINT('Ctrl Pts',(1.57468751898544,1.77486086093433,9.48155956001868));
#63043=CARTESIAN_POINT('Ctrl Pts',(1.64323979885341,1.71045596652806,9.4748901458056));
#63044=CARTESIAN_POINT('Ctrl Pts',(1.66219982478415,1.69203679525596,9.47303072381381));
#63045=CARTESIAN_POINT('Ctrl Pts',(1.69487649721588,1.65921278116701,9.46980564328797));
#63046=CARTESIAN_POINT('Ctrl Pts',(1.70872703141753,1.64494540646239,9.46843192967085));
#63047=CARTESIAN_POINT('Ctrl Pts',(1.7292760149873,1.62323832224529,9.46638589875089));
#63048=CARTESIAN_POINT('Ctrl Pts',(1.73610908038843,1.61592804817882,9.46570418368012));
#63049=CARTESIAN_POINT('Ctrl Pts',(1.74841753056706,1.60259180210318,9.46447408334904));
#63050=CARTESIAN_POINT('Ctrl Pts',(1.75390830782466,1.5965807206913,9.46392459147162));
#63051=CARTESIAN_POINT('Ctrl Pts',(1.76626342866086,1.58291417242978,9.46268637846542));
#63052=CARTESIAN_POINT('Ctrl Pts',(1.77310905229181,1.57524222744087,9.46199901923663));
#63053=CARTESIAN_POINT('Ctrl Pts',(1.79397675247366,1.55154723154073,9.4598988083296));
#63054=CARTESIAN_POINT('Ctrl Pts',(1.80783357313211,1.53537918721192,9.45849728624363));
#63055=CARTESIAN_POINT('Ctrl Pts',(1.91982800644748,1.40108613008783,9.44709098360785));
#63056=CARTESIAN_POINT('Ctrl Pts',(2.00651131288746,1.27385528842763,9.437739319127));
#63057=CARTESIAN_POINT('Ctrl Pts',(2.09671773686658,1.10911802167004,9.42620574617628));
#63058=CARTESIAN_POINT('Ctrl Pts',(2.11249491857299,1.07876467913218,9.42410355613875));
#63059=CARTESIAN_POINT('Ctrl Pts',(2.16351929548914,0.975184926706866,9.41697962961143));
#63060=CARTESIAN_POINT('Ctrl Pts',(2.19565642594743,0.900495856184954,9.41192286251095));
#63061=CARTESIAN_POINT('Ctrl Pts',(2.2423605662312,0.774493212381704,9.40337983031205));
#63062=CARTESIAN_POINT('Ctrl Pts',(2.25914512369835,0.724074093809713,9.39995890903668));
#63063=CARTESIAN_POINT('Ctrl Pts',(2.28014109210763,0.65313829929521,9.39511940802262));
#63064=CARTESIAN_POINT('Ctrl Pts',(2.28579613997125,0.633063187263666,9.39374696903231));
#63065=CARTESIAN_POINT('Ctrl Pts',(2.29503234694673,0.598536689844454,9.39138042922393));
#63066=CARTESIAN_POINT('Ctrl Pts',(2.29874359372843,0.584121148298664,9.39039053640619));
#63067=CARTESIAN_POINT('Ctrl Pts',(2.30557386243002,0.556516739073323,9.38849110059571));
#63068=CARTESIAN_POINT('Ctrl Pts',(2.308716026696,0.543334161472777,9.38758233790412));
#63069=CARTESIAN_POINT('Ctrl Pts',(2.31660952799268,0.50891257963218,9.38520468906432));
#63070=CARTESIAN_POINT('Ctrl Pts',(2.32118170813522,0.48763423008766,9.38373020890018));
#63071=CARTESIAN_POINT('Ctrl Pts',(2.33635735266499,0.411952011816685,9.37846766349362));
#63072=CARTESIAN_POINT('Ctrl Pts',(2.34534524198157,0.357246368536955,9.37463007053426));
#63073=CARTESIAN_POINT('Ctrl Pts',(2.37389291516638,0.13508206490017,9.35890200215186));
#63074=CARTESIAN_POINT('Ctrl Pts',(2.37748822584853,-0.0339119585594604,
9.3465660316688));
#63075=CARTESIAN_POINT('Ctrl Pts',(2.35507867162033,-0.296296172675962,
9.32740272814821));
#63076=CARTESIAN_POINT('Ctrl Pts',(2.34135262247255,-0.390202963455172,
9.32055418549568));
#63077=CARTESIAN_POINT('Ctrl Pts',(2.31753010546241,-0.504720199178202,
9.31238726450181));
#63078=CARTESIAN_POINT('Ctrl Pts',(2.31271731398419,-0.526333527072715,
9.31085432474736));
#63079=CARTESIAN_POINT('Ctrl Pts',(2.30519005896671,-0.558037548864441,
9.30862119984535));
#63080=CARTESIAN_POINT('Ctrl Pts',(2.30271063214854,-0.568182073585557,
9.30790900565085));
#63081=CARTESIAN_POINT('Ctrl Pts',(2.29836826453691,-0.58545335791376,9.30670087679319));
#63082=CARTESIAN_POINT('Ctrl Pts',(2.29653903018043,-0.592588222853283,
9.30620309306734));
#63083=CARTESIAN_POINT('Ctrl Pts',(2.29226946753881,-0.608924764427316,
9.30506636427981));
#63084=CARTESIAN_POINT('Ctrl Pts',(2.28980694963943,-0.618120394228029,
9.30442868296862));
#63085=CARTESIAN_POINT('Ctrl Pts',(2.28278423371278,-0.643726885693345,
9.30265838774089));
#63086=CARTESIAN_POINT('Ctrl Pts',(2.27810242281787,-0.660104198444361,
9.30153237371654));
#63087=CARTESIAN_POINT('Ctrl Pts',(2.24026524832242,-0.787261654335602,
9.29282808508605));
#63088=CARTESIAN_POINT('Ctrl Pts',(2.19922021800222,-0.895548334966029,
9.28563923534048));
#63089=CARTESIAN_POINT('Ctrl Pts',(2.11397473538188,-1.07878601617863,9.27319129731505));
#63090=CARTESIAN_POINT('Ctrl Pts',(2.07326119708041,-1.15510016887345,9.26791370880281));
#63091=CARTESIAN_POINT('Ctrl Pts',(1.98884516503763,-1.2944269891429,9.25784473318693));
#63092=CARTESIAN_POINT('Ctrl Pts',(1.94607946948904,-1.35787323693729,9.25307374877631));
#63093=CARTESIAN_POINT('Ctrl Pts',(1.86982443788483,-1.4599839827616,9.24496009623301));
#63094=CARTESIAN_POINT('Ctrl Pts',(1.8380156683664,-1.49983148107835,9.24167412807066));
#63095=CARTESIAN_POINT('Ctrl Pts',(1.79162477340676,-1.55425243141779,9.23699397390853));
#63096=CARTESIAN_POINT('Ctrl Pts',(1.77809783518523,-1.56970952548147,9.23564185770807));
#63097=CARTESIAN_POINT('Ctrl Pts',(1.75446220637669,-1.59602015397974,9.23329937049808));
#63098=CARTESIAN_POINT('Ctrl Pts',(1.74444917781166,-1.60695831143951,9.23231298566059));
#63099=CARTESIAN_POINT('Ctrl Pts',(1.72504676233704,-1.62775831317476,9.23041259565368));
#63100=CARTESIAN_POINT('Ctrl Pts',(1.715673702457,-1.63763463318999,9.22949930410942));
#63101=CARTESIAN_POINT('Ctrl Pts',(1.69333844260084,-1.66076690291513,9.22733380888859));
#63102=CARTESIAN_POINT('Ctrl Pts',(1.68030498020774,-1.67395248644821,9.22607856577313));
#63103=CARTESIAN_POINT('Ctrl Pts',(1.64049010737506,-1.71329852070843,9.22226825102614));
#63104=CARTESIAN_POINT('Ctrl Pts',(1.61324368154949,-1.73897790821269,9.21969298702677));
#63105=CARTESIAN_POINT('Ctrl Pts',(1.43439512744109,-1.89971872952771,9.20298380336546));
#63106=CARTESIAN_POINT('Ctrl Pts',(1.26660425165898,-2.01546671432156,9.18807757817609));
#63107=CARTESIAN_POINT('Ctrl Pts',(1.03162676163839,-2.13651808003215,9.168891356934));
#63108=CARTESIAN_POINT('Ctrl Pts',(0.976004717201496,-2.16249370260018,
9.16446885523825));
#63109=CARTESIAN_POINT('Ctrl Pts',(0.896520059949574,-2.19592071483974,
9.15836608020356));
#63110=CARTESIAN_POINT('Ctrl Pts',(0.873454428309954,-2.20519692336756,
9.15662012720267));
#63111=CARTESIAN_POINT('Ctrl Pts',(0.832537062710284,-2.2209097156853,9.15357168092312));
#63112=CARTESIAN_POINT('Ctrl Pts',(0.814746206923005,-2.22749783399454,
9.15226223685996));
#63113=CARTESIAN_POINT('Ctrl Pts',(0.787626362086828,-2.2371721550558,9.15029235507755));
#63114=CARTESIAN_POINT('Ctrl Pts',(0.778354565483334,-2.24041485368655,
9.14962349416447));
#63115=CARTESIAN_POINT('Ctrl Pts',(0.7613523158724,-2.24624289619348,9.14840571604894));
#63116=CARTESIAN_POINT('Ctrl Pts',(0.753628529272592,-2.24884604659254,
9.14785582546228));
#63117=CARTESIAN_POINT('Ctrl Pts',(0.735926133014581,-2.25471084375293,
9.14660298911896));
#63118=CARTESIAN_POINT('Ctrl Pts',(0.725939126502567,-2.25794611475101,
9.14590155507408));
#63119=CARTESIAN_POINT('Ctrl Pts',(0.694542943237828,-2.26788700326566,
9.14371228777933));
#63120=CARTESIAN_POINT('Ctrl Pts',(0.673059197512471,-2.27435546142892,
9.14223721706842));
#63121=CARTESIAN_POINT('Ctrl Pts',(0.52236135636481,-2.31740599318907,9.1320292638117));
#63122=CARTESIAN_POINT('Ctrl Pts',(0.390319733023683,-2.34326517904431,
9.12378589617284));
#63123=CARTESIAN_POINT('Ctrl Pts',(0.141675797779439,-2.37034453767382,
9.10842866581614));
#63124=CARTESIAN_POINT('Ctrl Pts',(0.0258078210196054,-2.37443404509145,
9.10133597575133));
#63125=CARTESIAN_POINT('Ctrl Pts',(-0.156236704289563,-2.36752961991268,
9.08984765738798));
#63126=CARTESIAN_POINT('Ctrl Pts',(-0.222444214608251,-2.36222855776211,
9.08559936600194));
#63127=CARTESIAN_POINT('Ctrl Pts',(-0.310742829760694,-2.35141371596325,
9.07979294479662));
#63128=CARTESIAN_POINT('Ctrl Pts',(-0.333106702136198,-2.34834993937831,
9.07831025484754));
#63129=CARTESIAN_POINT('Ctrl Pts',(-0.370468028076421,-2.34268714530822,
9.07581139182127));
#63130=CARTESIAN_POINT('Ctrl Pts',(-0.385490629303042,-2.34026207447042,
9.0748006801923));
#63131=CARTESIAN_POINT('Ctrl Pts',(-0.415091836924292,-2.33519085814491,
9.07279689314523));
#63132=CARTESIAN_POINT('Ctrl Pts',(-0.429671054061224,-2.33255232424078,
9.07180409904083));
#63133=CARTESIAN_POINT('Ctrl Pts',(-0.465133949345981,-2.32579052791769,
9.06937437220082));
#63134=CARTESIAN_POINT('Ctrl Pts',(-0.485988352777718,-2.32152244027249,
9.0679329507757));
#63135=CARTESIAN_POINT('Ctrl Pts',(-0.557735312622603,-2.30582953392651,
9.06292892076605));
#63136=CARTESIAN_POINT('Ctrl Pts',(-0.608303510587483,-2.29300776955365,
9.059323060125));
#63137=CARTESIAN_POINT('Ctrl Pts',(-0.823356595925388,-2.23086597162423,
9.04363832515264));
#63138=CARTESIAN_POINT('Ctrl Pts',(-0.982625874559098,-2.16543520297995,
9.03107990166978));
#63139=CARTESIAN_POINT('Ctrl Pts',(-1.19614029231164,-2.04927937633003,
9.01338872448353));
#63140=CARTESIAN_POINT('Ctrl Pts',(-1.25730007813356,-2.01233578751767,
9.00821881329493));
#63141=CARTESIAN_POINT('Ctrl Pts',(-1.33944313510384,-1.9575080231577,9.0012090523693));
#63142=CARTESIAN_POINT('Ctrl Pts',(-1.36192041597794,-1.94193678812602,
8.99928387345556));
#63143=CARTESIAN_POINT('Ctrl Pts',(-1.40069277935262,-1.91407264469806,
8.99595705600795));
#63144=CARTESIAN_POINT('Ctrl Pts',(-1.41710752370737,-1.90195180973846,
8.99454668844659));
#63145=CARTESIAN_POINT('Ctrl Pts',(-1.44141864018205,-1.88351070116848,
8.99245739103078));
#63146=CARTESIAN_POINT('Ctrl Pts',(-1.44943385285639,-1.8773496672767,8.99176848709025));
#63147=CARTESIAN_POINT('Ctrl Pts',(-1.46383119453235,-1.86613572664205,
8.99053126864363));
#63148=CARTESIAN_POINT('Ctrl Pts',(-1.47022691318475,-1.86110105719123,
8.98998177388721));
#63149=CARTESIAN_POINT('Ctrl Pts',(-1.48455768547101,-1.84969998272741,
8.98875073919286));
#63150=CARTESIAN_POINT('Ctrl Pts',(-1.49247782027438,-1.84331535908052,
8.98807048484977));
#63151=CARTESIAN_POINT('Ctrl Pts',(-1.5164104116554,-1.82376730487328,8.98601437392899));
#63152=CARTESIAN_POINT('Ctrl Pts',(-1.53229209125323,-1.81044434793005,
8.98464916902821));
#63153=CARTESIAN_POINT('Ctrl Pts',(-1.66879189941941,-1.69285310562152,
8.97288809503347));
#63154=CARTESIAN_POINT('Ctrl Pts',(-1.77880288974573,-1.57686166355601,
8.96320197064748));
#63155=CARTESIAN_POINT('Ctrl Pts',(-1.96797081049228,-1.33218852471019,
8.94420386499854));
#63156=CARTESIAN_POINT('Ctrl Pts',(-2.04814739152945,-1.2052882129219,8.93494150105376));
#63157=CARTESIAN_POINT('Ctrl Pts',(-2.12826538272142,-1.04711186545144,
8.92343336652158));
#63158=CARTESIAN_POINT('Ctrl Pts',(-2.14028231036323,-1.02232496216988,
8.92163196743653));
#63159=CARTESIAN_POINT('Ctrl Pts',(-2.15870439118753,-0.982577221843002,
8.91874338617778));
#63160=CARTESIAN_POINT('Ctrl Pts',(-2.16539219677101,-0.96774958413176,
8.91766585047418));
#63161=CARTESIAN_POINT('Ctrl Pts',(-2.17776847267248,-0.939539231070214,
8.9156152422617));
#63162=CARTESIAN_POINT('Ctrl Pts',(-2.18348743879779,-0.926170651588775,
8.91464325505616));
#63163=CARTESIAN_POINT('Ctrl Pts',(-2.19623418181204,-0.895599672843647,
8.91241959323735));
#63164=CARTESIAN_POINT('Ctrl Pts',(-2.20318336293789,-0.878365750027235,
8.91116536156537));
#63165=CARTESIAN_POINT('Ctrl Pts',(-2.22086888988578,-0.83297505921796,
8.90785939404667));
#63166=CARTESIAN_POINT('Ctrl Pts',(-2.23127208802867,-0.804692985741374,
8.90579690498634));
#63167=CARTESIAN_POINT('Ctrl Pts',(-2.29777435372505,-0.612685363880377,
8.89177191727566));
#63168=CARTESIAN_POINT('Ctrl Pts',(-2.33633596332856,-0.44346836933917,
8.87924453169628));
#63169=CARTESIAN_POINT('Ctrl Pts',(-2.36658112276971,-0.181087885413271,
8.85998287512962));
#63170=CARTESIAN_POINT('Ctrl Pts',(-2.37179094824305,-0.0900468686838555,
8.85334087044894));
#63171=CARTESIAN_POINT('Ctrl Pts',(-2.37172892309297,0.0471615849229897,
8.84355947082574));
#63172=CARTESIAN_POINT('Ctrl Pts',(-2.37036462550106,0.0932442653156125,
8.8403138512315));
#63173=CARTESIAN_POINT('Ctrl Pts',(-2.36699861119947,0.150471749008194,
8.83635476923397));
#63174=CARTESIAN_POINT('Ctrl Pts',(-2.36625960457586,0.161677663697427,
8.83558295171082));
#63175=CARTESIAN_POINT('Ctrl Pts',(-2.36544101854848,0.172878137045581,
8.83481520889907));
#63176=CARTESIAN_POINT('Ctrl Pts',(-2.36544103037033,0.172877975290479,
8.63916402106918));
#63177=CARTESIAN_POINT('Ctrl Pts',(-2.36969110373298,0.114725409024034,
8.64339148986364));
#63178=CARTESIAN_POINT('Ctrl Pts',(-2.37179807639038,0.0563978649742825,
8.64764768427651));
#63179=CARTESIAN_POINT('Ctrl Pts',(-2.37172922193285,-0.0257972780762,8.65363963955622));
#63180=CARTESIAN_POINT('Ctrl Pts',(-2.37135071963491,-0.0496062506427067,
8.65537450011653));
#63181=CARTESIAN_POINT('Ctrl Pts',(-2.36752241566682,-0.173240244889286,
8.66436993795079));
#63182=CARTESIAN_POINT('Ctrl Pts',(-2.35812718016877,-0.272791361719819,
8.67157241560903));
#63183=CARTESIAN_POINT('Ctrl Pts',(-2.33979591461862,-0.388390117061927,
8.67969388238334));
#63184=CARTESIAN_POINT('Ctrl Pts',(-2.33692812120695,-0.40528854325954,
8.68087483945892));
#63185=CARTESIAN_POINT('Ctrl Pts',(-2.33215578260783,-0.431672343114279,
8.68270737349088));
#63186=CARTESIAN_POINT('Ctrl Pts',(-2.33037603146268,-0.441179290541376,
8.68336538761148));
#63187=CARTESIAN_POINT('Ctrl Pts',(-2.32710321772572,-0.458089184916654,
8.68453135861992));
#63188=CARTESIAN_POINT('Ctrl Pts',(-2.32563293743243,-0.465496004095176,
8.68504052548217));
#63189=CARTESIAN_POINT('Ctrl Pts',(-2.32197008549597,-0.48349770857284,
8.68627439277048));
#63190=CARTESIAN_POINT('Ctrl Pts',(-2.31974036097812,-0.494084791326151,
8.68699702096028));
#63191=CARTESIAN_POINT('Ctrl Pts',(-2.31245728566126,-0.527529475203023,
8.68927128501116));
#63192=CARTESIAN_POINT('Ctrl Pts',(-2.30713776898514,-0.550328501778816,
8.69080900581221));
#63193=CARTESIAN_POINT('Ctrl Pts',(-2.29359972583681,-0.604700316003327,
8.69445405567242));
#63194=CARTESIAN_POINT('Ctrl Pts',(-2.285065516087,-0.636190201856579,8.69654709393603));
#63195=CARTESIAN_POINT('Ctrl Pts',(-2.24900109106115,-0.759154993822237,
8.70468480811763));
#63196=CARTESIAN_POINT('Ctrl Pts',(-2.21660355898122,-0.849113301685393,
8.71056300510052));
#63197=CARTESIAN_POINT('Ctrl Pts',(-2.11366517557661,-1.08851380876652,
8.72657174633265));
#63198=CARTESIAN_POINT('Ctrl Pts',(-2.03282120082926,-1.23291259183521,
8.73666928093543));
#63199=CARTESIAN_POINT('Ctrl Pts',(-1.91990059253567,-1.39288434100355,
8.74929915538806));
#63200=CARTESIAN_POINT('Ctrl Pts',(-1.90166713696624,-1.41767663285545,
8.75130040492403));
#63201=CARTESIAN_POINT('Ctrl Pts',(-1.8714127756611,-1.45717973023777,8.75456568377653));
#63202=CARTESIAN_POINT('Ctrl Pts',(-1.85968813330553,-1.47211363539139,
8.75581838269655));
#63203=CARTESIAN_POINT('Ctrl Pts',(-1.8384604931022,-1.498493354043,8.75806505374931));
#63204=CARTESIAN_POINT('Ctrl Pts',(-1.82902662392166,-1.50999367838631,
8.75905626319781));
#63205=CARTESIAN_POINT('Ctrl Pts',(-1.80879385440372,-1.53419055274483,
8.76116738037484));
#63206=CARTESIAN_POINT('Ctrl Pts',(-1.797968082871,-1.54686347443788,8.76228833775034));
#63207=CARTESIAN_POINT('Ctrl Pts',(-1.76838952118473,-1.58075886430365,
8.76532874533101));
#63208=CARTESIAN_POINT('Ctrl Pts',(-1.74938921009142,-1.60176070563365,
8.76725825401839));
#63209=CARTESIAN_POINT('Ctrl Pts',(-1.6197929068788,-1.73995206569927,8.78026989254322));
#63210=CARTESIAN_POINT('Ctrl Pts',(-1.49789679410241,-1.84592790123689,
8.79184388857896));
#63211=CARTESIAN_POINT('Ctrl Pts',(-1.24821512516698,-2.02188035806493,
8.81409382046256));
#63212=CARTESIAN_POINT('Ctrl Pts',(-1.1228471065884,-2.09410175812764,8.8246815597713));
#63213=CARTESIAN_POINT('Ctrl Pts',(-0.971659512126865,-2.16369166523987,
8.83630008420685));
#63214=CARTESIAN_POINT('Ctrl Pts',(-0.951510080256589,-2.17262801291885,
8.83782585534649));
#63215=CARTESIAN_POINT('Ctrl Pts',(-0.921523094717212,-2.18543012534301,
8.84006019157753));
#63216=CARTESIAN_POINT('Ctrl Pts',(-0.911780220517392,-2.1895128423743,
8.8407805223917));
#63217=CARTESIAN_POINT('Ctrl Pts',(-0.894303673782871,-2.19669944103258,
8.84206221057335));
#63218=CARTESIAN_POINT('Ctrl Pts',(-0.886580583446402,-2.19982780471648,
8.84262495682947));
#63219=CARTESIAN_POINT('Ctrl Pts',(-0.869340728826177,-2.20670554778219,
8.84387304950858));
#63220=CARTESIAN_POINT('Ctrl Pts',(-0.859816047487276,-2.21043413190396,
8.84455718570671));
#63221=CARTESIAN_POINT('Ctrl Pts',(-0.83130020326974,-2.22138489244577,
8.84659014982574));
#63222=CARTESIAN_POINT('Ctrl Pts',(-0.812239496907764,-2.22842498974693,
8.84792891853767));
#63223=CARTESIAN_POINT('Ctrl Pts',(-0.673796550087457,-2.277546653924,8.8575241768069));
#63224=CARTESIAN_POINT('Ctrl Pts',(-0.551289798213978,-2.31026155370225,
8.86533442631666));
#63225=CARTESIAN_POINT('Ctrl Pts',(-0.257386274511344,-2.36402025350706,
8.88369868649895));
#63226=CARTESIAN_POINT('Ctrl Pts',(-0.0851790809236598,-2.37646303448863,
8.89420424301676));
#63227=CARTESIAN_POINT('Ctrl Pts',(0.117218371160872,-2.36904650700781,
8.90727269603405));
#63228=CARTESIAN_POINT('Ctrl Pts',(0.14756074138742,-2.36735024740952,8.90924946709203));
#63229=CARTESIAN_POINT('Ctrl Pts',(0.196682960348062,-2.36365609634398,
8.91248274732521));
#63230=CARTESIAN_POINT('Ctrl Pts',(0.215486795199738,-2.36201603209922,
8.91372829507624));
#63231=CARTESIAN_POINT('Ctrl Pts',(0.249059014345419,-2.35868365430675,
8.91596708881466));
#63232=CARTESIAN_POINT('Ctrl Pts',(0.263834994614235,-2.35707659025862,
8.91695764741032));
#63233=CARTESIAN_POINT('Ctrl Pts',(0.295212293031634,-2.35336520227598,
8.91907267189971));
#63234=CARTESIAN_POINT('Ctrl Pts',(0.311808328060308,-2.35122385476407,
8.92019823709332));
#63235=CARTESIAN_POINT('Ctrl Pts',(0.356736790576114,-2.34494280325636,
8.92326471678894));
#63236=CARTESIAN_POINT('Ctrl Pts',(0.385018389970618,-2.34046546748684,
8.92521598845843));
#63237=CARTESIAN_POINT('Ctrl Pts',(0.566627292253324,-2.30833379650326,
8.937886718477));
#63238=CARTESIAN_POINT('Ctrl Pts',(0.716968722902595,-2.26614457234044,
8.94906243748415));
#63239=CARTESIAN_POINT('Ctrl Pts',(1.00153815751344,-2.1551180028078,8.97130230461971));
#63240=CARTESIAN_POINT('Ctrl Pts',(1.13555647389969,-2.08761361022277,8.98229720666778));
#63241=CARTESIAN_POINT('Ctrl Pts',(1.28066162070134,-1.99639001492484,8.99425690028263));
#63242=CARTESIAN_POINT('Ctrl Pts',(1.29884212010733,-1.98460991305389,8.99575593134402));
#63243=CARTESIAN_POINT('Ctrl Pts',(1.3255847528977,-1.96675702246259,8.99795892334738));
#63244=CARTESIAN_POINT('Ctrl Pts',(1.3342715277231,-1.96087419872322,8.99867419677291));
#63245=CARTESIAN_POINT('Ctrl Pts',(1.34978597597072,-1.95021672772141,8.99995067948742));
#63246=CARTESIAN_POINT('Ctrl Pts',(1.35662781040202,-1.94546355811187,9.00051322552578));
#63247=CARTESIAN_POINT('Ctrl Pts',(1.37186825897043,-1.93475619133123,9.00176549047198));
#63248=CARTESIAN_POINT('Ctrl Pts',(1.38025328877524,-1.92878327151087,9.00245395085806));
#63249=CARTESIAN_POINT('Ctrl Pts',(1.4053422714649,-1.91066420249992,9.00451322830024));
#63250=CARTESIAN_POINT('Ctrl Pts',(1.42192722808726,-1.89835392453265,9.00587359584243));
#63251=CARTESIAN_POINT('Ctrl Pts',(1.46032030898519,-1.86907093409941,9.00902610570363));
#63252=CARTESIAN_POINT('Ctrl Pts',(1.48199716105387,-1.85193037472327,9.01080861712011));
#63253=CARTESIAN_POINT('Ctrl Pts',(1.5590991940925,-1.7887423981917,9.01717836782274));
#63254=CARTESIAN_POINT('Ctrl Pts',(1.61272173268814,-1.74055155225078,9.02166555640838));
#63255=CARTESIAN_POINT('Ctrl Pts',(1.78881180502335,-1.567162324042,9.03692570653259));
#63256=CARTESIAN_POINT('Ctrl Pts',(1.89956320930316,-1.4309094780823,9.0475093584347));
#63257=CARTESIAN_POINT('Ctrl Pts',(2.02040849530408,-1.24317025477864,9.06174042270349));
#63258=CARTESIAN_POINT('Ctrl Pts',(2.04526116988756,-1.20184400705704,9.06485015871237));
#63259=CARTESIAN_POINT('Ctrl Pts',(2.07807619458399,-1.14330855506922,9.0692405821331));
#63260=CARTESIAN_POINT('Ctrl Pts',(2.08711886449137,-1.1267164392501,9.07048347262085));
#63261=CARTESIAN_POINT('Ctrl Pts',(2.10247328876188,-1.09772386524254,9.07265348747314));
#63262=CARTESIAN_POINT('Ctrl Pts',(2.1088760491729,-1.08537247508891,9.07357740239453));
#63263=CARTESIAN_POINT('Ctrl Pts',(2.12204237441756,-1.05941730051279,9.0755181584421));
#63264=CARTESIAN_POINT('Ctrl Pts',(2.12878461544259,-1.04580347016109,9.07653568206859));
#63265=CARTESIAN_POINT('Ctrl Pts',(2.14459076840625,-1.01310166329334,9.07897934956259));
#63266=CARTESIAN_POINT('Ctrl Pts',(2.15353115172818,-0.993955770140758,
9.08040962233996));
#63267=CARTESIAN_POINT('Ctrl Pts',(2.18402890161604,-0.926300993892744,
9.08546369969597));
#63268=CARTESIAN_POINT('Ctrl Pts',(2.20421115454798,-0.877193363210987,
9.08913268420984));
#63269=CARTESIAN_POINT('Ctrl Pts',(2.25088625676115,-0.751813408810636,
9.09850675869672));
#63270=CARTESIAN_POINT('Ctrl Pts',(2.27516275698209,-0.674792296983518,
9.10427277130544));
#63271=CARTESIAN_POINT('Ctrl Pts',(2.33424262951194,-0.447512162946366,
9.12124935201723));
#63272=CARTESIAN_POINT('Ctrl Pts',(2.35838562298804,-0.294912238489469,
9.13262263793216));
#63273=CARTESIAN_POINT('Ctrl Pts',(2.37027110054534,-0.0954107725242537,
9.14686640411079));
#63274=CARTESIAN_POINT('Ctrl Pts',(2.37167005911244,-0.0496998372567961,
9.15008544845627));
#63275=CARTESIAN_POINT('Ctrl Pts',(2.37177071217618,0.0103752464815843,
9.15423463620473));
#63276=CARTESIAN_POINT('Ctrl Pts',(2.37166453690988,0.0247246146822026,
9.15521958679712));
#63277=CARTESIAN_POINT('Ctrl Pts',(2.37128045049076,0.0480359387389798,
9.15680882991398));
#63278=CARTESIAN_POINT('Ctrl Pts',(2.37108194591365,0.0569985853377878,
9.1574172461428));
#63279=CARTESIAN_POINT('Ctrl Pts',(2.37059070320885,0.0746555425380767,
9.15861044060898));
#63280=CARTESIAN_POINT('Ctrl Pts',(2.37030094293751,0.0833497220091635,
9.15919535427092));
#63281=CARTESIAN_POINT('Ctrl Pts',(2.369454711778,0.105139032489686,9.16065515535903));
#63282=CARTESIAN_POINT('Ctrl Pts',(2.36883750353173,0.118231757663547,9.16152678940569));
#63283=CARTESIAN_POINT('Ctrl Pts',(2.36597292280751,0.169889509056894,9.16494638937481));
#63284=CARTESIAN_POINT('Ctrl Pts',(2.36289192527264,0.208404577931597,9.1674531636235));
#63285=CARTESIAN_POINT('Ctrl Pts',(2.35196738337655,0.312806873967035,9.17417319520786));
#63286=CARTESIAN_POINT('Ctrl Pts',(2.34229809410907,0.378470003194304,9.1783185098135));
#63287=CARTESIAN_POINT('Ctrl Pts',(2.30097554920606,0.595483189855097,9.19199181287162));
#63288=CARTESIAN_POINT('Ctrl Pts',(2.25729131104077,0.744126445343541,9.201337930195));
#63289=CARTESIAN_POINT('Ctrl Pts',(2.17316880613711,0.952612701511904,9.21547654532826));
#63290=CARTESIAN_POINT('Ctrl Pts',(2.1440017754646,1.01655722927408,9.21996008780387));
#63291=CARTESIAN_POINT('Ctrl Pts',(2.10113432665654,1.10045779208825,9.22610055730908));
#63292=CARTESIAN_POINT('Ctrl Pts',(2.08990384524729,1.12163927380636,9.22767349731689));
#63293=CARTESIAN_POINT('Ctrl Pts',(2.07076790264729,1.15644556001664,9.23029812410213));
#63294=CARTESIAN_POINT('Ctrl Pts',(2.06304418638892,1.17016866515129,9.23134341206431));
#63295=CARTESIAN_POINT('Ctrl Pts',(2.04759205729515,1.19699466014047,9.23340799325484));
#63296=CARTESIAN_POINT('Ctrl Pts',(2.03987309711524,1.21010213568609,9.23442691281994));
#63297=CARTESIAN_POINT('Ctrl Pts',(2.02107518299485,1.24133166206136,9.23687949603385));
#63298=CARTESIAN_POINT('Ctrl Pts',(2.00987799385751,1.25938063743353,9.23831736675421));
#63299=CARTESIAN_POINT('Ctrl Pts',(1.96944765578644,1.32263837838641,9.24343100964493));
#63300=CARTESIAN_POINT('Ctrl Pts',(1.93892119410322,1.3669967650531,9.24715339965342));
#63301=CARTESIAN_POINT('Ctrl Pts',(1.85790595105463,1.47654211669806,9.25670478737249));
#63302=CARTESIAN_POINT('Ctrl Pts',(1.8054813240699,1.54020326325481,9.26259778430103));
#63303=CARTESIAN_POINT('Ctrl Pts',(1.6297996334736,1.73221887539952,9.28142553029935));
#63304=CARTESIAN_POINT('Ctrl Pts',(1.49536649525984,1.84951652990295,9.29459465223122));
#63305=CARTESIAN_POINT('Ctrl Pts',(1.32808994357103,1.96520396407011,9.30885609830946));
#63306=CARTESIAN_POINT('Ctrl Pts',(1.30686355317677,1.97938306056233,9.31062959341449));
#63307=CARTESIAN_POINT('Ctrl Pts',(1.27666754142965,1.99885624859202,9.31309768649173));
#63308=CARTESIAN_POINT('Ctrl Pts',(1.26788648379674,2.00443762387957,9.31380900791315));
#63309=CARTESIAN_POINT('Ctrl Pts',(1.25189033752674,2.01445784158312,9.3150928281774));
#63310=CARTESIAN_POINT('Ctrl Pts',(1.24468766128208,2.01891615663986,9.31566654168909));
#63311=CARTESIAN_POINT('Ctrl Pts',(1.22963952105555,2.0281195154152,9.31685590251305));
#63312=CARTESIAN_POINT('Ctrl Pts',(1.22179020862177,2.03285779476494,9.31747112850516));
#63313=CARTESIAN_POINT('Ctrl Pts',(1.20078591549016,2.04537154277977,9.31910427150307));
#63314=CARTESIAN_POINT('Ctrl Pts',(1.18758268057096,2.0530657489581,9.32011719501711));
#63315=CARTESIAN_POINT('Ctrl Pts',(1.1206229276701,2.09122453215934,9.32519047295354));
#63316=CARTESIAN_POINT('Ctrl Pts',(1.06576013446699,2.11971048827659,9.32914198925722));
#63317=CARTESIAN_POINT('Ctrl Pts',(0.868104849406729,2.21272005143675,9.34288640433982));
#63318=CARTESIAN_POINT('Ctrl Pts',(0.720102892398409,2.26521369056948,9.35232418308173));
#63319=CARTESIAN_POINT('Ctrl Pts',(0.469402536932037,2.32705223044951,9.36834515896069));
#63320=CARTESIAN_POINT('Ctrl Pts',(0.369356448200614,2.34501237798579,9.37474192578317));
#63321=CARTESIAN_POINT('Ctrl Pts',(0.241984795319236,2.35952373528033,9.38307137193066));
#63322=CARTESIAN_POINT('Ctrl Pts',(0.21544655113751,2.36209474613533,9.38481646850575));
#63323=CARTESIAN_POINT('Ctrl Pts',(0.172608860409931,2.36551694207414,9.38765161016746));
#63324=CARTESIAN_POINT('Ctrl Pts',(0.156333655671251,2.36664826027426,9.3887329791187));
#63325=CARTESIAN_POINT('Ctrl Pts',(0.125116053418824,2.36849483661091,9.39081585160927));
#63326=CARTESIAN_POINT('Ctrl Pts',(0.110175976349677,2.36923680848318,9.39181647825584));
#63327=CARTESIAN_POINT('Ctrl Pts',(0.0755782586266434,2.37062709223273,
9.39414297296713));
#63328=CARTESIAN_POINT('Ctrl Pts',(0.0559178148986994,2.37117229267772,
9.39547195401794));
#63329=CARTESIAN_POINT('Ctrl Pts',(-0.00759176972708754,2.37214318125126,
9.3997885073408));
#63330=CARTESIAN_POINT('Ctrl Pts',(-0.0514443800924831,2.37159734085096,
9.40280542318398));
#63331=CARTESIAN_POINT('Ctrl Pts',(-0.314738314500225,2.36101438413367,
9.42114844721092));
#63332=CARTESIAN_POINT('Ctrl Pts',(-0.531911557557401,2.32174203550533,
9.43737740328743));
#63333=CARTESIAN_POINT('Ctrl Pts',(-0.807335969270521,2.23122237939522,
9.45829548987956));
#63334=CARTESIAN_POINT('Ctrl Pts',(-0.873149099615852,2.20629944966075,
9.46330773665482));
#63335=CARTESIAN_POINT('Ctrl Pts',(-0.952769312213094,2.17202569596862,
9.46931378367047));
#63336=CARTESIAN_POINT('Ctrl Pts',(-0.967709183547159,2.16541080605382,
9.47043813163747));
#63337=CARTESIAN_POINT('Ctrl Pts',(-0.991134066135066,2.15474816579871,
9.47219557354606));
#63338=CARTESIAN_POINT('Ctrl Pts',(-0.999665088160347,2.15080359730926,
9.47283445450126));
#63339=CARTESIAN_POINT('Ctrl Pts',(-1.0158390312485,2.14320807688906,9.47404319462444));
#63340=CARTESIAN_POINT('Ctrl Pts',(-1.02348589576222,2.13956687709165,9.47461355948928));
#63341=CARTESIAN_POINT('Ctrl Pts',(-1.04179792388996,2.13072661603665,9.47597703956171));
#63342=CARTESIAN_POINT('Ctrl Pts',(-1.05244385886684,2.12548835918394,9.47676778860926));
#63343=CARTESIAN_POINT('Ctrl Pts',(-1.08952073235049,2.10689806862577,9.47951654661126));
#63344=CARTESIAN_POINT('Ctrl Pts',(-1.11574174014033,2.09313054052115,9.48145118469449));
#63345=CARTESIAN_POINT('Ctrl Pts',(-1.1811297912143,2.05722000819529,9.48626937657015));
#63346=CARTESIAN_POINT('Ctrl Pts',(-1.21993845281494,2.03444645896966,9.48912330004573));
#63347=CARTESIAN_POINT('Ctrl Pts',(-1.42214459709699,1.90792032730895,9.50408729962109));
#63348=CARTESIAN_POINT('Ctrl Pts',(-1.57302976684585,1.78556392645479,9.51564900818305));
#63349=CARTESIAN_POINT('Ctrl Pts',(-1.7529378803204,1.59897336871174,9.53199001684069));
#63350=CARTESIAN_POINT('Ctrl Pts',(-1.7965155368893,1.54985089642644,9.53618780621946));
#63351=CARTESIAN_POINT('Ctrl Pts',(-1.85283569250154,1.48079342399289,9.54199901086684));
#63352=CARTESIAN_POINT('Ctrl Pts',(-1.86740263087196,1.46238046289781,9.54354013243447));
#63353=CARTESIAN_POINT('Ctrl Pts',(-1.89026557830815,1.43258242695924,9.54602275896612));
#63354=CARTESIAN_POINT('Ctrl Pts',(-1.89873790866833,1.4213341290635,9.54695737318403));
#63355=CARTESIAN_POINT('Ctrl Pts',(-1.91606753494523,1.3978949590008,9.54890011003865));
#63356=CARTESIAN_POINT('Ctrl Pts',(-1.92490980056579,1.38569381780829,9.54990874947502));
#63357=CARTESIAN_POINT('Ctrl Pts',(-1.94544837205442,1.35677738625094,9.55229350503431));
#63358=CARTESIAN_POINT('Ctrl Pts',(-1.95704629843104,1.33999402435167,9.5536732375475));
#63359=CARTESIAN_POINT('Ctrl Pts',(-1.99536836053763,1.28297927189882,9.55834693565643));
#63360=CARTESIAN_POINT('Ctrl Pts',(-2.02107826053437,1.24208405186535,9.56167746367964));
#63361=CARTESIAN_POINT('Ctrl Pts',(-2.11990997075654,1.07367652851818,9.57531440363025));
#63362=CARTESIAN_POINT('Ctrl Pts',(-2.18234618852898,0.940294325538168,
9.58596604376384));
#63363=CARTESIAN_POINT('Ctrl Pts',(-2.26345742274058,0.714558909791934,
9.60345463387719));
#63364=CARTESIAN_POINT('Ctrl Pts',(-2.289716188443,0.625328240950382,9.61023252754985));
#63365=CARTESIAN_POINT('Ctrl Pts',(-2.32126694420569,0.48900484363474,9.62021316956104));
#63366=CARTESIAN_POINT('Ctrl Pts',(-2.33049997824004,0.44291816469533,9.62352390107418));
#63367=CARTESIAN_POINT('Ctrl Pts',(-2.34078042033313,0.382302146062441,
9.62777121849047));
#63368=CARTESIAN_POINT('Ctrl Pts',(-2.34307182890227,0.367997741472551,
9.62876576136883));
#63369=CARTESIAN_POINT('Ctrl Pts',(-2.34657335094488,0.344778874157576,
9.63036659347512));
#63370=CARTESIAN_POINT('Ctrl Pts',(-2.3478640242078,0.335877200775326,9.63097711420203));
#63371=CARTESIAN_POINT('Ctrl Pts',(-2.35018518307835,0.319200828476313,
9.63211459384491));
#63372=CARTESIAN_POINT('Ctrl Pts',(-2.35122779282664,0.311428053561827,
9.63264220855057));
#63373=CARTESIAN_POINT('Ctrl Pts',(-2.35333889442491,0.29507436395037,9.63374717934676));
#63374=CARTESIAN_POINT('Ctrl Pts',(-2.35439905964234,0.286492418602906,
9.63432408236932));
#63375=CARTESIAN_POINT('Ctrl Pts',(-2.35682411179554,0.265938618886863,
9.63569911596267));
#63376=CARTESIAN_POINT('Ctrl Pts',(-2.35814476549191,0.253961654898472,
9.63649497337361));
#63377=CARTESIAN_POINT('Ctrl Pts',(-2.36173336889086,0.218971002775416,
9.63880570166824));
#63378=CARTESIAN_POINT('Ctrl Pts',(-2.36375581492573,0.195936286500906,
9.64030877126689));
#63379=CARTESIAN_POINT('Ctrl Pts',(-2.36544101901418,0.172878130673515,
9.64179857564526));
#63380=CARTESIAN_POINT('Origin',(0.,0.,-1.84858989190501));
#63381=CARTESIAN_POINT('',(-2.36342245950295,0.172714633282403,10.8368568258743));
#63382=CARTESIAN_POINT('',(-2.36544102832235,0.172878003312457,10.6380411716245));
#63383=CARTESIAN_POINT('',(-2.36544101854889,0.172878137039864,-1.84858989190501));
#63384=CARTESIAN_POINT('',(-2.36840389010906,0.000992657309442972,9.8486171864275));
#63385=CARTESIAN_POINT('Ctrl Pts',(-2.36835645684558,0.00099074781327764,
9.84858989190503));
#63386=CARTESIAN_POINT('Ctrl Pts',(-2.36661646666674,-0.456757128880904,
9.87920456926939));
#63387=CARTESIAN_POINT('Ctrl Pts',(-2.01853982608692,-1.70439405627733,
9.96248421030043));
#63388=CARTESIAN_POINT('Ctrl Pts',(-0.00283249851198579,-2.79870028674429,
10.0984288149982));
#63389=CARTESIAN_POINT('Ctrl Pts',(2.34239313895008,-1.53164150527581,10.2564237059982));
#63390=CARTESIAN_POINT('Ctrl Pts',(2.56269918704329,1.12485741087042,10.4144185969983));
#63391=CARTESIAN_POINT('Ctrl Pts',(0.458233353927178,2.76093344928963,10.5724134879983));
#63392=CARTESIAN_POINT('Ctrl Pts',(-1.78785214186282,1.98686117431254,10.713226230957));
#63393=CARTESIAN_POINT('Ctrl Pts',(-2.32054658323031,0.700757067499405,
10.8013740102491));
#63394=CARTESIAN_POINT('Ctrl Pts',(-2.36342245950295,0.172714633282403,
10.8368568258743));
#63395=CARTESIAN_POINT('Ctrl Pts',(-2.37174973207207,0.00112734912545944,
9.85054248424486));
#63396=CARTESIAN_POINT('Ctrl Pts',(-2.37172246228312,0.0584983207034222,
9.84657087381565));
#63397=CARTESIAN_POINT('Ctrl Pts',(-2.36961357827909,0.11578635994523,9.84254327253529));
#63398=CARTESIAN_POINT('Ctrl Pts',(-2.36544098814985,0.172878552980629,
9.83847008213863));
#63399=CARTESIAN_POINT('',(-2.37174935477677,0.00174946163004134,9.65263340565988));
#63400=CARTESIAN_POINT('Ctrl Pts',(-2.36544101901418,0.172878130673515,
9.64179857564526));
#63401=CARTESIAN_POINT('Ctrl Pts',(-2.36960227195145,0.115940920917956,
9.64547733057349));
#63402=CARTESIAN_POINT('Ctrl Pts',(-2.3717072280224,0.0588608042184611,
9.6490754070573));
#63403=CARTESIAN_POINT('Ctrl Pts',(-2.37174935477677,0.00174946162997413,
9.65263340565988));
#63404=CARTESIAN_POINT('Ctrl Pts',(-2.37174935259837,0.0017524123925753,
9.6526332218293));
#63405=CARTESIAN_POINT('Ctrl Pts',(-2.37189696828361,-0.198033555437239,
9.66507975964639));
#63406=CARTESIAN_POINT('Ctrl Pts',(-2.34680234990767,-0.397041953603912,
9.67703688754385));
#63407=CARTESIAN_POINT('Ctrl Pts',(-2.28444680226741,-0.639579868005419,
9.69298420833203));
#63408=CARTESIAN_POINT('Ctrl Pts',(-2.27027959600028,-0.688178450613413,
9.69624710276722));
#63409=CARTESIAN_POINT('Ctrl Pts',(-2.24812457344293,-0.756019162610858,
9.7009177805947));
#63410=CARTESIAN_POINT('Ctrl Pts',(-2.24142094803958,-0.775668202873776,
9.7022844840852));
#63411=CARTESIAN_POINT('Ctrl Pts',(-2.22938819730055,-0.809478337383775,
9.7046615899808));
#63412=CARTESIAN_POINT('Ctrl Pts',(-2.22417984286543,-0.823681322903598,
9.70566800719936));
#63413=CARTESIAN_POINT('Ctrl Pts',(-2.21322217939644,-0.852700533225414,
9.7077409082246));
#63414=CARTESIAN_POINT('Ctrl Pts',(-2.20745911926852,-0.86751070914359,
9.70880780316681));
#63415=CARTESIAN_POINT('Ctrl Pts',(-2.1923718049639,-0.905158777718782,
9.7115434511026));
#63416=CARTESIAN_POINT('Ctrl Pts',(-2.18283948693289,-0.927910685051638,
9.71321903300169));
#63417=CARTESIAN_POINT('Ctrl Pts',(-2.14219244083099,-1.02083370810906,
9.720157291347));
#63418=CARTESIAN_POINT('Ctrl Pts',(-2.10803802273787,-1.08961616571965,
9.72552008268168));
#63419=CARTESIAN_POINT('Ctrl Pts',(-1.99153094959514,-1.29819103162955,
9.74250231450349));
#63420=CARTESIAN_POINT('Ctrl Pts',(-1.89814132261071,-1.43127430452756,
9.75443100791042));
#63421=CARTESIAN_POINT('Ctrl Pts',(-1.75518481734824,-1.59614192310762,
9.77023714630915));
#63422=CARTESIAN_POINT('Ctrl Pts',(-1.71695385698451,-1.63719669212105,
9.77426797587678));
#63423=CARTESIAN_POINT('Ctrl Pts',(-1.66062531935576,-1.69354005801802,
9.77989754426118));
#63424=CARTESIAN_POINT('Ctrl Pts',(-1.64370084065891,-1.70997134979475,
9.78155180578109));
#63425=CARTESIAN_POINT('Ctrl Pts',(-1.61364265102402,-1.7382949040952,9.78442138122552));
#63426=CARTESIAN_POINT('Ctrl Pts',(-1.60061577677476,-1.75029739179488,
9.78564329703428));
#63427=CARTESIAN_POINT('Ctrl Pts',(-1.58040473826532,-1.76850472888952,
9.78750442533477));
#63428=CARTESIAN_POINT('Ctrl Pts',(-1.5733160709537,-1.77481397939371,9.78815077141662));
#63429=CARTESIAN_POINT('Ctrl Pts',(-1.5599322125769,-1.78658304751176,9.78935882124527));
#63430=CARTESIAN_POINT('Ctrl Pts',(-1.55364599731484,-1.79205234670469,
9.78992117026506));
#63431=CARTESIAN_POINT('Ctrl Pts',(-1.53932901511499,-1.80437682326645,
9.79119060200072));
#63432=CARTESIAN_POINT('Ctrl Pts',(-1.53128116589691,-1.81121162169856,
9.79189623683382));
#63433=CARTESIAN_POINT('Ctrl Pts',(-1.50631449331585,-1.83212971000257,
9.79406193584163));
#63434=CARTESIAN_POINT('Ctrl Pts',(-1.48924450155775,-1.84603183220491,
9.79550989709972));
#63435=CARTESIAN_POINT('Ctrl Pts',(-1.35898877087792,-1.94913163910465,
9.80633594102442));
#63436=CARTESIAN_POINT('Ctrl Pts',(-1.23806316720064,-2.0280964565922,9.81514692234843));
#63437=CARTESIAN_POINT('Ctrl Pts',(-0.968094416981237,-2.17118428167353,
9.83391011966802));
#63438=CARTESIAN_POINT('Ctrl Pts',(-0.818162954298518,-2.23200555721507,
9.8438406924624));
#63439=CARTESIAN_POINT('Ctrl Pts',(-0.636025910893141,-2.28505400205844,
9.85614499011183));
#63440=CARTESIAN_POINT('Ctrl Pts',(-0.608685618214998,-2.2924882681643,
9.85799689387449));
#63441=CARTESIAN_POINT('Ctrl Pts',(-0.565058162149105,-2.30351583815349,
9.86096309319629));
#63442=CARTESIAN_POINT('Ctrl Pts',(-0.548854435514508,-2.30743033009552,
9.86206716745091));
#63443=CARTESIAN_POINT('Ctrl Pts',(-0.518116864625605,-2.31451381888413,
9.86416670008757));
#63444=CARTESIAN_POINT('Ctrl Pts',(-0.503591787347632,-2.31771754055666,
9.86516100404022));
#63445=CARTESIAN_POINT('Ctrl Pts',(-0.470463666611901,-2.32469832858261,
9.86743414716486));
#63446=CARTESIAN_POINT('Ctrl Pts',(-0.451843681657343,-2.32838906368685,
9.86871563555951));
#63447=CARTESIAN_POINT('Ctrl Pts',(-0.402940520373667,-2.33747365721108,
9.87209222031347));
#63448=CARTESIAN_POINT('Ctrl Pts',(-0.372594041330407,-2.3425024417487,
9.87419847837966));
#63449=CARTESIAN_POINT('Ctrl Pts',(-0.178488731972618,-2.37080099062955,
9.88774546478855));
#63450=CARTESIAN_POINT('Ctrl Pts',(-0.0127978964774504,-2.3774721637237,
9.89969441778271));
#63451=CARTESIAN_POINT('Ctrl Pts',(0.247311519571186,-2.36074503467751,
9.91869703591491));
#63452=CARTESIAN_POINT('Ctrl Pts',(0.341964252868863,-2.34890235623918,
9.9256521829863));
#63453=CARTESIAN_POINT('Ctrl Pts',(0.467675137770763,-2.32541165297936,
9.93477691163778));
#63454=CARTESIAN_POINT('Ctrl Pts',(0.499573820109125,-2.31876812153278,
9.93708193359391));
#63455=CARTESIAN_POINT('Ctrl Pts',(0.554118736770761,-2.30623012680582,
9.940994920712));
#63456=CARTESIAN_POINT('Ctrl Pts',(0.576832790482701,-2.30065403857896,
9.9426158099575));
#63457=CARTESIAN_POINT('Ctrl Pts',(0.6099252771058,-2.29200920102225,9.94496114813725));
#63458=CARTESIAN_POINT('Ctrl Pts',(0.62037031996651,-2.2892041627286,9.94569903808636));
#63459=CARTESIAN_POINT('Ctrl Pts',(0.638074917294891,-2.28431947791222,
9.94694532121363));
#63460=CARTESIAN_POINT('Ctrl Pts',(0.645344204936719,-2.28227648200979,
9.94745573191827));
#63461=CARTESIAN_POINT('Ctrl Pts',(0.661905050982908,-2.27753668758164,
9.94861551355769));
#63462=CARTESIAN_POINT('Ctrl Pts',(0.671190004016461,-2.27481771720609,
9.9492636164745));
#63463=CARTESIAN_POINT('Ctrl Pts',(0.696888540505749,-2.26712121252731,
9.9510521462279));
#63464=CARTESIAN_POINT('Ctrl Pts',(0.713265537282157,-2.26202222465746,
9.95218595151629));
#63465=CARTESIAN_POINT('Ctrl Pts',(0.825583057221632,-2.22571094517473,
9.95992986188339));
#63466=CARTESIAN_POINT('Ctrl Pts',(0.919514131052333,-2.18857839074197,
9.96624676617244));
#63467=CARTESIAN_POINT('Ctrl Pts',(1.03179075061727,-2.13568352032923,9.97391954991515));
#63468=CARTESIAN_POINT('Ctrl Pts',(1.05263133129648,-2.12548901492121,9.97534902856974));
#63469=CARTESIAN_POINT('Ctrl Pts',(1.18774129844156,-2.05692316014143,9.98467001472017));
#63470=CARTESIAN_POINT('Ctrl Pts',(1.29725706456724,-1.98966944818795,9.99249186079622));
#63471=CARTESIAN_POINT('Ctrl Pts',(1.45771111815406,-1.87223165718302,10.0050024211273));
#63472=CARTESIAN_POINT('Ctrl Pts',(1.51273723112318,-1.82805845665418,10.0095066563379));
#63473=CARTESIAN_POINT('Ctrl Pts',(1.58324729280076,-1.76608923666427,10.01562923608));
#63474=CARTESIAN_POINT('Ctrl Pts',(1.60055554172562,-1.75041854337613,10.0171620206678));
#63475=CARTESIAN_POINT('Ctrl Pts',(1.62905135931443,-1.72384270645276,10.0197378614953));
#63476=CARTESIAN_POINT('Ctrl Pts',(1.64036783860305,-1.71307773974128,10.0207750140567));
#63477=CARTESIAN_POINT('Ctrl Pts',(1.66243229935759,-1.69166949634559,10.0228259821768));
#63478=CARTESIAN_POINT('Ctrl Pts',(1.67318643037672,-1.68103360642867,10.0238394526183));
#63479=CARTESIAN_POINT('Ctrl Pts',(1.69905037083895,-1.65495997136972,10.0263112715902));
#63480=CARTESIAN_POINT('Ctrl Pts',(1.71405218430938,-1.63941749591492,10.0277741779942));
#63481=CARTESIAN_POINT('Ctrl Pts',(1.76479964833593,-1.585383081048,10.0328258730662));
#63482=CARTESIAN_POINT('Ctrl Pts',(1.79947552136426,-1.54591216470964,10.0364582794382));
#63483=CARTESIAN_POINT('Ctrl Pts',(1.94129249893621,-1.37324275081368,10.0521188421248));
#63484=CARTESIAN_POINT('Ctrl Pts',(2.03516643270432,-1.22983508180745,10.064618333903));
#63485=CARTESIAN_POINT('Ctrl Pts',(2.14502800773871,-1.0144371271919,10.0822127012073));
#63486=CARTESIAN_POINT('Ctrl Pts',(2.1744032986397,-0.949841751574492,10.0873458723951));
#63487=CARTESIAN_POINT('Ctrl Pts',(2.21104009186348,-0.858631780811633,
10.0943222945228));
#63488=CARTESIAN_POINT('Ctrl Pts',(2.22079957839519,-0.833064337761657,
10.096249090814));
#63489=CARTESIAN_POINT('Ctrl Pts',(2.23709290343086,-0.788056883134659,
10.0995843611732));
#63490=CARTESIAN_POINT('Ctrl Pts',(2.24382107317067,-0.768690686169711,
10.1010014571952));
#63491=CARTESIAN_POINT('Ctrl Pts',(2.2535400834804,-0.739500176684509,10.1031080225628));
#63492=CARTESIAN_POINT('Ctrl Pts',(2.25671942301165,-0.729740278961135,
10.103807464271));
#63493=CARTESIAN_POINT('Ctrl Pts',(2.26236448246739,-0.712021366587215,
10.1050680593437));
#63494=CARTESIAN_POINT('Ctrl Pts',(2.26485170806518,-0.704069757499664,
10.1056303847271));
#63495=CARTESIAN_POINT('Ctrl Pts',(2.27038572663566,-0.686044793136716,
10.1068975082129));
#63496=CARTESIAN_POINT('Ctrl Pts',(2.2734074316233,-0.675964101217361,10.1076008831616));
#63497=CARTESIAN_POINT('Ctrl Pts',(2.28249102437409,-0.644910366171897,
10.1097523965818));
#63498=CARTESIAN_POINT('Ctrl Pts',(2.2883307141886,-0.623872808507573,10.1111886595128));
#63499=CARTESIAN_POINT('Ctrl Pts',(2.33109489386882,-0.461127435375906,
10.1221573914015));
#63500=CARTESIAN_POINT('Ctrl Pts',(2.35511886311573,-0.316336120004382,
10.131102497151));
#63501=CARTESIAN_POINT('Ctrl Pts',(2.37691494453227,-0.0134562447597651,
10.1497507797876));
#63502=CARTESIAN_POINT('Ctrl Pts',(2.37258311042138,0.144038363818025,10.1594289844395));
#63503=CARTESIAN_POINT('Ctrl Pts',(2.34897565927689,0.329214987849362,10.1715222979813));
#63504=CARTESIAN_POINT('Ctrl Pts',(2.34469717691383,0.358419001594101,10.1734497324591));
#63505=CARTESIAN_POINT('Ctrl Pts',(2.33711038642924,0.404226892874554,10.1765086158826));
#63506=CARTESIAN_POINT('Ctrl Pts',(2.33416729165211,0.420888784848467,10.1776286874421));
#63507=CARTESIAN_POINT('Ctrl Pts',(2.32830935124672,0.452099268480903,10.1797414524958));
#63508=CARTESIAN_POINT('Ctrl Pts',(2.32543575071495,0.466654836014901,10.1807328060753));
#63509=CARTESIAN_POINT('Ctrl Pts',(2.31865527081592,0.499380820835648,10.1829757710508));
#63510=CARTESIAN_POINT('Ctrl Pts',(2.31467102813681,0.517534024829609,10.1842297648244));
#63511=CARTESIAN_POINT('Ctrl Pts',(2.30383592185284,0.564271236033883,10.1874844960903));
#63512=CARTESIAN_POINT('Ctrl Pts',(2.29666646803133,0.59277734818792,10.1894951184429));
#63513=CARTESIAN_POINT('Ctrl Pts',(2.24089316067131,0.798307538488215,10.2041826415171));
#63514=CARTESIAN_POINT('Ctrl Pts',(2.17241863239951,0.969262788708023,10.2175040804772));
#63515=CARTESIAN_POINT('Ctrl Pts',(2.029065362032,1.23362584189697,10.2394253353511));
#63516=CARTESIAN_POINT('Ctrl Pts',(1.9656191104642,1.33239857826465,10.2479439564619));
#63517=CARTESIAN_POINT('Ctrl Pts',(1.88296421062956,1.44223878139379,10.2575191368997));
#63518=CARTESIAN_POINT('Ctrl Pts',(1.87059958548463,1.45824009647451,10.2589165186127));
#63519=CARTESIAN_POINT('Ctrl Pts',(1.85168643000596,1.48207950051417,10.2609997962191));
#63520=CARTESIAN_POINT('Ctrl Pts',(1.84528981056551,1.49003617592114,10.2616953530094));
#63521=CARTESIAN_POINT('Ctrl Pts',(1.83357866390065,1.50441244048723,10.2629521554821));
#63522=CARTESIAN_POINT('Ctrl Pts',(1.82828153294526,1.51084550792069,10.2635145323511));
#63523=CARTESIAN_POINT('Ctrl Pts',(1.81617883535609,1.5253866872513,10.264785769289));
#63524=CARTESIAN_POINT('Ctrl Pts',(1.80935278444664,1.53347729674108,10.265493162269));
#63525=CARTESIAN_POINT('Ctrl Pts',(1.78807304939942,1.55835928805388,10.2676699371144));
#63526=CARTESIAN_POINT('Ctrl Pts',(1.77343762327078,1.57499459759057,10.2691270370286));
#63527=CARTESIAN_POINT('Ctrl Pts',(1.66233599385471,1.69776525548381,10.279915728994));
#63528=CARTESIAN_POINT('Ctrl Pts',(1.55664058149877,1.79517374732517,10.2886868068831));
#63529=CARTESIAN_POINT('Ctrl Pts',(1.31430550141054,1.98090883246258,10.3074365109161));
#63530=CARTESIAN_POINT('Ctrl Pts',(1.17610804970284,2.06595257120173,10.3173939329292));
#63531=CARTESIAN_POINT('Ctrl Pts',(1.00481904177262,2.14856682916893,10.3297284572614));
#63532=CARTESIAN_POINT('Ctrl Pts',(0.979083180604796,2.16041587233054,10.3315803322242));
#63533=CARTESIAN_POINT('Ctrl Pts',(0.937877769959852,2.17849976558698,10.3345464961994));
#63534=CARTESIAN_POINT('Ctrl Pts',(0.922543571243064,2.18503759134694,10.335650564338));
#63535=CARTESIAN_POINT('Ctrl Pts',(0.89339883359168,2.19710214324928,10.337750092124));
#63536=CARTESIAN_POINT('Ctrl Pts',(0.879602677463094,2.20266166634965,10.3387443974142));
#63537=CARTESIAN_POINT('Ctrl Pts',(0.848083034370927,2.21501998942308,10.3410175531051));
#63538=CARTESIAN_POINT('Ctrl Pts',(0.830328573856182,2.22173644031019,10.3422990528386));
#63539=CARTESIAN_POINT('Ctrl Pts',(0.783597756079672,2.23877617298577,10.3456756881765));
#63540=CARTESIAN_POINT('Ctrl Pts',(0.75449864286222,2.24874983982022,10.3477819860328));
#63541=CARTESIAN_POINT('Ctrl Pts',(0.567748495047655,2.30872536457436,10.3613281002155));
#63542=CARTESIAN_POINT('Ctrl Pts',(0.405450364494166,2.34267865474243,10.3732760495036));
#63543=CARTESIAN_POINT('Ctrl Pts',(0.146156633887866,2.36916020515457,10.3922783545669));
#63544=CARTESIAN_POINT('Ctrl Pts',(0.0508390205520596,2.37312008888871,
10.3992341827757));
#63545=CARTESIAN_POINT('Ctrl Pts',(-0.0770361610597585,2.37072244975007,
10.4083596990675));
#63546=CARTESIAN_POINT('Ctrl Pts',(-0.109595841219814,2.36944053910416,
10.4106648477868));
#63547=CARTESIAN_POINT('Ctrl Pts',(-0.165465339254681,2.36608669272603,
10.414578026264));
#63548=CARTESIAN_POINT('Ctrl Pts',(-0.188789443928183,2.36434000580312,
10.4161989816768));
#63549=CARTESIAN_POINT('Ctrl Pts',(-0.222856535826352,2.36128142951531,
10.4185443968077));
#63550=CARTESIAN_POINT('Ctrl Pts',(-0.233621649172559,2.36024065749635,
10.4192822987401));
#63551=CARTESIAN_POINT('Ctrl Pts',(-0.251890166376688,2.3583482401123,10.4205285952718));
#63552=CARTESIAN_POINT('Ctrl Pts',(-0.259397114464808,2.35753435192281,
10.4210390075136));
#63553=CARTESIAN_POINT('Ctrl Pts',(-0.276513377142015,2.35559589273409,
10.4221987832332));
#63554=CARTESIAN_POINT('Ctrl Pts',(-0.286119840559264,2.3544483648302,10.4228468787794));
#63555=CARTESIAN_POINT('Ctrl Pts',(-0.312736197410932,2.35110363098444,
10.4246353678878));
#63556=CARTESIAN_POINT('Ctrl Pts',(-0.329730074791131,2.34878060531698,
10.4257691403868));
#63557=CARTESIAN_POINT('Ctrl Pts',(-0.446456614498282,2.33153247007922,
10.4335099576443));
#63558=CARTESIAN_POINT('Ctrl Pts',(-0.545186597271174,2.31044232772754,
10.4398240793893));
#63559=CARTESIAN_POINT('Ctrl Pts',(-0.663414950866502,2.27718257967988,
10.4474169113792));
#63560=CARTESIAN_POINT('Ctrl Pts',(-0.684462145524698,2.27094506470677,
10.4487697368993));
#63561=CARTESIAN_POINT('Ctrl Pts',(-0.800337493661663,2.23484711805594,
10.4562376646973));
#63562=CARTESIAN_POINT('Ctrl Pts',(-0.893299901973538,2.19934001456066,
10.4623078060687));
#63563=CARTESIAN_POINT('Ctrl Pts',(-1.04187266082449,2.1316140374058,10.4724630956405));
#63564=CARTESIAN_POINT('Ctrl Pts',(-1.09888925499292,2.10278828842802,10.4764764716026));
#63565=CARTESIAN_POINT('Ctrl Pts',(-1.19404951007999,2.0497502928577,10.4834414070272));
#63566=CARTESIAN_POINT('Ctrl Pts',(-1.23279261940857,2.02668508578709,10.486356464352));
#63567=CARTESIAN_POINT('Ctrl Pts',(-1.2876351910465,1.99188070576603,10.4906130051567));
#63568=CARTESIAN_POINT('Ctrl Pts',(-1.30428232660842,1.98102011709773,10.4919228874475));
#63569=CARTESIAN_POINT('Ctrl Pts',(-1.33323941820297,1.96160530036622,10.4942340205658));
#63570=CARTESIAN_POINT('Ctrl Pts',(-1.34560860219892,1.95314110421553,10.4952319022128));
#63571=CARTESIAN_POINT('Ctrl Pts',(-1.37119656429182,1.93527289912736,10.4973190295664));
#63572=CARTESIAN_POINT('Ctrl Pts',(-1.3844007053726,1.92584939094815,10.4984089744894));
#63573=CARTESIAN_POINT('Ctrl Pts',(-1.41869733937242,1.90083765099661,10.5012746867894));
#63574=CARTESIAN_POINT('Ctrl Pts',(-1.43962925860995,1.88503406312493,10.5030586040423));
#63575=CARTESIAN_POINT('Ctrl Pts',(-1.53460997740724,1.81081888955236,10.51131884108));
#63576=CARTESIAN_POINT('Ctrl Pts',(-1.60538674456188,1.74837703192024,10.517950779524));
#63577=CARTESIAN_POINT('Ctrl Pts',(-1.7882257216775,1.56658637890967,10.5364257575791));
#63578=CARTESIAN_POINT('Ctrl Pts',(-1.8919531697296,1.43960138715518,10.548497385358));
#63579=CARTESIAN_POINT('Ctrl Pts',(-2.01632472267099,1.25043375420406,10.5647754803677));
#63580=CARTESIAN_POINT('Ctrl Pts',(-2.04876151676514,1.1965482384832,10.569237858778));
#63581=CARTESIAN_POINT('Ctrl Pts',(-2.08641154346434,1.12797195932742,10.5746500680487));
#63582=CARTESIAN_POINT('Ctrl Pts',(-2.09367114818095,1.11443933156233,10.5757055620591));
#63583=CARTESIAN_POINT('Ctrl Pts',(-2.10506210914811,1.09270121228457,10.5773800075954));
#63584=CARTESIAN_POINT('Ctrl Pts',(-2.10927797914548,1.08454084134036,10.5780038983954));
#63585=CARTESIAN_POINT('Ctrl Pts',(-2.11728695816243,1.0688150518666,10.5791969222604));
#63586=CARTESIAN_POINT('Ctrl Pts',(-2.12108711662803,1.06125356269191,10.5797664538227));
#63587=CARTESIAN_POINT('Ctrl Pts',(-2.13032041645303,1.04263358315963,10.5811591892522));
#63588=CARTESIAN_POINT('Ctrl Pts',(-2.1357081120458,1.03155258802487,10.5819796674777));
#63589=CARTESIAN_POINT('Ctrl Pts',(-2.15112252146199,0.999210927459784,
10.5843516083496));
#63590=CARTESIAN_POINT('Ctrl Pts',(-2.16092013987067,0.977841923262025,
10.5858904402346));
#63591=CARTESIAN_POINT('Ctrl Pts',(-2.23275512167892,0.814811811758568,
10.5974432430522));
#63592=CARTESIAN_POINT('Ctrl Pts',(-2.28112866501053,0.667516115389473,
10.6068356159993));
#63593=CARTESIAN_POINT('Ctrl Pts',(-2.34008065616195,0.403330972762036,
10.6234726127201));
#63594=CARTESIAN_POINT('Ctrl Pts',(-2.35699311800545,0.288468380828906,
10.6306390066344));
#63595=CARTESIAN_POINT('Ctrl Pts',(-2.36544102832235,0.172878003312455,
10.6380411716245));
#63596=CARTESIAN_POINT('Origin',(0.,0.,-1.84858989190501));
#63597=CARTESIAN_POINT('',(-2.36544101854889,0.172878137039869,11.8369824012687));
#63598=CARTESIAN_POINT('',(-2.3654410511783,0.172877690580661,11.6392156713196));
#63599=CARTESIAN_POINT('',(-2.36544101854889,0.172878137039864,-1.84858989190501));
#63600=CARTESIAN_POINT('',(-2.37174906171763,-0.00210967806991183,10.848589891905));
#63601=CARTESIAN_POINT('Ctrl Pts',(-2.37174906171763,-0.00210967806991183,
10.848589891905));
#63602=CARTESIAN_POINT('Ctrl Pts',(-2.37165805342341,-0.104423315161401,
10.8554530893873));
#63603=CARTESIAN_POINT('Ctrl Pts',(-2.3649427778268,-0.20644680868023,10.8623162868697));
#63604=CARTESIAN_POINT('Ctrl Pts',(-2.35173784392009,-0.307452721526542,
10.869179484352));
#63605=CARTESIAN_POINT('Ctrl Pts',(-2.33940885685767,-0.401758425857108,
10.8755874129008));
#63606=CARTESIAN_POINT('Ctrl Pts',(-2.3214231975442,-0.495177584694326,
10.8819953414496));
#63607=CARTESIAN_POINT('Ctrl Pts',(-2.29792715611661,-0.587136140670828,
10.8884032699985));
#63608=CARTESIAN_POINT('Ctrl Pts',(-2.27836238835693,-0.663708519756064,
10.8937390468469));
#63609=CARTESIAN_POINT('Ctrl Pts',(-2.25492967935947,-0.739444399516909,
10.8990748236953));
#63610=CARTESIAN_POINT('Ctrl Pts',(-2.2277173816223,-0.813924646461752,
10.9044106005437));
#63611=CARTESIAN_POINT('Ctrl Pts',(-2.20054398841307,-0.888298411444805,
10.9097387490072));
#63612=CARTESIAN_POINT('Ctrl Pts',(-2.16960189711789,-0.961419672718621,
10.9150668974708));
#63613=CARTESIAN_POINT('Ctrl Pts',(-2.13502985033385,-1.03288218141442,
10.9203950459344));
#63614=CARTESIAN_POINT('Ctrl Pts',(-2.10049745093925,-1.10426273656173,
10.9257170840517));
#63615=CARTESIAN_POINT('Ctrl Pts',(-2.06234357174016,-1.17398790033652,
10.9310391221689));
#63616=CARTESIAN_POINT('Ctrl Pts',(-2.02075532507061,-1.24167064018554,
10.9363611602862));
#63617=CARTESIAN_POINT('Ctrl Pts',(-1.97919312186946,-1.30931099562459,
10.941679865627));
#63618=CARTESIAN_POINT('Ctrl Pts',(-1.93420106461656,-1.37491106822296,
10.9469985709678));
#63619=CARTESIAN_POINT('Ctrl Pts',(-1.88601197135451,-1.43810879505254,
10.9523172763086));
#63620=CARTESIAN_POINT('Ctrl Pts',(-1.83783810539373,-1.50128655199349,
10.9576343009884));
#63621=CARTESIAN_POINT('Ctrl Pts',(-1.78646949321897,-1.56206309880546,
10.9629513256682));
#63622=CARTESIAN_POINT('Ctrl Pts',(-1.7321811517149,-1.62010694713147,10.968268350348));
#63623=CARTESIAN_POINT('Ctrl Pts',(-1.67789312333021,-1.67815046067743,
10.9735853443608));
#63624=CARTESIAN_POINT('Ctrl Pts',(-1.62068571986508,-1.73346096628657,
10.9789023383735));
#63625=CARTESIAN_POINT('Ctrl Pts',(-1.5608719499261,-1.78574265179334,10.9842193323863));
#63626=CARTESIAN_POINT('Ctrl Pts',(-1.50099899088266,-1.8380760729815,10.989541587865));
#63627=CARTESIAN_POINT('Ctrl Pts',(-1.43851486679859,-1.88737437859769,
10.9948638433437));
#63628=CARTESIAN_POINT('Ctrl Pts',(-1.37376646512047,-1.9333814320538,11.0001860988224));
#63629=CARTESIAN_POINT('Ctrl Pts',(-1.30898663816695,-1.97941081477655,
11.0055109374281));
#63630=CARTESIAN_POINT('Ctrl Pts',(-1.24194073947866,-2.02214551123571,
11.0108357760338));
#63631=CARTESIAN_POINT('Ctrl Pts',(-1.17300335952702,-2.06137361510191,
11.0161606146395));
#63632=CARTESIAN_POINT('Ctrl Pts',(-1.1039432766229,-2.10067154181557,11.0214949310267));
#63633=CARTESIAN_POINT('Ctrl Pts',(-1.03298540449351,-2.13645019403203,
11.0268292474138));
#63634=CARTESIAN_POINT('Ctrl Pts',(-0.960527347199169,-2.16854450675621,
11.0321635638009));
#63635=CARTESIAN_POINT('Ctrl Pts',(-0.896076023327083,-2.19709234561746,
11.0369084295334));
#63636=CARTESIAN_POINT('Ctrl Pts',(-0.830438246495536,-2.22272572395615,
11.041653295266));
#63637=CARTESIAN_POINT('Ctrl Pts',(-0.763903504479376,-2.24536177449072,
11.0463981609985));
#63638=CARTESIAN_POINT('Ctrl Pts',(-0.689082728510087,-2.2708168497575,
11.0517339378456));
#63639=CARTESIAN_POINT('Ctrl Pts',(-0.612849004292881,-2.29257540263513,
11.0570697146927));
#63640=CARTESIAN_POINT('Ctrl Pts',(-0.535601638208493,-2.31048240582965,
11.0624054915398));
#63641=CARTESIAN_POINT('Ctrl Pts',(-0.458464710145092,-2.32836380797013,
11.0677336400021));
#63642=CARTESIAN_POINT('Ctrl Pts',(-0.380317470439179,-2.34240449127473,
11.0730617884644));
#63643=CARTESIAN_POINT('Ctrl Pts',(-0.301575968684563,-2.352498671118,11.0783899369267));
#63644=CARTESIAN_POINT('Ctrl Pts',(-0.222924768062563,-2.36258127490732,
11.0837119750427));
#63645=CARTESIAN_POINT('Ctrl Pts',(-0.143681121640871,-2.368726310344,11.0890340131587));
#63646=CARTESIAN_POINT('Ctrl Pts',(-0.0642714153984966,-2.37087900316795,
11.0943560512748));
#63647=CARTESIAN_POINT('Ctrl Pts',(0.0150885627515715,-2.37303034792865,
11.0996747566143));
#63648=CARTESIAN_POINT('Ctrl Pts',(0.0946139276757409,-2.3711943000465,
11.1049934619538));
#63649=CARTESIAN_POINT('Ctrl Pts',(0.173874231148637,-2.36536800820559,
11.1103121672934));
#63650=CARTESIAN_POINT('Ctrl Pts',(0.253109489109495,-2.35954355741822,
11.1156291919719));
#63651=CARTESIAN_POINT('Ctrl Pts',(0.332079385536634,-2.34973140093729,
11.1209462166505));
#63652=CARTESIAN_POINT('Ctrl Pts',(0.410356020385786,-2.33598073601499,
11.126263241329));
#63653=CARTESIAN_POINT('Ctrl Pts',(0.488632203758231,-2.3222301504025,11.1315802353405));
#63654=CARTESIAN_POINT('Ctrl Pts',(0.566214672815223,-2.30454118394526,
11.136897229352));
#63655=CARTESIAN_POINT('Ctrl Pts',(0.642684647213917,-2.28301434658995,
11.1422142233636));
#63656=CARTESIAN_POINT('Ctrl Pts',(0.719230292972739,-2.26146620721283,
11.1475364788411));
#63657=CARTESIAN_POINT('Ctrl Pts',(0.794660793590124,-2.23607273810929,
11.1528587343185));
#63658=CARTESIAN_POINT('Ctrl Pts',(0.868572085318437,-2.20698450268813,
11.158180989796));
#63659=CARTESIAN_POINT('Ctrl Pts',(0.942519249479862,-2.17788214945419,
11.1635058284005));
#63660=CARTESIAN_POINT('Ctrl Pts',(1.01494530901105,-2.14508165082385,11.168830667005));
#63661=CARTESIAN_POINT('Ctrl Pts',(1.08546810594951,-2.10878094013257,11.1741555056095));
#63662=CARTESIAN_POINT('Ctrl Pts',(1.15611642775475,-2.07241561711631,11.1794898219955));
#63663=CARTESIAN_POINT('Ctrl Pts',(1.22485431254362,-2.03253786939297,11.1848241383814));
#63664=CARTESIAN_POINT('Ctrl Pts',(1.29132625734933,-1.98939049951993,11.1901584547674));
#63665=CARTESIAN_POINT('Ctrl Pts',(1.35045294407114,-1.95101098424007,11.1949033205111));
#63666=CARTESIAN_POINT('Ctrl Pts',(1.40778704258294,-1.91004527902808,11.1996481862548));
#63667=CARTESIAN_POINT('Ctrl Pts',(1.46310096839824,-1.86669055249448,11.2043930519985));
#63668=CARTESIAN_POINT('Ctrl Pts',(1.52530352176559,-1.8179365605985,11.2097288288448));
#63669=CARTESIAN_POINT('Ctrl Pts',(1.58518226374215,-1.76597935139275,11.2150646056912));
#63670=CARTESIAN_POINT('Ctrl Pts',(1.64238916785706,-1.71106863795869,11.2204003825375));
#63671=CARTESIAN_POINT('Ctrl Pts',(1.69951428514076,-1.65623642856746,11.225728530999));
#63672=CARTESIAN_POINT('Ctrl Pts',(1.75397481580564,-1.59845942225094,11.2310566794604));
#63673=CARTESIAN_POINT('Ctrl Pts',(1.80545482578562,-1.5380282619469,11.2363848279219));
#63674=CARTESIAN_POINT('Ctrl Pts',(1.85687579824254,-1.47766640438818,11.2417068660371));
#63675=CARTESIAN_POINT('Ctrl Pts',(1.90532274082491,-1.41465679630268,11.2470289041523));
#63676=CARTESIAN_POINT('Ctrl Pts',(1.95051679316291,-1.349326610606,11.2523509422675));
#63677=CARTESIAN_POINT('Ctrl Pts',(1.99568254399822,-1.28403733609853,11.2576696476062));
#63678=CARTESIAN_POINT('Ctrl Pts',(2.03759918247399,-1.21643075243213,11.2629883529449));
#63679=CARTESIAN_POINT('Ctrl Pts',(2.07602911453367,-1.14686580649549,11.2683070582836));
#63680=CARTESIAN_POINT('Ctrl Pts',(2.1144469030954,-1.07732284242905,11.2736240829613));
#63681=CARTESIAN_POINT('Ctrl Pts',(2.14937994709338,-1.00582315437657,11.278941107639));
#63682=CARTESIAN_POINT('Ctrl Pts',(2.18063563607361,-0.932751995541057,
11.2842581323167));
#63683=CARTESIAN_POINT('Ctrl Pts',(2.21189114478014,-0.859681258158691,
11.2895751263273));
#63684=CARTESIAN_POINT('Ctrl Pts',(2.23946915794707,-0.785039498887169,
11.294892120338));
#63685=CARTESIAN_POINT('Ctrl Pts',(2.26322502323928,-0.709232371429521,
11.3002091143486));
#63686=CARTESIAN_POINT('Ctrl Pts',(2.28700439630235,-0.633350228536371,
11.3055313698253));
#63687=CARTESIAN_POINT('Ctrl Pts',(2.30695392636338,-0.556300861602376,
11.3108536253019));
#63688=CARTESIAN_POINT('Ctrl Pts',(2.32297892284745,-0.478504949301994,
11.3161758807785));
#63689=CARTESIAN_POINT('Ctrl Pts',(2.33901169697415,-0.400671279189647,
11.3215007193821));
#63690=CARTESIAN_POINT('Ctrl Pts',(2.35111607163671,-0.322090805013658,
11.3268255579857));
#63691=CARTESIAN_POINT('Ctrl Pts',(2.35924899885723,-0.243191743057085,
11.3321503965894));
#63692=CARTESIAN_POINT('Ctrl Pts',(2.36739640202951,-0.164152247160374,
11.3374847129744));
#63693=CARTESIAN_POINT('Ctrl Pts',(2.37155820928297,-0.0847934988890727,
11.3428190293595));
#63694=CARTESIAN_POINT('Ctrl Pts',(2.37174351593979,-0.00554590818296819,
11.3481533457446));
#63695=CARTESIAN_POINT('Ctrl Pts',(2.37190834590974,0.0649446948997903,
11.3528982114959));
#63696=CARTESIAN_POINT('Ctrl Pts',(2.36892770638879,0.135347135622957,11.3576430772473));
#63697=CARTESIAN_POINT('Ctrl Pts',(2.36284237116327,0.205363072472949,11.3623879429986));
#63698=CARTESIAN_POINT('Ctrl Pts',(2.35599918685866,0.284098580438945,11.3677237198513));
#63699=CARTESIAN_POINT('Ctrl Pts',(2.34520349453185,0.362638177910462,11.3730594967039));
#63700=CARTESIAN_POINT('Ctrl Pts',(2.33047426245826,0.440553940533523,11.3783952735566));
#63701=CARTESIAN_POINT('Ctrl Pts',(2.31576608828375,0.51835830955121,11.3837234220245));
#63702=CARTESIAN_POINT('Ctrl Pts',(2.29713562905319,0.595540158857205,11.3890515704923));
#63703=CARTESIAN_POINT('Ctrl Pts',(2.27465366819779,0.671676076881063,11.3943797189602));
#63704=CARTESIAN_POINT('Ctrl Pts',(2.2521974897632,0.74772468186805,11.3997017570817));
#63705=CARTESIAN_POINT('Ctrl Pts',(2.22589871938598,0.822729292707825,11.4050237952033));
#63706=CARTESIAN_POINT('Ctrl Pts',(2.19587899259207,0.896277586684419,11.4103458333249));
#63707=CARTESIAN_POINT('Ctrl Pts',(2.16587806480675,0.969779823112926,11.4156645386699));
#63708=CARTESIAN_POINT('Ctrl Pts',(2.13216098228431,1.04182712074477,11.420983244015));
#63709=CARTESIAN_POINT('Ctrl Pts',(2.0948985403765,1.11202435586116,11.42630194936));
#63710=CARTESIAN_POINT('Ctrl Pts',(2.05764787305077,1.18219940930977,11.4316189740441));
#63711=CARTESIAN_POINT('Ctrl Pts',(2.0168542904177,1.2505251481216,11.4369359987282));
#63712=CARTESIAN_POINT('Ctrl Pts',(1.97273519963897,1.31662974848869,11.4422530234122));
#63713=CARTESIAN_POINT('Ctrl Pts',(1.92861636332647,1.38273396758345,11.4475700174292));
#63714=CARTESIAN_POINT('Ctrl Pts',(1.88117231803757,1.44661668525981,11.4528870114462));
#63715=CARTESIAN_POINT('Ctrl Pts',(1.83066376190132,1.5079350958716,11.4582040054632));
#63716=CARTESIAN_POINT('Ctrl Pts',(1.78010522469597,1.56931418451406,11.4635262609461));
#63717=CARTESIAN_POINT('Ctrl Pts',(1.7264764175646,1.62812353542051,11.468848516429));
#63718=CARTESIAN_POINT('Ctrl Pts',(1.67007792237415,1.68405397648011,11.4741707719119));
#63719=CARTESIAN_POINT('Ctrl Pts',(1.6136520544891,1.74001156306684,11.4794956105217));
#63720=CARTESIAN_POINT('Ctrl Pts',(1.5544541694805,1.79308714344333,11.4848204491316));
#63721=CARTESIAN_POINT('Ctrl Pts',(1.49281938065313,1.84301067800662,11.4901452877414));
#63722=CARTESIAN_POINT('Ctrl Pts',(1.4310748868951,1.89302307241677,11.4954796041326));
#63723=CARTESIAN_POINT('Ctrl Pts',(1.36688520168584,1.93987193466428,11.5008139205238));
#63724=CARTESIAN_POINT('Ctrl Pts',(1.30061576774694,1.98332969704687,11.5061482369149));
#63725=CARTESIAN_POINT('Ctrl Pts',(1.24166921477974,2.02198530552065,11.5108931026095));
#63726=CARTESIAN_POINT('Ctrl Pts',(1.18107774744107,2.05795837654709,11.5156379683041));
#63727=CARTESIAN_POINT('Ctrl Pts',(1.11911350953335,2.09112003846741,11.5203828339987));
#63728=CARTESIAN_POINT('Ctrl Pts',(1.04943243382725,2.12841155294148,11.525718610841));
#63729=CARTESIAN_POINT('Ctrl Pts',(0.977755700919738,2.16228575080617,11.5310543876833));
#63730=CARTESIAN_POINT('Ctrl Pts',(0.904452066617334,2.19252469123876,11.5363901645256));
#63731=CARTESIAN_POINT('Ctrl Pts',(0.831253232111973,2.22272040005194,11.5417183129831));
#63732=CARTESIAN_POINT('Ctrl Pts',(0.756432544572834,2.2492909959733,11.5470464614406));
#63733=CARTESIAN_POINT('Ctrl Pts',(0.680383293204182,2.27206439979782,11.5523746098981));
#63734=CARTESIAN_POINT('Ctrl Pts',(0.604421255481801,2.2948116869736,11.5576966480094));
#63735=CARTESIAN_POINT('Ctrl Pts',(0.527233899998554,2.31377030249646,11.5630186861207));
#63736=CARTESIAN_POINT('Ctrl Pts',(0.449233015590976,2.32881681551019,11.568340724232));
#63737=CARTESIAN_POINT('Ctrl Pts',(0.37128097704024,2.34385390606896,11.5736594295669));
#63738=CARTESIAN_POINT('Ctrl Pts',(0.292516879159635,2.35498366858037,11.5789781349017));
#63739=CARTESIAN_POINT('Ctrl Pts',(0.213364968417591,2.3621332419557,11.5842968402365));
#63740=CARTESIAN_POINT('Ctrl Pts',(0.134238068935938,2.369280556133,11.5896138649104));
#63741=CARTESIAN_POINT('Ctrl Pts',(0.0547240657327129,2.37245013677191,
11.5949308895843));
#63742=CARTESIAN_POINT('Ctrl Pts',(-0.0247468389610155,2.37162089222992,
11.6002479142582));
#63743=CARTESIAN_POINT('Ctrl Pts',(-0.104217285290536,2.37079165247077,
11.6055649082651));
#63744=CARTESIAN_POINT('Ctrl Pts',(-0.183644165643882,2.36596363975148,
11.610881902272));
#63745=CARTESIAN_POINT('Ctrl Pts',(-0.262597925701454,2.357167875209,11.6161988962789));
#63746=CARTESIAN_POINT('Ctrl Pts',(-0.341629814967029,2.34836340676036,
11.6215211517519));
#63747=CARTESIAN_POINT('Ctrl Pts',(-0.420187182575315,2.33558339576522,
11.6268434072249));
#63748=CARTESIAN_POINT('Ctrl Pts',(-0.497846849324561,2.31891064448754,
11.6321656626979));
#63749=CARTESIAN_POINT('Ctrl Pts',(-0.575544207760615,2.30222980118287,
11.637490501298));
#63750=CARTESIAN_POINT('Ctrl Pts',(-0.652342544751022,2.28165257506089,
11.642815339898));
#63751=CARTESIAN_POINT('Ctrl Pts',(-0.727832586269522,2.2573120716605,11.648140178498));
#63752=CARTESIAN_POINT('Ctrl Pts',(-0.803456993949874,2.23292824413478,
11.6534744948797));
#63753=CARTESIAN_POINT('Ctrl Pts',(-0.877768014758273,2.20476792196589,
11.6588088112613));
#63754=CARTESIAN_POINT('Ctrl Pts',(-0.950375372694002,2.17301281944602,
11.6641431276429));
#63755=CARTESIAN_POINT('Ctrl Pts',(-1.01495950002739,2.14476670716573,11.6688879934282));
#63756=CARTESIAN_POINT('Ctrl Pts',(-1.07819579016902,2.11367716630258,11.6736328592135));
#63757=CARTESIAN_POINT('Ctrl Pts',(-1.13982760658501,2.07990170194812,11.6783777249987));
#63758=CARTESIAN_POINT('Ctrl Pts',(-1.20913486069273,2.04191994468787,11.6837135018395));
#63759=CARTESIAN_POINT('Ctrl Pts',(-1.2766705457286,2.00039950921893,11.6890492786802));
#63760=CARTESIAN_POINT('Ctrl Pts',(-1.34205063796326,1.95553014490762,11.694385055521));
#63761=CARTESIAN_POINT('Ctrl Pts',(-1.40733725842716,1.91072492885293,11.6997132039768));
#63762=CARTESIAN_POINT('Ctrl Pts',(-1.47047402371722,1.86258055520362,11.7050413524327));
#63763=CARTESIAN_POINT('Ctrl Pts',(-1.53110191412093,1.8113323800659,11.7103695008885));
#63764=CARTESIAN_POINT('Ctrl Pts',(-1.59166027616738,1.76014297658273,11.715691538998));
#63765=CARTESIAN_POINT('Ctrl Pts',(-1.64971512556803,1.70585714597935,11.7210135771075));
#63766=CARTESIAN_POINT('Ctrl Pts',(-1.70493807752139,1.64875232048894,11.726335615217));
#63767=CARTESIAN_POINT('Ctrl Pts',(-1.76012644765555,1.59168325528806,11.7316543205499));
#63768=CARTESIAN_POINT('Ctrl Pts',(-1.81248611598677,1.53179903486834,11.7369730258828));
#63769=CARTESIAN_POINT('Ctrl Pts',(-1.86172424331017,1.46941515725515,11.7422917312158));
#63770=CARTESIAN_POINT('Ctrl Pts',(-1.91094681184696,1.40705099236242,11.7476087558877));
#63771=CARTESIAN_POINT('Ctrl Pts',(-1.95704950847581,1.34218910597912,11.7529257805596));
#63772=CARTESIAN_POINT('Ctrl Pts',(-1.99977959709141,1.27517827206902,11.7582428052315));
#63773=CARTESIAN_POINT('Ctrl Pts',(-2.04250943925208,1.20816782465824,11.7635597992363));
#63774=CARTESIAN_POINT('Ctrl Pts',(-2.08186646170133,1.13900884976351,11.7688767932411));
#63775=CARTESIAN_POINT('Ctrl Pts',(-2.11764192736636,1.06807805424515,11.7741937872459));
#63776=CARTESIAN_POINT('Ctrl Pts',(-2.15345279487587,0.997077068697235,
11.7795160427167));
#63777=CARTESIAN_POINT('Ctrl Pts',(-2.18567481505506,0.924301179164118,
11.7848382981875));
#63778=CARTESIAN_POINT('Ctrl Pts',(-2.21414610156846,0.850150047585235,
11.7901605536583));
#63779=CARTESIAN_POINT('Ctrl Pts',(-2.24263120646184,0.775962927168565,
11.7954853922561));
#63780=CARTESIAN_POINT('Ctrl Pts',(-2.26736180543186,0.700399680352984,
11.8008102308538));
#63781=CARTESIAN_POINT('Ctrl Pts',(-2.28822573974705,0.623875810124956,
11.8061350694516));
#63782=CARTESIAN_POINT('Ctrl Pts',(-2.30912681017575,0.547215733604843,
11.8114693858309));
#63783=CARTESIAN_POINT('Ctrl Pts',(-2.32614736421891,0.469592075524575,
11.8168037022101));
#63784=CARTESIAN_POINT('Ctrl Pts',(-2.33922633441086,0.391430988679662,
11.8221380185894));
#63785=CARTESIAN_POINT('Ctrl Pts',(-2.3508600572708,0.321906828180753,11.8268828843925));
#63786=CARTESIAN_POINT('Ctrl Pts',(-2.35937589195445,0.251957785728667,
11.8316277501956));
#63787=CARTESIAN_POINT('Ctrl Pts',(-2.36476551897855,0.181884861244936,
11.8363726159987));
#63788=CARTESIAN_POINT('Ctrl Pts',(-2.36499640117885,0.178883059652061,
11.8365758777554));
#63789=CARTESIAN_POINT('Ctrl Pts',(-2.3652215681227,0.175880813078295,11.8367791395121));
#63790=CARTESIAN_POINT('Ctrl Pts',(-2.36544101854889,0.172878137039869,
11.8369824012687));
#63791=CARTESIAN_POINT('Ctrl Pts',(-2.36342245950295,0.172714633282403,
10.8368568258743));
#63792=CARTESIAN_POINT('Ctrl Pts',(-2.36814836675846,0.114512217657902,
10.8407678478846));
#63793=CARTESIAN_POINT('Ctrl Pts',(-2.37079004863033,0.0561842181634697,
10.8446788698948));
#63794=CARTESIAN_POINT('Ctrl Pts',(-2.37130727717011,-0.00210928510120129,
10.848589891905));
#63795=CARTESIAN_POINT('Ctrl Pts',(-2.36544102832235,0.172878003312457,
10.6380411716245));
#63796=CARTESIAN_POINT('Ctrl Pts',(-2.36761077134982,0.143190020574595,
10.6399423276824));
#63797=CARTESIAN_POINT('Ctrl Pts',(-2.36922213530041,0.113453987121819,
10.6418583939412));
#63798=CARTESIAN_POINT('Ctrl Pts',(-2.37125543553081,0.0558635986214012,
10.6455979483888));
#63799=CARTESIAN_POINT('Ctrl Pts',(-2.37174775862709,0.0280276099855107,
10.647418367514));
#63800=CARTESIAN_POINT('Ctrl Pts',(-2.3717513215929,-0.0163748061093179,
10.6503459252659));
#63801=CARTESIAN_POINT('Ctrl Pts',(-2.37157910610943,-0.0329391262577879,
10.6514433088954));
#63802=CARTESIAN_POINT('Ctrl Pts',(-2.37092253239266,-0.0643914778828075,
10.6535376418931));
#63803=CARTESIAN_POINT('Ctrl Pts',(-2.37047140185951,-0.0792794600979941,
10.6545335165904));
#63804=CARTESIAN_POINT('Ctrl Pts',(-2.36911911123579,-0.113314094809938,
10.6568209357159));
#63805=CARTESIAN_POINT('Ctrl Pts',(-2.36812602299492,-0.13245583975935,
10.6581152541651));
#63806=CARTESIAN_POINT('Ctrl Pts',(-2.36428118966396,-0.19249121106912,
10.6622003329518));
#63807=CARTESIAN_POINT('Ctrl Pts',(-2.36060135304912,-0.233322319521807,
10.6650161982669));
#63808=CARTESIAN_POINT('Ctrl Pts',(-2.34230835635987,-0.390586038447003,
10.6760131053646));
#63809=CARTESIAN_POINT('Ctrl Pts',(-2.32012269553777,-0.505954487331847,
10.6844135510187));
#63810=CARTESIAN_POINT('Ctrl Pts',(-2.25236810346385,-0.75647991857096,
10.7032574373893));
#63811=CARTESIAN_POINT('Ctrl Pts',(-2.20296585817177,-0.890150470362178,
10.7137238106242));
#63812=CARTESIAN_POINT('Ctrl Pts',(-2.12484445951778,-1.05442319004706,
10.726634683633));
#63813=CARTESIAN_POINT('Ctrl Pts',(-2.10690726831195,-1.08982312265966,
10.7294184178092));
#63814=CARTESIAN_POINT('Ctrl Pts',(-2.08162241119225,-1.13676389103889,
10.7330962606637));
#63815=CARTESIAN_POINT('Ctrl Pts',(-2.07505211827638,-1.14871351306282,
10.7340313179125));
#63816=CARTESIAN_POINT('Ctrl Pts',(-2.06449511933105,-1.16752771136826,
10.7355008359058));
#63817=CARTESIAN_POINT('Ctrl Pts',(-2.06057651099288,-1.1744298623332,10.7360393619083));
#63818=CARTESIAN_POINT('Ctrl Pts',(-2.05231975665899,-1.18880458139498,
10.7371595004205));
#63819=CARTESIAN_POINT('Ctrl Pts',(-2.04797530950731,-1.19627331794074,
10.7377406648065));
#63820=CARTESIAN_POINT('Ctrl Pts',(-2.03708631554236,-1.21475990338113,
10.739177499455));
#63821=CARTESIAN_POINT('Ctrl Pts',(-2.03049298046604,-1.22574897685172,
10.7400301336276));
#63822=CARTESIAN_POINT('Ctrl Pts',(-2.00487588430864,-1.26767087300146,
10.7432793128472));
#63823=CARTESIAN_POINT('Ctrl Pts',(-1.98523066488482,-1.29822043580283,
10.7456397010797));
#63824=CARTESIAN_POINT('Ctrl Pts',(-1.93105609487217,-1.37835775045932,
10.7518453519994));
#63825=CARTESIAN_POINT('Ctrl Pts',(-1.89531960939131,-1.42709925120586,
10.7556347162636));
#63826=CARTESIAN_POINT('Ctrl Pts',(-1.73637989334765,-1.62736136242325,
10.771505895477));
#63827=CARTESIAN_POINT('Ctrl Pts',(-1.59658873820786,-1.76471638290985,
10.7832267961463));
#63828=CARTESIAN_POINT('Ctrl Pts',(-1.40484857468159,-1.91147430753635,
10.7986394693922));
#63829=CARTESIAN_POINT('Ctrl Pts',(-1.36734161650525,-1.93848136595417,
10.8016232323118));
#63830=CARTESIAN_POINT('Ctrl Pts',(-1.31368368177447,-1.97478566701633,
10.8058639566675));
#63831=CARTESIAN_POINT('Ctrl Pts',(-1.29817430171207,-1.98501554069485,
10.8070865122338));
#63832=CARTESIAN_POINT('Ctrl Pts',(-1.27090800807103,-2.00254396643393,
10.809231228289));
#63833=CARTESIAN_POINT('Ctrl Pts',(-1.25920428893038,-2.00992389099941,
10.8101503679546));
#63834=CARTESIAN_POINT('Ctrl Pts',(-1.23445581852363,-2.02522834338775,
10.8120913134238));
#63835=CARTESIAN_POINT('Ctrl Pts',(-1.2213978454651,-2.03313017174818,10.813113884953));
#63836=CARTESIAN_POINT('Ctrl Pts',(-1.18974505492012,-2.05186938146257,
10.8155894653238));
#63837=CARTESIAN_POINT('Ctrl Pts',(-1.17107750343702,-2.0625805881903,10.817046883762));
#63838=CARTESIAN_POINT('Ctrl Pts',(-1.10347823765448,-2.10015466966398,
10.8223168767987));
#63839=CARTESIAN_POINT('Ctrl Pts',(-1.05375083457926,-2.12554043740749,
10.8261799589875));
#63840=CARTESIAN_POINT('Ctrl Pts',(-0.924312301932151,-2.18595968829431,
10.8362067745672));
#63841=CARTESIAN_POINT('Ctrl Pts',(-0.843487664042719,-2.21840009660104,
10.8424432069615));
#63842=CARTESIAN_POINT('Ctrl Pts',(-0.640680912583949,-2.28711244447997,
10.8579608773524));
#63843=CARTESIAN_POINT('Ctrl Pts',(-0.517208556455046,-2.31815678329798,
10.8673040560055));
#63844=CARTESIAN_POINT('Ctrl Pts',(-0.332564843551434,-2.34908731494332,
10.8807537646472));
#63845=CARTESIAN_POINT('Ctrl Pts',(-0.272924869608937,-2.35676131774492,
10.8850172485117));
#63846=CARTESIAN_POINT('Ctrl Pts',(-0.197423086596382,-2.36357112465351,
10.8902645798494));
#63847=CARTESIAN_POINT('Ctrl Pts',(-0.18177928371521,-2.36482571474434,
10.8913437065873));
#63848=CARTESIAN_POINT('Ctrl Pts',(-0.15688801513545,-2.36657345777885,
10.8930466647778));
#63849=CARTESIAN_POINT('Ctrl Pts',(-0.147648444124111,-2.36716786996808,
10.8936757206684));
#63850=CARTESIAN_POINT('Ctrl Pts',(-0.129894574831891,-2.36820568029223,
10.8948782447475));
#63851=CARTESIAN_POINT('Ctrl Pts',(-0.121381083391091,-2.3686572946643,
10.8954521155643));
#63852=CARTESIAN_POINT('Ctrl Pts',(-0.100680069077297,-2.36964351774111,
10.8968411175852));
#63853=CARTESIAN_POINT('Ctrl Pts',(-0.088490294262907,-2.37013003041661,
10.8976536596307));
#63854=CARTESIAN_POINT('Ctrl Pts',(-0.0444747156983343,-2.37154670376562,
10.9005700042944));
#63855=CARTESIAN_POINT('Ctrl Pts',(-0.0126331809773593,-2.37193010158469,
10.9026464820383));
#63856=CARTESIAN_POINT('Ctrl Pts',(0.234909305702097,-2.3699252497085,10.9185976786031));
#63857=CARTESIAN_POINT('Ctrl Pts',(0.449385021978406,-2.33876122690857,
10.9313684147293));
#63858=CARTESIAN_POINT('Ctrl Pts',(0.735429006861394,-2.2563362729168,10.9499817859639));
#63859=CARTESIAN_POINT('Ctrl Pts',(0.812912209166751,-2.22959207883852,
10.9551834577116));
#63860=CARTESIAN_POINT('Ctrl Pts',(0.912215256774717,-2.18945117654963,
10.9621541304073));
#63861=CARTESIAN_POINT('Ctrl Pts',(0.935426394144762,-2.17963540800888,
10.9638056863942));
#63862=CARTESIAN_POINT('Ctrl Pts',(0.973115105759387,-2.1629843241158,10.9665262485121));
#63863=CARTESIAN_POINT('Ctrl Pts',(0.98768804011086,-2.15636882510184,10.9675878476797));
#63864=CARTESIAN_POINT('Ctrl Pts',(1.01585407474009,-2.14323721608009,10.9696590619744));
#63865=CARTESIAN_POINT('Ctrl Pts',(1.02945423087269,-2.13673798913953,10.9706680629007));
#63866=CARTESIAN_POINT('Ctrl Pts',(1.06134117481704,-2.12112480094123,10.9730553065989));
#63867=CARTESIAN_POINT('Ctrl Pts',(1.07957371991653,-2.11190341846424,10.9744371872994));
#63868=CARTESIAN_POINT('Ctrl Pts',(1.14067138262331,-2.08000443512069,10.9791265242894));
#63869=CARTESIAN_POINT('Ctrl Pts',(1.1829570542001,-2.05624941945276,10.9824708782442));
#63870=CARTESIAN_POINT('Ctrl Pts',(1.28509771722023,-1.99467575258601,10.9908012014855));
#63871=CARTESIAN_POINT('Ctrl Pts',(1.34404188475828,-1.95544301648385,10.9958317623906));
#63872=CARTESIAN_POINT('Ctrl Pts',(1.51486902019203,-1.83036563751252,11.0110654913835));
#63873=CARTESIAN_POINT('Ctrl Pts',(1.62094253909181,-1.73712668850761,11.0214378693496));
#63874=CARTESIAN_POINT('Ctrl Pts',(1.76723933350045,-1.58339593837949,11.0367549985814));
#63875=CARTESIAN_POINT('Ctrl Pts',(1.81402443566845,-1.5295734402061,11.0418361765889));
#63876=CARTESIAN_POINT('Ctrl Pts',(1.86849836130648,-1.4608834176921,11.0479108587597));
#63877=CARTESIAN_POINT('Ctrl Pts',(1.87854563774639,-1.44794088627373,11.0490384236365));
#63878=CARTESIAN_POINT('Ctrl Pts',(1.89415039470531,-1.42740353928194,11.0507997369866));
#63879=CARTESIAN_POINT('Ctrl Pts',(1.89979795836684,-1.4198782718048,11.0514393133437));
#63880=CARTESIAN_POINT('Ctrl Pts',(1.91044215978607,-1.40551787396807,11.0526485263231));
#63881=CARTESIAN_POINT('Ctrl Pts',(1.91544701612256,-1.39868955472059,11.0532186768001));
#63882=CARTESIAN_POINT('Ctrl Pts',(1.92736505835354,-1.38224536155758,11.0545805014306));
#63883=CARTESIAN_POINT('Ctrl Pts',(1.93424296748527,-1.37260426378177,11.0553698248556));
#63884=CARTESIAN_POINT('Ctrl Pts',(1.95798344764781,-1.33879325382507,11.0581079151122));
#63885=CARTESIAN_POINT('Ctrl Pts',(1.97446827870506,-1.31435983054275,11.0600335517433));
#63886=CARTESIAN_POINT('Ctrl Pts',(2.01479148050235,-1.25212223920481,11.0648239532593));
#63887=CARTESIAN_POINT('Ctrl Pts',(2.03802544404504,-1.21393886611671,11.0676595226463));
#63888=CARTESIAN_POINT('Ctrl Pts',(2.1541080301262,-1.01042800271325,11.0823612869461));
#63889=CARTESIAN_POINT('Ctrl Pts',(2.2279627070365,-0.835065408478117,11.0936966926515));
#63890=CARTESIAN_POINT('Ctrl Pts',(2.29920364538345,-0.586219332223322,
11.1099838615966));
#63891=CARTESIAN_POINT('Ctrl Pts',(2.31533249142618,-0.518868587837711,
11.1144038952656));
#63892=CARTESIAN_POINT('Ctrl Pts',(2.33302969587434,-0.427481175567841,
11.1204713484972));
#63893=CARTESIAN_POINT('Ctrl Pts',(2.33721323425537,-0.40398260840325,11.1220374615554));
#63894=CARTESIAN_POINT('Ctrl Pts',(2.3435636306448,-0.364903900029264,11.1246537816613));
#63895=CARTESIAN_POINT('Ctrl Pts',(2.34593146247775,-0.349357840263814,
11.1256976749986));
#63896=CARTESIAN_POINT('Ctrl Pts',(2.35028727496787,-0.318715560680419,
11.1277618571478));
#63897=CARTESIAN_POINT('Ctrl Pts',(2.35228482079826,-0.303621453306717,
11.1287817942581));
#63898=CARTESIAN_POINT('Ctrl Pts',(2.35673019692726,-0.267348729313647,
11.1312408306455));
#63899=CARTESIAN_POINT('Ctrl Pts',(2.35903802805765,-0.24615461678996,11.1326841936868));
#63900=CARTESIAN_POINT('Ctrl Pts',(2.36621770004242,-0.170791527576243,
11.1378413086496));
#63901=CARTESIAN_POINT('Ctrl Pts',(2.36951145418653,-0.116492909905071,
11.1416027431029));
#63902=CARTESIAN_POINT('Ctrl Pts',(2.37312828622778,0.021522725271247,11.1512848411506));
#63903=CARTESIAN_POINT('Ctrl Pts',(2.3708913620756,0.105227906048028,11.1572718299163));
#63904=CARTESIAN_POINT('Ctrl Pts',(2.34977445630342,0.369897151067537,11.1764891291856));
#63905=CARTESIAN_POINT('Ctrl Pts',(2.31451467985329,0.548899113046853,11.1899595373143));
#63906=CARTESIAN_POINT('Ctrl Pts',(2.25241475606172,0.743178785510291,11.2041990487165));
#63907=CARTESIAN_POINT('Ctrl Pts',(2.24538834530105,0.764145408762086,11.2057297957282));
#63908=CARTESIAN_POINT('Ctrl Pts',(2.23456871303429,0.794992199088426,11.2079699578168));
#63909=CARTESIAN_POINT('Ctrl Pts',(2.23100117392993,0.804949503036919,11.2086912238168));
#63910=CARTESIAN_POINT('Ctrl Pts',(2.2245040019162,0.822708604311988,11.2099738808063));
#63911=CARTESIAN_POINT('Ctrl Pts',(2.22159973937641,0.830519178814453,11.2105366703035));
#63912=CARTESIAN_POINT('Ctrl Pts',(2.21504322617145,0.847871416691498,11.2117840190212));
#63913=CARTESIAN_POINT('Ctrl Pts',(2.21137043624777,0.857404943012496,11.2124673767437));
#63914=CARTESIAN_POINT('Ctrl Pts',(2.20023157663559,0.885770536000592,11.2144956232393));
#63915=CARTESIAN_POINT('Ctrl Pts',(2.19258550364321,0.904531541103641,11.215830522011));
#63916=CARTESIAN_POINT('Ctrl Pts',(2.13767282300085,1.0344802222361,11.225046094202));
#63917=CARTESIAN_POINT('Ctrl Pts',(2.0822049834673,1.14202639380956,11.2325208211302));
#63918=CARTESIAN_POINT('Ctrl Pts',(1.92478727761452,1.3973031746124,11.2509672519315));
#63919=CARTESIAN_POINT('Ctrl Pts',(1.81385292076667,1.53856827820668,11.2618675513927));
#63920=CARTESIAN_POINT('Ctrl Pts',(1.66712983933618,1.68723626408464,11.2753528739307));
#63921=CARTESIAN_POINT('Ctrl Pts',(1.64577558268649,1.70807222262501,11.2772944201427));
#63922=CARTESIAN_POINT('Ctrl Pts',(1.61039621403862,1.74131338657186,11.2804816109504));
#63923=CARTESIAN_POINT('Ctrl Pts',(1.59660684952368,1.75396545332463,11.2817168153476));
#63924=CARTESIAN_POINT('Ctrl Pts',(1.57161115605591,1.77636057423984,11.2839443036673));
#63925=CARTESIAN_POINT('Ctrl Pts',(1.56046020912751,1.78616416780128,11.2849340090133));
#63926=CARTESIAN_POINT('Ctrl Pts',(1.53647135246248,1.80685839018196,11.2870551166591));
#63927=CARTESIAN_POINT('Ctrl Pts',(1.52360812240843,1.81771827393775,11.2881876929057));
#63928=CARTESIAN_POINT('Ctrl Pts',(1.4881893830893,1.8469807224303,11.2912939379937));
#63929=CARTESIAN_POINT('Ctrl Pts',(1.46540957983616,1.8651059119781,11.2932784266632));
#63930=CARTESIAN_POINT('Ctrl Pts',(1.31362172298315,1.98138129192633,11.306420999138));
#63931=CARTESIAN_POINT('Ctrl Pts',(1.17519698880692,2.066486899303,11.3180753149664));
#63932=CARTESIAN_POINT('Ctrl Pts',(0.90179295237735,2.19817372794707,11.3401852438487));
#63933=CARTESIAN_POINT('Ctrl Pts',(0.769136605695957,2.24802882554433,11.3505491621864));
#63934=CARTESIAN_POINT('Ctrl Pts',(0.6112428012686,2.29174203047535,11.3619907041922));
#63935=CARTESIAN_POINT('Ctrl Pts',(0.589581697081399,2.29741002180713,11.3635410637796));
#63936=CARTESIAN_POINT('Ctrl Pts',(0.557522524435657,2.30531552682975,11.3658041680821));
#63937=CARTESIAN_POINT('Ctrl Pts',(0.547185171992227,2.30779103079777,11.3665291021671));
#63938=CARTESIAN_POINT('Ctrl Pts',(0.528712634281577,2.31208358076373,11.3678155771344));
#63939=CARTESIAN_POINT('Ctrl Pts',(0.520584132205729,2.31392733287147,11.3683785541912));
#63940=CARTESIAN_POINT('Ctrl Pts',(0.502515649423265,2.31792569304389,11.3696230644751));
#63941=CARTESIAN_POINT('Ctrl Pts',(0.492571371706077,2.32005925562388,11.3703034298462));
#63942=CARTESIAN_POINT('Ctrl Pts',(0.463004703721785,2.32620416518914,11.3723135966938));
#63943=CARTESIAN_POINT('Ctrl Pts',(0.443344334692556,2.33003112403478,11.3736336712399));
#63944=CARTESIAN_POINT('Ctrl Pts',(0.397523497086638,2.3383493159859,11.376676772031));
#63945=CARTESIAN_POINT('Ctrl Pts',(0.371331042469932,2.34265145380631,11.3783910661869));
#63946=CARTESIAN_POINT('Ctrl Pts',(0.278277250044224,2.35633564891823,11.3844097795754));
#63947=CARTESIAN_POINT('Ctrl Pts',(0.211090062245934,2.3633023808543,11.388625463039));
#63948=CARTESIAN_POINT('Ctrl Pts',(-0.0147137151474146,2.37700793182493,
11.4026199782668));
#63949=CARTESIAN_POINT('Ctrl Pts',(-0.173679367568807,2.37069984916276,
11.412214325951));
#63950=CARTESIAN_POINT('Ctrl Pts',(-0.395677426188681,2.33942876304294,
11.4263494876972));
#63951=CARTESIAN_POINT('Ctrl Pts',(-0.460120206294244,2.32761160746172,
11.4305380562791));
#63952=CARTESIAN_POINT('Ctrl Pts',(-0.546868208946277,2.30796092207109,
11.4363385691125));
#63953=CARTESIAN_POINT('Ctrl Pts',(-0.569670106830477,2.3024387855898,11.4378785807993));
#63954=CARTESIAN_POINT('Ctrl Pts',(-0.606018341044855,2.29306302731454,
11.4403598823669));
#63955=CARTESIAN_POINT('Ctrl Pts',(-0.619619154701768,2.28942533526242,
11.4412942954518));
#63956=CARTESIAN_POINT('Ctrl Pts',(-0.64770977849127,2.28164353414745,11.4432369703262));
#63957=CARTESIAN_POINT('Ctrl Pts',(-0.662194053312797,2.2774819849947,11.4442457518201));
#63958=CARTESIAN_POINT('Ctrl Pts',(-0.69620181060596,2.26735920867427,11.4466314862691));
#63959=CARTESIAN_POINT('Ctrl Pts',(-0.715689673645624,2.26128348256856,
11.4480120640872));
#63960=CARTESIAN_POINT('Ctrl Pts',(-0.7810884612337,2.23996405351457,11.4526919107012));
#63961=CARTESIAN_POINT('Ctrl Pts',(-0.826608184854206,2.22356840957802,
11.4560278735314));
#63962=CARTESIAN_POINT('Ctrl Pts',(-0.937187266862924,2.1798744485167,11.4643319443174));
#63963=CARTESIAN_POINT('Ctrl Pts',(-1.0015881620851,2.15104445090205,11.4693442712427));
#63964=CARTESIAN_POINT('Ctrl Pts',(-1.14670359972957,2.07815060360049,11.4810272672697));
#63965=CARTESIAN_POINT('Ctrl Pts',(-1.22633412951655,2.03217674291938,11.4877326025311));
#63966=CARTESIAN_POINT('Ctrl Pts',(-1.39500302750715,1.92126637996043,11.5024449495047));
#63967=CARTESIAN_POINT('Ctrl Pts',(-1.48260568405541,1.8545034109025,11.5104319205716));
#63968=CARTESIAN_POINT('Ctrl Pts',(-1.58248008890892,1.76677104990736,11.5197212673895));
#63969=CARTESIAN_POINT('Ctrl Pts',(-1.59947707349315,1.75139840170692,11.5213088720311));
#63970=CARTESIAN_POINT('Ctrl Pts',(-1.62410058739057,1.72847054689037,11.5236154544296));
#63971=CARTESIAN_POINT('Ctrl Pts',(-1.63190234091686,1.72110659466795,11.5243472757942));
#63972=CARTESIAN_POINT('Ctrl Pts',(-1.64567981851533,1.70792433899507,11.5256409932386));
#63973=CARTESIAN_POINT('Ctrl Pts',(-1.65167513402508,1.70212716071313,11.5262043959674));
#63974=CARTESIAN_POINT('Ctrl Pts',(-1.65776914061374,1.69617203476208,11.526777512244));
#63975=CARTESIAN_POINT('Ctrl Pts',(-1.65789822136299,1.69604586691564,11.5267896519781));
#63976=CARTESIAN_POINT('Ctrl Pts',(-1.65815019483043,1.69579952336018,11.5268133499097));
#63977=CARTESIAN_POINT('Ctrl Pts',(-1.65827308888625,1.69567934902814,11.5268249082123));
#63978=CARTESIAN_POINT('Ctrl Pts',(-1.65851316707359,1.69544453286398,11.5268474881894));
#63979=CARTESIAN_POINT('Ctrl Pts',(-1.65863035238019,1.69532989224459,11.5268585099559));
#63980=CARTESIAN_POINT('Ctrl Pts',(-1.65885944312666,1.69510572973115,11.5268800572581));
#63981=CARTESIAN_POINT('Ctrl Pts',(-1.65897134959819,1.69499620891324,11.5268905828744));
#63982=CARTESIAN_POINT('Ctrl Pts',(-1.65919027053181,1.6947819125488,11.5269111743109));
#63983=CARTESIAN_POINT('Ctrl Pts',(-1.65929728591611,1.69467713794736,11.5269212402034));
#63984=CARTESIAN_POINT('Ctrl Pts',(-1.65950677542559,1.69447199604805,11.526940945143));
#63985=CARTESIAN_POINT('Ctrl Pts',(-1.65960925036564,1.69437162959469,11.5269505842539));
#63986=CARTESIAN_POINT('Ctrl Pts',(-1.65980997692845,1.69417499742773,11.5269694655003));
#63987=CARTESIAN_POINT('Ctrl Pts',(-1.65990822928521,1.69407873245954,11.5269787076932));
#63988=CARTESIAN_POINT('Ctrl Pts',(-1.6601007996036,1.69389002449895,11.5269968222487));
#63989=CARTESIAN_POINT('Ctrl Pts',(-1.66019511821752,1.6937975821769,11.5270056946621));
#63990=CARTESIAN_POINT('Ctrl Pts',(-1.6603800841846,1.69361626546828,11.5270230943815));
#63991=CARTESIAN_POINT('Ctrl Pts',(-1.66047073211945,1.69352739168586,11.5270316217328));
#63992=CARTESIAN_POINT('Ctrl Pts',(-1.66064859689912,1.69335298004889,11.5270483538946));
#63993=CARTESIAN_POINT('Ctrl Pts',(-1.66073581426663,1.69326744273775,11.5270565587457));
#63994=CARTESIAN_POINT('Ctrl Pts',(-1.66090703756157,1.69309949173918,11.5270726665461));
#63995=CARTESIAN_POINT('Ctrl Pts',(-1.66099104397026,1.69301707853158,11.5270805695329));
#63996=CARTESIAN_POINT('Ctrl Pts',(-1.66115604667892,1.69285518103593,11.5270960925235));
#63997=CARTESIAN_POINT('Ctrl Pts',(-1.66123704340525,1.69277569718978,11.5271037125603));
#63998=CARTESIAN_POINT('Ctrl Pts',(-1.66139621161197,1.6926194795465,11.5271186870225));
#63999=CARTESIAN_POINT('Ctrl Pts',(-1.66147438347757,1.69254274615051,11.5271260414777));
#64000=CARTESIAN_POINT('Ctrl Pts',(-1.66162807201355,1.692391864787,11.527140500757));
#64001=CARTESIAN_POINT('Ctrl Pts',(-1.6617035890396,1.69231771717772,11.5271476056089));
#64002=CARTESIAN_POINT('Ctrl Pts',(-1.66185212461924,1.69217185559656,11.5271615804098));
#64003=CARTESIAN_POINT('Ctrl Pts',(-1.66192514349472,1.6921001419522,11.5271684503839));
#64004=CARTESIAN_POINT('Ctrl Pts',(-1.66206882746833,1.6919590080941,11.5271819690281));
#64005=CARTESIAN_POINT('Ctrl Pts',(-1.66213949285173,1.69188958818693,11.5271886177201));
#64006=CARTESIAN_POINT('Ctrl Pts',(-1.66227860359914,1.69175291213719,11.5272017063711));
#64007=CARTESIAN_POINT('Ctrl Pts',(-1.66234704923766,1.69168565626094,11.5272081463515));
#64008=CARTESIAN_POINT('Ctrl Pts',(-1.66248184440961,1.69155318809765,11.5272208292255));
#64009=CARTESIAN_POINT('Ctrl Pts',(-1.66254819418398,1.69148797606442,11.5272270721378));
#64010=CARTESIAN_POINT('Ctrl Pts',(-1.66267891255589,1.69135948408067,11.5272393716776));
#64011=CARTESIAN_POINT('Ctrl Pts',(-1.66274328137291,1.69129620436425,11.5272454283221));
#64012=CARTESIAN_POINT('Ctrl Pts',(-1.66287014457589,1.69117147340533,11.5272573653597));
#64013=CARTESIAN_POINT('Ctrl Pts',(-1.6629326391694,1.69111002237196,11.5272632457689));
#64014=CARTESIAN_POINT('Ctrl Pts',(-1.66305585324881,1.69098885233702,11.5272748396719));
#64015=CARTESIAN_POINT('Ctrl Pts',(-1.66311657291818,1.6909291335352,11.5272805531797));
#64016=CARTESIAN_POINT('Ctrl Pts',(-1.66323632965187,1.69081133811092,11.527291821975));
#64017=CARTESIAN_POINT('Ctrl Pts',(-1.66329536689234,1.69075326166556,11.5272973772761));
#64018=CARTESIAN_POINT('Ctrl Pts',(-1.66341184505365,1.69063866711044,11.5273083377688));
#64019=CARTESIAN_POINT('Ctrl Pts',(-1.66346928614063,1.69058214916062,11.5273137429733));
#64020=CARTESIAN_POINT('Ctrl Pts',(-1.66358265260062,1.69047059324412,11.5273244108499));
#64021=CARTESIAN_POINT('Ctrl Pts',(-1.66363857812016,1.6904155554322,11.5273296735333));
#64022=CARTESIAN_POINT('Ctrl Pts',(-1.66374898881376,1.69030688650497,11.5273400634528));
#64023=CARTESIAN_POINT('Ctrl Pts',(-1.66380347412451,1.69025325553189,11.5273451906995));
#64024=CARTESIAN_POINT('Ctrl Pts',(-1.6639110749565,1.69014733165275,11.5273553163783));
#64025=CARTESIAN_POINT('Ctrl Pts',(-1.66396419060955,1.69009503887353,11.5273603148207));
#64026=CARTESIAN_POINT('Ctrl Pts',(-1.66406911828847,1.68999172700522,11.527370189111));
#64027=CARTESIAN_POINT('Ctrl Pts',(-1.66412093042876,1.68994070804166,11.5273750649676));
#64028=CARTESIAN_POINT('Ctrl Pts',(-1.66422331313304,1.68983988340981,11.5273846999199));
#64029=CARTESIAN_POINT('Ctrl Pts',(-1.66427388381735,1.68979007784443,11.527389459025));
#64030=CARTESIAN_POINT('Ctrl Pts',(-1.66437384194789,1.68969162320983,11.5273988659589));
#64031=CARTESIAN_POINT('Ctrl Pts',(-1.66442322949193,1.68964297425033,11.5274035137951));
#64032=CARTESIAN_POINT('Ctrl Pts',(-1.66452087619098,1.68954677940979,11.5274127033481));
#64033=CARTESIAN_POINT('Ctrl Pts',(-1.66456913543723,1.68949923363087,11.5274172450717));
#64034=CARTESIAN_POINT('Ctrl Pts',(-1.66466457717607,1.68940519484906,11.5274262272541));
#64035=CARTESIAN_POINT('Ctrl Pts',(-1.66471175975834,1.68935870193694,11.5274306677198));
#64036=CARTESIAN_POINT('Ctrl Pts',(-1.67252159931882,1.6816623742972,11.5281656759792));
#64037=CARTESIAN_POINT('Ctrl Pts',(-1.6802316227727,1.67395894408148,11.5288922017329));
#64038=CARTESIAN_POINT('Ctrl Pts',(-1.70631987731404,1.6475311451034,11.5313548386357));
#64039=CARTESIAN_POINT('Ctrl Pts',(-1.72444114075359,1.62855435476854,11.5330727974936));
#64040=CARTESIAN_POINT('Ctrl Pts',(-1.76871060836043,1.58062717568079,11.5373003135647));
#64041=CARTESIAN_POINT('Ctrl Pts',(-1.79446718892364,1.55132437826418,11.5397876671384));
#64042=CARTESIAN_POINT('Ctrl Pts',(-1.90616184075693,1.41774502401846,11.5507704828611));
#64043=CARTESIAN_POINT('Ctrl Pts',(-1.98382205172522,1.30686968575048,11.5589620211415));
#64044=CARTESIAN_POINT('Ctrl Pts',(-2.11463327291961,1.0813403608795,11.5750343610985));
#64045=CARTESIAN_POINT('Ctrl Pts',(-2.16890960460965,0.967882344875475,
11.5828716916835));
#64046=CARTESIAN_POINT('Ctrl Pts',(-2.22386900861041,0.824845476334893,
11.5928172274308));
#64047=CARTESIAN_POINT('Ctrl Pts',(-2.23333867670243,0.79885022351086,11.5946265254691));
#64048=CARTESIAN_POINT('Ctrl Pts',(-2.24773589165326,0.757069747605381,
11.5975404347685));
#64049=CARTESIAN_POINT('Ctrl Pts',(-2.25295700637494,0.741387851102285,
11.598635453568));
#64050=CARTESIAN_POINT('Ctrl Pts',(-2.26257331235674,0.711464801394712,
11.6007280023598));
#64051=CARTESIAN_POINT('Ctrl Pts',(-2.26699902113685,0.697234234919124,
11.6017244862371));
#64052=CARTESIAN_POINT('Ctrl Pts',(-2.27682935038138,0.664542090379139,
11.6040172174803));
#64053=CARTESIAN_POINT('Ctrl Pts',(-2.28214400558302,0.646054781726542,
11.6053162851375));
#64054=CARTESIAN_POINT('Ctrl Pts',(-2.2927865396314,0.607263149794055,11.6080480848004));
#64055=CARTESIAN_POINT('Ctrl Pts',(-2.29807088805373,0.5869487153479,11.609482075427));
#64056=CARTESIAN_POINT('Ctrl Pts',(-2.3115401225282,0.53219655220293,11.6133568907369));
#64057=CARTESIAN_POINT('Ctrl Pts',(-2.31922459673377,0.497642396052019,
11.6158127786441));
#64058=CARTESIAN_POINT('Ctrl Pts',(-2.34520742514599,0.367083970263016,
11.6251326921883));
#64059=CARTESIAN_POINT('Ctrl Pts',(-2.35832728678283,0.270213502234134,
11.6321350057906));
#64060=CARTESIAN_POINT('Ctrl Pts',(-2.3654410511783,0.172877690580661,11.6392156713196));
#64061=CARTESIAN_POINT('Origin',(0.,0.,-1.84858989190501));
#64062=CARTESIAN_POINT('',(-2.3654409861093,0.172878580900717,12.8383513775306));
#64063=CARTESIAN_POINT('',(-2.3654410188404,0.172878133051282,12.6417724606485));
#64064=CARTESIAN_POINT('',(-2.36544101854889,0.172878137039864,-1.84858989190501));
#64065=CARTESIAN_POINT('',(-2.37174976881083,0.001047208561118,11.848589891905));
#64066=CARTESIAN_POINT('Ctrl Pts',(-2.36544098610933,0.172878580900381,
12.8383513775307));
#64067=CARTESIAN_POINT('Ctrl Pts',(-2.35368532029865,0.333727504941463,
12.8268323824084));
#64068=CARTESIAN_POINT('Ctrl Pts',(-2.32554364816744,0.49308856543647,12.8149340599441));
#64069=CARTESIAN_POINT('Ctrl Pts',(-2.26150281083728,0.718392965099194,
12.7980181616257));
#64070=CARTESIAN_POINT('Ctrl Pts',(-2.23841878234253,0.78737976057016,12.7928320854961));
#64071=CARTESIAN_POINT('Ctrl Pts',(-2.20634816523779,0.870338527495156,
12.7866697169524));
#64072=CARTESIAN_POINT('Ctrl Pts',(-2.20034166505561,0.885414011477231,
12.7855529926201));
#64073=CARTESIAN_POINT('Ctrl Pts',(-2.19067082483952,0.908980127465351,
12.7838135283743));
#64074=CARTESIAN_POINT('Ctrl Pts',(-2.18711088689246,0.917512676005192,
12.7831850124943));
#64075=CARTESIAN_POINT('Ctrl Pts',(-2.18027890830946,0.933622006436859,
12.7820011238744));
#64076=CARTESIAN_POINT('Ctrl Pts',(-2.17701720325093,0.941202564651642,
12.7814452152662));
#64077=CARTESIAN_POINT('Ctrl Pts',(-2.16914548539114,0.959237436417395,
12.7801252439033));
#64078=CARTESIAN_POINT('Ctrl Pts',(-2.16449939473682,0.969675708424831,
12.779363329515));
#64079=CARTESIAN_POINT('Ctrl Pts',(-2.14828857028532,1.00539908994135,12.7767615291189));
#64080=CARTESIAN_POINT('Ctrl Pts',(-2.13635426851358,1.03051526562823,12.7749421896048));
#64081=CARTESIAN_POINT('Ctrl Pts',(-2.10553822376845,1.09253120133172,12.7704605957774));
#64082=CARTESIAN_POINT('Ctrl Pts',(-2.0861253111776,1.12915774582066,12.7678233119092));
#64083=CARTESIAN_POINT('Ctrl Pts',(-1.98888111531938,1.30155148936724,12.7553678304165));
#64084=CARTESIAN_POINT('Ctrl Pts',(-1.89869843969871,1.42990695370422,12.7459422120141));
#64085=CARTESIAN_POINT('Ctrl Pts',(-1.72929980948198,1.62644484348827,12.7298519306799));
#64086=CARTESIAN_POINT('Ctrl Pts',(-1.65707394369871,1.69997143375175,12.7233688064913));
#64087=CARTESIAN_POINT('Ctrl Pts',(-1.56061726833879,1.78616038658732,12.7149630512803));
#64088=CARTESIAN_POINT('Ctrl Pts',(-1.54063728172853,1.80342226364561,12.7132347377168));
#64089=CARTESIAN_POINT('Ctrl Pts',(-1.50807652429115,1.83061737590564,12.7104358615175));
#64090=CARTESIAN_POINT('Ctrl Pts',(-1.495675631454,1.84076320163941,12.7093739064254));
#64091=CARTESIAN_POINT('Ctrl Pts',(-1.47178349728129,1.85990979161744,12.7073349171214));
#64092=CARTESIAN_POINT('Ctrl Pts',(-1.46031006244873,1.86893167373904,12.7063587831407));
#64093=CARTESIAN_POINT('Ctrl Pts',(-1.43367806708608,1.88947819304339,12.7040994795357));
#64094=CARTESIAN_POINT('Ctrl Pts',(-1.4184626978491,1.90092718967656,12.7028134490074));
#64095=CARTESIAN_POINT('Ctrl Pts',(-1.36946747856372,1.93687848270104,12.6986862716378));
#64096=CARTESIAN_POINT('Ctrl Pts',(-1.33517974749175,1.96067184809507,12.6958187016042));
#64097=CARTESIAN_POINT('Ctrl Pts',(-1.19849640655294,2.05027252305485,12.6844605512025));
#64098=CARTESIAN_POINT('Ctrl Pts',(-1.09173740694761,2.10905504589217,12.6757321868461));
#64099=CARTESIAN_POINT('Ctrl Pts',(-0.842299405949466,2.22236861898381,
12.655816883615));
#64100=CARTESIAN_POINT('Ctrl Pts',(-0.697894923088279,2.27185782186304,
12.6446014806088));
#64101=CARTESIAN_POINT('Ctrl Pts',(-0.522127663977529,2.31373859353405,
12.6318960163141));
#64102=CARTESIAN_POINT('Ctrl Pts',(-0.49440162142858,2.31982128340238,12.62991970416));
#64103=CARTESIAN_POINT('Ctrl Pts',(-0.454952763714559,2.3277363420113,12.6271532658853));
#64104=CARTESIAN_POINT('Ctrl Pts',(-0.443316283008119,2.32998051130195,
12.6263428059367));
#64105=CARTESIAN_POINT('Ctrl Pts',(-0.423561780313416,2.33363693873078,
12.6249769266042));
#64106=CARTESIAN_POINT('Ctrl Pts',(-0.41545242661444,2.33509426646395,12.6244190737827));
#64107=CARTESIAN_POINT('Ctrl Pts',(-0.398438393101934,2.33806040787042,
12.623254813285));
#64108=CARTESIAN_POINT('Ctrl Pts',(-0.389532473530618,2.33956066020504,
12.6226488748526));
#64109=CARTESIAN_POINT('Ctrl Pts',(-0.365572673081522,2.34345621452128,
12.6210275432804));
#64110=CARTESIAN_POINT('Ctrl Pts',(-0.350503614549928,2.34575737334082,
12.6200171957994));
#64111=CARTESIAN_POINT('Ctrl Pts',(-0.271644435512103,2.35702286198107,
12.6147737477271));
#64112=CARTESIAN_POINT('Ctrl Pts',(-0.207524935239054,2.36353178006703,
12.6106598601183));
#64113=CARTESIAN_POINT('Ctrl Pts',(0.0323455344874606,2.37804243515194,
12.5955636758481));
#64114=CARTESIAN_POINT('Ctrl Pts',(0.208545808667721,2.36910247484388,12.585020887531));
#64115=CARTESIAN_POINT('Ctrl Pts',(0.463872134455581,2.3274187607184,12.5688536040343));
#64116=CARTESIAN_POINT('Ctrl Pts',(0.544836975535693,2.3098064739618,12.5635980380843));
#64117=CARTESIAN_POINT('Ctrl Pts',(0.648981343053251,2.28137114932725,12.556573147168));
#64118=CARTESIAN_POINT('Ctrl Pts',(0.67314542774841,2.2743584281003,12.5549244373256));
#64119=CARTESIAN_POINT('Ctrl Pts',(0.712253810154569,2.26233084807667,12.5522231639617));
#64120=CARTESIAN_POINT('Ctrl Pts',(0.727268120722198,2.2575489843552,12.5511781312591));
#64121=CARTESIAN_POINT('Ctrl Pts',(0.756177224827359,2.24802348906941,12.5491499969445));
#64122=CARTESIAN_POINT('Ctrl Pts',(0.770077843566041,2.24329973500468,12.5481675820223));
#64123=CARTESIAN_POINT('Ctrl Pts',(0.802472724444302,2.23195462517863,12.5458607511447));
#64124=CARTESIAN_POINT('Ctrl Pts',(0.820930126365432,2.22523203509207,12.5445330719799));
#64125=CARTESIAN_POINT('Ctrl Pts',(0.881643202165655,2.20226083877156,12.5401204476021));
#64126=CARTESIAN_POINT('Ctrl Pts',(0.923514936174089,2.18503254449068,12.5370036550561));
#64127=CARTESIAN_POINT('Ctrl Pts',(1.02386875026566,2.1403417082127,12.5293486531496));
#64128=CARTESIAN_POINT('Ctrl Pts',(1.08176915624401,2.11166856676646,12.52477425959));
#64129=CARTESIAN_POINT('Ctrl Pts',(1.22522830575137,2.03317596098664,12.5130497465472));
#64130=CARTESIAN_POINT('Ctrl Pts',(1.30897160389477,1.98029800870965,12.505832247627));
#64131=CARTESIAN_POINT('Ctrl Pts',(1.41012696802889,1.90719925165595,12.4967324586226));
#64132=CARTESIAN_POINT('Ctrl Pts',(1.43084184121407,1.89170787831256,12.4948477653999));
#64133=CARTESIAN_POINT('Ctrl Pts',(1.52833192470601,1.81628341550561,12.4858864199982));
#64134=CARTESIAN_POINT('Ctrl Pts',(1.60162924079109,1.75199082577809,12.4788696989353));
#64135=CARTESIAN_POINT('Ctrl Pts',(1.68274088301113,1.67148604037625,12.4709420472858));
#64136=CARTESIAN_POINT('Ctrl Pts',(1.69458371924528,1.65947838825293,12.4697802548858));
#64137=CARTESIAN_POINT('Ctrl Pts',(1.71288365923934,1.64052355585521,12.4679796629568));
#64138=CARTESIAN_POINT('Ctrl Pts',(1.71942861923611,1.63366251060502,12.4673345883049));
#64139=CARTESIAN_POINT('Ctrl Pts',(1.73098854127184,1.62139787640107,12.4661935766336));
#64140=CARTESIAN_POINT('Ctrl Pts',(1.73601953380098,1.61601008167037,12.4656964567333));
#64141=CARTESIAN_POINT('Ctrl Pts',(1.74815369405448,1.60289329280881,12.4644960186554));
#64142=CARTESIAN_POINT('Ctrl Pts',(1.75523078227935,1.59514048203293,12.4637946343759));
#64143=CARTESIAN_POINT('Ctrl Pts',(1.77726816945934,1.57067470503781,12.4616056864818));
#64144=CARTESIAN_POINT('Ctrl Pts',(1.79204349565567,1.55379579532073,12.4601308801083));
#64145=CARTESIAN_POINT('Ctrl Pts',(1.86980097058446,1.46238296476312,12.4523142780117));
#64146=CARTESIAN_POINT('Ctrl Pts',(1.92838435086007,1.38421733200816,12.4462246371086));
#64147=CARTESIAN_POINT('Ctrl Pts',(2.07900939374692,1.15504151312781,12.4292964407797));
#64148=CARTESIAN_POINT('Ctrl Pts',(2.1592282462606,0.997061184076536,12.4186204101356));
#64149=CARTESIAN_POINT('Ctrl Pts',(2.23767390085516,0.787547144207726,12.4043491932527));
#64150=CARTESIAN_POINT('Ctrl Pts',(2.25286608628951,0.742973027089248,12.4013104008901));
#64151=CARTESIAN_POINT('Ctrl Pts',(2.27215918249905,0.680317713848536,12.3970197048892));
#64152=CARTESIAN_POINT('Ctrl Pts',(2.27739067092952,0.662594327493564,12.3958039224706));
#64153=CARTESIAN_POINT('Ctrl Pts',(2.28611218479078,0.631723146044363,12.3936817505051));
#64154=CARTESIAN_POINT('Ctrl Pts',(2.28969723843485,0.618602940546634,12.3927784384338));
#64155=CARTESIAN_POINT('Ctrl Pts',(2.29695787914994,0.591103065859568,12.3908818289405));
#64156=CARTESIAN_POINT('Ctrl Pts',(2.3006117219288,0.576718320223502,12.3898878829898));
#64157=CARTESIAN_POINT('Ctrl Pts',(2.30901656719768,0.542277913208629,12.3875032563217));
#64158=CARTESIAN_POINT('Ctrl Pts',(2.31364154954401,0.522193045536226,12.3861086508924));
#64159=CARTESIAN_POINT('Ctrl Pts',(2.32889464825206,0.451768435767889,12.381203558638));
#64160=CARTESIAN_POINT('Ctrl Pts',(2.33814546612742,0.401148454201618,12.3776506046863));
#64161=CARTESIAN_POINT('Ctrl Pts',(2.3571895640957,0.273611310385184,12.3686257073142));
#64162=CARTESIAN_POINT('Ctrl Pts',(2.36487078730657,0.196443417582445,12.3630977796077));
#64163=CARTESIAN_POINT('Ctrl Pts',(2.37340848897089,0.02655862949043,12.3508179698316));
#64164=CARTESIAN_POINT('Ctrl Pts',(2.37263581298928,-0.0661172918759338,
12.3440465442837));
#64165=CARTESIAN_POINT('Ctrl Pts',(2.3592343941836,-0.266195358355569,12.3294441449788));
#64166=CARTESIAN_POINT('Ctrl Pts',(2.34467808124429,-0.373278367396632,
12.3216388838325));
#64167=CARTESIAN_POINT('Ctrl Pts',(2.31945173486574,-0.495609799991988,
12.3129731164611));
#64168=CARTESIAN_POINT('Ctrl Pts',(2.31585007807841,-0.512175634678752,
12.3118051729443));
#64169=CARTESIAN_POINT('Ctrl Pts',(2.30995297241232,-0.537964314934816,
12.3099971417989));
#64170=CARTESIAN_POINT('Ctrl Pts',(2.30777927145049,-0.547214017554594,
12.3093506988199));
#64171=CARTESIAN_POINT('Ctrl Pts',(2.30382123515826,-0.563613407636575,
12.3082085210499));
#64172=CARTESIAN_POINT('Ctrl Pts',(2.30205914411235,-0.570767952927958,
12.3077115889613));
#64173=CARTESIAN_POINT('Ctrl Pts',(2.29771286406004,-0.588067381207843,
12.3065132100097));
#64174=CARTESIAN_POINT('Ctrl Pts',(2.29509481447099,-0.598203521663688,
12.3058136783417));
#64175=CARTESIAN_POINT('Ctrl Pts',(2.28669573221546,-0.629854736198219,
12.3036365848373));
#64176=CARTESIAN_POINT('Ctrl Pts',(2.28067843902456,-0.651306613803576,
12.3021715845777));
#64177=CARTESIAN_POINT('Ctrl Pts',(2.24710031706686,-0.764837106980526,
12.2944588900615));
#64178=CARTESIAN_POINT('Ctrl Pts',(2.21426078692,-0.85527122940738,12.2884560253101));
#64179=CARTESIAN_POINT('Ctrl Pts',(2.10746758559104,-1.10157876651784,12.2718774423619));
#64180=CARTESIAN_POINT('Ctrl Pts',(2.02189348217914,-1.25173459712863,12.261463388681));
#64181=CARTESIAN_POINT('Ctrl Pts',(1.89057804057558,-1.43302770738922,12.2472261660712));
#64182=CARTESIAN_POINT('Ctrl Pts',(1.85899783180382,-1.4737639547733,12.2439076486273));
#64183=CARTESIAN_POINT('Ctrl Pts',(1.81260931044947,-1.52973647821582,12.2391539853959));
#64184=CARTESIAN_POINT('Ctrl Pts',(1.79888367453573,-1.54585370693393,12.2377614108665));
#64185=CARTESIAN_POINT('Ctrl Pts',(1.77520242778473,-1.57291871322669,12.235380764051));
#64186=CARTESIAN_POINT('Ctrl Pts',(1.76535659331639,-1.58396118000503,12.234397206941));
#64187=CARTESIAN_POINT('Ctrl Pts',(1.74515660347387,-1.60619391789739,12.2323913826264));
#64188=CARTESIAN_POINT('Ctrl Pts',(1.73479658690927,-1.61737789524186,12.2313688974264));
#64189=CARTESIAN_POINT('Ctrl Pts',(1.70873661193864,-1.64497203974724,12.2288117871193));
#64190=CARTESIAN_POINT('Ctrl Pts',(1.69290769110749,-1.66125774886385,12.2272717145065));
#64191=CARTESIAN_POINT('Ctrl Pts',(1.62903907429867,-1.72510864579499,12.2211070983148));
#64192=CARTESIAN_POINT('Ctrl Pts',(1.57921323242279,-1.77083374788939,12.2164053069193));
#64193=CARTESIAN_POINT('Ctrl Pts',(1.43609012774958,-1.89132852362624,12.2031801109847));
#64194=CARTESIAN_POINT('Ctrl Pts',(1.33899600834075,-1.96126562739898,12.1945047158915));
#64195=CARTESIAN_POINT('Ctrl Pts',(1.12713663128748,-2.09077947933883,12.1763970009083));
#64196=CARTESIAN_POINT('Ctrl Pts',(1.01191440422633,-2.14891390102675,12.1669880622536));
#64197=CARTESIAN_POINT('Ctrl Pts',(0.87159487385442,-2.20590822281858,12.1564078992929));
#64198=CARTESIAN_POINT('Ctrl Pts',(0.850537031371892,-2.21411281600388,
12.1548426858484));
#64199=CARTESIAN_POINT('Ctrl Pts',(0.819500968268428,-2.22569698345398,
12.1525719080389));
#64200=CARTESIAN_POINT('Ctrl Pts',(0.809613084207701,-2.22931280073484,
12.1518537713408));
#64201=CARTESIAN_POINT('Ctrl Pts',(0.79202610336444,-2.23561158917672,12.1505862841361));
#64202=CARTESIAN_POINT('Ctrl Pts',(0.784336862511593,-2.2383208480322,12.1500354587246));
#64203=CARTESIAN_POINT('Ctrl Pts',(0.767375387368757,-2.24419898467767,
12.1488277705183));
#64204=CARTESIAN_POINT('Ctrl Pts',(0.758097348306255,-2.24735010333356,
12.1481719256916));
#64205=CARTESIAN_POINT('Ctrl Pts',(0.730911226940141,-2.25639585879313,
12.146263376365));
#64206=CARTESIAN_POINT('Ctrl Pts',(0.712951592034295,-2.2621347384588,12.1450192050823));
#64207=CARTESIAN_POINT('Ctrl Pts',(0.67134820903718,-2.27488410682514,12.1421712433914));
#64208=CARTESIAN_POINT('Ctrl Pts',(0.647659428560118,-2.28174132695525,
12.1405748423353));
#64209=CARTESIAN_POINT('Ctrl Pts',(0.565409896985093,-2.30416600205678,
12.1351050529145));
#64210=CARTESIAN_POINT('Ctrl Pts',(0.506359434364415,-2.31785901602653,
12.1313047780662));
#64211=CARTESIAN_POINT('Ctrl Pts',(0.300133764570324,-2.3574211173756,12.1182716193439));
#64212=CARTESIAN_POINT('Ctrl Pts',(0.151092572164565,-2.37164215166157,
12.1092470524373));
#64213=CARTESIAN_POINT('Ctrl Pts',(-0.0804971057218945,-2.37180839463319,
12.0947703755599));
#64214=CARTESIAN_POINT('Ctrl Pts',(-0.162636564098529,-2.36759415143137,
12.0895521603162));
#64215=CARTESIAN_POINT('Ctrl Pts',(-0.269356245101135,-2.35653887927567,
12.0825701508277));
#64216=CARTESIAN_POINT('Ctrl Pts',(-0.294283230403527,-2.35355594343502,
12.0809250470722));
#64217=CARTESIAN_POINT('Ctrl Pts',(-0.334759586720019,-2.3480591982231,
12.0782281902113));
#64218=CARTESIAN_POINT('Ctrl Pts',(-0.350339938890633,-2.34578513220333,
12.0771839204764));
#64219=CARTESIAN_POINT('Ctrl Pts',(-0.380406299027762,-2.34109051227903,
12.0751562220014));
#64220=CARTESIAN_POINT('Ctrl Pts',(-0.394894770862997,-2.33869019804239,
12.0741734699246));
#64221=CARTESIAN_POINT('Ctrl Pts',(-0.428738079874039,-2.33275990439674,
12.0718642268873));
#64222=CARTESIAN_POINT('Ctrl Pts',(-0.448072895481977,-2.32912338721785,
12.0705344523123));
#64223=CARTESIAN_POINT('Ctrl Pts',(-0.511923530421011,-2.31628981801075,
12.0661070692974));
#64224=CARTESIAN_POINT('Ctrl Pts',(-0.556217784749888,-2.30605409999189,
12.0629773186715));
#64225=CARTESIAN_POINT('Ctrl Pts',(-0.663029625108726,-2.27811523462277,
12.0552829380522));
#64226=CARTESIAN_POINT('Ctrl Pts',(-0.725164353940703,-2.25910441217664,
12.050681623877));
#64227=CARTESIAN_POINT('Ctrl Pts',(-0.879322709689901,-2.2049225193488,
12.0389635274988));
#64228=CARTESIAN_POINT('Ctrl Pts',(-0.97008154028637,-2.1665252294242,12.0317816429962));
#64229=CARTESIAN_POINT('Ctrl Pts',(-1.16005427195128,-2.07181762736532,
12.0163043676642));
#64230=CARTESIAN_POINT('Ctrl Pts',(-1.25814406690428,-2.01376080469628,
12.0080285677111));
#64231=CARTESIAN_POINT('Ctrl Pts',(-1.37047279748793,-1.93585246179476,
11.9984760667337));
#64232=CARTESIAN_POINT('Ctrl Pts',(-1.38906498154816,-1.92255533460683,
11.9968926174823));
#64233=CARTESIAN_POINT('Ctrl Pts',(-1.41588488353937,-1.90278152875475,
11.9946082751795));
#64234=CARTESIAN_POINT('Ctrl Pts',(-1.42426592222551,-1.89651631753648,
11.9938944118124));
#64235=CARTESIAN_POINT('Ctrl Pts',(-1.43885556712512,-1.88545862423564,
11.992652078047));
#64236=CARTESIAN_POINT('Ctrl Pts',(-1.44508222439617,-1.88069054815789,
11.9921220005331));
#64237=CARTESIAN_POINT('Ctrl Pts',(-1.45139280023392,-1.87580836451055,
11.991584943202));
#64238=CARTESIAN_POINT('Ctrl Pts',(-1.45150019277676,-1.87572526541273,
11.9915758036702));
#64239=CARTESIAN_POINT('Ctrl Pts',(-1.45175595634967,-1.87552732342296,
11.9915540372653));
#64240=CARTESIAN_POINT('Ctrl Pts',(-1.45190432092828,-1.87541247211718,
11.9915414109756));
#64241=CARTESIAN_POINT('Ctrl Pts',(-1.45219308286609,-1.87518888224929,
11.9915168365695));
#64242=CARTESIAN_POINT('Ctrl Pts',(-1.45233348163533,-1.87508014552885,
11.9915048883256));
#64243=CARTESIAN_POINT('Ctrl Pts',(-1.45260701429589,-1.87486824947377,
11.9914816102156));
#64244=CARTESIAN_POINT('Ctrl Pts',(-1.45274014940653,-1.87476509172984,
11.9914702802395));
#64245=CARTESIAN_POINT('Ctrl Pts',(-1.45299977556276,-1.87456388003426,
11.9914481858123));
#64246=CARTESIAN_POINT('Ctrl Pts',(-1.45312626767412,-1.8744658274586,11.9914374212653));
#64247=CARTESIAN_POINT('Ctrl Pts',(-1.45337315879328,-1.87427440547349,
11.9914164107914));
#64248=CARTESIAN_POINT('Ctrl Pts',(-1.45349355872528,-1.87418103726879,
11.9914061647814));
#64249=CARTESIAN_POINT('Ctrl Pts',(-1.45372875626543,-1.87399860907556,
11.9913861496014));
#64250=CARTESIAN_POINT('Ctrl Pts',(-1.45384355468032,-1.87390955014501,
11.9913763803589));
#64251=CARTESIAN_POINT('Ctrl Pts',(-1.45406798788894,-1.87373540510821,
11.9913572813675));
#64252=CARTESIAN_POINT('Ctrl Pts',(-1.45417762339537,-1.87365031993049,
11.9913479515547));
#64253=CARTESIAN_POINT('Ctrl Pts',(-1.45439212423638,-1.87348382140975,
11.9913296979298));
#64254=CARTESIAN_POINT('Ctrl Pts',(-1.4544969902062,-1.8734024088823,11.9913207740608));
#64255=CARTESIAN_POINT('Ctrl Pts',(-1.4547023059679,-1.87324298468929,11.9913033021895));
#64256=CARTESIAN_POINT('Ctrl Pts',(-1.45480275631614,-1.8731649737519,11.9912947541374));
#64257=CARTESIAN_POINT('Ctrl Pts',(-1.45499956024397,-1.87301210809677,
11.9912780067108));
#64258=CARTESIAN_POINT('Ctrl Pts',(-1.45509591431884,-1.87293725402638,
11.9912698072919));
#64259=CARTESIAN_POINT('Ctrl Pts',(-1.45528481472938,-1.87279048060783,
11.9912537325288));
#64260=CARTESIAN_POINT('Ctrl Pts',(-1.45537736150449,-1.8727185618393,11.9912458571453));
#64261=CARTESIAN_POINT('Ctrl Pts',(-1.45555890951743,-1.8725774579793,11.9912304081341));
#64262=CARTESIAN_POINT('Ctrl Pts',(-1.4556479111605,-1.87250827339745,11.9912228344703));
#64263=CARTESIAN_POINT('Ctrl Pts',(-1.45582260741477,-1.87237245494151,
11.9912079685969));
#64264=CARTESIAN_POINT('Ctrl Pts',(-1.45590830238647,-1.87230582152751,
11.9912006763552));
#64265=CARTESIAN_POINT('Ctrl Pts',(-1.45607660277043,-1.87217493849164,
11.9911863548153));
#64266=CARTESIAN_POINT('Ctrl Pts',(-1.45615920849617,-1.87211068929257,
11.991179325489));
#64267=CARTESIAN_POINT('Ctrl Pts',(-1.45632152908978,-1.87198442210673,
11.991165512867));
#64268=CARTESIAN_POINT('Ctrl Pts',(-1.45640124424951,-1.87192240449469,
11.9911587295452));
#64269=CARTESIAN_POINT('Ctrl Pts',(-1.4565579657066,-1.87180046066822,11.9911453934413));
#64270=CARTESIAN_POINT('Ctrl Pts',(-1.45663497226408,-1.87174053479598,
11.991138840636));
#64271=CARTESIAN_POINT('Ctrl Pts',(-1.45678644353232,-1.87162264608685,
11.9911259513495));
#64272=CARTESIAN_POINT('Ctrl Pts',(-1.45686090848133,-1.87156468355855,
11.9911196148472));
#64273=CARTESIAN_POINT('Ctrl Pts',(-1.45700745011316,-1.8714506034515,11.9911071450946));
#64274=CARTESIAN_POINT('Ctrl Pts',(-1.45707952701537,-1.87139448615114,
11.991101011825));
#64275=CARTESIAN_POINT('Ctrl Pts',(-1.45722143405187,-1.87128398766017,
11.9910889364945));
#64276=CARTESIAN_POINT('Ctrl Pts',(-1.45729126438516,-1.87122960672395,
11.991082994416));
#64277=CARTESIAN_POINT('Ctrl Pts',(-1.45742880891731,-1.87112248043925,
11.9910712903492));
#64278=CARTESIAN_POINT('Ctrl Pts',(-1.45749652328378,-1.87106973533404,
11.991065528346));
#64279=CARTESIAN_POINT('Ctrl Pts',(-1.45762995661824,-1.87096578777106,
11.9910541741539));
#64280=CARTESIAN_POINT('Ctrl Pts',(-1.45769567575834,-1.87091458552124,
11.9910485819497));
#64281=CARTESIAN_POINT('Ctrl Pts',(-1.45782523050553,-1.87081363752543,
11.9910375578346));
#64282=CARTESIAN_POINT('Ctrl Pts',(-1.45788906626306,-1.87076389197575,
11.9910321259103));
#64283=CARTESIAN_POINT('Ctrl Pts',(-1.45801495799662,-1.87066577745695,
11.9910214135246));
#64284=CARTESIAN_POINT('Ctrl Pts',(-1.45807701411725,-1.8706174086631,11.9910161330505));
#64285=CARTESIAN_POINT('Ctrl Pts',(-1.45819944302822,-1.87052197333053,
11.9910057153562));
#64286=CARTESIAN_POINT('Ctrl Pts',(-1.45825981593289,-1.87047490696762,
11.991000578126));
#64287=CARTESIAN_POINT('Ctrl Pts',(-1.45837896808324,-1.87038200737393,
11.9909904392876));
#64288=CARTESIAN_POINT('Ctrl Pts',(-1.45843774746246,-1.8703361742832,11.9909854376678));
#64289=CARTESIAN_POINT('Ctrl Pts',(-1.45855379622822,-1.87024567671815,
11.9909755629297));
#64290=CARTESIAN_POINT('Ctrl Pts',(-1.45861106570686,-1.87020101239739,
11.9909706898032));
#64291=CARTESIAN_POINT('Ctrl Pts',(-1.45872417265534,-1.87011279222028,
11.9909610654147));
#64292=CARTESIAN_POINT('Ctrl Pts',(-1.45878001023926,-1.87006923648332,
11.9909563141427));
#64293=CARTESIAN_POINT('Ctrl Pts',(-1.45889032634701,-1.86998317718785,
11.9909469272547));
#64294=CARTESIAN_POINT('Ctrl Pts',(-1.45894480495845,-1.86994067375391,
11.990942291631));
#64295=CARTESIAN_POINT('Ctrl Pts',(-1.45905247134113,-1.86985666641185,
11.9909331302338));
#64296=CARTESIAN_POINT('Ctrl Pts',(-1.45910565920336,-1.8698151626116,11.9909286044522));
#64297=CARTESIAN_POINT('Ctrl Pts',(-1.45921080801912,-1.86973310517965,
11.9909196572982));
#64298=CARTESIAN_POINT('Ctrl Pts',(-1.45926276905571,-1.86969255164918,
11.9909152359185));
#64299=CARTESIAN_POINT('Ctrl Pts',(-1.4593655241983,-1.86961234843846,11.9909064924639));
#64300=CARTESIAN_POINT('Ctrl Pts',(-1.45941631837631,-1.86957269885637,
11.9909021703825));
#64301=CARTESIAN_POINT('Ctrl Pts',(-1.4595167961498,-1.86949426001518,11.9908936207292));
#64302=CARTESIAN_POINT('Ctrl Pts',(-1.45956647980392,-1.86945547085397,
11.9908893931519));
#64303=CARTESIAN_POINT('Ctrl Pts',(-1.45966478945822,-1.86937871195809,
11.9908810280022));
#64304=CARTESIAN_POINT('Ctrl Pts',(-1.45971341553625,-1.86934074229652,
11.9908768904229));
#64305=CARTESIAN_POINT('Ctrl Pts',(-1.4598096599376,-1.86926558383323,11.9908687010226));
#64306=CARTESIAN_POINT('Ctrl Pts',(-1.4598572783116,-1.86922839511686,11.990864649197));
#64307=CARTESIAN_POINT('Ctrl Pts',(-1.45995155428373,-1.86915476222533,
11.9908566273061));
#64308=CARTESIAN_POINT('Ctrl Pts',(-1.45999821194105,-1.86911831812062,
11.9908526572355));
#64309=CARTESIAN_POINT('Ctrl Pts',(-1.46009061081547,-1.86904614016821,
11.9908447950813));
#64310=CARTESIAN_POINT('Ctrl Pts',(-1.46013635208901,-1.86901040638552,
11.9908409029928));
#64311=CARTESIAN_POINT('Ctrl Pts',(-1.46022696008722,-1.86893961667475,
11.9908331932378));
#64312=CARTESIAN_POINT('Ctrl Pts',(-1.46027182685854,-1.86890456081234,
11.9908293755671));
#64313=CARTESIAN_POINT('Ctrl Pts',(-1.4687285525005,-1.862296556564,11.9901098015401));
#64314=CARTESIAN_POINT('Ctrl Pts',(-1.47709613636665,-1.85566673736044,
11.9893979360074));
#64315=CARTESIAN_POINT('Ctrl Pts',(-1.49538883683277,-1.84097089686564,
11.9878412569181));
#64316=CARTESIAN_POINT('Ctrl Pts',(-1.50529411804956,-1.83288058841192,
11.9869980432305));
#64317=CARTESIAN_POINT('Ctrl Pts',(-1.5326543267251,-1.81016225672793,11.9846665662472));
#64318=CARTESIAN_POINT('Ctrl Pts',(-1.54996518159996,-1.79536199651148,
11.983188718568));
#64319=CARTESIAN_POINT('Ctrl Pts',(-1.60727462691208,-1.74491731003007,
11.9782764228534));
#64320=CARTESIAN_POINT('Ctrl Pts',(-1.64628019526784,-1.70816579910932,
11.9748999217458));
#64321=CARTESIAN_POINT('Ctrl Pts',(-1.75404302393251,-1.59950690725286,
11.9653611689266));
#64322=CARTESIAN_POINT('Ctrl Pts',(-1.81956733866899,-1.52455411286104,
11.9592956704791));
#64323=CARTESIAN_POINT('Ctrl Pts',(-1.96445427157441,-1.33612342304257,
11.9446764098377));
#64324=CARTESIAN_POINT('Ctrl Pts',(-2.03896259118745,-1.21939779014186,
11.9360909821371));
#64325=CARTESIAN_POINT('Ctrl Pts',(-2.11561349903799,-1.07244384190076,
11.92533343761));
#64326=CARTESIAN_POINT('Ctrl Pts',(-2.12792124447116,-1.04781074008785,
11.923532650185));
#64327=CARTESIAN_POINT('Ctrl Pts',(-2.14681182692223,-1.00829636466461,
11.9206448197545));
#64328=CARTESIAN_POINT('Ctrl Pts',(-2.15367544310135,-0.993551530121191,
11.9195674143209));
#64329=CARTESIAN_POINT('Ctrl Pts',(-2.16638722206217,-0.965492569921478,
11.9175169085102));
#64330=CARTESIAN_POINT('Ctrl Pts',(-2.17226566500195,-0.952192923259751,
11.9165448919243));
#64331=CARTESIAN_POINT('Ctrl Pts',(-2.18537830895178,-0.921772821031553,
11.9143209582364));
#64332=CARTESIAN_POINT('Ctrl Pts',(-2.19253422637532,-0.904619875512886,
11.9130664817441));
#64333=CARTESIAN_POINT('Ctrl Pts',(-2.21414692200013,-0.851050279136837,
11.9091462701112));
#64334=CARTESIAN_POINT('Ctrl Pts',(-2.22790279728864,-0.814359860423141,
11.9064577176621));
#64335=CARTESIAN_POINT('Ctrl Pts',(-2.31373562872294,-0.566942400451359,
11.8882942262351));
#64336=CARTESIAN_POINT('Ctrl Pts',(-2.35671860544731,-0.34732802550277,
11.8718600667347));
#64337=CARTESIAN_POINT('Ctrl Pts',(-2.37066663023684,-0.0830754162589632,
11.8527358073335));
#64338=CARTESIAN_POINT('Ctrl Pts',(-2.37176604780075,-0.0410838677914949,
11.8497212300524));
#64339=CARTESIAN_POINT('Ctrl Pts',(-2.37174982303164,0.00091621470674144,
11.8467427388015));
#64340=CARTESIAN_POINT('Ctrl Pts',(-2.36544101854889,0.172878137039869,
11.8369824012687));
#64341=CARTESIAN_POINT('Ctrl Pts',(-2.36961833947221,0.115721075835709,
11.8408515648142));
#64342=CARTESIAN_POINT('Ctrl Pts',(-2.37172444190719,0.058408349480251,
11.8447207283596));
#64343=CARTESIAN_POINT('Ctrl Pts',(-2.37174976881083,0.001047208561118,
11.848589891905));
#64344=CARTESIAN_POINT('',(-2.37174934418356,-0.00196579904219032,11.65195718999));
#64345=CARTESIAN_POINT('Ctrl Pts',(-2.3654410511783,0.172877690580661,11.6392156713196));
#64346=CARTESIAN_POINT('Ctrl Pts',(-2.36969121283375,0.114723819944284,
11.6434460578567));
#64347=CARTESIAN_POINT('Ctrl Pts',(-2.37179752731082,0.0564037460590684,
11.6477030248798));
#64348=CARTESIAN_POINT('Ctrl Pts',(-2.37174918657996,-0.00196429562807089,
11.6519573558634));
#64349=CARTESIAN_POINT('Ctrl Pts',(-2.37174918535101,-0.0019657789382381,
11.6519574639789));
#64350=CARTESIAN_POINT('Ctrl Pts',(-2.37167497384227,-0.0915033571298152,
11.6584836805817));
#64351=CARTESIAN_POINT('Ctrl Pts',(-2.36653051349874,-0.180972548701005,
11.6649920740709));
#64352=CARTESIAN_POINT('Ctrl Pts',(-2.35248817208768,-0.303548324308444,
11.6737404926746));
#64353=CARTESIAN_POINT('Ctrl Pts',(-2.34791967395338,-0.337069216544892,
11.6761150148799));
#64354=CARTESIAN_POINT('Ctrl Pts',(-2.34082399987725,-0.381936558039573,
11.6792596032624));
#64355=CARTESIAN_POINT('Ctrl Pts',(-2.33892858794854,-0.393377180619818,
11.680058473185));
#64356=CARTESIAN_POINT('Ctrl Pts',(-2.33550234516674,-0.413157027951826,
11.6814339978809));
#64357=CARTESIAN_POINT('Ctrl Pts',(-2.33401058861634,-0.421502682903235,
11.6820126217831));
#64358=CARTESIAN_POINT('Ctrl Pts',(-2.3309408428091,-0.43816027009921,11.6831637992376));
#64359=CARTESIAN_POINT('Ctrl Pts',(-2.32936306051245,-0.44647214532998,
11.6837363451214));
#64360=CARTESIAN_POINT('Ctrl Pts',(-2.32593336843323,-0.464026806104101,
11.6849414236367));
#64361=CARTESIAN_POINT('Ctrl Pts',(-2.32407079820625,-0.473267201202765,
11.6855733673658));
#64362=CARTESIAN_POINT('Ctrl Pts',(-2.31880369261213,-0.498616664358954,
11.6873010575767));
#64363=CARTESIAN_POINT('Ctrl Pts',(-2.3152863554122,-0.514702119883485,
11.688390754045));
#64364=CARTESIAN_POINT('Ctrl Pts',(-2.29550587306111,-0.600853001049982,
11.6941978272971));
#64365=CARTESIAN_POINT('Ctrl Pts',(-2.27622773060333,-0.670194724058452,
11.6987684459377));
#64366=CARTESIAN_POINT('Ctrl Pts',(-2.22202953050266,-0.835588715945488,
11.7096514363538));
#64367=CARTESIAN_POINT('Ctrl Pts',(-2.18400002231236,-0.930467229131064,
11.7158817334689));
#64368=CARTESIAN_POINT('Ctrl Pts',(-2.10204868021794,-1.10196460729585,
11.7275694528838));
#64369=CARTESIAN_POINT('Ctrl Pts',(-2.05974125457172,-1.1791518860656,11.7330046471257));
#64370=CARTESIAN_POINT('Ctrl Pts',(-2.00736387867571,-1.26325459984847,
11.7392607087811));
#64371=CARTESIAN_POINT('Ctrl Pts',(-2.00141406039578,-1.27266007997351,
11.7399651984782));
#64372=CARTESIAN_POINT('Ctrl Pts',(-1.97243146645444,-1.31776988584319,
11.7433684149852));
#64373=CARTESIAN_POINT('Ctrl Pts',(-1.94850931087567,-1.35289116354973,
11.7460924093145));
#64374=CARTESIAN_POINT('Ctrl Pts',(-1.90772646410503,-1.40943945436466,
11.7506171927791));
#64375=CARTESIAN_POINT('Ctrl Pts',(-1.89141633536604,-1.43125259324117,
11.7523980077808));
#64376=CARTESIAN_POINT('Ctrl Pts',(-1.86452043772451,-1.46596032342567,
11.7552922937405));
#64377=CARTESIAN_POINT('Ctrl Pts',(-1.85416765304805,-1.47903293516779,
11.7563967311374));
#64378=CARTESIAN_POINT('Ctrl Pts',(-1.83432186664118,-1.50355663748159,
11.758496552076));
#64379=CARTESIAN_POINT('Ctrl Pts',(-1.82485727614539,-1.51502976113639,
11.7594907769));
#64380=CARTESIAN_POINT('Ctrl Pts',(-1.8030753480022,-1.54093390567706,11.7617631753499));
#64381=CARTESIAN_POINT('Ctrl Pts',(-1.79069163034447,-1.55530751343312,
11.7630439916683));
#64382=CARTESIAN_POINT('Ctrl Pts',(-1.75780448053989,-1.59256569708522,
11.766417578738));
#64383=CARTESIAN_POINT('Ctrl Pts',(-1.7370270191405,-1.6152024872212,11.768521478921));
#64384=CARTESIAN_POINT('Ctrl Pts',(-1.60109620869237,-1.7576406707858,11.7821186431199));
#64385=CARTESIAN_POINT('Ctrl Pts',(-1.4740792983213,-1.86544415627209,11.7941254336972));
#64386=CARTESIAN_POINT('Ctrl Pts',(-1.2585822710186,-2.01249882590599,11.8131461888694));
#64387=CARTESIAN_POINT('Ctrl Pts',(-1.17715995538558,-2.06118340178794,
11.820062216178));
#64388=CARTESIAN_POINT('Ctrl Pts',(-1.06421613217573,-2.11983416497274,
11.8291416905219));
#64389=CARTESIAN_POINT('Ctrl Pts',(-1.03508714139557,-2.13420891289673,
11.8314394151011));
#64390=CARTESIAN_POINT('Ctrl Pts',(-0.98453981984614,-2.15787483358758,
11.8353413837852));
#64391=CARTESIAN_POINT('Ctrl Pts',(-0.963263117133661,-2.16745627914078,
11.8369584616639));
#64392=CARTESIAN_POINT('Ctrl Pts',(-0.931931147594175,-2.18101332951712,
11.8392993666904));
#64393=CARTESIAN_POINT('Ctrl Pts',(-0.921985322390353,-2.185236345108,11.8400365658365));
#64394=CARTESIAN_POINT('Ctrl Pts',(-0.905041581319549,-2.19229441354389,
11.8412820765689));
#64395=CARTESIAN_POINT('Ctrl Pts',(-0.89805853691285,-2.19516421475892,
11.8417923989916));
#64396=CARTESIAN_POINT('Ctrl Pts',(-0.882089699840957,-2.20163792392421,
11.8429525234988));
#64397=CARTESIAN_POINT('Ctrl Pts',(-0.873095413329371,-2.20522021441734,
11.8436010525805));
#64398=CARTESIAN_POINT('Ctrl Pts',(-0.848079395640629,-2.21500667603205,
11.8453919327832));
#64399=CARTESIAN_POINT('Ctrl Pts',(-0.832011440220698,-2.22109212799873,
11.8465276342917));
#64400=CARTESIAN_POINT('Ctrl Pts',(-0.71554194041701,-2.26376155528429,
11.8546646811357));
#64401=CARTESIAN_POINT('Ctrl Pts',(-0.612822725794605,-2.29370241073513,
11.8613361363706));
#64402=CARTESIAN_POINT('Ctrl Pts',(-0.370568688761269,-2.34686938907974,
11.8766448927312));
#64403=CARTESIAN_POINT('Ctrl Pts',(-0.230294523961769,-2.36475800737835,
11.885208242189));
#64404=CARTESIAN_POINT('Ctrl Pts',(-0.015215546199552,-2.37285849549867,
11.8987249824446));
#64405=CARTESIAN_POINT('Ctrl Pts',(0.0589161247387191,-2.37217541749953,
11.9034495321975));
#64406=CARTESIAN_POINT('Ctrl Pts',(0.156579348232306,-2.36669473265056,
11.9098264853198));
#64407=CARTESIAN_POINT('Ctrl Pts',(0.180247420646461,-2.3650099051179,11.9113836147958));
#64408=CARTESIAN_POINT('Ctrl Pts',(0.219523866893952,-2.36162099240057,
11.9139890114895));
#64409=CARTESIAN_POINT('Ctrl Pts',(0.235148071145408,-2.36011648116872,
11.9150310764083));
#64410=CARTESIAN_POINT('Ctrl Pts',(0.265742772822165,-2.35686359111583,
11.9170831978626));
#64411=CARTESIAN_POINT('Ctrl Pts',(0.280713831725573,-2.35512737134034,
11.9180928301899));
#64412=CARTESIAN_POINT('Ctrl Pts',(0.316802596939105,-2.35059310403269,
11.920540284206));
#64413=CARTESIAN_POINT('Ctrl Pts',(0.337900806670581,-2.34765304509489,
11.9219824474648));
#64414=CARTESIAN_POINT('Ctrl Pts',(0.40899151441259,-2.33676833445001,11.9268815948784));
#64415=CARTESIAN_POINT('Ctrl Pts',(0.458765455680081,-2.3275080882638,11.9303787147761));
#64416=CARTESIAN_POINT('Ctrl Pts',(0.676992314021041,-2.27963607908064,
11.9460171415026));
#64417=CARTESIAN_POINT('Ctrl Pts',(0.841210715220259,-2.22427683493749,
11.9586502487233));
#64418=CARTESIAN_POINT('Ctrl Pts',(1.06273544759074,-2.12153116639698,11.9764207887479));
#64419=CARTESIAN_POINT('Ctrl Pts',(1.12615304829603,-2.08855971127362,11.9815923084801));
#64420=CARTESIAN_POINT('Ctrl Pts',(1.21177794851088,-2.03900655370253,11.9886148829339));
#64421=CARTESIAN_POINT('Ctrl Pts',(1.23532703183532,-2.02482611202863,11.9905505137406));
#64422=CARTESIAN_POINT('Ctrl Pts',(1.27605961554106,-1.99932314258323,11.9938994389281));
#64423=CARTESIAN_POINT('Ctrl Pts',(1.29335191225893,-1.98818059350367,11.9953214467544));
#64424=CARTESIAN_POINT('Ctrl Pts',(1.31906440387144,-1.97113490173564,11.9974338090302));
#64425=CARTESIAN_POINT('Ctrl Pts',(1.32759424463532,-1.965400018779,11.9981342141073));
#64426=CARTESIAN_POINT('Ctrl Pts',(1.3429702619161,-1.95491645549979,11.9993957565948));
#64427=CARTESIAN_POINT('Ctrl Pts',(1.34982891669337,-1.95018700975994,11.9999580761221));
#64428=CARTESIAN_POINT('Ctrl Pts',(1.36528245175797,-1.93941030180508,12.0012242101416));
#64429=CARTESIAN_POINT('Ctrl Pts',(1.37386220627893,-1.93334196156205,12.001926612142));
#64430=CARTESIAN_POINT('Ctrl Pts',(1.40007744911805,-1.91453764493427,12.0040720357569));
#64431=CARTESIAN_POINT('Ctrl Pts',(1.41757884566627,-1.90161551183372,12.00550327878));
#64432=CARTESIAN_POINT('Ctrl Pts',(1.55251136731188,-1.79908996166132,12.0165510143658));
#64433=CARTESIAN_POINT('Ctrl Pts',(1.66153306121014,-1.69892197049655,12.0255691063844));
#64434=CARTESIAN_POINT('Ctrl Pts',(1.86331984497369,-1.47538678445643,12.0440630153602));
#64435=CARTESIAN_POINT('Ctrl Pts',(1.9548032712851,-1.35183713609888,12.053510569405));
#64436=CARTESIAN_POINT('Ctrl Pts',(2.04966696774308,-1.19374395171846,12.0654372298339));
#64437=CARTESIAN_POINT('Ctrl Pts',(2.06509583259137,-1.1668497590746,12.067459701207));
#64438=CARTESIAN_POINT('Ctrl Pts',(2.0882723392337,-1.12455040344599,12.0706351011929));
#64439=CARTESIAN_POINT('Ctrl Pts',(2.0963870229493,-1.10934953766589,12.0717751217301));
#64440=CARTESIAN_POINT('Ctrl Pts',(2.11116605487177,-1.08092332521409,12.0739056793087));
#64441=CARTESIAN_POINT('Ctrl Pts',(2.11787359498922,-1.0677212955679,12.0748946528817));
#64442=CARTESIAN_POINT('Ctrl Pts',(2.1325324233703,-1.03818758023562,12.0771063346396));
#64443=CARTESIAN_POINT('Ctrl Pts',(2.14042053630489,-1.02182576046515,12.0783311417036));
#64444=CARTESIAN_POINT('Ctrl Pts',(2.15997409230534,-0.980046955587586,
12.0814581563107));
#64445=CARTESIAN_POINT('Ctrl Pts',(2.17137907569643,-0.954511869872516,
12.0833689867123));
#64446=CARTESIAN_POINT('Ctrl Pts',(2.2590104290717,-0.748607270073845,12.0987794598873));
#64447=CARTESIAN_POINT('Ctrl Pts',(2.31306992452865,-0.559660126662052,
12.1130282552086));
#64448=CARTESIAN_POINT('Ctrl Pts',(2.35922076886864,-0.264398485667585,
12.1347973142268));
#64449=CARTESIAN_POINT('Ctrl Pts',(2.36848527963057,-0.161588031708222,
12.1422686867567));
#64450=CARTESIAN_POINT('Ctrl Pts',(2.37160053456625,-0.0353093846962169,
12.1510982735963));
#64451=CARTESIAN_POINT('Ctrl Pts',(2.37183243525361,-0.0121180069424332,
12.152705310845));
#64452=CARTESIAN_POINT('Ctrl Pts',(2.37167381896125,0.0218526859785101,
12.1550345313741));
#64453=CARTESIAN_POINT('Ctrl Pts',(2.37155001354541,0.0326310879798007,
12.1557699055898));
#64454=CARTESIAN_POINT('Ctrl Pts',(2.37121460813197,0.0509538592425347,
12.15701337888));
#64455=CARTESIAN_POINT('Ctrl Pts',(2.37104047617629,0.0584985450088929,
12.1575234711148));
#64456=CARTESIAN_POINT('Ctrl Pts',(2.37056026376969,0.0757374503522885,
12.1586845161773));
#64457=CARTESIAN_POINT('Ctrl Pts',(2.37023073098655,0.0854307655534443,
12.159334182723));
#64458=CARTESIAN_POINT('Ctrl Pts',(2.36914954893606,0.112367019877441,12.1611313414907));
#64459=CARTESIAN_POINT('Ctrl Pts',(2.3682691204173,0.129604582230312,12.1622721088702));
#64460=CARTESIAN_POINT('Ctrl Pts',(2.36007604591103,0.261692297545161,12.170952695441));
#64461=CARTESIAN_POINT('Ctrl Pts',(2.34460005619444,0.375898046438222,12.1781089334486));
#64462=CARTESIAN_POINT('Ctrl Pts',(2.30254473525346,0.575688206585353,12.1906879991891));
#64463=CARTESIAN_POINT('Ctrl Pts',(2.27930684793615,0.661732101267775,12.1961260056565));
#64464=CARTESIAN_POINT('Ctrl Pts',(2.22785364384537,0.816952889794791,12.2062427079913));
#64465=CARTESIAN_POINT('Ctrl Pts',(2.20110704587178,0.886493339973293,12.2108935938381));
#64466=CARTESIAN_POINT('Ctrl Pts',(2.1573101261585,0.986098775526492,12.2178244176621));
#64467=CARTESIAN_POINT('Ctrl Pts',(2.14280426729861,1.01723520966622,12.2200306646666));
#64468=CARTESIAN_POINT('Ctrl Pts',(2.11515070134807,1.07337452049931,12.2240900542522));
#64469=CARTESIAN_POINT('Ctrl Pts',(2.10222256874422,1.09847872671453,12.2259358564495));
#64470=CARTESIAN_POINT('Ctrl Pts',(2.08096397692257,1.13800887291864,12.228894567147));
#64471=CARTESIAN_POINT('Ctrl Pts',(2.07292416993712,1.15258866481411,12.2299973454221));
#64472=CARTESIAN_POINT('Ctrl Pts',(2.0574106250297,1.18003429389195,12.2320958539988));
#64473=CARTESIAN_POINT('Ctrl Pts',(2.04996799200713,1.19291685768597,12.2330904452065));
#64474=CARTESIAN_POINT('Ctrl Pts',(2.03273712719069,1.22210452857911,12.2353662700093));
#64475=CARTESIAN_POINT('Ctrl Pts',(2.02287310479298,1.23836346553517,12.2366501763271));
#64476=CARTESIAN_POINT('Ctrl Pts',(1.99648138951181,1.28070827863653,12.2400375542884));
#64477=CARTESIAN_POINT('Ctrl Pts',(1.97963834608529,1.30659232306072,12.2421523042127));
#64478=CARTESIAN_POINT('Ctrl Pts',(1.87116441259609,1.46637886098409,12.2554916578287));
#64479=CARTESIAN_POINT('Ctrl Pts',(1.76651416460043,1.59089093361851,12.2672030799314));
#64480=CARTESIAN_POINT('Ctrl Pts',(1.55245579894765,1.79819861378936,12.2889260311413));
#64481=CARTESIAN_POINT('Ctrl Pts',(1.4469695547581,1.88412397004255,12.2988518671792));
#64482=CARTESIAN_POINT('Ctrl Pts',(1.31800242342718,1.97192183331187,12.3097189272458));
#64483=CARTESIAN_POINT('Ctrl Pts',(1.30115925694379,1.98307608523859,12.3111148857916));
#64484=CARTESIAN_POINT('Ctrl Pts',(1.27559549682919,1.99953952877235,12.3131964809662));
#64485=CARTESIAN_POINT('Ctrl Pts',(1.26698026413232,2.00500953079047,12.3138917561725));
#64486=CARTESIAN_POINT('Ctrl Pts',(1.25126583485465,2.01484523499068,12.3151482856301));
#64487=CARTESIAN_POINT('Ctrl Pts',(1.24417873794932,2.01922925473189,12.3157106681003));
#64488=CARTESIAN_POINT('Ctrl Pts',(1.22803319238963,2.02909947580363,12.3169822113783));
#64489=CARTESIAN_POINT('Ctrl Pts',(1.21896095781306,2.03456245866863,12.3176899018509));
#64490=CARTESIAN_POINT('Ctrl Pts',(1.19077590306894,2.0512783128576,12.3198685536537));
#64491=CARTESIAN_POINT('Ctrl Pts',(1.17154098961669,2.06232435942036,12.3213272025687));
#64492=CARTESIAN_POINT('Ctrl Pts',(1.02695536630034,2.14267978077985,12.3321048848252));
#64493=CARTESIAN_POINT('Ctrl Pts',(0.895694664394937,2.20078528271987,12.340865085487));
#64494=CARTESIAN_POINT('Ctrl Pts',(0.606598915363746,2.29857621266965,12.3596062804192));
#64495=CARTESIAN_POINT('Ctrl Pts',(0.448330855646171,2.33461040037506,12.369566117304));
#64496=CARTESIAN_POINT('Ctrl Pts',(0.259459930672364,2.35768623107378,12.3819067149446));
#64497=CARTESIAN_POINT('Ctrl Pts',(0.231225076976445,2.36062251807222,12.3837620755276));
#64498=CARTESIAN_POINT('Ctrl Pts',(0.186325213078974,2.36447864042204,12.386732517611));
#64499=CARTESIAN_POINT('Ctrl Pts',(0.169690928763128,2.36573060408042,12.3878373260575));
#64500=CARTESIAN_POINT('Ctrl Pts',(0.13820407173097,2.3677666431033,12.389937442526));
#64501=CARTESIAN_POINT('Ctrl Pts',(0.123354571519996,2.36858668285574,12.3909315874561));
#64502=CARTESIAN_POINT('Ctrl Pts',(0.0895559997636695,2.37013446050989,
12.3932032293259));
#64503=CARTESIAN_POINT('Ctrl Pts',(0.0706041426167315,2.37077469557539,
12.3944833623162));
#64504=CARTESIAN_POINT('Ctrl Pts',(0.020963555476188,2.37185592288384,12.3978539019316));
#64505=CARTESIAN_POINT('Ctrl Pts',(-0.00972878240669629,2.37192858018127,
12.3999554052154));
#64506=CARTESIAN_POINT('Ctrl Pts',(-0.207294558031061,2.3685617305641,12.4136007322531));
#64507=CARTESIAN_POINT('Ctrl Pts',(-0.373382413760315,2.34811050327965,
12.4256632230052));
#64508=CARTESIAN_POINT('Ctrl Pts',(-0.627757951115977,2.28910601890843,
12.4447016328042));
#64509=CARTESIAN_POINT('Ctrl Pts',(-0.718250184669095,2.26234497776169,
12.4515802350739));
#64510=CARTESIAN_POINT('Ctrl Pts',(-0.837362368212341,2.21925006998316,
12.4606163829121));
#64511=CARTESIAN_POINT('Ctrl Pts',(-0.867584732140789,2.20761037118771,
12.4629070949889));
#64512=CARTESIAN_POINT('Ctrl Pts',(-0.919109598390386,2.18654466758929,
12.4667984708824));
#64513=CARTESIAN_POINT('Ctrl Pts',(-0.940528634475465,2.17741728312332,
12.4684118819509));
#64514=CARTESIAN_POINT('Ctrl Pts',(-0.971678581013751,2.16359777610425,
12.470748520895));
#64515=CARTESIAN_POINT('Ctrl Pts',(-0.981516637414081,2.15915254285377,
12.4714850545158));
#64516=CARTESIAN_POINT('Ctrl Pts',(-0.998181765352541,2.15148511638033,
12.4727298217306));
#64517=CARTESIAN_POINT('Ctrl Pts',(-1.00502425055415,2.14829730353386,12.4732400597154));
#64518=CARTESIAN_POINT('Ctrl Pts',(-1.0206133142889,2.14094380408955,12.4744005174537));
#64519=CARTESIAN_POINT('Ctrl Pts',(-1.02934972025902,2.13675713903471,12.4750494593805));
#64520=CARTESIAN_POINT('Ctrl Pts',(-1.05353360908341,2.12498497584489,12.4768426178083));
#64521=CARTESIAN_POINT('Ctrl Pts',(-1.06892491043338,2.11728453227802,12.4779801574411));
#64522=CARTESIAN_POINT('Ctrl Pts',(-1.18379779517616,2.05824034632913,12.4864526450614));
#64523=CARTESIAN_POINT('Ctrl Pts',(-1.27962930665314,2.00007147080152,12.4934248034534));
#64524=CARTESIAN_POINT('Ctrl Pts',(-1.48300257376349,1.85600118054244,12.5087903979374));
#64525=CARTESIAN_POINT('Ctrl Pts',(-1.58789939250964,1.76709115416447,12.5171298934038));
#64526=CARTESIAN_POINT('Ctrl Pts',(-1.73595384741521,1.61771479228139,12.5303450339128));
#64527=CARTESIAN_POINT('Ctrl Pts',(-1.78496020370499,1.56347446698995,12.5350058273635));
#64528=CARTESIAN_POINT('Ctrl Pts',(-1.8463905117887,1.48882437875424,12.5413092503845));
#64529=CARTESIAN_POINT('Ctrl Pts',(-1.86112525479835,1.47036344953181,12.5428594756417));
#64530=CARTESIAN_POINT('Ctrl Pts',(-1.88517523844693,1.43929082063817,12.5454564830382));
#64531=CARTESIAN_POINT('Ctrl Pts',(-1.89464575431619,1.4268010344555,12.54649714805));
#64532=CARTESIAN_POINT('Ctrl Pts',(-1.91298706008569,1.40210775621875,12.548548897046));
#64533=CARTESIAN_POINT('Ctrl Pts',(-1.92186659237952,1.38991166455625,12.5495595789913));
#64534=CARTESIAN_POINT('Ctrl Pts',(-1.94305009503871,1.3602248638427,12.5520137464494));
#64535=CARTESIAN_POINT('Ctrl Pts',(-1.95523484029815,1.34265111621546,12.5534616329772));
#64536=CARTESIAN_POINT('Ctrl Pts',(-1.99579951207146,1.28242236230203,12.5584087662337));
#64537=CARTESIAN_POINT('Ctrl Pts',(-2.02303267927108,1.23901610117099,12.5619492658185));
#64538=CARTESIAN_POINT('Ctrl Pts',(-2.15506681764593,1.0125979207379,12.580303066425));
#64539=CARTESIAN_POINT('Ctrl Pts',(-2.23651645768568,0.81708958512084,12.5958956052405));
#64540=CARTESIAN_POINT('Ctrl Pts',(-2.30298201998029,0.568860631470241,
12.6144171164765));
#64541=CARTESIAN_POINT('Ctrl Pts',(-2.3136172064994,0.523931794267859,12.6177158551158));
#64542=CARTESIAN_POINT('Ctrl Pts',(-2.32902205938667,0.449181281508012,
12.6230883587012));
#64543=CARTESIAN_POINT('Ctrl Pts',(-2.33454566095764,0.4195287115111,12.6251898078999));
#64544=CARTESIAN_POINT('Ctrl Pts',(-2.34146607873374,0.377991307388502,
12.6280849400354));
#64545=CARTESIAN_POINT('Ctrl Pts',(-2.34334065659209,0.366190399276157,
12.6289020099896));
#64546=CARTESIAN_POINT('Ctrl Pts',(-2.34639349027772,0.345987876029962,
12.6302909197348));
#64547=CARTESIAN_POINT('Ctrl Pts',(-2.34761598249118,0.337593290355653,
12.6308651259901));
#64548=CARTESIAN_POINT('Ctrl Pts',(-2.35009278510104,0.31992123849544,12.6320676145371));
#64549=CARTESIAN_POINT('Ctrl Pts',(-2.35133724216032,0.310642686289107,
12.6326953629443));
#64550=CARTESIAN_POINT('Ctrl Pts',(-2.35458085988286,0.285321548060174,
12.6343992542525));
#64551=CARTESIAN_POINT('Ctrl Pts',(-2.35647103066586,0.269265163371451,
12.6354696209421));
#64552=CARTESIAN_POINT('Ctrl Pts',(-2.36106678317317,0.226460620983871,
12.6382992727383));
#64553=CARTESIAN_POINT('Ctrl Pts',(-2.36348176316326,0.199686056432405,
12.6400445342361));
#64554=CARTESIAN_POINT('Ctrl Pts',(-2.3654410188404,0.172878133051282,12.6417724606485));
#64555=CARTESIAN_POINT('Origin',(0.,0.,-1.84858989190501));
#64556=CARTESIAN_POINT('',(-2.36544101497364,0.172878185958964,13.8381597463488));
#64557=CARTESIAN_POINT('',(-2.3654410187889,0.172878133755955,13.6380106975316));
#64558=CARTESIAN_POINT('',(-2.36544101854889,0.172878137039864,-1.84858989190501));
#64559=CARTESIAN_POINT('Ctrl Pts',(-2.36544101497364,0.172878185958964,
13.8381597463488));
#64560=CARTESIAN_POINT('Ctrl Pts',(-2.36276108291472,0.20954690257207,13.8358629187249));
#64561=CARTESIAN_POINT('Ctrl Pts',(-2.35922832534139,0.246155734497383,
13.8335498568797));
#64562=CARTESIAN_POINT('Ctrl Pts',(-2.34943075770665,0.327775080991724,
13.8283318218708));
#64563=CARTESIAN_POINT('Ctrl Pts',(-2.34272273041678,0.372707920858889,
13.8254173289339));
#64564=CARTESIAN_POINT('Ctrl Pts',(-2.3313675139366,0.436220587174823,13.8212225507192));
#64565=CARTESIAN_POINT('Ctrl Pts',(-2.32777900537393,0.454981047943001,
13.819974129542));
#64566=CARTESIAN_POINT('Ctrl Pts',(-2.32108537077806,0.487820207276247,
13.8177712569735));
#64567=CARTESIAN_POINT('Ctrl Pts',(-2.31807770452967,0.501917915292993,
13.8168198548091));
#64568=CARTESIAN_POINT('Ctrl Pts',(-2.31174678358148,0.530321171818991,
13.8148909845316));
#64569=CARTESIAN_POINT('Ctrl Pts',(-2.3084187938634,0.544625001659661,13.8139134058292));
#64570=CARTESIAN_POINT('Ctrl Pts',(-2.30124693043164,0.574202640406508,
13.8118786355917));
#64571=CARTESIAN_POINT('Ctrl Pts',(-2.29738333245326,0.58947087318232,13.8108208596796));
#64572=CARTESIAN_POINT('Ctrl Pts',(-2.28696353669542,0.628988747778604,
13.8080632497421));
#64573=CARTESIAN_POINT('Ctrl Pts',(-2.28017377773735,0.653174190257341,
13.8063560489414));
#64574=CARTESIAN_POINT('Ctrl Pts',(-2.24901281768177,0.75775783947841,13.7988859445409));
#64575=CARTESIAN_POINT('Ctrl Pts',(-2.22076635737281,0.836928612087447,
13.7930009567286));
#64576=CARTESIAN_POINT('Ctrl Pts',(-2.13519938762358,1.04170530817572,13.7771697356733));
#64577=CARTESIAN_POINT('Ctrl Pts',(-2.07101572650728,1.16409398572356,13.7670585861267));
#64578=CARTESIAN_POINT('Ctrl Pts',(-1.95689686009889,1.34207103573256,13.7516866178795));
#64579=CARTESIAN_POINT('Ctrl Pts',(-1.914367453418,1.40206946177415,13.7463788282227));
#64580=CARTESIAN_POINT('Ctrl Pts',(-1.84860173026452,1.48626391194827,13.7388351630916));
#64581=CARTESIAN_POINT('Ctrl Pts',(-1.82753352662377,1.51209465773799,13.7365070339046));
#64582=CARTESIAN_POINT('Ctrl Pts',(-1.79786161812875,1.54694746208743,13.7333560489755));
#64583=CARTESIAN_POINT('Ctrl Pts',(-1.78972197703129,1.55635732086554,13.7325043225996));
#64584=CARTESIAN_POINT('Ctrl Pts',(-1.7759429784471,1.57203551987203,13.7310841677081));
#64585=CARTESIAN_POINT('Ctrl Pts',(-1.77034363402645,1.57833854549753,13.7305129423225));
#64586=CARTESIAN_POINT('Ctrl Pts',(-1.75879600369852,1.59119862025627,13.7293471033848));
#64587=CARTESIAN_POINT('Ctrl Pts',(-1.7528444320212,1.59775243240796,13.7287527398659));
#64588=CARTESIAN_POINT('Ctrl Pts',(-1.73709755496473,1.61489884779452,13.7271966582382));
#64589=CARTESIAN_POINT('Ctrl Pts',(-1.72724187719481,1.62543585759475,13.7262393032648));
#64590=CARTESIAN_POINT('Ctrl Pts',(-1.68399671261342,1.67083306674584,13.7221063918393));
#64591=CARTESIAN_POINT('Ctrl Pts',(-1.64964116954359,1.70476180499079,13.7189959727027));
#64592=CARTESIAN_POINT('Ctrl Pts',(-1.50059241295543,1.84322995517101,13.7060830834404));
#64593=CARTESIAN_POINT('Ctrl Pts',(-1.37681631989302,1.93743606687906,13.6967229276606));
#64594=CARTESIAN_POINT('Ctrl Pts',(-1.17760731229289,2.06025595884288,13.6822713203688));
#64595=CARTESIAN_POINT('Ctrl Pts',(-1.10848145045337,2.09825668096637,13.6773590490224));
#64596=CARTESIAN_POINT('Ctrl Pts',(-0.990791265609828,2.15551382549267,
13.6690325845493));
#64597=CARTESIAN_POINT('Ctrl Pts',(-0.943253273120034,2.17673604777566,
13.6656792976149));
#64598=CARTESIAN_POINT('Ctrl Pts',(-0.875889899825235,2.20418769407958,
13.6609195960509));
#64599=CARTESIAN_POINT('Ctrl Pts',(-0.856620603374425,2.21174763588929,
13.659557257492));
#64600=CARTESIAN_POINT('Ctrl Pts',(-0.823354614845609,2.22429898570321,
13.6572026922286));
#64601=CARTESIAN_POINT('Ctrl Pts',(-0.809405214337752,2.22941292309398,
13.6562145629784));
#64602=CARTESIAN_POINT('Ctrl Pts',(-0.782612725164148,2.23895061995955,
13.6543147350375));
#64603=CARTESIAN_POINT('Ctrl Pts',(-0.769777837705112,2.24339577953811,
13.6534037838277));
#64604=CARTESIAN_POINT('Ctrl Pts',(-0.739464041401159,2.25360371442001,
13.6512499603246));
#64605=CARTESIAN_POINT('Ctrl Pts',(-0.721955046812446,2.25927369915118,
13.6500041280289));
#64606=CARTESIAN_POINT('Ctrl Pts',(-0.659890299322825,2.27857716095646,
13.6455806728019));
#64607=CARTESIAN_POINT('Ctrl Pts',(-0.615003115657367,2.29110011385842,
13.6423680046136));
#64608=CARTESIAN_POINT('Ctrl Pts',(-0.397796932936669,2.34485501004911,
13.6267491743822));
#64609=CARTESIAN_POINT('Ctrl Pts',(-0.221609048674075,2.36800726341303,
13.6138032128394));
#64610=CARTESIAN_POINT('Ctrl Pts',(0.0532131251998344,2.37316706764431,
13.5937911028067));
#64611=CARTESIAN_POINT('Ctrl Pts',(0.150978027962253,2.36895818706504,13.5867218428623));
#64612=CARTESIAN_POINT('Ctrl Pts',(0.27053684975708,2.35637683342352,13.5783250202505));
#64613=CARTESIAN_POINT('Ctrl Pts',(0.292827966065009,2.35371065359643,13.5767703803196));
#64614=CARTESIAN_POINT('Ctrl Pts',(0.32548576232331,2.34933338007757,13.5745119381951));
#64615=CARTESIAN_POINT('Ctrl Pts',(0.3358835532825,2.34786936631262,13.573795749026));
#64616=CARTESIAN_POINT('Ctrl Pts',(0.353564247253944,2.34526005546162,13.5725831923355));
#64617=CARTESIAN_POINT('Ctrl Pts',(0.360851966552392,2.34414979648057,13.5720849376955));
#64618=CARTESIAN_POINT('Ctrl Pts',(0.377499095017051,2.34153418775725,13.5709503762176));
#64619=CARTESIAN_POINT('Ctrl Pts',(0.386854783468157,2.34000668875643,13.5703153036658));
#64620=CARTESIAN_POINT('Ctrl Pts',(0.412817733444255,2.33560776131276,13.5685593766704));
#64621=CARTESIAN_POINT('Ctrl Pts',(0.429404301207037,2.33261528788169,13.5674449523658));
#64622=CARTESIAN_POINT('Ctrl Pts',(0.541072625177116,2.31123707450552,13.5599832545991));
#64623=CARTESIAN_POINT('Ctrl Pts',(0.634994675150038,2.28721724239256,13.5539072192625));
#64624=CARTESIAN_POINT('Ctrl Pts',(0.752763202386717,2.24928148800337,13.5462497207829));
#64625=CARTESIAN_POINT('Ctrl Pts',(0.778190347992261,2.24061140479784,13.5445941767885));
#64626=CARTESIAN_POINT('Ctrl Pts',(0.89746754378451,2.19766514761424,13.5367961068051));
#64627=CARTESIAN_POINT('Ctrl Pts',(0.989235361902849,2.157914024441,13.5306975304384));
#64628=CARTESIAN_POINT('Ctrl Pts',(1.16364308231315,2.06889596386664,13.5185189138606));
#64629=CARTESIAN_POINT('Ctrl Pts',(1.2463322226425,2.02016052602677,13.5124593168942));
#64630=CARTESIAN_POINT('Ctrl Pts',(1.34678813917956,1.95243390240448,13.5045765917239));
#64631=CARTESIAN_POINT('Ctrl Pts',(1.36750999009039,1.93797646603168,13.5029211090723));
#64632=CARTESIAN_POINT('Ctrl Pts',(1.40079162581702,1.91395660384901,13.5002115505319));
#64633=CARTESIAN_POINT('Ctrl Pts',(1.41349420843968,1.90459475031936,13.4991650951147));
#64634=CARTESIAN_POINT('Ctrl Pts',(1.43782598667334,1.88628464889105,13.4971361580608));
#64635=CARTESIAN_POINT('Ctrl Pts',(1.44946744639308,1.87735384249763,13.4961543819207));
#64636=CARTESIAN_POINT('Ctrl Pts',(1.47618735296003,1.85645884487857,13.4938748396358));
#64637=CARTESIAN_POINT('Ctrl Pts',(1.4912043355533,1.84441810222092,13.4925741035197));
#64638=CARTESIAN_POINT('Ctrl Pts',(1.54018547728282,1.80415540479429,13.4882651976858));
#64639=CARTESIAN_POINT('Ctrl Pts',(1.57350635300837,1.77516910179508,13.4852267765631));
#64640=CARTESIAN_POINT('Ctrl Pts',(1.75296568613457,1.61003079356689,13.4682467245569));
#64641=CARTESIAN_POINT('Ctrl Pts',(1.88224455140966,1.45678315504625,13.4535789826234));
#64642=CARTESIAN_POINT('Ctrl Pts',(2.02392927071146,1.23799410808772,13.434661184738));
#64643=CARTESIAN_POINT('Ctrl Pts',(2.05510129259139,1.18552887387326,13.4302654724022));
#64644=CARTESIAN_POINT('Ctrl Pts',(2.09603637601082,1.11015443708886,13.4241955516293));
#64645=CARTESIAN_POINT('Ctrl Pts',(2.10751435959628,1.0882070998676,13.4224563385966));
#64646=CARTESIAN_POINT('Ctrl Pts',(2.12714916505769,1.04918648279608,13.4194184320745));
#64647=CARTESIAN_POINT('Ctrl Pts',(2.13544928551196,1.03218808885265,13.418112850886));
#64648=CARTESIAN_POINT('Ctrl Pts',(2.14774445456061,1.00622466370559,13.4161475635831));
#64649=CARTESIAN_POINT('Ctrl Pts',(2.15188847690972,0.997331593542218,13.4154794912224));
#64650=CARTESIAN_POINT('Ctrl Pts',(2.1593744176129,0.981002872365718,13.4142624524404));
#64651=CARTESIAN_POINT('Ctrl Pts',(2.16273325517824,0.973575565507571,13.4137125208669));
#64652=CARTESIAN_POINT('Ctrl Pts',(2.17033582878251,0.956530683535731,13.4124587149267));
#64653=CARTESIAN_POINT('Ctrl Pts',(2.17455399201601,0.946902056394619,13.4117563620212));
#64654=CARTESIAN_POINT('Ctrl Pts',(2.18760335821565,0.916567677119023,13.4095612122662));
#64655=CARTESIAN_POINT('Ctrl Pts',(2.19620418741125,0.895763370741718,13.4080812754844));
#64656=CARTESIAN_POINT('Ctrl Pts',(2.25334194099725,0.751781850841294,13.3979929702021));
#64657=CARTESIAN_POINT('Ctrl Pts',(2.29179304771167,0.624835519677969,13.389859547353));
#64658=CARTESIAN_POINT('Ctrl Pts',(2.33254490601527,0.434009183669126,13.3778774738183));
#64659=CARTESIAN_POINT('Ctrl Pts',(2.34320310696718,0.372194480841895,13.3740339847284));
#64660=CARTESIAN_POINT('Ctrl Pts',(2.36127416211096,0.235136382124309,13.3654859635678));
#64661=CARTESIAN_POINT('Ctrl Pts',(2.36756454390981,0.159817576288654,13.3607706665713));
#64662=CARTESIAN_POINT('Ctrl Pts',(2.3714762831625,0.0498719840989109,13.3537644492922));
#64663=CARTESIAN_POINT('Ctrl Pts',(2.37195065036051,0.0153918972247291,
13.3515499613032));
#64664=CARTESIAN_POINT('Ctrl Pts',(2.3714462627868,-0.0472877138775438,
13.347484410659));
#64665=CARTESIAN_POINT('Ctrl Pts',(2.3707162842125,-0.0754830842777611,
13.3456409061781));
#64666=CARTESIAN_POINT('Ctrl Pts',(2.36876669650036,-0.120048147461304,
13.3427006328884));
#64667=CARTESIAN_POINT('Ctrl Pts',(2.36787963828969,-0.136430261247075,
13.3416141312154));
#64668=CARTESIAN_POINT('Ctrl Pts',(2.36588745321069,-0.167288259135244,
13.3395562715876));
#64669=CARTESIAN_POINT('Ctrl Pts',(2.3648192258425,-0.181765827482735,13.3385861016556));
#64670=CARTESIAN_POINT('Ctrl Pts',(2.36209994905798,-0.214519500125747,
13.3363801655352));
#64671=CARTESIAN_POINT('Ctrl Pts',(2.36036957833212,-0.232787900038322,
13.3351419952159));
#64672=CARTESIAN_POINT('Ctrl Pts',(2.35532272406598,-0.280202361761902,
13.3319073193338));
#64673=CARTESIAN_POINT('Ctrl Pts',(2.35167727542628,-0.309309485877959,
13.3299008031946));
#64674=CARTESIAN_POINT('Ctrl Pts',(2.32145481303518,-0.519000715961252,
13.3152897984617));
#64675=CARTESIAN_POINT('Ctrl Pts',(2.27465286048027,-0.696020697804163,
13.3020472537032));
#64676=CARTESIAN_POINT('Ctrl Pts',(2.16362472731613,-0.979145516434845,
13.2798725412824));
#64677=CARTESIAN_POINT('Ctrl Pts',(2.1105575749877,-1.08883001911628,13.27102629108));
#64678=CARTESIAN_POINT('Ctrl Pts',(2.04002817664888,-1.20988532455299,13.2612891067581));
#64679=CARTESIAN_POINT('Ctrl Pts',(2.03056843600912,-1.22569545093014,13.2600181648935));
#64680=CARTESIAN_POINT('Ctrl Pts',(2.01584283715474,-1.24966795606068,13.2580940681641));
#64681=CARTESIAN_POINT('Ctrl Pts',(2.01070972275329,-1.25791047522443,13.257433052148));
#64682=CARTESIAN_POINT('Ctrl Pts',(2.0011693805951,-1.27302229954661,13.2562224938037));
#64683=CARTESIAN_POINT('Ctrl Pts',(1.9967772539878,-1.27990049078457,13.2556720606271));
#64684=CARTESIAN_POINT('Ctrl Pts',(1.98667020532569,-1.29554974371605,13.2544208513494));
#64685=CARTESIAN_POINT('Ctrl Pts',(1.98093262397,-1.30430578955758,13.2537215594881));
#64686=CARTESIAN_POINT('Ctrl Pts',(1.96247041277676,-1.33207786782794,13.2515051008533));
#64687=CARTESIAN_POINT('Ctrl Pts',(1.94952807285545,-1.35094853857973,13.2500013527538));
#64688=CARTESIAN_POINT('Ctrl Pts',(1.86762807893217,-1.46673465403492,13.2407692874927));
#64689=CARTESIAN_POINT('Ctrl Pts',(1.79172595625999,-1.55854744537032,13.2334198121188));
#64690=CARTESIAN_POINT('Ctrl Pts',(1.62167193288928,-1.73531974947297,13.2183409291342));
#64691=CARTESIAN_POINT('Ctrl Pts',(1.52696977510027,-1.8192074619561,13.2106354271467));
#64692=CARTESIAN_POINT('Ctrl Pts',(1.37033005973527,-1.9370737213977,13.1982958981603));
#64693=CARTESIAN_POINT('Ctrl Pts',(1.31280257796597,-1.97651386864463,13.1938414955082));
#64694=CARTESIAN_POINT('Ctrl Pts',(1.23414662316862,-2.02548925008237,13.1877964634833));
#64695=CARTESIAN_POINT('Ctrl Pts',(1.21449337606589,-2.03733413295289,13.1862897686535));
#64696=CARTESIAN_POINT('Ctrl Pts',(1.18146061079586,-2.05659494466532,13.1837618046922));
#64697=CARTESIAN_POINT('Ctrl Pts',(1.16817538238523,-2.06417009930813,13.1827462821234));
#64698=CARTESIAN_POINT('Ctrl Pts',(1.14192640862472,-2.07880253508793,13.1807416280576));
#64699=CARTESIAN_POINT('Ctrl Pts',(1.12896819037678,-2.08586833498525,13.1797528558857));
#64700=CARTESIAN_POINT('Ctrl Pts',(1.09743504360342,-2.10268267428213,13.1773483400488));
#64701=CARTESIAN_POINT('Ctrl Pts',(1.07879537409456,-2.11230646351584,13.1759283278761));
#64702=CARTESIAN_POINT('Ctrl Pts',(1.01493590948249,-2.14421182400213,13.1710664772113));
#64703=CARTESIAN_POINT('Ctrl Pts',(0.969137145392655,-2.16529715804273,
13.1675845334342));
#64704=CARTESIAN_POINT('Ctrl Pts',(0.76289046654408,-2.25239686541711,13.1519167606892));
#64705=CARTESIAN_POINT('Ctrl Pts',(0.596172939465782,-2.30214132199112,
13.1392320196889));
#64706=CARTESIAN_POINT('Ctrl Pts',(0.330618992596286,-2.35057478795073,
13.119583194056));
#64707=CARTESIAN_POINT('Ctrl Pts',(0.23470488584106,-2.36208127946849,13.1126077479123));
#64708=CARTESIAN_POINT('Ctrl Pts',(0.116068011500286,-2.36901337800748,
13.1043085360878));
#64709=CARTESIAN_POINT('Ctrl Pts',(0.0937694494648238,-2.37000074846898,
13.1027630484942));
#64710=CARTESIAN_POINT('Ctrl Pts',(0.0609880869604961,-2.37098887845012,
13.1005152755374));
#64711=CARTESIAN_POINT('Ctrl Pts',(0.0505146464855438,-2.37123514003166,
13.0998007634007));
#64712=CARTESIAN_POINT('Ctrl Pts',(0.0326715872010758,-2.37153640791543,
13.0985900646363));
#64713=CARTESIAN_POINT('Ctrl Pts',(0.0253029142285122,-2.37162647450572,
13.0980920069092));
#64714=CARTESIAN_POINT('Ctrl Pts',(0.00843780228341203,-2.37175400110903,
13.0969565352849));
#64715=CARTESIAN_POINT('Ctrl Pts',(-0.00105856972606136,-2.37176877572306,
13.096320368005));
#64716=CARTESIAN_POINT('Ctrl Pts',(-0.0274829177625788,-2.37165117851174,
13.0945584306821));
#64717=CARTESIAN_POINT('Ctrl Pts',(-0.0444101559562398,-2.37139461103667,
13.0934391614116));
#64718=CARTESIAN_POINT('Ctrl Pts',(-0.163171860820531,-2.36832238964647,
13.0856433428351));
#64719=CARTESIAN_POINT('Ctrl Pts',(-0.264747740045853,-2.35912903464265,
13.0792675432846));
#64720=CARTESIAN_POINT('Ctrl Pts',(-0.398032333988223,-2.33834496628121,
13.070931468768));
#64721=CARTESIAN_POINT('Ctrl Pts',(-0.430526881505042,-2.33258088271208,
13.0689017925701));
#64722=CARTESIAN_POINT('Ctrl Pts',(-0.58201546543949,-2.30243537538697,
13.0594131921702));
#64723=CARTESIAN_POINT('Ctrl Pts',(-0.699136499344073,-2.26961597894804,
13.0519901050512));
#64724=CARTESIAN_POINT('Ctrl Pts',(-0.877315031907168,-2.20457957383278,
13.0400408777054));
#64725=CARTESIAN_POINT('Ctrl Pts',(-0.940360124192913,-2.17843390654501,
13.0356791065165));
#64726=CARTESIAN_POINT('Ctrl Pts',(-1.02283359773433,-2.13998328209318,
13.0297412162558));
#64727=CARTESIAN_POINT('Ctrl Pts',(-1.04334013740576,-2.13006063654149,
13.0282451537603));
#64728=CARTESIAN_POINT('Ctrl Pts',(-1.07733857292259,-2.11300082989485,
13.0257300896777));
#64729=CARTESIAN_POINT('Ctrl Pts',(-1.0909105056597,-2.10602591584364,13.0247167078207));
#64730=CARTESIAN_POINT('Ctrl Pts',(-1.11749704804048,-2.09203656014731,
13.0227124988813));
#64731=CARTESIAN_POINT('Ctrl Pts',(-1.13051525674968,-2.08503042153271,
13.0217219969079));
#64732=CARTESIAN_POINT('Ctrl Pts',(-1.16196239482079,-2.06772511057704,
13.0193065737755));
#64733=CARTESIAN_POINT('Ctrl Pts',(-1.18032066910222,-2.05730085509232,
13.0178772890568));
#64734=CARTESIAN_POINT('Ctrl Pts',(-1.24273495558209,-2.02075018165785,
13.0129503254845));
#64735=CARTESIAN_POINT('Ctrl Pts',(-1.28607988100212,-1.99344408435901,
13.0094110898422));
#64736=CARTESIAN_POINT('Ctrl Pts',(-1.47154385160806,-1.86803949707763,
12.9937346775241));
#64737=CARTESIAN_POINT('Ctrl Pts',(-1.60357683029832,-1.7560005506902,12.9811074481034));
#64738=CARTESIAN_POINT('Ctrl Pts',(-1.78841747518489,-1.56077551703415,
12.9615386626739));
#64739=CARTESIAN_POINT('Ctrl Pts',(-1.85026800854569,-1.48693280262806,
12.9545840306608));
#64740=CARTESIAN_POINT('Ctrl Pts',(-1.92071197005659,-1.3916035373627,12.9463064964809));
#64741=CARTESIAN_POINT('Ctrl Pts',(-1.93370575283272,-1.37349081801791,
12.944763053749));
#64742=CARTESIAN_POINT('Ctrl Pts',(-1.95242561740281,-1.34660384084437,
12.9425176661053));
#64743=CARTESIAN_POINT('Ctrl Pts',(-1.95835158985206,-1.33797113441267,
12.9418035300652));
#64744=CARTESIAN_POINT('Ctrl Pts',(-1.9683502080345,-1.32319681708584,12.9405932477136));
#64745=CARTESIAN_POINT('Ctrl Pts',(-1.97245164549792,-1.31707511924756,
12.9400952338928));
#64746=CARTESIAN_POINT('Ctrl Pts',(-1.98177552176051,-1.30301730292257,
12.9389595563739));
#64747=CARTESIAN_POINT('Ctrl Pts',(-1.9869788820073,-1.29506881694029,12.9383231420749));
#64748=CARTESIAN_POINT('Ctrl Pts',(-2.00133008231086,-1.27285627518941,
12.9365598476668));
#64749=CARTESIAN_POINT('Ctrl Pts',(-2.01037323685284,-1.25852480476586,
12.9354394843266));
#64750=CARTESIAN_POINT('Ctrl Pts',(-2.07460506315104,-1.15427176704404,
12.9274043463363));
#64751=CARTESIAN_POINT('Ctrl Pts',(-2.12389974386801,-1.06084164991093,
12.920812726887));
#64752=CARTESIAN_POINT('Ctrl Pts',(-2.17330310257412,-0.949845497337405,
12.913312109175));
#64753=CARTESIAN_POINT('Ctrl Pts',(-2.17964637370493,-0.935197592217239,
12.9123287025405));
#64754=CARTESIAN_POINT('Ctrl Pts',(-2.22325952109642,-0.83163127010402,
12.9054140620019));
#64755=CARTESIAN_POINT('Ctrl Pts',(-2.25522424853189,-0.740578601250993,
12.8995290600494));
#64756=CARTESIAN_POINT('Ctrl Pts',(-2.30909958737916,-0.550839106575901,
12.8872837562639));
#64757=CARTESIAN_POINT('Ctrl Pts',(-2.33042460006533,-0.452197111838367,
12.8809257199156));
#64758=CARTESIAN_POINT('Ctrl Pts',(-2.34921242200156,-0.327191553254358,
12.8727040766289));
#64759=CARTESIAN_POINT('Ctrl Pts',(-2.35260677218798,-0.30181883540353,
12.8710273276736));
#64760=CARTESIAN_POINT('Ctrl Pts',(-2.35743687358524,-0.26065435011963,
12.8682916945888));
#64761=CARTESIAN_POINT('Ctrl Pts',(-2.35912615581418,-0.244893984667378,
12.8672407140727));
#64762=CARTESIAN_POINT('Ctrl Pts',(-2.36207231405805,-0.214539039336571,
12.8652090077865));
#64763=CARTESIAN_POINT('Ctrl Pts',(-2.36335220466617,-0.199947384392037,
12.8642290455479));
#64764=CARTESIAN_POINT('Ctrl Pts',(-2.3659882613244,-0.166318504377655,
12.8619624894185));
#64765=CARTESIAN_POINT('Ctrl Pts',(-2.36724994513088,-0.147275110785489,
12.8606730324435));
#64766=CARTESIAN_POINT('Ctrl Pts',(-2.37061613006155,-0.0850996774214071,
12.8564425883442));
#64767=CARTESIAN_POINT('Ctrl Pts',(-2.37177243490227,-0.04192720419408,
12.8534728544509));
#64768=CARTESIAN_POINT('Ctrl Pts',(-2.37171944942813,0.0585716059263682,
12.846480727164));
#64769=CARTESIAN_POINT('Ctrl Pts',(-2.36961122643535,0.115818548722168,
12.8424376605832));
#64770=CARTESIAN_POINT('Ctrl Pts',(-2.36544098610933,0.17287858090038,12.8383513775307));
#64771=CARTESIAN_POINT('Ctrl Pts',(-2.3654410188404,0.172878133051282,12.6417724606485));
#64772=CARTESIAN_POINT('Ctrl Pts',(-2.36840946129808,0.132261801607106,
12.6443904191857));
#64773=CARTESIAN_POINT('Ctrl Pts',(-2.37033179351654,0.0915688979090119,
12.6469686252575));
#64774=CARTESIAN_POINT('Ctrl Pts',(-2.37155557740686,0.0344908708101321,
12.6505468214597));
#64775=CARTESIAN_POINT('Ctrl Pts',(-2.3717370196609,0.0181383935128824,
12.6515675627952));
#64776=CARTESIAN_POINT('Ctrl Pts',(-2.37187300748867,-0.162536444707336,
12.6628090630617));
#64777=CARTESIAN_POINT('Ctrl Pts',(-2.35492008404575,-0.326423957580101,
12.6727066142147));
#64778=CARTESIAN_POINT('Ctrl Pts',(-2.30585543483136,-0.560160392558652,
12.6876935499561));
#64779=CARTESIAN_POINT('Ctrl Pts',(-2.28712362018204,-0.632307563801859,
12.6924394762415));
#64780=CARTESIAN_POINT('Ctrl Pts',(-2.25778087046183,-0.726788042997782,
12.6988836597969));
#64781=CARTESIAN_POINT('Ctrl Pts',(-2.25017236855946,-0.750013038853927,
12.7004864050573));
#64782=CARTESIAN_POINT('Ctrl Pts',(-2.23704191239831,-0.788094269532373,
12.7031473477744));
#64783=CARTESIAN_POINT('Ctrl Pts',(-2.23172740660467,-0.803020459096754,
12.7041987703312));
#64784=CARTESIAN_POINT('Ctrl Pts',(-2.22103815400418,-0.832116106440198,
12.7062654487943));
#64785=CARTESIAN_POINT('Ctrl Pts',(-2.21567635457738,-0.84628953068378,
12.7072802373006));
#64786=CARTESIAN_POINT('Ctrl Pts',(-2.20259291891659,-0.879897608825033,
12.7097062041929));
#64787=CARTESIAN_POINT('Ctrl Pts',(-2.19474944749005,-0.899283149570606,
12.7111213568444));
#64788=CARTESIAN_POINT('Ctrl Pts',(-2.16666264788104,-0.96614421099116,
12.7160588191024));
#64789=CARTESIAN_POINT('Ctrl Pts',(-2.14512808256747,-1.01305798049471,
12.7196235633563));
#64790=CARTESIAN_POINT('Ctrl Pts',(-2.08749767102967,-1.12851596004621,
12.7286562824752));
#64791=CARTESIAN_POINT('Ctrl Pts',(-2.04954386228103,-1.19606138550838,
12.7341795082623));
#64792=CARTESIAN_POINT('Ctrl Pts',(-1.96183689698446,-1.33568055303906,
12.746082098946));
#64793=CARTESIAN_POINT('Ctrl Pts',(-1.91125660761959,-1.40710476898585,
12.752471505137));
#64794=CARTESIAN_POINT('Ctrl Pts',(-1.78721622481081,-1.56319655725212,
12.7669940221214));
#64795=CARTESIAN_POINT('Ctrl Pts',(-1.7114592033492,-1.6457940881261,12.7750993442954));
#64796=CARTESIAN_POINT('Ctrl Pts',(-1.61764470502298,-1.73456616440675,
12.7840622917513));
#64797=CARTESIAN_POINT('Ctrl Pts',(-1.60501689916595,-1.74625741692137,
12.7852480878166));
#64798=CARTESIAN_POINT('Ctrl Pts',(-1.58508290657565,-1.76431405467799,
12.7870864745226));
#64799=CARTESIAN_POINT('Ctrl Pts',(-1.57786335410403,-1.77077360165624,
12.7877455660819));
#64800=CARTESIAN_POINT('Ctrl Pts',(-1.56494787997788,-1.78218775075735,
12.7889124398645));
#64801=CARTESIAN_POINT('Ctrl Pts',(-1.5592677939541,-1.78715947665374,12.7894214436933));
#64802=CARTESIAN_POINT('Ctrl Pts',(-1.5454064951305,-1.79917574901716,12.7906536217159));
#64803=CARTESIAN_POINT('Ctrl Pts',(-1.53720078707583,-1.80619167377828,
12.791374739274));
#64804=CARTESIAN_POINT('Ctrl Pts',(-1.51114815912431,-1.82816065673567,
12.7936392074242));
#64805=CARTESIAN_POINT('Ctrl Pts',(-1.4931281998876,-1.84290760012197,12.7951688117805));
#64806=CARTESIAN_POINT('Ctrl Pts',(-1.44953110248083,-1.87752668962281,
12.7987909185952));
#64807=CARTESIAN_POINT('Ctrl Pts',(-1.42375790559918,-1.8971453610175,12.8008693700763));
#64808=CARTESIAN_POINT('Ctrl Pts',(-1.32140260834384,-1.97179748699354,
12.8089167159968));
#64809=CARTESIAN_POINT('Ctrl Pts',(-1.2419639118952,-2.0227748982854,12.8147228981608));
#64810=CARTESIAN_POINT('Ctrl Pts',(-1.01414552366624,-2.15047627957305,
12.8307687889671));
#64811=CARTESIAN_POINT('Ctrl Pts',(-0.860408968650429,-2.21646756000236,
12.8409696508369));
#64812=CARTESIAN_POINT('Ctrl Pts',(-0.671706066392747,-2.27485188619683,
12.8537113053155));
#64813=CARTESIAN_POINT('Ctrl Pts',(-0.64221188979384,-2.28335365108502,
12.8557074631192));
#64814=CARTESIAN_POINT('Ctrl Pts',(-0.594242234073739,-2.29617809277502,
12.8589660890472));
#64815=CARTESIAN_POINT('Ctrl Pts',(-0.575864770778239,-2.30085579685789,
12.8602173040168));
#64816=CARTESIAN_POINT('Ctrl Pts',(-0.542978031122819,-2.30880793966486,
12.8624623379565));
#64817=CARTESIAN_POINT('Ctrl Pts',(-0.528490169099001,-2.31216724496456,
12.8634534098897));
#64818=CARTESIAN_POINT('Ctrl Pts',(-0.497687503886618,-2.31900484282395,
12.8655653233746));
#64819=CARTESIAN_POINT('Ctrl Pts',(-0.481365746859044,-2.32244769714399,
12.8666872247679));
#64820=CARTESIAN_POINT('Ctrl Pts',(-0.437176345450544,-2.33128302714323,
12.8697329647625));
#64821=CARTESIAN_POINT('Ctrl Pts',(-0.409246743096404,-2.33634772517161,
12.8716669225954));
#64822=CARTESIAN_POINT('Ctrl Pts',(-0.223276815545454,-2.36663426442617,
12.8846085288236));
#64823=CARTESIAN_POINT('Ctrl Pts',(-0.0631498173451738,-2.3763007143207,
12.8961006065482));
#64824=CARTESIAN_POINT('Ctrl Pts',(0.242130365687578,-2.36384343476796,
12.9183545657598));
#64825=CARTESIAN_POINT('Ctrl Pts',(0.386715371032393,-2.34453423882222,
12.9290318715257));
#64826=CARTESIAN_POINT('Ctrl Pts',(0.549985073679765,-2.30720491429947,
12.9407217903089));
#64827=CARTESIAN_POINT('Ctrl Pts',(0.571275899405755,-2.30202563599738,
12.9422383520892));
#64828=CARTESIAN_POINT('Ctrl Pts',(0.602697180513232,-2.29391918585775,
12.9444619006601));
#64829=CARTESIAN_POINT('Ctrl Pts',(0.612884140030201,-2.29121848894177,
12.9451804961823));
#64830=CARTESIAN_POINT('Ctrl Pts',(0.6310922926893,-2.28626114029126,12.946460391651));
#64831=CARTESIAN_POINT('Ctrl Pts',(0.639119942504405,-2.28403003234786,
12.9470230626226));
#64832=CARTESIAN_POINT('Ctrl Pts',(0.656997706323036,-2.27895966413714,
12.9482725576811));
#64833=CARTESIAN_POINT('Ctrl Pts',(0.666841329599441,-2.27609880885453,
12.9489581551867));
#64834=CARTESIAN_POINT('Ctrl Pts',(0.696247748937998,-2.26734526328648,
12.9509999940704));
#64835=CARTESIAN_POINT('Ctrl Pts',(0.715753843541684,-2.26126335801083,
12.9523460453813));
#64836=CARTESIAN_POINT('Ctrl Pts',(0.865863382007861,-2.21232281913067,
12.9626573447264));
#64837=CARTESIAN_POINT('Ctrl Pts',(0.992614154654155,-2.15842973952103,
12.9710955722125));
#64838=CARTESIAN_POINT('Ctrl Pts',(1.25530444528176,-2.01867018343394,12.9893705191329));
#64839=CARTESIAN_POINT('Ctrl Pts',(1.38862444655848,-1.92938683600411,12.9991802526417));
#64840=CARTESIAN_POINT('Ctrl Pts',(1.53577984665586,-1.80763281003834,13.0114972490739));
#64841=CARTESIAN_POINT('Ctrl Pts',(1.55923830393702,-1.78743723948182,13.0135098550013));
#64842=CARTESIAN_POINT('Ctrl Pts',(1.59647583808682,-1.75408819568557,13.0167899692906));
#64843=CARTESIAN_POINT('Ctrl Pts',(1.61050387876314,-1.74121731027292,13.0180459741507));
#64844=CARTESIAN_POINT('Ctrl Pts',(1.63521757458232,-1.71798805738148,13.0202963009484));
#64845=CARTESIAN_POINT('Ctrl Pts',(1.64596366008834,-1.70769525798722,13.0212878253483));
#64846=CARTESIAN_POINT('Ctrl Pts',(1.66851829685136,-1.68568133432917,13.0233972083325));
#64847=CARTESIAN_POINT('Ctrl Pts',(1.68030173998804,-1.67393575332826,13.0245160940969));
#64848=CARTESIAN_POINT('Ctrl Pts',(1.71170811942719,-1.64196451739063,13.0275448010512));
#64849=CARTESIAN_POINT('Ctrl Pts',(1.73109524371255,-1.62151204195831,13.0294645479227));
#64850=CARTESIAN_POINT('Ctrl Pts',(1.86015380971549,-1.48040862044347,13.0425959401033));
#64851=CARTESIAN_POINT('Ctrl Pts',(1.95747589028711,-1.34909294981243,13.0543126512743));
#64852=CARTESIAN_POINT('Ctrl Pts',(2.11309377871672,-1.08641146176599,13.0765560869538));
#64853=CARTESIAN_POINT('Ctrl Pts',(2.17447308091316,-0.957668263108391,
13.0869887401408));
#64854=CARTESIAN_POINT('Ctrl Pts',(2.23168820749158,-0.803282596906085,
13.0984858734064));
#64855=CARTESIAN_POINT('Ctrl Pts',(2.23914137381111,-0.782266695243478,
13.1000297351353));
#64856=CARTESIAN_POINT('Ctrl Pts',(2.24970297438995,-0.751097331600258,
13.1022852408903));
#64857=CARTESIAN_POINT('Ctrl Pts',(2.25304115524079,-0.741023776973954,
13.1030089617295));
#64858=CARTESIAN_POINT('Ctrl Pts',(2.25888014592064,-0.722999314383953,
13.1042941687939));
#64859=CARTESIAN_POINT('Ctrl Pts',(2.26140678265523,-0.715057264809579,
13.1048570787688));
#64860=CARTESIAN_POINT('Ctrl Pts',(2.26692819258393,-0.697379645861272,
13.106102506855));
#64861=CARTESIAN_POINT('Ctrl Pts',(2.26990216980819,-0.687637949632474,
13.1067838461194));
#64862=CARTESIAN_POINT('Ctrl Pts',(2.2785589414793,-0.658613183684788,13.108799896842));
#64863=CARTESIAN_POINT('Ctrl Pts',(2.28405959854197,-0.639276145941719,
13.110124796041));
#64864=CARTESIAN_POINT('Ctrl Pts',(2.29628436772607,-0.594127483823742,
13.1131809513696));
#64865=CARTESIAN_POINT('Ctrl Pts',(2.30282038132163,-0.56826734930511,13.1149033706462));
#64866=CARTESIAN_POINT('Ctrl Pts',(2.32447708730503,-0.476061087632978,
13.1209632938333));
#64867=CARTESIAN_POINT('Ctrl Pts',(2.33717844807057,-0.409177286231348,
13.1252107660865));
#64868=CARTESIAN_POINT('Ctrl Pts',(2.37013013059669,-0.182936568363289,
13.1393510471256));
#64869=CARTESIAN_POINT('Ctrl Pts',(2.3770765442375,-0.0221045916504001,
13.1490583632207));
#64870=CARTESIAN_POINT('Ctrl Pts',(2.36402588730863,0.201494965036854,13.1631970952294));
#64871=CARTESIAN_POINT('Ctrl Pts',(2.35779463704632,0.2646167048838,13.1672561260194));
#64872=CARTESIAN_POINT('Ctrl Pts',(2.34583997113291,0.350387124139192,13.1729054396145));
#64873=CARTESIAN_POINT('Ctrl Pts',(2.34230042325414,0.373316182912867,13.1744287490258));
#64874=CARTESIAN_POINT('Ctrl Pts',(2.33608135038002,0.410022999767895,13.1768901275722));
#64875=CARTESIAN_POINT('Ctrl Pts',(2.33361484278695,0.423835684305044,13.17782152859));
#64876=CARTESIAN_POINT('Ctrl Pts',(2.32823957619533,0.452467215399191,13.1797633747636));
#64877=CARTESIAN_POINT('Ctrl Pts',(2.32531155966412,0.467281754083812,13.1807743839614));
#64878=CARTESIAN_POINT('Ctrl Pts',(2.31805498045391,0.502238584117538,13.1831752957166));
#64879=CARTESIAN_POINT('Ctrl Pts',(2.31360510513128,0.522354151211805,13.1845689546825));
#64880=CARTESIAN_POINT('Ctrl Pts',(2.29755555855379,0.590672933837754,13.1893448506171));
#64881=CARTESIAN_POINT('Ctrl Pts',(2.28470748160061,0.638566486290968,13.192765870189));
#64882=CARTESIAN_POINT('Ctrl Pts',(2.2492376553112,0.755953244806758,13.2013376824374));
#64883=CARTESIAN_POINT('Ctrl Pts',(2.22488816760373,0.824867460799703,13.2065365808122));
#64884=CARTESIAN_POINT('Ctrl Pts',(2.14306287386725,1.02631751120825,13.2221998015429));
#64885=CARTESIAN_POINT('Ctrl Pts',(2.07662676769961,1.15484423705883,13.2328341078078));
#64886=CARTESIAN_POINT('Ctrl Pts',(1.96406528930488,1.33110433832273,13.2478897109991));
#64887=CARTESIAN_POINT('Ctrl Pts',(1.92698902791874,1.38423483697416,13.2524929420564));
#64888=CARTESIAN_POINT('Ctrl Pts',(1.87809706872479,1.44851833535258,13.2580859192617));
#64889=CARTESIAN_POINT('Ctrl Pts',(1.86828405012235,1.46115321235797,13.2591863595671));
#64890=CARTESIAN_POINT('Ctrl Pts',(1.85254977401225,1.4809943772317,13.2609150112656));
#64891=CARTESIAN_POINT('Ctrl Pts',(1.84671277023413,1.48826642853051,13.2615487094573));
#64892=CARTESIAN_POINT('Ctrl Pts',(1.83547486344484,1.50209929579979,13.2627540619901));
#64893=CARTESIAN_POINT('Ctrl Pts',(1.83008141844705,1.50866572598866,13.263326174956));
#64894=CARTESIAN_POINT('Ctrl Pts',(1.81696413502696,1.52446194921286,13.2647026194063));
#64895=CARTESIAN_POINT('Ctrl Pts',(1.80920498867873,1.53366235746264,13.2655044785323));
#64896=CARTESIAN_POINT('Ctrl Pts',(1.78138661044474,1.56614306928139,13.2683375463508));
#64897=CARTESIAN_POINT('Ctrl Pts',(1.7609444287249,1.58909323255431,13.2703434364619));
#64898=CARTESIAN_POINT('Ctrl Pts',(1.70785313724778,1.64641498386317,13.2753837011017));
#64899=CARTESIAN_POINT('Ctrl Pts',(1.67460825682304,1.68021795200097,13.2783848442467));
#64900=CARTESIAN_POINT('Ctrl Pts',(1.47116415658264,1.87503582381759,13.2960214023276));
#64901=CARTESIAN_POINT('Ctrl Pts',(1.2788936983792,2.01109927157288,13.3099220162397));
#64902=CARTESIAN_POINT('Ctrl Pts',(1.04165564399438,2.13099634566499,13.3270544861575));
#64903=CARTESIAN_POINT('Ctrl Pts',(1.01323985779057,2.14465306033068,13.3291034543336));
#64904=CARTESIAN_POINT('Ctrl Pts',(0.967091970049809,2.16571002258847,13.3324310458546));
#64905=CARTESIAN_POINT('Ctrl Pts',(0.949526882590109,2.17346852843598,13.3336976037676));
#64906=CARTESIAN_POINT('Ctrl Pts',(0.918169143497226,2.18686658625315,13.3359596806725));
#64907=CARTESIAN_POINT('Ctrl Pts',(0.904413761317703,2.19259110948139,13.336952290945));
#64908=CARTESIAN_POINT('Ctrl Pts',(0.875269932601788,2.20439887413349,13.3390565046697));
#64909=CARTESIAN_POINT('Ctrl Pts',(0.859869988747321,2.21045140862487,13.3401690657902));
#64910=CARTESIAN_POINT('Ctrl Pts',(0.818475309363497,2.2262224440055,13.3431620356483));
#64911=CARTESIAN_POINT('Ctrl Pts',(0.792371894677743,2.23564640999891,13.3450519685062));
#64912=CARTESIAN_POINT('Ctrl Pts',(0.631775327267986,2.29045978657781,13.3566997173279));
#64913=CARTESIAN_POINT('Ctrl Pts',(0.49361882114513,2.32415017957269,13.3668320034302));
#64914=CARTESIAN_POINT('Ctrl Pts',(0.208149752466547,2.36715422716738,13.3878034996021));
#64915=CARTESIAN_POINT('Ctrl Pts',(0.0612764048750438,2.37549870898118,
13.3986086049959));
#64916=CARTESIAN_POINT('Ctrl Pts',(-0.119512532297057,2.36898246446797,
13.4113934682666));
#64917=CARTESIAN_POINT('Ctrl Pts',(-0.153566352071415,2.36701897447235,
13.4137778375838));
#64918=CARTESIAN_POINT('Ctrl Pts',(-0.200410867308527,2.36330267303301,
13.4170147551339));
#64919=CARTESIAN_POINT('Ctrl Pts',(-0.213245594425363,2.36217915814911,
13.4178971564725));
#64920=CARTESIAN_POINT('Ctrl Pts',(-0.233830949630623,2.36020802478089,
13.4193045783921));
#64921=CARTESIAN_POINT('Ctrl Pts',(-0.241587445752562,2.35942669810265,
13.4198330999844));
#64922=CARTESIAN_POINT('Ctrl Pts',(-0.258087931508426,2.35768234969891,
13.4209534185395));
#64923=CARTESIAN_POINT('Ctrl Pts',(-0.26683072612777,2.3567088941761,13.4215446152658));
#64924=CARTESIAN_POINT('Ctrl Pts',(-0.289050397931817,2.35410963862184,
13.4230414743531));
#64925=CARTESIAN_POINT('Ctrl Pts',(-0.302519331985634,2.3524167144305,13.4239435272546));
#64926=CARTESIAN_POINT('Ctrl Pts',(-0.358237426548172,2.34492697857831,
13.4276559171999));
#64927=CARTESIAN_POINT('Ctrl Pts',(-0.400343674750294,2.33810651117025,
13.4304155863227));
#64928=CARTESIAN_POINT('Ctrl Pts',(-0.518360279303401,2.31570782880167,
13.4380787316155));
#64929=CARTESIAN_POINT('Ctrl Pts',(-0.593726521661219,2.29754012201324,
13.4428889035842));
#64930=CARTESIAN_POINT('Ctrl Pts',(-0.855378932721612,2.22072782047201,
13.4596976516556));
#64931=CARTESIAN_POINT('Ctrl Pts',(-1.03516035886966,2.14283482619258,13.471515828387));
#64932=CARTESIAN_POINT('Ctrl Pts',(-1.22752141257753,2.02957513379975,13.4859544124786));
#64933=CARTESIAN_POINT('Ctrl Pts',(-1.25142523327983,2.01492402397062,13.4877815667973));
#64934=CARTESIAN_POINT('Ctrl Pts',(-1.29039613613172,1.99007702179657,13.4908187469689));
#64935=CARTESIAN_POINT('Ctrl Pts',(-1.30561600623997,1.98012513611661,13.4920199464396));
#64936=CARTESIAN_POINT('Ctrl Pts',(-1.33302014770862,1.96175295502885,13.494211107932));
#64937=CARTESIAN_POINT('Ctrl Pts',(-1.34524295406418,1.95339160141212,13.495198849232));
#64938=CARTESIAN_POINT('Ctrl Pts',(-1.36136779109533,1.94213783549373,13.4965161435903));
#64939=CARTESIAN_POINT('Ctrl Pts',(-1.36534058910176,1.93934698025914,13.4968418540968));
#64940=CARTESIAN_POINT('Ctrl Pts',(-1.37132372985496,1.93511638013127,13.4973341452362));
#64941=CARTESIAN_POINT('Ctrl Pts',(-1.37334045470343,1.93368564459462,13.4975003843192));
#64942=CARTESIAN_POINT('Ctrl Pts',(-1.377406463844,1.9307915053146,13.4978361613133));
#64943=CARTESIAN_POINT('Ctrl Pts',(-1.37945566204042,1.92932798663551,13.4980057034387));
#64944=CARTESIAN_POINT('Ctrl Pts',(-1.40023502014631,1.91443752907382,13.4997281243367));
#64945=CARTESIAN_POINT('Ctrl Pts',(-1.41877028355022,1.90074195578745,13.5012911726827));
#64946=CARTESIAN_POINT('Ctrl Pts',(-1.49107076552093,1.8456728620222,13.5074963261497));
#64947=CARTESIAN_POINT('Ctrl Pts',(-1.54324548457178,1.80227416217043,13.5122157864676));
#64948=CARTESIAN_POINT('Ctrl Pts',(-1.6820412019242,1.67637418663608,13.5254648155077));
#64949=CARTESIAN_POINT('Ctrl Pts',(-1.76438873548279,1.58947167111063,13.5341451307449));
#64950=CARTESIAN_POINT('Ctrl Pts',(-1.92000926340729,1.39817960703495,13.552124114471));
#64951=CARTESIAN_POINT('Ctrl Pts',(-1.99214913740489,1.29332489655779,13.5613985112742));
#64952=CARTESIAN_POINT('Ctrl Pts',(-2.06703141223117,1.16323227623332,13.571888920859));
#64953=CARTESIAN_POINT('Ctrl Pts',(-2.07822689018659,1.14311035222473,13.5734842405068));
#64954=CARTESIAN_POINT('Ctrl Pts',(-2.09421633577458,1.11336046291501,13.5757998058157));
#64955=CARTESIAN_POINT('Ctrl Pts',(-2.09924032387422,1.10385853040896,13.5765330327748));
#64956=CARTESIAN_POINT('Ctrl Pts',(-2.10804802681143,1.08692278727384,13.577828228231));
#64957=CARTESIAN_POINT('Ctrl Pts',(-2.11185732770483,1.07950278514011,13.5783917178547));
#64958=CARTESIAN_POINT('Ctrl Pts',(-2.12017987403082,1.06307892070894,13.5796302123124));
#64959=CARTESIAN_POINT('Ctrl Pts',(-2.1246749895009,1.05406626360807,13.5803041222944));
#64960=CARTESIAN_POINT('Ctrl Pts',(-2.13772093839215,1.02748671402799,13.5822756175935));
#64961=CARTESIAN_POINT('Ctrl Pts',(-2.14611252144664,1.00984199910224,13.5835640267986));
#64962=CARTESIAN_POINT('Ctrl Pts',(-2.16503301813163,0.968757068978621,
13.5865217774907));
#64963=CARTESIAN_POINT('Ctrl Pts',(-2.17540111867858,0.945245107796463,
13.5881830541251));
#64964=CARTESIAN_POINT('Ctrl Pts',(-2.21029677456371,0.862494367268822,
13.5939367358987));
#64965=CARTESIAN_POINT('Ctrl Pts',(-2.2328042368885,0.802430501282534,13.5979485190075));
#64966=CARTESIAN_POINT('Ctrl Pts',(-2.31350866745295,0.557239622330448,
13.613942060782));
#64967=CARTESIAN_POINT('Ctrl Pts',(-2.35130711032184,0.366268275802427,
13.6256063379384));
#64968=CARTESIAN_POINT('Ctrl Pts',(-2.3654410187889,0.172878133755955,13.6380106975316));
#64969=CARTESIAN_POINT('Origin',(0.,0.,-1.84858989190501));
#64970=CARTESIAN_POINT('',(-2.36929349484951,0.173162376944888,14.8369729823432));
#64971=CARTESIAN_POINT('',(-2.36544101854889,0.172878137039872,14.63965844111));
#64972=CARTESIAN_POINT('',(-2.36544101854889,0.172878137039864,-1.84858989190501));
#64973=CARTESIAN_POINT('',(-2.37103408855011,-0.00209831677342502,13.8485903224414));
#64974=CARTESIAN_POINT('Ctrl Pts',(-2.37103408855011,-0.00209831677342502,
13.8485903224414));
#64975=CARTESIAN_POINT('Ctrl Pts',(-2.37284029274397,-0.209416860088268,
13.8624956146275));
#64976=CARTESIAN_POINT('Ctrl Pts',(-2.25333046601257,-1.19988580892436,
13.9290658704801));
#64977=CARTESIAN_POINT('Ctrl Pts',(-0.869666078203209,-2.66015561356989,
14.0483010899995));
#64978=CARTESIAN_POINT('Ctrl Pts',(1.75267763866885,-2.18191305067097,14.2062959809995));
#64979=CARTESIAN_POINT('Ctrl Pts',(2.78512620401791,0.275629071355557,14.3642908719996));
#64980=CARTESIAN_POINT('Ctrl Pts',(1.29091271455523,2.48320730756548,14.5222857629997));
#64981=CARTESIAN_POINT('Ctrl Pts',(-1.36682061392716,2.43810610823687,14.6798464664475));
#64982=CARTESIAN_POINT('Ctrl Pts',(-2.3122698979759,0.94596955261334,14.7847422062287));
#64983=CARTESIAN_POINT('Ctrl Pts',(-2.36929349484953,0.173162376944586,
14.8369729823432));
#64984=CARTESIAN_POINT('Ctrl Pts',(-2.3717490991011,-0.00206722352871417,
13.8490012910668));
#64985=CARTESIAN_POINT('Ctrl Pts',(-2.37179998906972,0.0563194170761172,
13.8454099352406));
#64986=CARTESIAN_POINT('Ctrl Pts',(-2.36969484767437,0.114674253025937,
13.8418054807329));
#64987=CARTESIAN_POINT('Ctrl Pts',(-2.36544101497364,0.172878185958964,
13.8381597463488));
#64988=CARTESIAN_POINT('',(-2.37174998280982,0.000285554948450898,13.651410108095));
#64989=CARTESIAN_POINT('Ctrl Pts',(-2.3654410187889,0.172878133755955,13.6380106975316));
#64990=CARTESIAN_POINT('Ctrl Pts',(-2.36637511213128,0.160097207334322,
13.6388304870286));
#64991=CARTESIAN_POINT('Ctrl Pts',(-2.3672058393811,0.147305694585705,13.6396531778704));
#64992=CARTESIAN_POINT('Ctrl Pts',(-2.36952297024855,0.10651302519473,13.6422846450463));
#64993=CARTESIAN_POINT('Ctrl Pts',(-2.3706164545265,0.0784962032887724,
13.6441037981315));
#64994=CARTESIAN_POINT('Ctrl Pts',(-2.37156998763884,0.0336944680560588,
13.6470352721048));
#64995=CARTESIAN_POINT('Ctrl Pts',(-2.37174898697047,0.0169185798481951,
13.648137976221));
#64996=CARTESIAN_POINT('Ctrl Pts',(-2.37174999571231,0.000142613750890254,
13.6492461020341));
#64997=CARTESIAN_POINT('Ctrl Pts',(-2.37174998280982,0.000285554948450898,
13.651410108095));
#64998=CARTESIAN_POINT('Ctrl Pts',(-2.37175993590189,-0.082382408167183,
13.6569281379447));
#64999=CARTESIAN_POINT('Ctrl Pts',(-2.36744344666263,-0.164985957670592,
13.6624461677945));
#65000=CARTESIAN_POINT('Ctrl Pts',(-2.35884659186433,-0.247064401624429,
13.6679641976442));
#65001=CARTESIAN_POINT('Ctrl Pts',(-2.35023020288839,-0.329329348077393,
13.6734947658208));
#65002=CARTESIAN_POINT('Ctrl Pts',(-2.33731405720822,-0.411066390836204,
13.6790253339974));
#65003=CARTESIAN_POINT('Ctrl Pts',(-2.32019591278182,-0.491822110941082,
13.6845559021739));
#65004=CARTESIAN_POINT('Ctrl Pts',(-2.30305844536776,-0.572668988226546,
13.6900927132644));
#65005=CARTESIAN_POINT('Ctrl Pts',(-2.28170963114255,-0.652531933827544,
13.6956295243548));
#65006=CARTESIAN_POINT('Ctrl Pts',(-2.25629726319919,-0.730972449945869,
13.7011663354452));
#65007=CARTESIAN_POINT('Ctrl Pts',(-2.23081935718109,-0.809615262852067,
13.7067174258794));
#65008=CARTESIAN_POINT('Ctrl Pts',(-2.20125709223112,-0.886827922498776,
13.7122685163137));
#65009=CARTESIAN_POINT('Ctrl Pts',(-2.16780691071137,-0.962190864835064,
13.7178196067479));
#65010=CARTESIAN_POINT('Ctrl Pts',(-2.13547394943128,-1.0350367205466,13.7231852933875));
#65011=CARTESIAN_POINT('Ctrl Pts',(-2.0995088878053,-1.10615419575088,13.7285509800271));
#65012=CARTESIAN_POINT('Ctrl Pts',(-2.06012841898357,-1.17518890387727,
13.7339166666667));
#65013=CARTESIAN_POINT('Ctrl Pts',(-2.02096290085725,-1.24384679936117,
13.7392530657404));
#65014=CARTESIAN_POINT('Ctrl Pts',(-1.97828872257431,-1.31067205434257,
13.7445894648141));
#65015=CARTESIAN_POINT('Ctrl Pts',(-1.93230231440578,-1.37528390823207,
13.7499258638878));
#65016=CARTESIAN_POINT('Ctrl Pts',(-1.88638153493216,-1.43980355244885,
13.7552546472133));
#65017=CARTESIAN_POINT('Ctrl Pts',(-1.83715818247681,-1.50211569089093,
13.7605834305388));
#65018=CARTESIAN_POINT('Ctrl Pts',(-1.7848738524587,-1.56186535697199,13.7659122138643));
#65019=CARTESIAN_POINT('Ctrl Pts',(-1.73264933883228,-1.62154666587168,
13.7712349007438));
#65020=CARTESIAN_POINT('Ctrl Pts',(-1.6773711137276,-1.67867097815146,13.7765575876234));
#65021=CARTESIAN_POINT('Ctrl Pts',(-1.61932231096069,-1.73291468795349,
13.781880274503));
#65022=CARTESIAN_POINT('Ctrl Pts',(-1.56130975717306,-1.78712452489304,
13.7871996375936));
#65023=CARTESIAN_POINT('Ctrl Pts',(-1.50053040095659,-1.83845701136883,
13.7925190006843));
#65024=CARTESIAN_POINT('Ctrl Pts',(-1.43730482004822,-1.88662474190448,
13.7978383637749));
#65025=CARTESIAN_POINT('Ctrl Pts',(-1.37409911990853,-1.93477732648979,
13.8031560542352));
#65026=CARTESIAN_POINT('Ctrl Pts',(-1.30844909455567,-1.97976684805962,
13.8084737446955));
#65027=CARTESIAN_POINT('Ctrl Pts',(-1.24070789877305,-2.02134657404963,
13.8137914351558));
#65028=CARTESIAN_POINT('Ctrl Pts',(-1.17296700344431,-2.06292611562025,
13.8191091020304));
#65029=CARTESIAN_POINT('Ctrl Pts',(-1.10313535565988,-2.10109564821282,
13.8244267689051));
#65030=CARTESIAN_POINT('Ctrl Pts',(-1.03159327904617,-2.13565291401173,
13.8297444357797));
#65031=CARTESIAN_POINT('Ctrl Pts',(-0.959980502109187,-2.17024433048082,
13.8350673577543));
#65032=CARTESIAN_POINT('Ctrl Pts',(-0.886654342325077,-2.20121614581692,
13.8403902797289));
#65033=CARTESIAN_POINT('Ctrl Pts',(-0.812017264618513,-2.22841334237198,
13.8457132017036));
#65034=CARTESIAN_POINT('Ctrl Pts',(-0.73734389526598,-2.25562376333318,
13.8510387119039));
#65035=CARTESIAN_POINT('Ctrl Pts',(-0.661358785788709,-2.27905577112385,
13.8563642221041));
#65036=CARTESIAN_POINT('Ctrl Pts',(-0.584479384209729,-2.29860434001457,
13.8616897323044));
#65037=CARTESIAN_POINT('Ctrl Pts',(-0.50746364867594,-2.31818757532638,
13.8670246864891));
#65038=CARTESIAN_POINT('Ctrl Pts',(-0.429550912080691,-2.33387351945313,
13.8723596406738));
#65039=CARTESIAN_POINT('Ctrl Pts',(-0.35116838442565,-2.34560841324375,
13.8776945948584));
#65040=CARTESIAN_POINT('Ctrl Pts',(-0.282197128288541,-2.35593431608957,
13.8823889891649));
#65041=CARTESIAN_POINT('Ctrl Pts',(-0.212862435259374,-2.36320177056976,
13.8870833834713));
#65042=CARTESIAN_POINT('Ctrl Pts',(-0.143455852460942,-2.3674075443182,
13.8917777777778));
#65043=CARTESIAN_POINT('Ctrl Pts',(-0.064560343655558,-2.37218831073004,
13.8971139665427));
#65044=CARTESIAN_POINT('Ctrl Pts',(0.0147208745263364,-2.37302977826968,
13.9024501553077));
#65045=CARTESIAN_POINT('Ctrl Pts',(0.0939616444336405,-2.36988802939618,
13.9077863440726));
#65046=CARTESIAN_POINT('Ctrl Pts',(0.173089315342885,-2.36675076468721,
13.9131149165864));
#65047=CARTESIAN_POINT('Ctrl Pts',(0.252176188878941,-2.35964159268616,
13.9184434891002));
#65048=CARTESIAN_POINT('Ctrl Pts',(0.330792984760269,-2.34856851374053,
13.923772061614));
#65049=CARTESIAN_POINT('Ctrl Pts',(0.40931983826296,-2.33750810306824,13.929094537918));
#65050=CARTESIAN_POINT('Ctrl Pts',(0.487377221848571,-2.32249286279898,
13.9344170142219));
#65051=CARTESIAN_POINT('Ctrl Pts',(0.564539376960543,-2.30358272140616,
13.9397394905259));
#65052=CARTESIAN_POINT('Ctrl Pts',(0.64165334927425,-2.28468438817923,13.945058643286));
#65053=CARTESIAN_POINT('Ctrl Pts',(0.717872749447858,-2.2618960926493,13.9503777960462));
#65054=CARTESIAN_POINT('Ctrl Pts',(0.792781632525433,-2.23532891218056,
13.9556969488063));
#65055=CARTESIAN_POINT('Ctrl Pts',(0.867666967735637,-2.2087700831972,13.9610144294723));
#65056=CARTESIAN_POINT('Ctrl Pts',(0.941242163291927,-2.17843488466003,
13.9663319101384));
#65057=CARTESIAN_POINT('Ctrl Pts',(1.01310749493875,-2.14448391605042,13.9716493908044));
#65058=CARTESIAN_POINT('Ctrl Pts',(1.08497251901454,-2.110533092745,13.9769668487125));
#65059=CARTESIAN_POINT('Ctrl Pts',(1.15512727130074,-2.07296673136787,13.9822843066206));
#65060=CARTESIAN_POINT('Ctrl Pts',(1.22319439008194,-2.03199250652459,13.9876017645288));
#65061=CARTESIAN_POINT('Ctrl Pts',(1.29132881283307,-1.99097776684762,13.992924480277));
#65062=CARTESIAN_POINT('Ctrl Pts',(1.35737107712532,-1.94654867490852,13.9982471960253));
#65063=CARTESIAN_POINT('Ctrl Pts',(1.42097124946717,-1.89895728511405,14.0035699117735));
#65064=CARTESIAN_POINT('Ctrl Pts',(1.48460236219264,-1.85134274293172,14.0088952169309));
#65065=CARTESIAN_POINT('Ctrl Pts',(1.54578865572984,-1.80056313736407,14.0142205220882));
#65066=CARTESIAN_POINT('Ctrl Pts',(1.60421384537677,-1.74691041579168,14.0195458272456));
#65067=CARTESIAN_POINT('Ctrl Pts',(1.66274269488672,-1.69316250182365,14.0248805807318));
#65068=CARTESIAN_POINT('Ctrl Pts',(1.71850032353031,-1.63653162096747,14.030215334218));
#65069=CARTESIAN_POINT('Ctrl Pts',(1.77120801884488,-1.57734594064828,14.0355500877042));
#65070=CARTESIAN_POINT('Ctrl Pts',(1.81760742868406,-1.52524385913339,14.0402463547658));
#65071=CARTESIAN_POINT('Ctrl Pts',(1.86164374629265,-1.47116260311739,14.0449426218273));
#65072=CARTESIAN_POINT('Ctrl Pts',(1.90315456387766,-1.41534475252203,14.0496388888889));
#65073=CARTESIAN_POINT('Ctrl Pts',(1.95032416329439,-1.35191777598767,14.0549753541511));
#65074=CARTESIAN_POINT('Ctrl Pts',(1.99440705959551,-1.28601247874764,14.0603118194133));
#65075=CARTESIAN_POINT('Ctrl Pts',(2.03513332155307,-1.21796158642397,14.0656482846755));
#65076=CARTESIAN_POINT('Ctrl Pts',(2.07580145221783,-1.15000782764891,14.0709771328472));
#65077=CARTESIAN_POINT('Ctrl Pts',(2.11312222544839,-1.07991495422045,14.0763059810188));
#65078=CARTESIAN_POINT('Ctrl Pts',(2.14686746081374,-1.00804670933403,14.0816348291905));
#65079=CARTESIAN_POINT('Ctrl Pts',(2.18057407555734,-0.936260715949818,
14.0869575786218));
#65080=CARTESIAN_POINT('Ctrl Pts',(2.21071308696344,-0.862703810504251,
14.0922803280531));
#65081=CARTESIAN_POINT('Ctrl Pts',(2.23710170881016,-0.787765197846848,
14.0976030774844));
#65082=CARTESIAN_POINT('Ctrl Pts',(2.26347384522741,-0.712873400639668,
14.1029225017018));
#65083=CARTESIAN_POINT('Ctrl Pts',(2.28610008780648,-0.636602049795984,
14.1082419259193));
#65084=CARTESIAN_POINT('Ctrl Pts',(2.30484583411056,-0.559360119675312,
14.1135613501368));
#65085=CARTESIAN_POINT('Ctrl Pts',(2.32358568075857,-0.482142499113462,
14.1188791002265));
#65086=CARTESIAN_POINT('Ctrl Pts',(2.33844734622214,-0.403955360241968,
14.1241968503162));
#65087=CARTESIAN_POINT('Ctrl Pts',(2.34934655535866,-0.32522119445757,14.129514600406));
#65088=CARTESIAN_POINT('Ctrl Pts',(2.36024571293403,-0.246487401142772,
14.1348323253389));
#65089=CARTESIAN_POINT('Ctrl Pts',(2.36718238878815,-0.167207049704571,
14.1401500502719));
#65090=CARTESIAN_POINT('Ctrl Pts',(2.37012394706579,-0.0878096694291725,
14.1454677752048));
#65091=CARTESIAN_POINT('Ctrl Pts',(2.37306841069168,-0.0083338691404468,
14.1507907524025));
#65092=CARTESIAN_POINT('Ctrl Pts',(2.37200985761628,0.0712587222624321,
14.1561137296001));
#65093=CARTESIAN_POINT('Ctrl Pts',(2.36696780673544,0.150537252459319,14.1614367067978));
#65094=CARTESIAN_POINT('Ctrl Pts',(2.36192330561845,0.22985430886828,14.1667622707506));
#65095=CARTESIAN_POINT('Ctrl Pts',(2.35289150344097,0.308856534625879,14.1720878347035));
#65096=CARTESIAN_POINT('Ctrl Pts',(2.33994372181595,0.387119414695437,14.1774133986563));
#65097=CARTESIAN_POINT('Ctrl Pts',(2.32697298694027,0.465521035713479,14.1827484035318));
#65098=CARTESIAN_POINT('Ctrl Pts',(2.31007250191994,0.54318023410877,14.1880834084072));
#65099=CARTESIAN_POINT('Ctrl Pts',(2.28936446340997,0.619684126128467,14.1934184132827));
#65100=CARTESIAN_POINT('Ctrl Pts',(2.27114504613167,0.686994042103818,14.1981122755218));
#65101=CARTESIAN_POINT('Ctrl Pts',(2.24997907262273,0.753409670215016,14.2028061377609));
#65102=CARTESIAN_POINT('Ctrl Pts',(2.22598053518453,0.818662762973606,14.2075));
#65103=CARTESIAN_POINT('Ctrl Pts',(2.1986955606952,0.892851824530099,14.2128366548599));
#65104=CARTESIAN_POINT('Ctrl Pts',(2.16764701274257,0.96581289382715,14.2181733097198));
#65105=CARTESIAN_POINT('Ctrl Pts',(2.13296575399468,1.03713796323628,14.2235099645797));
#65106=CARTESIAN_POINT('Ctrl Pts',(2.09833397300293,1.10836127727327,14.2288390059412));
#65107=CARTESIAN_POINT('Ctrl Pts',(2.06007997676588,1.17795280942164,14.2341680473027));
#65108=CARTESIAN_POINT('Ctrl Pts',(2.01838343264649,1.24552253344456,14.2394970886642));
#65109=CARTESIAN_POINT('Ctrl Pts',(1.97673457284241,1.31301498449215,14.2448200357152));
#65110=CARTESIAN_POINT('Ctrl Pts',(1.93165123356707,1.3784898262756,14.2501429827661));
#65111=CARTESIAN_POINT('Ctrl Pts',(1.88335922953472,1.44158110247964,14.2554659298171));
#65112=CARTESIAN_POINT('Ctrl Pts',(1.8350973696749,1.5046329967124,14.260785554251));
#65113=CARTESIAN_POINT('Ctrl Pts',(1.78363110438294,1.5653039081915,14.266105178685));
#65114=CARTESIAN_POINT('Ctrl Pts',(1.72922915705936,1.62325739945203,14.2714248031189));
#65115=CARTESIAN_POINT('Ctrl Pts',(1.67484430700169,1.68119267727906,14.2767427557187));
#65116=CARTESIAN_POINT('Ctrl Pts',(1.61752592712794,1.73641189007495,14.2820607083185));
#65117=CARTESIAN_POINT('Ctrl Pts',(1.55758158864451,1.78861333362346,14.2873786609183));
#65118=CARTESIAN_POINT('Ctrl Pts',(1.49763751126917,1.84081454979072,14.292696590354));
#65119=CARTESIAN_POINT('Ctrl Pts',(1.4350678518109,1.88999771675696,14.2980145197896));
#65120=CARTESIAN_POINT('Ctrl Pts',(1.37021432386846,1.93590050600895,14.3033324492252));
#65121=CARTESIAN_POINT('Ctrl Pts',(1.30529672305414,1.9818486455083,14.3086556325772));
#65122=CARTESIAN_POINT('Ctrl Pts',(1.23809112950543,2.02450966293762,14.3139788159292));
#65123=CARTESIAN_POINT('Ctrl Pts',(1.16896889790373,2.06366416314131,14.3193019992812));
#65124=CARTESIAN_POINT('Ctrl Pts',(1.09981306102228,2.10283769915886,14.3246277706148));
#65125=CARTESIAN_POINT('Ctrl Pts',(1.02873914840437,2.13850111171075,14.3299535419485));
#65126=CARTESIAN_POINT('Ctrl Pts',(0.956141551439548,2.17048183501055,14.3352793132821));
#65127=CARTESIAN_POINT('Ctrl Pts',(0.883415266843213,2.20251924783877,14.340614525161));
#65128=CARTESIAN_POINT('Ctrl Pts',(0.809160339463884,2.23086076116328,14.3459497370398));
#65129=CARTESIAN_POINT('Ctrl Pts',(0.733789258690845,2.25538275827628,14.3512849489187));
#65130=CARTESIAN_POINT('Ctrl Pts',(0.667504133771765,2.2769486377254,14.3559770029829));
#65131=CARTESIAN_POINT('Ctrl Pts',(0.600356174241293,2.29556108606254,14.360669057047));
#65132=CARTESIAN_POINT('Ctrl Pts',(0.532631938092542,2.31116881274904,14.3653611111112));
#65133=CARTESIAN_POINT('Ctrl Pts',(0.455623932109421,2.32891607692514,14.37069636106));
#65134=CARTESIAN_POINT('Ctrl Pts',(0.377584696267147,2.3428433025856,14.3760316110088));
#65135=CARTESIAN_POINT('Ctrl Pts',(0.298927131925522,2.35283672028018,14.3813668609576));
#65136=CARTESIAN_POINT('Ctrl Pts',(0.220381878725929,2.36281586888107,14.3866944929739));
#65137=CARTESIAN_POINT('Ctrl Pts',(0.141220510988674,2.36887230598976,14.3920221249902));
#65138=CARTESIAN_POINT('Ctrl Pts',(0.0618675983092391,2.37094294802288,
14.3973497570065));
#65139=CARTESIAN_POINT('Ctrl Pts',(-0.0173945417789801,2.37301122142786,
14.4026712946912));
#65140=CARTESIAN_POINT('Ctrl Pts',(-0.0968473257635621,2.37110274848552,
14.407992832376));
#65141=CARTESIAN_POINT('Ctrl Pts',(-0.17606106878112,2.36520624101994,14.4133143700607));
#65142=CARTESIAN_POINT('Ctrl Pts',(-0.255225362854192,2.35931341443167,
14.4186325857913));
#65143=CARTESIAN_POINT('Ctrl Pts',(-0.334150446549355,2.34943752959353,
14.4239508015218));
#65144=CARTESIAN_POINT('Ctrl Pts',(-0.41240785669708,2.33561936587161,14.4292690172524));
#65145=CARTESIAN_POINT('Ctrl Pts',(-0.49064070436756,2.32180553922566,14.4345855637666));
#65146=CARTESIAN_POINT('Ctrl Pts',(-0.568205834015373,2.30405197229394,
14.4399021102808));
#65147=CARTESIAN_POINT('Ctrl Pts',(-0.644682594492096,2.28245096658372,
14.4452186567949));
#65148=CARTESIAN_POINT('Ctrl Pts',(-0.721159087558693,2.26085003640399,
14.4505351847192));
#65149=CARTESIAN_POINT('Ctrl Pts',(-0.79654676896273,2.23540182288431,14.4558517126434));
#65150=CARTESIAN_POINT('Ctrl Pts',(-0.870439263776206,2.20624875083857,
14.4611682405676));
#65151=CARTESIAN_POINT('Ctrl Pts',(-0.944405015211498,2.17706677659404,
14.4664900392691));
#65152=CARTESIAN_POINT('Ctrl Pts',(-1.01687218280534,2.1441727795042,14.4718118379705));
#65153=CARTESIAN_POINT('Ctrl Pts',(-1.08745411003328,2.10775748630428,14.4771336366719));
#65154=CARTESIAN_POINT('Ctrl Pts',(-1.15807045526469,2.07132443584358,14.4824580304524));
#65155=CARTESIAN_POINT('Ctrl Pts',(-1.22679932362353,2.031366904202,14.487782424233));
#65156=CARTESIAN_POINT('Ctrl Pts',(-1.29328065728895,1.9881205204872,14.4931068180135));
#65157=CARTESIAN_POINT('Ctrl Pts',(-1.35988021411545,1.94479723211501,14.4984406801159));
#65158=CARTESIAN_POINT('Ctrl Pts',(-1.42422387078254,1.89817368150386,14.5037745422183));
#65159=CARTESIAN_POINT('Ctrl Pts',(-1.48598264397024,1.84852742590399,14.5091084043207));
#65160=CARTESIAN_POINT('Ctrl Pts',(-1.54045549821504,1.8047381291692,14.5138130102879));
#65161=CARTESIAN_POINT('Ctrl Pts',(-1.59291773557545,1.75859800492949,14.5185176162551));
#65162=CARTESIAN_POINT('Ctrl Pts',(-1.64316804155503,1.71032068622005,14.5232222222222));
#65163=CARTESIAN_POINT('Ctrl Pts',(-1.69933498648107,1.65635903467842,14.5284807642173));
#65164=CARTESIAN_POINT('Ctrl Pts',(-1.75295966586774,1.59951330178753,14.5337393062124));
#65165=CARTESIAN_POINT('Ctrl Pts',(-1.80372544079536,1.54005603687904,14.5389978482074));
#65166=CARTESIAN_POINT('Ctrl Pts',(-1.8544254792806,1.48067576299599,14.544249580933));
#65167=CARTESIAN_POINT('Ctrl Pts',(-1.9022736438561,1.41869102593679,14.5495013136585));
#65168=CARTESIAN_POINT('Ctrl Pts',(-1.94698872974409,1.35441239980646,14.5547530463841));
#65169=CARTESIAN_POINT('Ctrl Pts',(-1.99166074834241,1.29019568356976,14.5599997209086));
#65170=CARTESIAN_POINT('Ctrl Pts',(-2.03320540028179,1.22368985496531,14.5652463954331));
#65171=CARTESIAN_POINT('Ctrl Pts',(-2.07138162539946,1.15523860066113,14.5704930699576));
#65172=CARTESIAN_POINT('Ctrl Pts',(-2.1095337380326,1.08683058085187,14.5757364306301));
#65173=CARTESIAN_POINT('Ctrl Pts',(-2.1443214124326,1.01647999482645,14.5809797913026));
#65174=CARTESIAN_POINT('Ctrl Pts',(-2.17554774381685,0.944558138429518,
14.5862231519752));
#65175=CARTESIAN_POINT('Ctrl Pts',(-2.20677350765612,0.872637589227062,
14.5914664173486));
#65176=CARTESIAN_POINT('Ctrl Pts',(-2.23443785121702,0.799146263057828,
14.596709682722));
#65177=CARTESIAN_POINT('Ctrl Pts',(-2.25839114180805,0.724477406896129,
14.6019529480953));
#65178=CARTESIAN_POINT('Ctrl Pts',(-2.28234418143799,0.649809333047704,
14.6071961585345));
#65179=CARTESIAN_POINT('Ctrl Pts',(-2.30258610691287,0.573964216339154,
14.6124393689737));
#65180=CARTESIAN_POINT('Ctrl Pts',(-2.31901714769678,0.497350511398446,
14.6176825794128));
#65181=CARTESIAN_POINT('Ctrl Pts',(-2.33546048118088,0.42067948876752,14.6229297125015));
#65182=CARTESIAN_POINT('Ctrl Pts',(-2.34808715120127,0.343239205000396,
14.6281768455901));
#65183=CARTESIAN_POINT('Ctrl Pts',(-2.3568487095738,0.265447212606071,14.6334239786788));
#65184=CARTESIAN_POINT('Ctrl Pts',(-2.3603187699915,0.234637292481815,14.6355021328225));
#65185=CARTESIAN_POINT('Ctrl Pts',(-2.36318312355598,0.203772254267595,
14.6375802869662));
#65186=CARTESIAN_POINT('Ctrl Pts',(-2.36544101854889,0.172878137039876,
14.63965844111));
#65187=CARTESIAN_POINT('Origin',(0.,0.,0.));
#65188=CARTESIAN_POINT('',(-2.94490570994055,0.00214417779480537,0.322176117089595));
#65189=CARTESIAN_POINT('',(1.29086451147292,2.64866566268225,6.84448539295995E-5));
#65190=CARTESIAN_POINT('Ctrl Pts',(-2.94490570994055,0.00214417779480537,
0.322176117089595));
#65191=CARTESIAN_POINT('Ctrl Pts',(-2.94584715833611,0.124808428590093,
0.315520895872749));
#65192=CARTESIAN_POINT('Ctrl Pts',(-2.88343765101094,1.21631589477965,0.256245304285532));
#65193=CARTESIAN_POINT('Ctrl Pts',(-1.5758107673324,3.04168494025884,0.148876080206978));
#65194=CARTESIAN_POINT('Ctrl Pts',(0.492178778194427,3.03189561568121,0.0481620773452684));
#65195=CARTESIAN_POINT('Ctrl Pts',(1.29086451147292,2.64866566268226,6.84448539295995E-5));
#65196=CARTESIAN_POINT('',(-1.28892185405328,2.64462557919715,0.));
#65197=CARTESIAN_POINT('Origin',(0.,0.,0.));
#65198=CARTESIAN_POINT('',(-2.94214443421968,0.0031336297816172,0.177823882910391));
#65199=CARTESIAN_POINT('Ctrl Pts',(-1.28892185405328,2.64462557919715,2.08166817117217E-15));
#65200=CARTESIAN_POINT('Ctrl Pts',(-2.16403831185616,2.21811653527939,0.0526649636666859));
#65201=CARTESIAN_POINT('Ctrl Pts',(-2.88384118710636,1.2152373497456,0.111939591303482));
#65202=CARTESIAN_POINT('Ctrl Pts',(-2.94548559297357,0.124877349165528,
0.171214218940278));
#65203=CARTESIAN_POINT('Ctrl Pts',(-2.94453111094736,0.00313617179185542,
0.177823882910391));
#65204=CARTESIAN_POINT('',(-2.94199991145336,0.000721809122472048,1.17782388287515));
#65205=CARTESIAN_POINT('Ctrl Pts',(-2.9419983312945,0.00313347416978786,
0.177823882910391));
#65206=CARTESIAN_POINT('Ctrl Pts',(-2.94209506616752,-0.0876902631826912,
0.182759245863396));
#65207=CARTESIAN_POINT('Ctrl Pts',(-2.93798190413056,-0.178703263263171,
0.1876946088164));
#65208=CARTESIAN_POINT('Ctrl Pts',(-2.92963295760384,-0.269471211303483,
0.192629971769405));
#65209=CARTESIAN_POINT('Ctrl Pts',(-2.92093784854289,-0.364002563842836,
0.197769963862351));
#65210=CARTESIAN_POINT('Ctrl Pts',(-2.90764798017833,-0.458267605499484,
0.202909955955296));
#65211=CARTESIAN_POINT('Ctrl Pts',(-2.88979424712816,-0.551772787717021,
0.208049948048242));
#65212=CARTESIAN_POINT('Ctrl Pts',(-2.87268923544769,-0.641356698797145,
0.212974387354032));
#65213=CARTESIAN_POINT('Ctrl Pts',(-2.85139553236819,-0.730242684954411,
0.217898826659821));
#65214=CARTESIAN_POINT('Ctrl Pts',(-2.82599323800431,-0.818001356205424,
0.22282326596561));
#65215=CARTESIAN_POINT('Ctrl Pts',(-2.80060282204545,-0.905718990492374,
0.227745402546939));
#65216=CARTESIAN_POINT('Ctrl Pts',(-2.77110775565445,-0.99230990960784,
0.232667539128269));
#65217=CARTESIAN_POINT('Ctrl Pts',(-2.73763880875135,-1.07735683634462,
0.237589675709598));
#65218=CARTESIAN_POINT('Ctrl Pts',(-2.70417526134609,-1.16239004258105,
0.242511018209598));
#65219=CARTESIAN_POINT('Ctrl Pts',(-2.66673927712545,-1.24587931828404,
0.247432360709598));
#65220=CARTESIAN_POINT('Ctrl Pts',(-2.62551038526634,-1.32742578581953,
0.252353703209598));
#65221=CARTESIAN_POINT('Ctrl Pts',(-2.58427551695018,-1.40898407416658,
0.257275759097486));
#65222=CARTESIAN_POINT('Ctrl Pts',(-2.53924686203539,-1.48859858140532,
0.262197814985374));
#65223=CARTESIAN_POINT('Ctrl Pts',(-2.49065000028613,-1.56589481641479,
0.267119870873263));
#65224=CARTESIAN_POINT('Ctrl Pts',(-2.44200245894562,-1.64327166036595,
0.272047059762985));
#65225=CARTESIAN_POINT('Ctrl Pts',(-2.38977953656764,-1.71832501562463,
0.276974248652708));
#65226=CARTESIAN_POINT('Ctrl Pts',(-2.33424989136487,-1.79070976002899,
0.281901437542431));
#65227=CARTESIAN_POINT('Ctrl Pts',(-2.27868603773292,-1.86313909626162,
0.286831661772854));
#65228=CARTESIAN_POINT('Ctrl Pts',(-2.21981171243828,-1.93289619995114,
0.291761886003278));
#65229=CARTESIAN_POINT('Ctrl Pts',(-2.15793396856311,-1.99967121980626,
0.296692110233701));
#65230=CARTESIAN_POINT('Ctrl Pts',(-2.09596038024424,-2.06654966965463,
0.301629971048285));
#65231=CARTESIAN_POINT('Ctrl Pts',(-2.03097442847363,-2.13043650193002,
0.306567831862868));
#65232=CARTESIAN_POINT('Ctrl Pts',(-1.96331739471672,-2.19106111452939,
0.311505692677451));
#65233=CARTESIAN_POINT('Ctrl Pts',(-1.94283752876775,-2.2094122580883,0.313000389118337));
#65234=CARTESIAN_POINT('Ctrl Pts',(-1.92211312278979,-2.22746478869269,
0.314495085559222));
#65235=CARTESIAN_POINT('Ctrl Pts',(-1.90115415235717,-2.24521199198986,
0.315989782000107));
#65236=CARTESIAN_POINT('Ctrl Pts',(-1.83014985636319,-2.30533554052147,
0.321053478656916));
#65237=CARTESIAN_POINT('Ctrl Pts',(-1.75616783242176,-2.36219158712132,
0.326117175313725));
#65238=CARTESIAN_POINT('Ctrl Pts',(-1.67954076700263,-2.41547237864071,
0.331180871970533));
#65239=CARTESIAN_POINT('Ctrl Pts',(-1.60301781255998,-2.46868077909042,
0.33623768872922));
#65240=CARTESIAN_POINT('Ctrl Pts',(-1.52385731868644,-2.51832332827906,
0.341294505487906));
#65241=CARTESIAN_POINT('Ctrl Pts',(-1.44242576961557,-2.56413180221863,
0.346351322246593));
#65242=CARTESIAN_POINT('Ctrl Pts',(-1.36108003456659,-2.60989200236958,
0.351402810041394));
#65243=CARTESIAN_POINT('Ctrl Pts',(-1.27746838515045,-2.65182594377412,
0.356454297836196));
#65244=CARTESIAN_POINT('Ctrl Pts',(-1.19198618132318,-2.68970870979268,
0.361505785630998));
#65245=CARTESIAN_POINT('Ctrl Pts',(-1.1065648040585,-2.72756451957549,0.366553678939173));
#65246=CARTESIAN_POINT('Ctrl Pts',(-1.01927592131206,-2.76137470613425,
0.371601572247347));
#65247=CARTESIAN_POINT('Ctrl Pts',(-0.930538472228052,-2.79096079365216,
0.376649465555521));
#65248=CARTESIAN_POINT('Ctrl Pts',(-0.841832764178936,-2.82053629834347,
0.381695553252206));
#65249=CARTESIAN_POINT('Ctrl Pts',(-0.751679938120826,-2.84589056656832,
0.38674164094889));
#65250=CARTESIAN_POINT('Ctrl Pts',(-0.660516895174555,-2.86689403905847,
0.391787728645575));
#65251=CARTESIAN_POINT('Ctrl Pts',(-0.569361295671956,-2.88789579661941,
0.396833404330239));
#65252=CARTESIAN_POINT('Ctrl Pts',(-0.477196073958768,-2.90454736594484,
0.401879080014903));
#65253=CARTESIAN_POINT('Ctrl Pts',(-0.384470115660988,-2.91676991381967,
0.406924755699566));
#65254=CARTESIAN_POINT('Ctrl Pts',(-0.291726132427484,-2.92899483762724,
0.411971412209682));
#65255=CARTESIAN_POINT('Ctrl Pts',(-0.198421634210417,-2.9367889726155,
0.417018068719797));
#65256=CARTESIAN_POINT('Ctrl Pts',(-0.105011336595889,-2.94012527270291,
0.422064725229913));
#65257=CARTESIAN_POINT('Ctrl Pts',(-0.0115016090678875,-2.94346512409074,
0.427116753616929));
#65258=CARTESIAN_POINT('Ctrl Pts',(0.0821137004248008,-2.94233765336725,
0.432168782003946));
#65259=CARTESIAN_POINT('Ctrl Pts',(0.175379475041113,-2.93676795810195,
0.437220810390963));
#65260=CARTESIAN_POINT('Ctrl Pts',(0.268701937369612,-2.93119487752963,
0.44227590944278));
#65261=CARTESIAN_POINT('Ctrl Pts',(0.361674002795658,-2.921174243566,0.447331008494597));
#65262=CARTESIAN_POINT('Ctrl Pts',(0.453847390536592,-2.90678285155653,
0.452386107546414));
#65263=CARTESIAN_POINT('Ctrl Pts',(0.546163258905372,-2.89236921348864,
0.45744902071578));
#65264=CARTESIAN_POINT('Ctrl Pts',(0.637677552843819,-2.87357141900821,
0.462511933885146));
#65265=CARTESIAN_POINT('Ctrl Pts',(0.727954087509513,-2.85051694372761,
0.467574847054513));
#65266=CARTESIAN_POINT('Ctrl Pts',(0.766051842354462,-2.84078768517142,
0.469711455703062));
#65267=CARTESIAN_POINT('Ctrl Pts',(0.803929369709169,-2.83030093979513,
0.471848064351611));
#65268=CARTESIAN_POINT('Ctrl Pts',(0.841554919396199,-2.81906887422781,
0.47398467300016));
#65269=CARTESIAN_POINT('Ctrl Pts',(0.930740388511047,-2.79244502301282,
0.479049168966884));
#65270=CARTESIAN_POINT('Ctrl Pts',(1.01881225662041,-2.76153967205838,0.484113664933607));
#65271=CARTESIAN_POINT('Ctrl Pts',(1.10533098686978,-2.72646426887745,0.48917816090033));
#65272=CARTESIAN_POINT('Ctrl Pts',(1.1917348781136,-2.69143542237171,0.494235934603807));
#65273=CARTESIAN_POINT('Ctrl Pts',(1.27658932259279,-2.65224768894435,0.499293708307284));
#65274=CARTESIAN_POINT('Ctrl Pts',(1.35946954869609,-2.60906238832421,0.504351482010761));
#65275=CARTESIAN_POINT('Ctrl Pts',(1.44661135021264,-2.56365656510189,0.509669318760322));
#65276=CARTESIAN_POINT('Ctrl Pts',(1.5315700051311,-2.51383121810154,0.514987155509882));
#65277=CARTESIAN_POINT('Ctrl Pts',(1.61387501033182,-2.45983158997247,0.520304992259443));
#65278=CARTESIAN_POINT('Ctrl Pts',(1.6920209146595,-2.40856071327166,0.525354103924619));
#65279=CARTESIAN_POINT('Ctrl Pts',(1.76777439658345,-2.35352740947702,0.530403215589796));
#65280=CARTESIAN_POINT('Ctrl Pts',(1.84075891398426,-2.29498815260286,0.535452327254972));
#65281=CARTESIAN_POINT('Ctrl Pts',(1.91372043576901,-2.23646734000049,0.540499848069961));
#65282=CARTESIAN_POINT('Ctrl Pts',(1.98391438227733,-2.17444304540529,0.545547368884949));
#65283=CARTESIAN_POINT('Ctrl Pts',(2.0509957297191,-2.10921324589858,0.550594889699937));
#65284=CARTESIAN_POINT('Ctrl Pts',(2.11807443805565,-2.04398601265374,0.55564221193605));
#65285=CARTESIAN_POINT('Ctrl Pts',(2.18204047452283,-1.97555383358849,0.560689534172162));
#65286=CARTESIAN_POINT('Ctrl Pts',(2.24258507684834,-1.90425212960289,0.565736856408275));
#65287=CARTESIAN_POINT('Ctrl Pts',(2.30314399100082,-1.83293357097441,0.570785371754917));
#65288=CARTESIAN_POINT('Ctrl Pts',(2.36027957882199,-1.75874447683552,0.575833887101558));
#65289=CARTESIAN_POINT('Ctrl Pts',(2.41372354800039,-1.68205310077548,0.5808824024482));
#65290=CARTESIAN_POINT('Ctrl Pts',(2.46722692088939,-1.6052764811907,0.585936529289444));
#65291=CARTESIAN_POINT('Ctrl Pts',(2.51703023276193,-1.52599239144779,0.590990656130688));
#65292=CARTESIAN_POINT('Ctrl Pts',(2.56290888110394,-1.44459754504794,0.596044782971933));
#65293=CARTESIAN_POINT('Ctrl Pts',(2.6088170703451,-1.36315028914965,0.601102164125514));
#65294=CARTESIAN_POINT('Ctrl Pts',(2.65079536683394,-1.27958996498174,0.606159545279095));
#65295=CARTESIAN_POINT('Ctrl Pts',(2.68866638945535,-1.1943353993804,0.611216926432676));
#65296=CARTESIAN_POINT('Ctrl Pts',(2.72659657450263,-1.10894764838904,0.616282208269072));
#65297=CARTESIAN_POINT('Ctrl Pts',(2.76040651923683,-1.02186078404611,0.621347490105469));
#65298=CARTESIAN_POINT('Ctrl Pts',(2.78996804485245,-0.933510743752968,
0.626412771941866));
#65299=CARTESIAN_POINT('Ctrl Pts',(2.80079750912478,-0.901144903868558,
0.628268369294649));
#65300=CARTESIAN_POINT('Ctrl Pts',(2.81105731798492,-0.868609657173925,
0.630123966647432));
#65301=CARTESIAN_POINT('Ctrl Pts',(2.82074288781733,-0.835926767622583,
0.631979564000215));
#65302=CARTESIAN_POINT('Ctrl Pts',(2.84709806122688,-0.746994135205994,
0.637028785765904));
#65303=CARTESIAN_POINT('Ctrl Pts',(2.86929096570047,-0.656653017668738,
0.642078007531594));
#65304=CARTESIAN_POINT('Ctrl Pts',(2.88717285259965,-0.565329036236088,
0.647127229297283));
#65305=CARTESIAN_POINT('Ctrl Pts',(2.9050300056007,-0.474131372460271,0.652169467071996));
#65306=CARTESIAN_POINT('Ctrl Pts',(2.91858790503137,-0.381953978906644,
0.657211704846709));
#65307=CARTESIAN_POINT('Ctrl Pts',(2.92774751912123,-0.289237729695639,
0.662253942621422));
#65308=CARTESIAN_POINT('Ctrl Pts',(2.93689730321423,-0.196620982541043,
0.667290769122148));
#65309=CARTESIAN_POINT('Ctrl Pts',(2.94165814031151,-0.1034669694437,0.672327595622874));
#65310=CARTESIAN_POINT('Ctrl Pts',(2.94198222867482,-0.0102257597046888,
0.6773644221236));
#65311=CARTESIAN_POINT('Ctrl Pts',(2.94230608195311,0.0829478153600106,
0.68239759504539));
#65312=CARTESIAN_POINT('Ctrl Pts',(2.93819958177322,0.176208017789602,0.687430767967179));
#65313=CARTESIAN_POINT('Ctrl Pts',(2.92966691956076,0.269101728778078,0.692463940888968));
#65314=CARTESIAN_POINT('Ctrl Pts',(2.92113736977366,0.361961555296011,0.697495277880232));
#65315=CARTESIAN_POINT('Ctrl Pts',(2.90818490597114,0.454454713415537,0.702526614871497));
#65316=CARTESIAN_POINT('Ctrl Pts',(2.89086573545834,0.54613121093095,0.707557951862761));
#65317=CARTESIAN_POINT('Ctrl Pts',(2.87354802183069,0.63779999663782,0.712588865618969));
#65318=CARTESIAN_POINT('Ctrl Pts',(2.85186441463844,0.728651821261133,0.717619779375176));
#65319=CARTESIAN_POINT('Ctrl Pts',(2.82592239528182,0.81824606069609,0.722650693131384));
#65320=CARTESIAN_POINT('Ctrl Pts',(2.79997527770826,0.907857907506256,0.727682595580467));
#65321=CARTESIAN_POINT('Ctrl Pts',(2.76976821013846,0.996211251182744,0.73271449802955));
#65322=CARTESIAN_POINT('Ctrl Pts',(2.73545843967439,1.08288093750613,0.737746400478632));
#65323=CARTESIAN_POINT('Ctrl Pts',(2.70111134687185,1.16964490354413,0.742783776656154));
#65324=CARTESIAN_POINT('Ctrl Pts',(2.66265280727058,1.25472114242027,0.747821152833675));
#65325=CARTESIAN_POINT('Ctrl Pts',(2.62028797139766,1.33770510462834,0.752858529011197));
#65326=CARTESIAN_POINT('Ctrl Pts',(2.57789699387572,1.42074027292682,0.757899013552468));
#65327=CARTESIAN_POINT('Ctrl Pts',(2.53159514237759,1.50168020867647,0.762939498093739));
#65328=CARTESIAN_POINT('Ctrl Pts',(2.48163212106294,1.58014746644376,0.76797998263501));
#65329=CARTESIAN_POINT('Ctrl Pts',(2.43158969263946,1.6587394336044,0.773028478107047));
#65330=CARTESIAN_POINT('Ctrl Pts',(2.37787473550395,1.73485051541562,0.778076973579084));
#65331=CARTESIAN_POINT('Ctrl Pts',(2.32077845266215,1.80813477751496,0.78312546905112));
#65332=CARTESIAN_POINT('Ctrl Pts',(2.29495877093069,1.84127487401779,0.785408464367503));
#65333=CARTESIAN_POINT('Ctrl Pts',(2.26844813894097,1.8738373779853,0.787691459683886));
#65334=CARTESIAN_POINT('Ctrl Pts',(2.24127592913026,1.90579280340264,0.789974455000268));
#65335=CARTESIAN_POINT('Ctrl Pts',(2.18108158057603,1.97658336586221,0.795031953701307));
#65336=CARTESIAN_POINT('Ctrl Pts',(2.11742442598073,2.04464353376129,0.800089452402345));
#65337=CARTESIAN_POINT('Ctrl Pts',(2.05058155168944,2.10961591287867,0.805146951103383));
#65338=CARTESIAN_POINT('Ctrl Pts',(1.9838296674296,2.17449984818088,0.810197565271541));
#65339=CARTESIAN_POINT('Ctrl Pts',(1.91390099653275,2.23630404141466,0.815248179439699));
#65340=CARTESIAN_POINT('Ctrl Pts',(1.84111245454658,2.29470454083167,0.820298793607857));
#65341=CARTESIAN_POINT('Ctrl Pts',(1.76840064344793,2.35304347668345,0.825344083612388));
#65342=CARTESIAN_POINT('Ctrl Pts',(1.69283529787275,2.40798557511709,0.83038937361692));
#65343=CARTESIAN_POINT('Ctrl Pts',(1.61476891579968,2.45924487364864,0.835434663621452));
#65344=CARTESIAN_POINT('Ctrl Pts',(1.53675761127843,2.51046800761618,0.840476394062772));
#65345=CARTESIAN_POINT('Ctrl Pts',(1.45624914716212,2.55801326391338,0.845518124504092));
#65346=CARTESIAN_POINT('Ctrl Pts',(1.37362688380007,2.60163663567795,0.850559854945412));
#65347=CARTESIAN_POINT('Ctrl Pts',(1.29103380369538,2.6452445991006,0.855599804582007));
#65348=CARTESIAN_POINT('Ctrl Pts',(1.20632879924938,2.68493322351417,0.860639754218602));
#65349=CARTESIAN_POINT('Ctrl Pts',(1.11992093775121,2.72050383076121,0.865679703855197));
#65350=CARTESIAN_POINT('Ctrl Pts',(1.0335195704517,2.75607176461043,0.870719274701789));
#65351=CARTESIAN_POINT('Ctrl Pts',(0.945416010489703,2.78752212828983,0.875758845548382));
#65352=CARTESIAN_POINT('Ctrl Pts',(0.856039414196785,2.81470433995147,0.880798416394974));
#65353=CARTESIAN_POINT('Ctrl Pts',(0.76664468403887,2.84189206668726,0.885839009734044));
#65354=CARTESIAN_POINT('Ctrl Pts',(0.67597682860988,2.8648097929073,0.890879603073113));
#65355=CARTESIAN_POINT('Ctrl Pts',(0.584479177086341,2.88335708706925,0.895920196412183));
#65356=CARTESIAN_POINT('Ctrl Pts',(0.492882185301544,2.90192451828408,0.90096626239291));
#65357=CARTESIAN_POINT('Ctrl Pts',(0.400454034134328,2.91611195822221,0.906012328373636));
#65358=CARTESIAN_POINT('Ctrl Pts',(0.307646922816162,2.92587036125693,0.911058394354362));
#65359=CARTESIAN_POINT('Ctrl Pts',(0.214782423521637,2.93563479847367,0.916107580607998));
#65360=CARTESIAN_POINT('Ctrl Pts',(0.121538939593842,2.94096472095991,0.921156766861633));
#65361=CARTESIAN_POINT('Ctrl Pts',(0.0283702941602265,2.94186320661061,
0.926205953115268));
#65362=CARTESIAN_POINT('Ctrl Pts',(-0.0649449852879284,2.94276310634818,
0.931263086060058));
#65363=CARTESIAN_POINT('Ctrl Pts',(-0.15818474898884,2.93921766386027,0.936320219004848));
#65364=CARTESIAN_POINT('Ctrl Pts',(-0.250898903538924,2.93128192779251,
0.941377351949637));
#65365=CARTESIAN_POINT('Ctrl Pts',(-0.291183333595817,2.92783383935204,
0.943574683299865));
#65366=CARTESIAN_POINT('Ctrl Pts',(-0.331368647522973,2.92355755823557,
0.945772014650093));
#65367=CARTESIAN_POINT('Ctrl Pts',(-0.371418589105699,2.91846059278976,
0.947969346000321));
#65368=CARTESIAN_POINT('Ctrl Pts',(-0.463589604632388,2.90673042633558,
0.953026288757175));
#65369=CARTESIAN_POINT('Ctrl Pts',(-0.555366086263561,2.89060897992472,
0.958083231514028));
#65370=CARTESIAN_POINT('Ctrl Pts',(-0.646297382647046,2.87013304450919,
0.963140174270881));
#65371=CARTESIAN_POINT('Ctrl Pts',(-0.737105123568885,2.84968493134797,
0.968190245764245));
#65372=CARTESIAN_POINT('Ctrl Pts',(-0.827069532619359,2.82489418394959,
0.973240317257609));
#65373=CARTESIAN_POINT('Ctrl Pts',(-0.915746207164976,2.79584922412904,
0.978290388750974));
#65374=CARTESIAN_POINT('Ctrl Pts',(-1.00432963801989,2.76683480513857,0.983335150084628));
#65375=CARTESIAN_POINT('Ctrl Pts',(-1.09162760686539,2.73357520298744,0.988379911418283));
#65376=CARTESIAN_POINT('Ctrl Pts',(-1.17720808957269,2.69620939725471,0.993424672751938));
#65377=CARTESIAN_POINT('Ctrl Pts',(-1.26272858078861,2.65886978476537,0.998465897733069));
#65378=CARTESIAN_POINT('Ctrl Pts',(-1.34653357386059,2.61742986709688,1.0035071227142));
#65379=CARTESIAN_POINT('Ctrl Pts',(-1.42820932323039,2.5720773956158,1.00854834769533));
#65380=CARTESIAN_POINT('Ctrl Pts',(-1.50985645895331,2.52674081256691,1.0135878065729));
#65381=CARTESIAN_POINT('Ctrl Pts',(-1.58937544583396,2.47749461396421,1.01862726545048));
#65382=CARTESIAN_POINT('Ctrl Pts',(-1.66637646224517,2.42457284610615,1.02366672432805));
#65383=CARTESIAN_POINT('Ctrl Pts',(-1.74337192617543,2.37165489439392,1.02870581981432));
#65384=CARTESIAN_POINT('Ctrl Pts',(-1.81784941553468,2.31506215176441,1.0337449153006));
#65385=CARTESIAN_POINT('Ctrl Pts',(-1.88944842091631,2.25507176486623,1.03878401078687));
#65386=CARTESIAN_POINT('Ctrl Pts',(-1.9610621834845,2.19506901342014,1.04382414487517));
#65387=CARTESIAN_POINT('Ctrl Pts',(-2.02979594425108,2.13166751179191,1.04886427896348));
#65388=CARTESIAN_POINT('Ctrl Pts',(-2.0953234593135,2.06518367242493,1.05390441305178));
#65389=CARTESIAN_POINT('Ctrl Pts',(-2.16092247946098,1.99862728441049,1.05895004704674));
#65390=CARTESIAN_POINT('Ctrl Pts',(-2.22330795890934,1.92898216128935,1.06399568104171));
#65391=CARTESIAN_POINT('Ctrl Pts',(-2.28219185000088,1.8566002153909,1.06904131503668));
#65392=CARTESIAN_POINT('Ctrl Pts',(-2.34111233073465,1.78417329234413,1.0740900843194));
#65393=CARTESIAN_POINT('Ctrl Pts',(-2.39652662849536,1.70900651726631,1.07913885360212));
#65394=CARTESIAN_POINT('Ctrl Pts',(-2.4481894708365,1.63148163179525,1.08418762288484));
#65395=CARTESIAN_POINT('Ctrl Pts',(-2.49993390695292,1.55383430729844,1.0892443659477));
#65396=CARTESIAN_POINT('Ctrl Pts',(-2.5479148330536,1.47382181766616,1.09430110901056));
#65397=CARTESIAN_POINT('Ctrl Pts',(-2.59193254713781,1.39185116700302,1.09935785207342));
#65398=CARTESIAN_POINT('Ctrl Pts',(-2.61110153655979,1.35615429886334,1.1015599803824));
#65399=CARTESIAN_POINT('Ctrl Pts',(-2.62951953427345,1.32008633759295,1.10376210869139));
#65400=CARTESIAN_POINT('Ctrl Pts',(-2.64717293912874,1.28368198177917,1.10596423700037));
#65401=CARTESIAN_POINT('Ctrl Pts',(-2.69070471588802,1.19391197404748,1.11139449585003));
#65402=CARTESIAN_POINT('Ctrl Pts',(-2.72971984887089,1.10181517866251,1.11682475469968));
#65403=CARTESIAN_POINT('Ctrl Pts',(-2.76398258188106,1.00785132190125,1.12225501354934));
#65404=CARTESIAN_POINT('Ctrl Pts',(-2.79813144968367,0.914199734860317,
1.12766722604084));
#65405=CARTESIAN_POINT('Ctrl Pts',(-2.82755928144001,0.818693772995606,
1.13307943853235));
#65406=CARTESIAN_POINT('Ctrl Pts',(-2.85207809395669,0.721813373367632,
1.13849165102385));
#65407=CARTESIAN_POINT('Ctrl Pts',(-2.87654556343054,0.625135843862536,
1.14389253019904));
#65408=CARTESIAN_POINT('Ctrl Pts',(-2.89612440031345,0.527089935859038,
1.14929340937424));
#65409=CARTESIAN_POINT('Ctrl Pts',(-2.91067553749488,0.428172763529981,
1.15469428854943));
#65410=CARTESIAN_POINT('Ctrl Pts',(-2.92518344663001,0.32954945112759,1.16007912296798));
#65411=CARTESIAN_POINT('Ctrl Pts',(-2.93469337094891,0.230060368059112,
1.16546395738653));
#65412=CARTESIAN_POINT('Ctrl Pts',(-2.93911694740661,0.130213553316331,
1.17084879180507));
#65413=CARTESIAN_POINT('Ctrl Pts',(-2.94102693177194,0.0871023158572045,
1.17317382216177));
#65414=CARTESIAN_POINT('Ctrl Pts',(-2.94198931181531,0.043924552416158,
1.17549885251846));
#65415=CARTESIAN_POINT('Ctrl Pts',(-2.94199991145336,0.000721809122473715,
1.17782388287515));
#65416=CARTESIAN_POINT('',(-2.9419988608317,-0.00258898917603258,2.17782388285735));
#65417=CARTESIAN_POINT('Ctrl Pts',(-2.94199991145352,0.000721808467689169,
1.17782388291039));
#65418=CARTESIAN_POINT('Ctrl Pts',(-2.94202355561543,-0.0956488013929025,
1.18301023396904));
#65419=CARTESIAN_POINT('Ctrl Pts',(-2.93730766573634,-0.191968159835166,
1.18819658502768));
#65420=CARTESIAN_POINT('Ctrl Pts',(-2.92789344151773,-0.287756833311465,
1.19338293608633));
#65421=CARTESIAN_POINT('Ctrl Pts',(-2.91847121359393,-0.383626943588707,
1.19857369643287));
#65422=CARTESIAN_POINT('Ctrl Pts',(-2.90434273592682,-0.478965067538306,
1.20376445677941));
#65423=CARTESIAN_POINT('Ctrl Pts',(-2.88560073246625,-0.573299583804366,
1.20895521712596));
#65424=CARTESIAN_POINT('Ctrl Pts',(-2.86682343567474,-0.667811742727869,
1.21415575226648));
#65425=CARTESIAN_POINT('Ctrl Pts',(-2.84341533879536,-0.761316120895031,
1.21935628740701));
#65426=CARTESIAN_POINT('Ctrl Pts',(-2.81551983296595,-0.8533534262985,1.22455682254754));
#65427=CARTESIAN_POINT('Ctrl Pts',(-2.78759562729326,-0.945485422805862,
1.22976270817514));
#65428=CARTESIAN_POINT('Ctrl Pts',(-2.75517494659144,-1.03614695707487,
1.23496859380275));
#65429=CARTESIAN_POINT('Ctrl Pts',(-2.71844963260622,-1.12489803759412,
1.24017447943036));
#65430=CARTESIAN_POINT('Ctrl Pts',(-2.68164772762766,-1.21383420934008,
1.24539122198219));
#65431=CARTESIAN_POINT('Ctrl Pts',(-2.64052342543697,-1.300851600445,1.25060796453403));
#65432=CARTESIAN_POINT('Ctrl Pts',(-2.59531509453087,-1.38553367339095,
1.25582470708587));
#65433=CARTESIAN_POINT('Ctrl Pts',(-2.57181744321684,-1.42954834464183,
1.25853618072406));
#65434=CARTESIAN_POINT('Ctrl Pts',(-2.54721719901399,-1.47293258280772,
1.26124765436224));
#65435=CARTESIAN_POINT('Ctrl Pts',(-2.52155234293504,-1.5156311496663,1.26395912800042));
#65436=CARTESIAN_POINT('Ctrl Pts',(-2.47369344260184,-1.5952539010805,1.26901538649674));
#65437=CARTESIAN_POINT('Ctrl Pts',(-2.42197520912676,-1.67274780387845,
1.27407164499306));
#65438=CARTESIAN_POINT('Ctrl Pts',(-2.36661265200757,-1.7477152386352,1.27912790348937));
#65439=CARTESIAN_POINT('Ctrl Pts',(-2.31132553580172,-1.82258051749376,
1.28417727197231));
#65440=CARTESIAN_POINT('Ctrl Pts',(-2.25240422582496,-1.89492581618144,
1.28922664045525));
#65441=CARTESIAN_POINT('Ctrl Pts',(-2.19010848152011,-1.96438001394172,
1.2942760089382));
#65442=CARTESIAN_POINT('Ctrl Pts',(-2.12787846816781,-2.0337609275535,1.29932004961257));
#65443=CARTESIAN_POINT('Ctrl Pts',(-2.0622813924961,-2.1002564756025,1.30436409028694));
#65444=CARTESIAN_POINT('Ctrl Pts',(-1.99361831361261,-2.16352721721461,
1.30940813096132));
#65445=CARTESIAN_POINT('Ctrl Pts',(-1.92500369041134,-2.2267533085285,1.31444861204536));
#65446=CARTESIAN_POINT('Ctrl Pts',(-1.85332769000155,-2.28675881734355,
1.3194890931294));
#65447=CARTESIAN_POINT('Ctrl Pts',(-1.77892865897807,-2.34324066759402,
1.32452957421344));
#65448=CARTESIAN_POINT('Ctrl Pts',(-1.70455590533159,-2.39970256872887,
1.329568275024));
#65449=CARTESIAN_POINT('Ctrl Pts',(-1.62746238469865,-2.45264301605041,
1.33460697583456));
#65450=CARTESIAN_POINT('Ctrl Pts',(-1.54801919157099,-2.50179946888793,
1.33964567664512));
#65451=CARTESIAN_POINT('Ctrl Pts',(-1.46858193675127,-2.55095224732436,
1.34468400081729));
#65452=CARTESIAN_POINT('Ctrl Pts',(-1.38679573589047,-2.59632136063284,
1.34972232498945));
#65453=CARTESIAN_POINT('Ctrl Pts',(-1.30305933650958,-2.63768845118889,
1.35476064916162));
#65454=CARTESIAN_POINT('Ctrl Pts',(-1.21930588068801,-2.67906396789331,
1.35979999960047));
#65455=CARTESIAN_POINT('Ctrl Pts',(-1.13360183506648,-2.71643564679005,
1.36483935003932));
#65456=CARTESIAN_POINT('Ctrl Pts',(-1.0463680943448,-2.74963230471589,1.36987870047817));
#65457=CARTESIAN_POINT('Ctrl Pts',(-0.959039389308916,-2.78286510115681,
1.37492353685004));
#65458=CARTESIAN_POINT('Ctrl Pts',(-0.870178080357952,-2.81191364693698,
1.37996837322192));
#65459=CARTESIAN_POINT('Ctrl Pts',(-0.780222177114766,-2.83665601621668,
1.38501320959379));
#65460=CARTESIAN_POINT('Ctrl Pts',(-0.690210530607099,-2.8614137176801,
1.39006117211567));
#65461=CARTESIAN_POINT('Ctrl Pts',(-0.599103371688591,-2.88185983316448,
1.39510913463755));
#65462=CARTESIAN_POINT('Ctrl Pts',(-0.507348789825996,-2.89792360241986,
1.40015709715944));
#65463=CARTESIAN_POINT('Ctrl Pts',(-0.415449388810102,-2.91401272562939,
1.40521302703994));
#65464=CARTESIAN_POINT('Ctrl Pts',(-0.322900964278842,-2.92570564006765,
1.41026895692043));
#65465=CARTESIAN_POINT('Ctrl Pts',(-0.230156378281364,-2.9329834710643,
1.41532488680093));
#65466=CARTESIAN_POINT('Ctrl Pts',(-0.189622052852163,-2.93616427096614,
1.41753459753412));
#65467=CARTESIAN_POINT('Ctrl Pts',(-0.149050251605291,-2.93850239437844,
1.4197443082673));
#65468=CARTESIAN_POINT('Ctrl Pts',(-0.108478607732732,-2.93999938633741,
1.42195401900049));
#65469=CARTESIAN_POINT('Ctrl Pts',(-0.0156461043132878,-2.94342467301267,
1.42701008672697));
#65470=CARTESIAN_POINT('Ctrl Pts',(0.0775123415620981,-2.94245481385698,
1.43206615445345));
#65471=CARTESIAN_POINT('Ctrl Pts',(0.170546264212455,-2.93705259942058,
1.43712222217993));
#65472=CARTESIAN_POINT('Ctrl Pts',(0.263453411334196,-2.9316577464774,1.44217140010062));
#65473=CARTESIAN_POINT('Ctrl Pts',(0.356235933449431,-2.92184256643932,
1.44722057802131));
#65474=CARTESIAN_POINT('Ctrl Pts',(0.448441103364991,-2.90762180773442,
1.45226975594201));
#65475=CARTESIAN_POINT('Ctrl Pts',(0.540548988733222,-2.89341605317815,
1.45731360653681));
#65476=CARTESIAN_POINT('Ctrl Pts',(0.632080296767727,-2.87481402687157,
1.46235745713162));
#65477=CARTESIAN_POINT('Ctrl Pts',(0.722586263894362,-2.85188237682258,
1.46740130772643));
#65478=CARTESIAN_POINT('Ctrl Pts',(0.813028386037383,-2.82896690328512,
1.47244160027342));
#65479=CARTESIAN_POINT('Ctrl Pts',(0.902446176311072,-2.80172798555608,
1.47748189282042));
#65480=CARTESIAN_POINT('Ctrl Pts',(0.990400951093039,-2.77028337107849,
1.48252218536741));
#65481=CARTESIAN_POINT('Ctrl Pts',(1.078324677722,-2.73884985659182,1.4875606986844));
#65482=CARTESIAN_POINT('Ctrl Pts',(1.16478599774774,-2.70321374407966,1.49259921200139));
#65483=CARTESIAN_POINT('Ctrl Pts',(1.24936228166699,-2.66354235730312,1.49763772531838));
#65484=CARTESIAN_POINT('Ctrl Pts',(1.33393226499431,-2.62387392588484,1.50267586328645));
#65485=CARTESIAN_POINT('Ctrl Pts',(1.4166170900887,-2.58017100652061,1.50771400125453));
#65486=CARTESIAN_POINT('Ctrl Pts',(1.4970160209526,-2.53264822527947,1.5127521392226));
#65487=CARTESIAN_POINT('Ctrl Pts',(1.57743135356895,-2.48511574917193,1.51779130499404));
#65488=CARTESIAN_POINT('Ctrl Pts',(1.65555948426003,-2.4337620894399,1.52283047076549));
#65489=CARTESIAN_POINT('Ctrl Pts',(1.73102708483011,-2.37884619754716,1.52786963653693));
#65490=CARTESIAN_POINT('Ctrl Pts',(1.8065768956395,-2.32387048331238,1.53291429169747));
#65491=CARTESIAN_POINT('Ctrl Pts',(1.87946003242905,-2.26532505280048,1.53795894685801));
#65492=CARTESIAN_POINT('Ctrl Pts',(1.94933506901085,-2.2035101063359,1.54300360201855));
#65493=CARTESIAN_POINT('Ctrl Pts',(2.01925343069665,-2.14165683232095,1.54805138505165));
#65494=CARTESIAN_POINT('Ctrl Pts',(2.08615966147826,-2.07653031548178,1.55309916808475));
#65495=CARTESIAN_POINT('Ctrl Pts',(2.14974968016417,-2.00846715498015,1.55814695111785));
#65496=CARTESIAN_POINT('Ctrl Pts',(2.21344012346541,-1.94029650564847,1.56320270586852));
#65497=CARTESIAN_POINT('Ctrl Pts',(2.27380361401271,-1.86918029259692,1.56825846061919));
#65498=CARTESIAN_POINT('Ctrl Pts',(2.33057691842516,-1.79548746230763,1.57331421536986));
#65499=CARTESIAN_POINT('Ctrl Pts',(2.35541155779665,-1.7632516274652,1.57552578024675));
#65500=CARTESIAN_POINT('Ctrl Pts',(2.37955978458651,-1.73052312151934,1.57773734512364));
#65501=CARTESIAN_POINT('Ctrl Pts',(2.40300228181253,-1.69733439062661,1.57994891000054));
#65502=CARTESIAN_POINT('Ctrl Pts',(2.45659386546322,-1.6214620707645,1.58500473929023));
#65503=CARTESIAN_POINT('Ctrl Pts',(2.50668306427918,-1.54291530114352,1.59006056857992));
#65504=CARTESIAN_POINT('Ctrl Pts',(2.5529925573868,-1.46205095736354,1.59511639786962));
#65505=CARTESIAN_POINT('Ctrl Pts',(2.59923890000525,-1.38129688520439,1.60016533271778));
#65506=CARTESIAN_POINT('Ctrl Pts',(2.64171556104463,-1.29823190093204,1.60521426756594));
#65507=CARTESIAN_POINT('Ctrl Pts',(2.68018749526955,-1.21324317026751,1.6102632024141));
#65508=CARTESIAN_POINT('Ctrl Pts',(2.71861880377871,-1.12834418627373,1.61530680567194));
#65509=CARTESIAN_POINT('Ctrl Pts',(2.75305360961187,-1.04152589584114,1.62035040892979));
#65510=CARTESIAN_POINT('Ctrl Pts',(2.78330249689689,-0.953200509214898,
1.62539401218763));
#65511=CARTESIAN_POINT('Ctrl Pts',(2.81353001308168,-0.864937525237457,
1.63043405209619));
#65512=CARTESIAN_POINT('Ctrl Pts',(2.83957734588901,-0.775169979961409,
1.63547409200476));
#65513=CARTESIAN_POINT('Ctrl Pts',(2.86130338179092,-0.684329567790158,
1.64051413191332));
#65514=CARTESIAN_POINT('Ctrl Pts',(2.88302173420405,-0.593521281649192,
1.6455523893941));
#65515=CARTESIAN_POINT('Ctrl Pts',(2.90042172289502,-0.501641313355758,
1.65059064687488));
#65516=CARTESIAN_POINT('Ctrl Pts',(2.91341252606591,-0.409135005789376,
1.65562890435566));
#65517=CARTESIAN_POINT('Ctrl Pts',(2.92640235399592,-0.316635642823058,
1.66066678360619));
#65518=CARTESIAN_POINT('Ctrl Pts',(2.93498359318536,-0.223510473307597,
1.66570466285673));
#65519=CARTESIAN_POINT('Ctrl Pts',(2.93911700049843,-0.130212354948023,
1.67074254210726));
#65520=CARTESIAN_POINT('Ctrl Pts',(2.94325124898259,-0.0368952499088041,
1.6757814465939));
#65521=CARTESIAN_POINT('Ctrl Pts',(2.94293584862796,0.0565944308396144,
1.68082035108054));
#65522=CARTESIAN_POINT('Ctrl Pts',(2.93818365541052,0.149802560320151,1.68585925556718));
#65523=CARTESIAN_POINT('Ctrl Pts',(2.93342628733005,0.243112188052422,1.69090364712881));
#65524=CARTESIAN_POINT('Ctrl Pts',(2.92422250559392,0.33613920900909,1.69594803869043));
#65525=CARTESIAN_POINT('Ctrl Pts',(2.91063714470086,0.428433672681843,1.70099243025206));
#65526=CARTESIAN_POINT('Ctrl Pts',(2.89704336452254,0.520785334203316,1.70603994798544));
#65527=CARTESIAN_POINT('Ctrl Pts',(2.87906268454813,0.612403099804473,1.71108746571883));
#65528=CARTESIAN_POINT('Ctrl Pts',(2.85681083026607,0.702848404760571,1.71613498345221));
#65529=CARTESIAN_POINT('Ctrl Pts',(2.8345238333228,0.793436551237681,1.72119047280016));
#65530=CARTESIAN_POINT('Ctrl Pts',(2.80795232305858,0.882848116377528,1.7262459621481));
#65531=CARTESIAN_POINT('Ctrl Pts',(2.77726143690243,0.970661069114589,1.73130145149605));
#65532=CARTESIAN_POINT('Ctrl Pts',(2.76381996906272,1.0091198797895,1.73351556799757));
#65533=CARTESIAN_POINT('Ctrl Pts',(2.74958897348094,1.04727233574671,1.73572968449908));
#65534=CARTESIAN_POINT('Ctrl Pts',(2.73458512827856,1.08508440971092,1.73794380100059));
#65535=CARTESIAN_POINT('Ctrl Pts',(2.70032328606808,1.17142969615842,1.74299981892048));
#65536=CARTESIAN_POINT('Ctrl Pts',(2.66190749143318,1.25630282867087,1.74805583684037));
#65537=CARTESIAN_POINT('Ctrl Pts',(2.61948513840147,1.33927652473037,1.75311185476026));
#65538=CARTESIAN_POINT('Ctrl Pts',(2.5771206111932,1.42213711951291,1.75816098083237));
#65539=CARTESIAN_POINT('Ctrl Pts',(2.53076057872994,1.50310303150586,1.76321010690448));
#65540=CARTESIAN_POINT('Ctrl Pts',(2.48060090216308,1.58176583734373,1.76825923297659));
#65541=CARTESIAN_POINT('Ctrl Pts',(2.43049416845524,1.66034561565582,1.77330302976454));
#65542=CARTESIAN_POINT('Ctrl Pts',(2.37659599970475,1.7366267478902,1.77834682655249));
#65543=CARTESIAN_POINT('Ctrl Pts',(2.3191481632378,1.81022534424606,1.78339062334044));
#65544=CARTESIAN_POINT('Ctrl Pts',(2.26174088289033,1.88377198262315,1.78843085938811));
#65545=CARTESIAN_POINT('Ctrl Pts',(2.20078918805151,1.95463950081475,1.79347109543578));
#65546=CARTESIAN_POINT('Ctrl Pts',(2.13657755592481,2.02247381874732,1.79851133148346));
#65547=CARTESIAN_POINT('Ctrl Pts',(2.07238861192725,2.09028416853402,1.80354978664622));
#65548=CARTESIAN_POINT('Ctrl Pts',(2.00494232364948,2.15506312558991,1.80858824180899));
#65549=CARTESIAN_POINT('Ctrl Pts',(1.93456207767309,2.21649127397993,1.81362669697176));
#65550=CARTESIAN_POINT('Ctrl Pts',(1.86418709696534,2.27791482682331,1.81866477519893));
#65551=CARTESIAN_POINT('Ctrl Pts',(1.79087892929389,2.33598777806775,1.8237028534261));
#65552=CARTESIAN_POINT('Ctrl Pts',(1.714995436969,2.39042980469528,1.82874093165327));
#65553=CARTESIAN_POINT('Ctrl Pts',(1.63909648677024,2.44488292145526,1.83378003616396));
#65554=CARTESIAN_POINT('Ctrl Pts',(1.56062153050848,2.49570338643916,1.83881914067465));
#65555=CARTESIAN_POINT('Ctrl Pts',(1.47995796014645,2.54265381760851,1.84385824518534));
#65556=CARTESIAN_POINT('Ctrl Pts',(1.39920654928022,2.58965537656117,1.84890283714816));
#65557=CARTESIAN_POINT('Ctrl Pts',(1.31626215101297,2.63277826650391,1.85394742911098));
#65558=CARTESIAN_POINT('Ctrl Pts',(1.23153706047447,2.67183092067554,1.85899202107381));
#65559=CARTESIAN_POINT('Ctrl Pts',(1.14675945673896,2.71090777995229,1.86403973970961));
#65560=CARTESIAN_POINT('Ctrl Pts',(1.06019937420788,2.74590921490711,1.86908745834541));
#65561=CARTESIAN_POINT('Ctrl Pts',(0.972287379531894,2.77669250216926,1.87413517698122));
#65562=CARTESIAN_POINT('Ctrl Pts',(0.884236569514481,2.80752439704801,1.87919086609691));
#65563=CARTESIAN_POINT('Ctrl Pts',(0.794830010497076,2.83412472241532,1.88424655521261));
#65564=CARTESIAN_POINT('Ctrl Pts',(0.704511421209433,2.85640117234703,1.8893022443283));
#65565=CARTESIAN_POINT('Ctrl Pts',(0.664991942728182,2.86614837600309,1.89151439355242));
#65566=CARTESIAN_POINT('Ctrl Pts',(0.625297954831822,2.87506841575694,1.89372654277653));
#65567=CARTESIAN_POINT('Ctrl Pts',(0.585466966754457,2.8831566781636,1.89593869200064));
#65568=CARTESIAN_POINT('Ctrl Pts',(0.494431293710531,2.9016427978279,1.90099466734074));
#65569=CARTESIAN_POINT('Ctrl Pts',(0.402358753236711,2.9158456024913,1.90605064268083));
#65570=CARTESIAN_POINT('Ctrl Pts',(0.309687730333526,2.92565505650972,1.91110661802092));
#65571=CARTESIAN_POINT('Ctrl Pts',(0.217143032101936,2.93545113875324,1.91615570129914));
#65572=CARTESIAN_POINT('Ctrl Pts',(0.12400190997247,2.94086572523229,1.92120478457735));
#65573=CARTESIAN_POINT('Ctrl Pts',(0.0307134383321627,2.94183967692086,
1.92625386785556));
#65574=CARTESIAN_POINT('Ctrl Pts',(-0.0624765649613562,2.94281260057873,
1.93129762169837));
#65575=CARTESIAN_POINT('Ctrl Pts',(-0.155813167463065,2.93935420188634,
1.93634137554119));
#65576=CARTESIAN_POINT('Ctrl Pts',(-0.248842757236273,2.93145719432692,
1.941385129384));
#65577=CARTESIAN_POINT('Ctrl Pts',(-0.341806670138463,2.92356576188342,
1.94642532244608));
#65578=CARTESIAN_POINT('Ctrl Pts',(-0.434463560481314,2.91124198663328,
1.95146551550816));
#65579=CARTESIAN_POINT('Ctrl Pts',(-0.526361444244065,2.89453064071074,
1.95650570857024));
#65580=CARTESIAN_POINT('Ctrl Pts',(-0.61822685699421,2.8778251995414,1.96154412074069));
#65581=CARTESIAN_POINT('Ctrl Pts',(-0.709333360089032,2.85673534703234,
1.96658253291114));
#65582=CARTESIAN_POINT('Ctrl Pts',(-0.799236739844116,2.83135738360302,
1.97162094508159));
#65583=CARTESIAN_POINT('Ctrl Pts',(-0.889133394581078,2.80598131851461,
1.97665898036506));
#65584=CARTESIAN_POINT('Ctrl Pts',(-0.977826678217004,2.7763179010643,1.98169701564853));
#65585=CARTESIAN_POINT('Ctrl Pts',(-1.06488627931391,2.7425136667169,1.98673505093199));
#65586=CARTESIAN_POINT('Ctrl Pts',(-1.15196361686693,2.70870254550911,1.99177411260303));
#65587=CARTESIAN_POINT('Ctrl Pts',(-1.23740619763973,2.67074909280154,1.99681317427406));
#65588=CARTESIAN_POINT('Ctrl Pts',(-1.32080353799129,2.62884803935672,2.00185223594509));
#65589=CARTESIAN_POINT('Ctrl Pts',(-1.40429170354303,2.58690135290309,2.00689678548639));
#65590=CARTESIAN_POINT('Ctrl Pts',(-1.4857297859912,2.54099868396863,2.0119413350277));
#65591=CARTESIAN_POINT('Ctrl Pts',(-1.56473206480836,2.49138065444857,2.016985884569));
#65592=CARTESIAN_POINT('Ctrl Pts',(-1.64378331300254,2.44173186930941,2.0220335609625));
#65593=CARTESIAN_POINT('Ctrl Pts',(-1.72039538815675,2.38836339198487,2.02708123735599));
#65594=CARTESIAN_POINT('Ctrl Pts',(-1.79421349276549,2.33155783594966,2.03212891374948));
#65595=CARTESIAN_POINT('Ctrl Pts',(-1.86814816897435,2.27466257408147,2.03718456130015));
#65596=CARTESIAN_POINT('Ctrl Pts',(-1.93927972961946,2.21431968527227,2.04224020885082));
#65597=CARTESIAN_POINT('Ctrl Pts',(-2.00728841587209,2.15085034707339,2.04729585640148));
#65598=CARTESIAN_POINT('Ctrl Pts',(-2.03705203244759,2.12307335047865,2.04950843193455));
#65599=CARTESIAN_POINT('Ctrl Pts',(-2.06621801832268,2.0946979882731,2.05172100746763));
#65600=CARTESIAN_POINT('Ctrl Pts',(-2.09476199980797,2.06575317116071,2.0539335830007));
#65601=CARTESIAN_POINT('Ctrl Pts',(-2.16135713544021,1.99822285754822,2.05909567882806));
#65602=CARTESIAN_POINT('Ctrl Pts',(-2.22482119968381,1.92732884677633,2.06425777465542));
#65603=CARTESIAN_POINT('Ctrl Pts',(-2.28479134284929,1.8534002588866,2.06941987048278));
#65604=CARTESIAN_POINT('Ctrl Pts',(-2.34263346067958,1.78209500820637,2.07439879064766));
#65605=CARTESIAN_POINT('Ctrl Pts',(-2.39722507039791,1.70796726967815,2.07937771081254));
#65606=CARTESIAN_POINT('Ctrl Pts',(-2.44827630613403,1.63135131986421,2.08435663097742));
#65607=CARTESIAN_POINT('Ctrl Pts',(-2.49928059877251,1.55480582064685,2.08933097288025));
#65608=CARTESIAN_POINT('Ctrl Pts',(-2.54675072770875,1.47577702963361,2.09430531478307));
#65609=CARTESIAN_POINT('Ctrl Pts',(-2.59043752705122,1.39463164256543,2.0992796566859));
#65610=CARTESIAN_POINT('Ctrl Pts',(-2.63409713182315,1.31353676764249,2.10425090211349));
#65611=CARTESIAN_POINT('Ctrl Pts',(-2.67397786788455,1.23032831423302,2.10922214754109));
#65612=CARTESIAN_POINT('Ctrl Pts',(-2.70987500029302,1.14540014090575,2.11419339296869));
#65613=CARTESIAN_POINT('Ctrl Pts',(-2.74576044686172,1.06049961482936,2.11916302007266));
#65614=CARTESIAN_POINT('Ctrl Pts',(-2.77766468977229,0.973880901981224,
2.12413264717664));
#65615=CARTESIAN_POINT('Ctrl Pts',(-2.80543045870139,0.885959333937228,
2.12910227428061));
#65616=CARTESIAN_POINT('Ctrl Pts',(-2.83320497738106,0.798010059410781,
2.13407346744953));
#65617=CARTESIAN_POINT('Ctrl Pts',(-2.85683827546653,0.708757544282162,
2.13904466061845));
#65618=CARTESIAN_POINT('Ctrl Pts',(-2.8762227310473,0.618633010278974,2.14401585378738));
#65619=CARTESIAN_POINT('Ctrl Pts',(-2.89561102794042,0.528490616786008,
2.14898803207067));
#65620=CARTESIAN_POINT('Ctrl Pts',(-2.91074872468526,0.437476310031793,
2.15396021035396));
#65621=CARTESIAN_POINT('Ctrl Pts',(-2.92157953159936,0.346030404068275,
2.15893238863725));
#65622=CARTESIAN_POINT('Ctrl Pts',(-2.93242016404137,0.254501539899681,
2.16390907759799));
#65623=CARTESIAN_POINT('Ctrl Pts',(-2.93894607405413,0.162540750341504,
2.16888576655873));
#65624=CARTESIAN_POINT('Ctrl Pts',(-2.94115297628147,0.0705915725185198,
2.17386245551947));
#65625=CARTESIAN_POINT('Ctrl Pts',(-2.94173853848186,0.0461944958277922,
2.17518293129876));
#65626=CARTESIAN_POINT('Ctrl Pts',(-2.94202032183177,0.0217982266268764,
2.17650340707806));
#65627=CARTESIAN_POINT('Ctrl Pts',(-2.9419988608317,-0.00258898917602336,
2.17782388285735));
#65628=CARTESIAN_POINT('',(-2.94199945032593,0.00179841093808543,3.17782388291039));
#65629=CARTESIAN_POINT('Ctrl Pts',(-2.94199886083084,-0.00258899015562637,
2.17782388291039));
#65630=CARTESIAN_POINT('Ctrl Pts',(-2.94188600231367,-0.130835761680184,
2.18476796201073));
#65631=CARTESIAN_POINT('Ctrl Pts',(-2.93338382342992,-0.258723098115673,
2.19171204111106));
#65632=CARTESIAN_POINT('Ctrl Pts',(-2.91665378210995,-0.385350120414867,
2.1986561202114));
#65633=CARTESIAN_POINT('Ctrl Pts',(-2.90599496404346,-0.466025019368996,
2.20308023814118));
#65634=CARTESIAN_POINT('Ctrl Pts',(-2.89199735598012,-0.546189033564816,
2.20750435607097));
#65635=CARTESIAN_POINT('Ctrl Pts',(-2.87471226218597,-0.625614425694941,
2.21192847400075));
#65636=CARTESIAN_POINT('Ctrl Pts',(-2.85495849231584,-0.716383439543999,
2.21698444931127));
#65637=CARTESIAN_POINT('Ctrl Pts',(-2.83086664751314,-0.806375944703539,
2.22204042462179));
#65638=CARTESIAN_POINT('Ctrl Pts',(-2.80251261705139,-0.895146374213621,
2.22709639993232));
#65639=CARTESIAN_POINT('Ctrl Pts',(-2.77419723852078,-0.983795792760766,
2.23214548298779));
#65640=CARTESIAN_POINT('Ctrl Pts',(-2.74163135430876,-1.07122602734494,
2.23719456604326));
#65641=CARTESIAN_POINT('Ctrl Pts',(-2.70494174390693,-1.15700223079722,
2.24224364909874));
#65642=CARTESIAN_POINT('Ctrl Pts',(-2.66829086171616,-1.24268789202583,
2.24728740252677));
#65643=CARTESIAN_POINT('Ctrl Pts',(-2.62752507927499,-1.32672258700668,
2.25233115595481));
#65644=CARTESIAN_POINT('Ctrl Pts',(-2.58282046295422,-1.40868820401996,
2.25737490938285));
#65645=CARTESIAN_POINT('Ctrl Pts',(-2.53814740965108,-1.49059595045009,
2.26241510174513));
#65646=CARTESIAN_POINT('Ctrl Pts',(-2.48954126199213,-1.57043713441029,
2.2674552941074));
#65647=CARTESIAN_POINT('Ctrl Pts',(-2.43722507816321,-1.64781610575098,
2.27249548646968));
#65648=CARTESIAN_POINT('Ctrl Pts',(-2.38492738147362,-1.72516773343395,
2.27753389776286));
#65649=CARTESIAN_POINT('Ctrl Pts',(-2.32892250146209,-1.80005851010918,
2.28257230905604));
#65650=CARTESIAN_POINT('Ctrl Pts',(-2.26947752827149,-1.8721206554789,2.28761072034922));
#65651=CARTESIAN_POINT('Ctrl Pts',(-2.21003700381689,-1.94417740787015,
2.29264875457836));
#65652=CARTESIAN_POINT('Ctrl Pts',(-2.14715718051741,-2.01340560796873,
2.2976867888075));
#65653=CARTESIAN_POINT('Ctrl Pts',(-2.08114552660342,-2.07947043669742,
2.30272482303664));
#65654=CARTESIAN_POINT('Ctrl Pts',(-2.01512042659782,-2.14554872234905,
2.30776388347654));
#65655=CARTESIAN_POINT('Ctrl Pts',(-1.94596254268457,-2.20846204348059,
2.31280294391645));
#65656=CARTESIAN_POINT('Ctrl Pts',(-1.87401546718772,-2.26791314400292,
2.31784200435635));
#65657=CARTESIAN_POINT('Ctrl Pts',(-1.80199004029304,-2.32742898762698,
2.3228865524054));
#65658=CARTESIAN_POINT('Ctrl Pts',(-1.72716970142457,-2.38347480208937,
2.32793110045444));
#65659=CARTESIAN_POINT('Ctrl Pts',(-1.64993006988533,-2.43579448322066,
2.33297564850348));
#65660=CARTESIAN_POINT('Ctrl Pts',(-1.57264256385075,-2.48814659301947,
2.338023323253));
#65661=CARTESIAN_POINT('Ctrl Pts',(-1.49293315807301,-2.53676774082672,
2.34307099800251));
#65662=CARTESIAN_POINT('Ctrl Pts',(-1.41120344823185,-2.58144704142823,
2.34811867275202));
#65663=CARTESIAN_POINT('Ctrl Pts',(-1.32934467648473,-2.62619689649155,
2.35317431844044));
#65664=CARTESIAN_POINT('Ctrl Pts',(-1.24545963043639,-2.66699228522441,
2.35822996412886));
#65665=CARTESIAN_POINT('Ctrl Pts',(-1.15997108707264,-2.7036699275532,2.36328560981727));
#65666=CARTESIAN_POINT('Ctrl Pts',(-1.12255733508012,-2.71972176514178,
2.36549819487845));
#65667=CARTESIAN_POINT('Ctrl Pts',(-1.08483666928519,-2.73498555357217,
2.36771077993963));
#65668=CARTESIAN_POINT('Ctrl Pts',(-1.04684537007887,-2.74945063078871,
2.36992336500081));
#65669=CARTESIAN_POINT('Ctrl Pts',(-0.960031640089006,-2.78250470722182,
2.37497933218523));
#65670=CARTESIAN_POINT('Ctrl Pts',(-0.871497829437372,-2.8115013151519,
2.38003529936965));
#65671=CARTESIAN_POINT('Ctrl Pts',(-0.781658570989003,-2.83626054487232,
2.38509126655407));
#65672=CARTESIAN_POINT('Ctrl Pts',(-0.691941781869693,-2.86098602268623,
2.3901403414186));
#65673=CARTESIAN_POINT('Ctrl Pts',(-0.600923505364346,-2.88148548455725,
2.39518941628312));
#65674=CARTESIAN_POINT('Ctrl Pts',(-0.509037204033009,-2.89762749933635,
2.40023849114764));
#65675=CARTESIAN_POINT('Ctrl Pts',(-0.417247895638188,-2.91375247499873,
2.405282236332));
#65676=CARTESIAN_POINT('Ctrl Pts',(-0.324592818251352,-2.92552907017723,
2.41032598151635));
#65677=CARTESIAN_POINT('Ctrl Pts',(-0.231518349837081,-2.93287627657368,
2.41536972670071));
#65678=CARTESIAN_POINT('Ctrl Pts',(-0.138509596146128,-2.94021829551493,
2.42040991077615));
#65679=CARTESIAN_POINT('Ctrl Pts',(-0.0450824808836744,-2.94313710717171,
2.42545009485159));
#65680=CARTESIAN_POINT('Ctrl Pts',(0.0483097523589236,-2.94160333284877,
2.43049027892703));
#65681=CARTESIAN_POINT('Ctrl Pts',(0.141668982798636,-2.94007010052863,
2.43552868191002));
#65682=CARTESIAN_POINT('Ctrl Pts',(0.23499291272157,-2.93408741556855,2.44056708489301));
#65683=CARTESIAN_POINT('Ctrl Pts',(0.32782757975047,-2.92367800517686,2.445605487876));
#65684=CARTESIAN_POINT('Ctrl Pts',(0.420655298983171,-2.91326937383103,
2.45064351378221));
#65685=CARTESIAN_POINT('Ctrl Pts',(0.512993387454905,-2.89843472551226,
2.45568153968842));
#65686=CARTESIAN_POINT('Ctrl Pts',(0.604393424651897,-2.87924861521848,
2.46071956559464));
#65687=CARTESIAN_POINT('Ctrl Pts',(0.695812079360467,-2.86005859685594,
2.46575861770946));
#65688=CARTESIAN_POINT('Ctrl Pts',(0.786291869415099,-2.83651544760013,
2.47079766982429));
#65689=CARTESIAN_POINT('Ctrl Pts',(0.875396094689752,-2.80874450197983,
2.47583672193912));
#65690=CARTESIAN_POINT('Ctrl Pts',(0.964597356741051,-2.78094331309061,
2.48088126171038));
#65691=CARTESIAN_POINT('Ctrl Pts',(1.052419639995,-2.74890527012251,2.48592580148163));
#65692=CARTESIAN_POINT('Ctrl Pts',(1.13844320924513,-2.71280501682735,2.49097034125289));
#65693=CARTESIAN_POINT('Ctrl Pts',(1.22452009777977,-2.67668238780781,2.49601800773992));
#65694=CARTESIAN_POINT('Ctrl Pts',(1.30879565281152,-2.63649272650979,2.50106567422696));
#65695=CARTESIAN_POINT('Ctrl Pts',(1.39087381644699,-2.59245714076861,2.50611334071399));
#65696=CARTESIAN_POINT('Ctrl Pts',(1.47308159411412,-2.54835201607151,2.51116897824198));
#65697=CARTESIAN_POINT('Ctrl Pts',(1.55308467393018,-2.5003890712952,2.51622461576997));
#65698=CARTESIAN_POINT('Ctrl Pts',(1.630515293901,-2.44883316629674,2.52128025329796));
#65699=CARTESIAN_POINT('Ctrl Pts',(1.66440384318929,-2.42626903303395,2.52349292086559));
#65700=CARTESIAN_POINT('Ctrl Pts',(1.69780006104988,-2.40301719778661,2.52570558843322));
#65701=CARTESIAN_POINT('Ctrl Pts',(1.73067519028839,-2.37910222262942,2.52791825600085));
#65702=CARTESIAN_POINT('Ctrl Pts',(1.80579514236009,-2.324456299428,2.53297422035692));
#65703=CARTESIAN_POINT('Ctrl Pts',(1.87845681597899,-2.26615270702094,2.53803018471299));
#65704=CARTESIAN_POINT('Ctrl Pts',(1.94828297072153,-2.20444039746972,2.54308614906906));
#65705=CARTESIAN_POINT('Ctrl Pts',(2.01801393706277,-2.14281221536486,2.54813522103407));
#65706=CARTESIAN_POINT('Ctrl Pts',(2.08491673656094,-2.07778484167878,2.55318429299909));
#65707=CARTESIAN_POINT('Ctrl Pts',(2.14864444107427,-2.00964948830402,2.55823336496411));
#65708=CARTESIAN_POINT('Ctrl Pts',(2.21230487529856,-1.9415860578857,2.5632771071823));
#65709=CARTESIAN_POINT('Ctrl Pts',(2.27279657535678,-1.87042149133203,2.5683208494005));
#65710=CARTESIAN_POINT('Ctrl Pts',(2.32980778546171,-1.79648536949289,2.57336459161869));
#65711=CARTESIAN_POINT('Ctrl Pts',(2.38677874210695,-1.72260145115364,2.57840477264123));
#65712=CARTESIAN_POINT('Ctrl Pts',(2.44027382346524,-1.6459502175064,2.58344495366376));
#65713=CARTESIAN_POINT('Ctrl Pts',(2.49002076251487,-1.56689521099685,2.5884851346863));
#65714=CARTESIAN_POINT('Ctrl Pts',(2.53975012153647,-1.4878681416681,2.59352353456359));
#65715=CARTESIAN_POINT('Ctrl Pts',(2.58573373385401,-1.40643936214698,2.59856193444088));
#65716=CARTESIAN_POINT('Ctrl Pts',(2.62774257888884,-1.32300148869707,2.60360033431818));
#65717=CARTESIAN_POINT('Ctrl Pts',(2.66974827954866,-1.23956986059769,2.60863835706969));
#65718=CARTESIAN_POINT('Ctrl Pts',(2.70777960533304,-1.15412983381828,2.6136763798212));
#65719=CARTESIAN_POINT('Ctrl Pts',(2.74165397014574,-1.06709770311069,2.61871440257271));
#65720=CARTESIAN_POINT('Ctrl Pts',(2.77553523461601,-0.980047845372544,
2.62375345148758));
#65721=CARTESIAN_POINT('Ctrl Pts',(2.80525769600541,-0.891405653015827,
2.62879250040244));
#65722=CARTESIAN_POINT('Ctrl Pts',(2.83068770085907,-0.801605351906549,
2.63383154931731));
#65723=CARTESIAN_POINT('Ctrl Pts',(2.85614539940599,-0.71170725679332,2.63887608583927));
#65724=CARTESIAN_POINT('Ctrl Pts',(2.8773011900834,-0.620648962894841,2.64392062236123));
#65725=CARTESIAN_POINT('Ctrl Pts',(2.89407198641106,-0.528877431425054,
2.64896515888319));
#65726=CARTESIAN_POINT('Ctrl Pts',(2.91085317754145,-0.437049018519976,
2.65401282208805));
#65727=CARTESIAN_POINT('Ctrl Pts',(2.9232439045966,-0.344506927092404,2.6590604852929));
#65728=CARTESIAN_POINT('Ctrl Pts',(2.93121293303732,-0.251703677356409,
2.66410814849776));
#65729=CARTESIAN_POINT('Ctrl Pts',(2.93919454577573,-0.15875387729379,2.66916378272404));
#65730=CARTESIAN_POINT('Ctrl Pts',(2.94274050481757,-0.065542538123331,
2.67421941695031));
#65731=CARTESIAN_POINT('Ctrl Pts',(2.94187167988244,0.0274776109886878,
2.67927505117659));
#65732=CARTESIAN_POINT('Ctrl Pts',(2.94149142141465,0.0681897244949632,
2.68148774978469));
#65733=CARTESIAN_POINT('Ctrl Pts',(2.94026616103632,0.108865279596634,2.68370044839281));
#65734=CARTESIAN_POINT('Ctrl Pts',(2.93820075641009,0.149466768986119,2.68591314700091));
#65735=CARTESIAN_POINT('Ctrl Pts',(2.93348135175555,0.242240289280005,2.69096911520086));
#65736=CARTESIAN_POINT('Ctrl Pts',(2.92435534782047,0.334953600743333,2.69602508340081));
#65737=CARTESIAN_POINT('Ctrl Pts',(2.91082511309175,0.427154727229405,2.70108105160076));
#65738=CARTESIAN_POINT('Ctrl Pts',(2.89731332287732,0.5192301644699,2.70613012746811));
#65739=CARTESIAN_POINT('Ctrl Pts',(2.87940929684365,0.610794369165965,2.71117920333547));
#65740=CARTESIAN_POINT('Ctrl Pts',(2.85716735980202,0.70139766044803,2.71622827920283));
#65741=CARTESIAN_POINT('Ctrl Pts',(2.83494890086353,0.791905312873912,2.72127202537594));
#65742=CARTESIAN_POINT('Ctrl Pts',(2.80840173806753,0.88145363966347,2.72631577154905));
#65743=CARTESIAN_POINT('Ctrl Pts',(2.77763154953919,0.969601451630791,2.73135951772215));
#65744=CARTESIAN_POINT('Ctrl Pts',(2.74688308628559,1.05768702688378,2.73639970276104));
#65745=CARTESIAN_POINT('Ctrl Pts',(2.71191766977773,1.14437363530412,2.74143988779993));
#65746=CARTESIAN_POINT('Ctrl Pts',(2.6728909988161,1.22923460268896,2.74648007283881));
#65747=CARTESIAN_POINT('Ctrl Pts',(2.63387811916186,1.31406558176944,2.75151847676905));
#65748=CARTESIAN_POINT('Ctrl Pts',(2.59080702151335,1.39707179904879,2.75655688069928));
#65749=CARTESIAN_POINT('Ctrl Pts',(2.54388138505031,1.47784691317962,2.76159528462952));
#65750=CARTESIAN_POINT('Ctrl Pts',(2.49695926068922,1.55861598177846,2.7666333114655));
#65751=CARTESIAN_POINT('Ctrl Pts',(2.44618339416343,1.63715389594888,2.77167133830147));
#65752=CARTESIAN_POINT('Ctrl Pts',(2.3918026683974,1.71308026532533,2.77670936513744));
#65753=CARTESIAN_POINT('Ctrl Pts',(2.33741086588451,1.78902210005574,2.78174841816325));
#65754=CARTESIAN_POINT('Ctrl Pts',(2.27941300431981,1.86235097323249,2.78678747118906));
#65755=CARTESIAN_POINT('Ctrl Pts',(2.21809972193437,1.93271767818134,2.79182652421486));
#65756=CARTESIAN_POINT('Ctrl Pts',(2.15671966824536,2.00316101377913,2.79687106486303));
#65757=CARTESIAN_POINT('Ctrl Pts',(2.09201727888038,2.07063540757098,2.8019156055112));
#65758=CARTESIAN_POINT('Ctrl Pts',(2.02432148890567,2.13482704441243,2.80696014615936));
#65759=CARTESIAN_POINT('Ctrl Pts',(1.95658373985626,2.19905846839112,2.81200781350504));
#65760=CARTESIAN_POINT('Ctrl Pts',(1.88584923210365,2.26000279538914,2.81705548085071));
#65761=CARTESIAN_POINT('Ctrl Pts',(1.81247988942131,2.31738659926291,2.82210314819639));
#65762=CARTESIAN_POINT('Ctrl Pts',(1.7389946858213,2.37486102055171,2.8271587865467));
#65763=CARTESIAN_POINT('Ctrl Pts',(1.66286670303201,2.42876343927813,2.83221442489702));
#65764=CARTESIAN_POINT('Ctrl Pts',(1.58448651068657,2.47886395299385,2.83727006324733));
#65765=CARTESIAN_POINT('Ctrl Pts',(1.55018251833043,2.50079101885213,2.83948272149854));
#65766=CARTESIAN_POINT('Ctrl Pts',(1.51544743317355,2.52199043688933,2.84169537974975));
#65767=CARTESIAN_POINT('Ctrl Pts',(1.48031532040129,2.54244578156255,2.84390803800096));
#65768=CARTESIAN_POINT('Ctrl Pts',(1.40003776517855,2.58918663863112,2.84896400477706));
#65769=CARTESIAN_POINT('Ctrl Pts',(1.31740277673951,2.63220402586784,2.85401997155316));
#65770=CARTESIAN_POINT('Ctrl Pts',(1.23279018373386,2.6712529574882,2.85907593832925));
#65771=CARTESIAN_POINT('Ctrl Pts',(1.14829293549576,2.71024865719849,2.86412501275881));
#65772=CARTESIAN_POINT('Ctrl Pts',(1.06182383933879,2.74528646765623,2.86917408718837));
#65773=CARTESIAN_POINT('Ctrl Pts',(0.97378919165651,2.7761661712176,2.87422316161793));
#65774=CARTESIAN_POINT('Ctrl Pts',(0.88584747165863,2.80701327875657,2.87926690634143));
#65775=CARTESIAN_POINT('Ctrl Pts',(0.796343901345705,2.83371085809587,2.88431065106493));
#65776=CARTESIAN_POINT('Ctrl Pts',(0.705705725800024,2.85610634055755,2.88935439578843));
#65777=CARTESIAN_POINT('Ctrl Pts',(0.615131545511419,2.87848601064604,2.89439457936632));
#65778=CARTESIAN_POINT('Ctrl Pts',(0.523424781669523,2.8965695154927,2.89943476294422));
#65779=CARTESIAN_POINT('Ctrl Pts',(0.431027855283761,2.91025411054937,2.90447494652212));
#65780=CARTESIAN_POINT('Ctrl Pts',(0.338663580399644,2.92393386970298,2.9095133489849));
#65781=CARTESIAN_POINT('Ctrl Pts',(0.245610065792039,2.93321774257587,2.91455175144768));
#65782=CARTESIAN_POINT('Ctrl Pts',(0.152318921004724,2.93805427899213,2.91959015391046));
#65783=CARTESIAN_POINT('Ctrl Pts',(0.0590347585864077,2.94289045341817,
2.92462817927438));
#65784=CARTESIAN_POINT('Ctrl Pts',(-0.0344865557569679,2.9432799305776,
2.92966620463829));
#65785=CARTESIAN_POINT('Ctrl Pts',(-0.127790446402868,2.93922329907208,
2.9347042300022));
#65786=CARTESIAN_POINT('Ctrl Pts',(-0.221113341964551,2.93516584127797,
2.9397432815532));
#65787=CARTESIAN_POINT('Ctrl Pts',(-0.314218282880421,2.92666049582177,
2.9447823331042));
#65788=CARTESIAN_POINT('Ctrl Pts',(-0.406653994202056,2.91375986124449,
2.9498213846552));
#65789=CARTESIAN_POINT('Ctrl Pts',(-0.499190369847777,2.90084517762014,
2.95486592383334));
#65790=CARTESIAN_POINT('Ctrl Pts',(-0.591055621380578,2.88352571237771,
2.95991046301148));
#65791=CARTESIAN_POINT('Ctrl Pts',(-0.681807188419884,2.86190547674429,
2.96495500218962));
#65792=CARTESIAN_POINT('Ctrl Pts',(-0.772615004949508,2.8402718404912,2.97000266806593));
#65793=CARTESIAN_POINT('Ctrl Pts',(-0.862307337098888,2.81433224992399,
2.97505033394223));
#65794=CARTESIAN_POINT('Ctrl Pts',(-0.950457424969032,2.78424041406651,
2.98009799981853));
#65795=CARTESIAN_POINT('Ctrl Pts',(-1.03874671501582,2.75410105869825,2.98515363671442));
#65796=CARTESIAN_POINT('Ctrl Pts',(-1.12548848753932,2.71979653200843,2.99020927361031));
#65797=CARTESIAN_POINT('Ctrl Pts',(-1.21027678148644,2.68152831650065,2.9952649105062));
#65798=CARTESIAN_POINT('Ctrl Pts',(-1.24738560838968,2.66477967681155,2.9974775833378));
#65799=CARTESIAN_POINT('Ctrl Pts',(-1.28412057603821,2.64727238009407,2.99969025616941));
#65800=CARTESIAN_POINT('Ctrl Pts',(-1.32044931328002,2.62902598143463,3.00190292900102));
#65801=CARTESIAN_POINT('Ctrl Pts',(-1.40346062756966,2.58733288531376,3.00695889553853));
#65802=CARTESIAN_POINT('Ctrl Pts',(-1.48464164879389,2.54163083150868,3.01201486207605));
#65803=CARTESIAN_POINT('Ctrl Pts',(-1.56357965235937,2.4921040649876,3.01707082861356));
#65804=CARTESIAN_POINT('Ctrl Pts',(-1.64241004668626,2.44264481395203,3.02211990279651));
#65805=CARTESIAN_POINT('Ctrl Pts',(-1.71900312724652,2.38937144515071,3.02716897697946));
#65806=CARTESIAN_POINT('Ctrl Pts',(-1.79296920068921,2.3325148328317,3.0322180511624));
#65807=CARTESIAN_POINT('Ctrl Pts',(-1.86685719684845,2.27571823735054,3.03726179563164));
#65808=CARTESIAN_POINT('Ctrl Pts',(-1.93812334822593,2.21534618574687,3.04230554010087));
#65809=CARTESIAN_POINT('Ctrl Pts',(-2.00640642116441,2.15167313342669,3.0473492845701));
#65810=CARTESIAN_POINT('Ctrl Pts',(-2.07464128256659,2.08804503771934,3.05238946788341));
#65811=CARTESIAN_POINT('Ctrl Pts',(-2.13989692866009,2.02112087565847,3.05742965119672));
#65812=CARTESIAN_POINT('Ctrl Pts',(-2.20184556156528,1.95121503761509,3.06246983451003));
#65813=CARTESIAN_POINT('Ctrl Pts',(-2.26377230279882,1.8813339031944,3.0675082367019));
#65814=CARTESIAN_POINT('Ctrl Pts',(-2.32239405882412,1.8084735177801,3.07254663889377));
#65815=CARTESIAN_POINT('Ctrl Pts',(-2.37742097052157,1.7329839955765,3.07758504108564));
#65816=CARTESIAN_POINT('Ctrl Pts',(-2.43244376366806,1.6575001234709,3.08262306617264));
#65817=CARTESIAN_POINT('Ctrl Pts',(-2.48387198649497,1.57938786439255,3.08766109125965));
#65818=CARTESIAN_POINT('Ctrl Pts',(-2.53145774217293,1.49902825176604,3.09269911634665));
#65819=CARTESIAN_POINT('Ctrl Pts',(-2.57905319046182,1.41865227091233,3.09773816761505));
#65820=CARTESIAN_POINT('Ctrl Pts',(-2.62280439156022,1.33602840910849,3.10277721888344));
#65821=CARTESIAN_POINT('Ctrl Pts',(-2.66250881106457,1.25156335477017,3.10781627015184));
#65822=CARTESIAN_POINT('Ctrl Pts',(-2.70225646941769,1.16700631642207,3.11286080904047));
#65823=CARTESIAN_POINT('Ctrl Pts',(-2.73794836091714,1.08060448532161,3.1179053479291));
#65824=CARTESIAN_POINT('Ctrl Pts',(-2.76942977164678,0.992785344330023,
3.12294988681773));
#65825=CARTESIAN_POINT('Ctrl Pts',(-2.80093069510763,0.904911771492653,
3.12799755240015));
#65826=CARTESIAN_POINT('Ctrl Pts',(-2.82821581271975,0.815619563584813,
3.13304521798257));
#65827=CARTESIAN_POINT('Ctrl Pts',(-2.85118066671101,0.725350126334424,
3.13809288356499));
#65828=CARTESIAN_POINT('Ctrl Pts',(-2.87418178562652,0.634938140200193,
3.14314852016303));
#65829=CARTESIAN_POINT('Ctrl Pts',(-2.89284893382899,0.54354627806371,3.14820415676108));
#65830=CARTESIAN_POINT('Ctrl Pts',(-2.90712902926765,0.45162463084879,3.15325979335912));
#65831=CARTESIAN_POINT('Ctrl Pts',(-2.91337892824233,0.411393736654406,
3.15547246890643));
#65832=CARTESIAN_POINT('Ctrl Pts',(-2.91878915727341,0.371061406909721,
3.15768514445375));
#65833=CARTESIAN_POINT('Ctrl Pts',(-2.92335840566048,0.33066543825171,3.15989782000106));
#65834=CARTESIAN_POINT('Ctrl Pts',(-2.93569771046495,0.221575686958495,
3.16587317430417));
#65835=CARTESIAN_POINT('Ctrl Pts',(-2.94193221819642,0.111782666421697,
3.17184852860728));
#65836=CARTESIAN_POINT('Ctrl Pts',(-2.94199945032593,0.00179841093808543,
3.17782388291039));
#65837=CARTESIAN_POINT('',(-2.93753500859377,0.000882026442511374,4.17782388291039));
#65838=CARTESIAN_POINT('Ctrl Pts',(-2.94526019727207,0.00177566248466101,
3.1778252256184));
#65839=CARTESIAN_POINT('Ctrl Pts',(-2.9390358564779,-0.858556525610316,
3.22451438741265));
#65840=CARTESIAN_POINT('Ctrl Pts',(-2.08902058352625,-2.70002933468896,
3.32386851287358));
#65841=CARTESIAN_POINT('Ctrl Pts',(1.03253827306806,-3.31449993698517,3.47588760200119));
#65842=CARTESIAN_POINT('Ctrl Pts',(3.34012933187308,-0.946351485827778,
3.63388249300123));
#65843=CARTESIAN_POINT('Ctrl Pts',(2.61769689100761,2.28028683820626,3.79187738400129));
#65844=CARTESIAN_POINT('Ctrl Pts',(-0.479399010889303,3.43834577670272,
3.94987227500133));
#65845=CARTESIAN_POINT('Ctrl Pts',(-2.64712497717356,1.84153222841377,4.07852110797104));
#65846=CARTESIAN_POINT('Ctrl Pts',(-2.9387088904313,0.433468688742346,4.15450497727406));
#65847=CARTESIAN_POINT('Ctrl Pts',(-2.93753500859377,0.000882026442511374,
4.17782388291039));
#65848=CARTESIAN_POINT('',(-2.94199883948398,-0.00261313506862708,5.1778238829104));
#65849=CARTESIAN_POINT('Ctrl Pts',(-2.93753500859377,0.000882026442511374,
4.17782388291039));
#65850=CARTESIAN_POINT('Ctrl Pts',(-2.93605771780397,-0.543513730930775,
4.20716994094074));
#65851=CARTESIAN_POINT('Ctrl Pts',(-2.53067828075829,-2.06693687065717,
4.28918096263777));
#65852=CARTESIAN_POINT('Ctrl Pts',(-0.0865207644540764,-3.47052722867771,
4.42385694800151));
#65853=CARTESIAN_POINT('Ctrl Pts',(2.85932621153643,-1.96883181171988,4.58185183900155));
#65854=CARTESIAN_POINT('Ctrl Pts',(3.21131386544662,1.31890422107431,4.73984673000161));
#65855=CARTESIAN_POINT('Ctrl Pts',(0.650133944399006,3.41018634994862,4.89784162100167));
#65856=CARTESIAN_POINT('Ctrl Pts',(-2.26144874453696,2.48403434461044,5.04383398224286));
#65857=CARTESIAN_POINT('Ctrl Pts',(-2.93533655136359,0.748725030981945,
5.13716137981739));
#65858=CARTESIAN_POINT('Ctrl Pts',(-2.94214528694468,-0.00261198679238441,
5.17782381372523));
#65859=CARTESIAN_POINT('',(-2.94199954141428,0.00164265582640845,6.1778238829446));
#65860=CARTESIAN_POINT('Ctrl Pts',(-2.94199883948398,-0.00261313506862708,
5.1778238829104));
#65861=CARTESIAN_POINT('Ctrl Pts',(-2.94188759074597,-0.127862557515314,
5.18460279148083));
#65862=CARTESIAN_POINT('Ctrl Pts',(-2.93377434766609,-0.252765317972737,
5.19138170005127));
#65863=CARTESIAN_POINT('Ctrl Pts',(-2.91781295978548,-0.376472484662446,
5.1981606086217));
#65864=CARTESIAN_POINT('Ctrl Pts',(-2.90551365305103,-0.471797051657878,
5.20338420674839));
#65865=CARTESIAN_POINT('Ctrl Pts',(-2.88855531595855,-0.566412456081979,
5.20860780487509));
#65866=CARTESIAN_POINT('Ctrl Pts',(-2.86702688068737,-0.659940046834597,
5.21383140300178));
#65867=CARTESIAN_POINT('Ctrl Pts',(-2.84618931765164,-0.750466229687144,
5.2188873698599));
#65868=CARTESIAN_POINT('Ctrl Pts',(-2.82102328837992,-0.840164100998177,
5.22394333671802));
#65869=CARTESIAN_POINT('Ctrl Pts',(-2.79161000243732,-0.928589034122145,
5.22899930357613));
#65870=CARTESIAN_POINT('Ctrl Pts',(-2.76223681300493,-1.01689342541886,
5.23404837808543));
#65871=CARTESIAN_POINT('Ctrl Pts',(-2.72862801161075,-1.10392790968113,
5.23909745259473));
#65872=CARTESIAN_POINT('Ctrl Pts',(-2.69091556626771,-1.18925918756936,
5.24414652710403));
#65873=CARTESIAN_POINT('Ctrl Pts',(-2.65324292947538,-1.27450039135944,
5.24919027190487));
#65874=CARTESIAN_POINT('Ctrl Pts',(-2.61147543751921,-1.3580415590014,5.25423401670572));
#65875=CARTESIAN_POINT('Ctrl Pts',(-2.56579414172501,-1.4394667145473,5.25927776150656));
#65876=CARTESIAN_POINT('Ctrl Pts',(-2.52014509933188,-1.52083437964436,
5.2643179451579));
#65877=CARTESIAN_POINT('Ctrl Pts',(-2.47058796226295,-1.60008861664314,
5.26935812880924));
#65878=CARTESIAN_POINT('Ctrl Pts',(-2.41735050179949,-1.67683647129044,
5.27439831246058));
#65879=CARTESIAN_POINT('Ctrl Pts',(-2.36413185457447,-1.75355720451464,
5.27943671499434));
#65880=CARTESIAN_POINT('Ctrl Pts',(-2.3072357203883,-1.82777295105162,5.28447511752809));
#65881=CARTESIAN_POINT('Ctrl Pts',(-2.24693356617299,-1.89911915087103,
5.28951352006185));
#65882=CARTESIAN_POINT('Ctrl Pts',(-2.18663592529874,-1.97046001075298,
5.29455154549417));
#65883=CARTESIAN_POINT('Ctrl Pts',(-2.12293305777881,-2.0389314124613,5.29958957092649));
#65884=CARTESIAN_POINT('Ctrl Pts',(-2.05613641171031,-2.10420223753304,
5.30462759635881));
#65885=CARTESIAN_POINT('Ctrl Pts',(-1.98932615997853,-2.1694863574769,5.30966664797555));
#65886=CARTESIAN_POINT('Ctrl Pts',(-1.91942119555477,-2.23156829638511,
5.31470569959229));
#65887=CARTESIAN_POINT('Ctrl Pts',(-1.84676863898251,-2.29015492796245,
5.31974475120903));
#65888=CARTESIAN_POINT('Ctrl Pts',(-1.77403696239967,-2.34880536149155,
5.32478929044845));
#65889=CARTESIAN_POINT('Ctrl Pts',(-1.69855206703457,-2.40395261129819,
5.32983382968787));
#65890=CARTESIAN_POINT('Ctrl Pts',(-1.62069260613675,-2.45534508295956,
5.3348783689273));
#65891=CARTESIAN_POINT('Ctrl Pts',(-1.54278488655175,-2.50676940859455,
5.33992603486241));
#65892=CARTESIAN_POINT('Ctrl Pts',(-1.46250005228599,-2.55443409661416,
5.34497370079753));
#65893=CARTESIAN_POINT('Ctrl Pts',(-1.38024219047631,-2.59813307889129,
5.35002136673264));
#65894=CARTESIAN_POINT('Ctrl Pts',(-1.29785443126904,-2.64190106836056,
5.35507700368298));
#65895=CARTESIAN_POINT('Ctrl Pts',(-1.21348782552278,-2.68169066238758,
5.36013264063332));
#65896=CARTESIAN_POINT('Ctrl Pts',(-1.12756707099972,-2.71734364782909,
5.36518827758366));
#65897=CARTESIAN_POINT('Ctrl Pts',(-1.0899626184658,-2.73294768908979,5.36740094972305));
#65898=CARTESIAN_POINT('Ctrl Pts',(-1.05206067194799,-2.74776000585019,
5.36961362186243));
#65899=CARTESIAN_POINT('Ctrl Pts',(-1.01389764111355,-2.76177036940879,
5.37182629400181));
#65900=CARTESIAN_POINT('Ctrl Pts',(-0.926694925595327,-2.79378411991534,
5.37688226085996));
#65901=CARTESIAN_POINT('Ctrl Pts',(-0.837820763837992,-2.82172012748783,
5.38193822771812));
#65902=CARTESIAN_POINT('Ctrl Pts',(-0.747691909956341,-2.84540345255042,
5.38699419457627));
#65903=CARTESIAN_POINT('Ctrl Pts',(-0.657685920705157,-2.86905449224759,
5.3920432690856));
#65904=CARTESIAN_POINT('Ctrl Pts',(-0.566429063623805,-2.88846425828712,
5.39709234359494));
#65905=CARTESIAN_POINT('Ctrl Pts',(-0.474356341582972,-2.90350651130663,
5.40214141810427));
#65906=CARTESIAN_POINT('Ctrl Pts',(-0.382380809782441,-2.91853288600569,
5.40718516290515));
#65907=CARTESIAN_POINT('Ctrl Pts',(-0.289591560303666,-2.92920084066322,
5.41222890770603));
#65908=CARTESIAN_POINT('Ctrl Pts',(-0.196435907659241,-2.93543470957575,
5.41727265250691));
#65909=CARTESIAN_POINT('Ctrl Pts',(-0.103346027812463,-2.94166417704847,
5.42231283615829));
#65910=CARTESIAN_POINT('Ctrl Pts',(-0.00989070028221488,-2.94346575221075,
5.42735301980967));
#65911=CARTESIAN_POINT('Ctrl Pts',(0.0834765125543756,-2.94081547735518,
5.43239320346105));
#65912=CARTESIAN_POINT('Ctrl Pts',(0.17681073096138,-2.93816613906293,5.43743160599484));
#65913=CARTESIAN_POINT('Ctrl Pts',(0.270056453670778,-2.93106808891615,
5.44247000852863));
#65914=CARTESIAN_POINT('Ctrl Pts',(0.362760022533932,-2.91954947997995,
5.44750841106243));
#65915=CARTESIAN_POINT('Ctrl Pts',(0.455456652958058,-2.90803173315906,
5.45254643649479));
#65916=CARTESIAN_POINT('Ctrl Pts',(0.54761077017085,-2.89209414039802,5.45758446192715));
#65917=CARTESIAN_POINT('Ctrl Pts',(0.638774877130006,-2.87181661258994,
5.46262248735951));
#65918=CARTESIAN_POINT('Ctrl Pts',(0.729957553107359,-2.85153495449643,
5.46766153897628));
#65919=CARTESIAN_POINT('Ctrl Pts',(0.820149385565806,-2.82691170232326,
5.47270059059306));
#65920=CARTESIAN_POINT('Ctrl Pts',(0.908915204120345,-2.79807740273904,
5.47773964220984));
#65921=CARTESIAN_POINT('Ctrl Pts',(0.997777690333067,-2.76921170205628,
5.4827841814493));
#65922=CARTESIAN_POINT('Ctrl Pts',(1.08521064059338,-2.73612593777001,5.48782872068876));
#65923=CARTESIAN_POINT('Ctrl Pts',(1.17079643775542,-2.69899975941815,5.49287325992821));
#65924=CARTESIAN_POINT('Ctrl Pts',(1.25643528252616,-2.66185056959655,5.49792092586337));
#65925=CARTESIAN_POINT('Ctrl Pts',(1.34022429725,-2.62065617545347,5.50296859179852));
#65926=CARTESIAN_POINT('Ctrl Pts',(1.42177009591575,-2.57564240420904,5.50801625773367));
#65927=CARTESIAN_POINT('Ctrl Pts',(1.50344466752548,-2.53055754952514,5.51307189468405));
#65928=CARTESIAN_POINT('Ctrl Pts',(1.58286857494277,-2.48164151034904,5.51812753163443));
#65929=CARTESIAN_POINT('Ctrl Pts',(1.65967724912457,-2.42916352449527,5.52318316858481));
#65930=CARTESIAN_POINT('Ctrl Pts',(1.69329366878947,-2.40619578010415,5.52539584072383));
#65931=CARTESIAN_POINT('Ctrl Pts',(1.7264095679016,-2.38254626630141,5.52760851286286));
#65932=CARTESIAN_POINT('Ctrl Pts',(1.75899648480085,-2.35823988738598,5.52982118500188));
#65933=CARTESIAN_POINT('Ctrl Pts',(1.83345775221901,-2.30269969050315,5.53487715186005));
#65934=CARTESIAN_POINT('Ctrl Pts',(1.90541718082672,-2.24353147452815,5.53993311871821));
#65935=CARTESIAN_POINT('Ctrl Pts',(1.97450053359559,-2.18098868470947,5.54498908557638));
#65936=CARTESIAN_POINT('Ctrl Pts',(2.04348971118917,-2.11853115389977,5.55003816008572));
#65937=CARTESIAN_POINT('Ctrl Pts',(2.10961027830197,-2.05270848617203,5.55508723459507));
#65938=CARTESIAN_POINT('Ctrl Pts',(2.17251881333806,-1.98381602113003,5.56013630910441));
#65939=CARTESIAN_POINT('Ctrl Pts',(2.23536094330328,-1.9149962776833,5.56518005390531));
#65940=CARTESIAN_POINT('Ctrl Pts',(2.2949974833367,-1.84311350388941,5.5702237987062));
#65941=CARTESIAN_POINT('Ctrl Pts',(2.35112064047022,-1.76850098500253,5.5752675435071));
#65942=CARTESIAN_POINT('Ctrl Pts',(2.40720417169855,-1.69394114648414,5.58030772715849));
#65943=CARTESIAN_POINT('Ctrl Pts',(2.45977898499771,-1.61665574732327,5.58534791080988));
#65944=CARTESIAN_POINT('Ctrl Pts',(2.50857717942338,-1.53701155977313,5.59038809446127));
#65945=CARTESIAN_POINT('Ctrl Pts',(2.55735812937383,-1.45739551716226,5.59542649699508));
#65946=CARTESIAN_POINT('Ctrl Pts',(2.60236488050688,-1.37542272001601,5.60046489952889));
#65947=CARTESIAN_POINT('Ctrl Pts',(2.64337312286579,-1.29148849522974,5.6055033020627));
#65948=CARTESIAN_POINT('Ctrl Pts',(2.68437829594491,-1.20756055253713,5.61054132749507));
#65949=CARTESIAN_POINT('Ctrl Pts',(2.72138536090392,-1.12167187269252,5.61557935292745));
#65950=CARTESIAN_POINT('Ctrl Pts',(2.7542167220698,-1.03424090417616,5.62061737835982));
#65951=CARTESIAN_POINT('Ctrl Pts',(2.78705477058403,-0.946792127036474,
5.62565642997661));
#65952=CARTESIAN_POINT('Ctrl Pts',(2.81571527053406,-0.857800852562817,
5.6306954815934));
#65953=CARTESIAN_POINT('Ctrl Pts',(2.84006976978777,-0.767702873993343,
5.63573453321018));
#65954=CARTESIAN_POINT('Ctrl Pts',(2.86445079155261,-0.677506777018114,
5.64077907244966));
#65955=CARTESIAN_POINT('Ctrl Pts',(2.88451633694319,-0.586201999060682,
5.64582361168913));
#65956=CARTESIAN_POINT('Ctrl Pts',(2.90018866945859,-0.494236463187442,
5.6508681509286));
#65957=CARTESIAN_POINT('Ctrl Pts',(2.91587071596613,-0.402213925429321,
5.65591581686377));
#65958=CARTESIAN_POINT('Ctrl Pts',(2.92715407496732,-0.309530254230438,
5.66096348279894));
#65959=CARTESIAN_POINT('Ctrl Pts',(2.93401292466136,-0.21663831129351,5.66601114873411));
#65960=CARTESIAN_POINT('Ctrl Pts',(2.94088260549915,-0.123599678163332,
5.6710667856845));
#65961=CARTESIAN_POINT('Ctrl Pts',(2.94331381839724,-0.030352559376767,
5.6761224226349));
#65962=CARTESIAN_POINT('Ctrl Pts',(2.94133284458672,0.0626505974064284,
5.68117805958529));
#65963=CARTESIAN_POINT('Ctrl Pts',(2.94046584294056,0.103354765023912,5.68339073172417));
#65964=CARTESIAN_POINT('Ctrl Pts',(2.93875435719679,0.144012274704711,5.68560340386305));
#65965=CARTESIAN_POINT('Ctrl Pts',(2.93620369291188,0.184585681271942,5.68781607600193));
#65966=CARTESIAN_POINT('Ctrl Pts',(2.93037541231659,0.277296117364836,5.69287204286007));
#65967=CARTESIAN_POINT('Ctrl Pts',(2.92014156979324,0.369893663846107,5.69792800971822));
#65968=CARTESIAN_POINT('Ctrl Pts',(2.90550993734058,0.461926405410154,5.70298397657637));
#65969=CARTESIAN_POINT('Ctrl Pts',(2.89089825088787,0.553833686943376,5.7080330510857));
#65970=CARTESIAN_POINT('Ctrl Pts',(2.87190075726029,0.645177259338613,5.71308212559503));
#65971=CARTESIAN_POINT('Ctrl Pts',(2.8485771536256,0.735508123573278,5.71813120010435));
#65972=CARTESIAN_POINT('Ctrl Pts',(2.82527816994991,0.825743636240132,5.72317494490523));
#65973=CARTESIAN_POINT('Ctrl Pts',(2.79766226379785,0.914968138495921,5.7282186897061));
#65974=CARTESIAN_POINT('Ctrl Pts',(2.76584038045652,1.00274173635895,5.73326243450698));
#65975=CARTESIAN_POINT('Ctrl Pts',(2.734040965041,1.09045336143851,5.73830261815835));
#65976=CARTESIAN_POINT('Ctrl Pts',(2.69804162599648,1.17671570261467,5.74334280180973));
#65977=CARTESIAN_POINT('Ctrl Pts',(2.65800315217212,1.26110397788727,5.7483829854611));
#65978=CARTESIAN_POINT('Ctrl Pts',(2.61797882728254,1.34546243173839,5.75342138799489));
#65979=CARTESIAN_POINT('Ctrl Pts',(2.57391839335713,1.42794773516738,5.75845979052868));
#65980=CARTESIAN_POINT('Ctrl Pts',(2.52603037309879,1.50815601122112,5.76349819306247));
#65981=CARTESIAN_POINT('Ctrl Pts',(2.47814593704021,1.58835828405145,5.76853621849482));
#65982=CARTESIAN_POINT('Ctrl Pts',(2.42643471186556,1.66628348776118,5.77357424392717));
#65983=CARTESIAN_POINT('Ctrl Pts',(2.37115011052428,1.74155423497539,5.77861226935953));
#65984=CARTESIAN_POINT('Ctrl Pts',(2.3158542483831,1.81684031392396,5.7836513209763));
#65985=CARTESIAN_POINT('Ctrl Pts',(2.25698382729643,1.88947050537935,5.78869037259306));
#65986=CARTESIAN_POINT('Ctrl Pts',(2.19483363970474,1.95909910265419,5.79372942420983));
#65987=CARTESIAN_POINT('Ctrl Pts',(2.13261576938121,2.0288035267907,5.79877396344929));
#65988=CARTESIAN_POINT('Ctrl Pts',(2.06711129917795,2.09549950097959,5.80381850268874));
#65989=CARTESIAN_POINT('Ctrl Pts',(1.99865289249164,2.15887716541141,5.8088630419282));
#65990=CARTESIAN_POINT('Ctrl Pts',(1.93015205405978,2.22229411245381,5.81391070786334));
#65991=CARTESIAN_POINT('Ctrl Pts',(1.85869397318406,2.28238836987287,5.81895837379849));
#65992=CARTESIAN_POINT('Ctrl Pts',(1.78464381671532,2.33889085838988,5.82400603973364));
#65993=CARTESIAN_POINT('Ctrl Pts',(1.71047672403643,2.39548257273959,5.82906167668401));
#65994=CARTESIAN_POINT('Ctrl Pts',(1.63370974931247,2.44847094457545,5.83411731363439));
#65995=CARTESIAN_POINT('Ctrl Pts',(1.55473618283181,2.4976307576969,5.83917295058476));
#65996=CARTESIAN_POINT('Ctrl Pts',(1.5201722669513,2.51914625612443,5.84138562272384));
#65997=CARTESIAN_POINT('Ctrl Pts',(1.48518598354178,2.53992899536583,5.84359829486291));
#65998=CARTESIAN_POINT('Ctrl Pts',(1.44981159240075,2.55996295804068,5.84581096700198));
#65999=CARTESIAN_POINT('Ctrl Pts',(1.36898093245885,2.60574066253328,5.85086693386014));
#66000=CARTESIAN_POINT('Ctrl Pts',(1.28583752617665,2.64776697737243,5.8559229007183));
#66001=CARTESIAN_POINT('Ctrl Pts',(1.20076410415281,2.68580147557077,5.86097886757645));
#66002=CARTESIAN_POINT('Ctrl Pts',(1.11580665513994,2.72378412472892,5.86602794208578));
#66003=CARTESIAN_POINT('Ctrl Pts',(1.02892482029024,2.75778559168595,5.87107701659512));
#66004=CARTESIAN_POINT('Ctrl Pts',(0.940527260799538,2.78761053084769,5.87612609110445));
#66005=CARTESIAN_POINT('Ctrl Pts',(0.852223012116351,2.81740398736247,5.88116983590533));
#66006=CARTESIAN_POINT('Ctrl Pts',(0.76240663717098,2.8430295384218,5.88621358070622));
#66007=CARTESIAN_POINT('Ctrl Pts',(0.67150717465237,2.86433973445721,5.8912573255071));
#66008=CARTESIAN_POINT('Ctrl Pts',(0.580671891942362,2.88563488437172,5.89629750915848));
#66009=CARTESIAN_POINT('Ctrl Pts',(0.488755472276119,2.90262063465239,5.90133769280986));
#66010=CARTESIAN_POINT('Ctrl Pts',(0.396201533479985,2.91519953774491,5.90637787646124));
#66011=CARTESIAN_POINT('Ctrl Pts',(0.303680301715806,2.92777399566101,5.91141627899504));
#66012=CARTESIAN_POINT('Ctrl Pts',(0.210522437427181,2.93594464071984,5.91645468152884));
#66013=CARTESIAN_POINT('Ctrl Pts',(0.117180133035207,2.93966542593232,5.92149308406263));
#66014=CARTESIAN_POINT('Ctrl Pts',(0.0238448148887003,2.94338593266101,
5.92653110949499));
#66015=CARTESIAN_POINT('Ctrl Pts',(-0.0696744727827794,2.9426572244103,
5.93156913492736));
#66016=CARTESIAN_POINT('Ctrl Pts',(-0.162923193874212,2.93748532471191,
5.93660716035972));
#66017=CARTESIAN_POINT('Ctrl Pts',(-0.256190908594257,2.93231237156055,
5.94164621197649));
#66018=CARTESIAN_POINT('Ctrl Pts',(-0.349187504554182,2.92269445444429,
5.94668526359326));
#66019=CARTESIAN_POINT('Ctrl Pts',(-0.441462367924965,2.90868956365338,
5.95172431521004));
#66020=CARTESIAN_POINT('Ctrl Pts',(-0.533837720370289,2.89466942127105,
5.9567688544495));
#66021=CARTESIAN_POINT('Ctrl Pts',(-0.625489332350595,2.87625283605432,
5.96181339368896));
#66022=CARTESIAN_POINT('Ctrl Pts',(-0.715975918679006,2.85354910311208,
5.96685793292842));
#66023=CARTESIAN_POINT('Ctrl Pts',(-0.806518590212959,2.83083129798986,
5.97190559886357));
#66024=CARTESIAN_POINT('Ctrl Pts',(-0.895894374358191,2.80382118311333,
5.97695326479873));
#66025=CARTESIAN_POINT('Ctrl Pts',(-0.98367837947304,2.77267755892338,5.98200093073389));
#66026=CARTESIAN_POINT('Ctrl Pts',(-1.07160100858761,2.741484754319,5.98705656768427));
#66027=CARTESIAN_POINT('Ctrl Pts',(-1.15792643126154,2.70614557834843,5.99211220463465));
#66028=CARTESIAN_POINT('Ctrl Pts',(-1.24225112439828,2.66686635284396,5.99716784158503));
#66029=CARTESIAN_POINT('Ctrl Pts',(-1.27915703773121,2.6496752355291,5.99938051372403));
#66030=CARTESIAN_POINT('Ctrl Pts',(-1.31568004813735,2.63172998579684,6.00159318586303));
#66031=CARTESIAN_POINT('Ctrl Pts',(-1.35178802061164,2.61305054435058,6.00380585800203));
#66032=CARTESIAN_POINT('Ctrl Pts',(-1.43429491755644,2.57036792761018,6.00886182486019));
#66033=CARTESIAN_POINT('Ctrl Pts',(-1.51492371998122,2.52369852257086,6.01391779171835));
#66034=CARTESIAN_POINT('Ctrl Pts',(-1.59326393563444,2.47323149571702,6.01897375857651));
#66035=CARTESIAN_POINT('Ctrl Pts',(-1.67149735705655,2.42283326606121,6.02402283308584));
#66036=CARTESIAN_POINT('Ctrl Pts',(-1.74744802186249,2.36864794057893,6.02907190759518));
#66037=CARTESIAN_POINT('Ctrl Pts',(-1.82072902491203,2.3109110363324,6.03412098210451));
#66038=CARTESIAN_POINT('Ctrl Pts',(-1.89393267390775,2.25323507808023,6.0391647269054));
#66039=CARTESIAN_POINT('Ctrl Pts',(-1.96447191621663,2.19201526617343,6.04420847170628));
#66040=CARTESIAN_POINT('Ctrl Pts',(-2.03198882542798,2.12753035544403,6.04925221650716));
#66041=CARTESIAN_POINT('Ctrl Pts',(-2.09945806414508,2.06309097445825,6.05429240015855));
#66042=CARTESIAN_POINT('Ctrl Pts',(-2.16390889160784,1.99539138246366,6.05933258380993));
#66043=CARTESIAN_POINT('Ctrl Pts',(-2.2250172922672,1.92474986663513,6.06437276746131));
#66044=CARTESIAN_POINT('Ctrl Pts',(-2.28610409822795,1.85413331435052,6.06941116999511));
#66045=CARTESIAN_POINT('Ctrl Pts',(-2.34385053420923,1.78057723879614,6.07444957252891));
#66046=CARTESIAN_POINT('Ctrl Pts',(-2.3979709478345,1.70443519482018,6.07948797506271));
#66047=CARTESIAN_POINT('Ctrl Pts',(-2.4520873107938,1.62829884972871,6.08452600049507));
#66048=CARTESIAN_POINT('Ctrl Pts',(-2.50257793434589,1.54957728269897,6.08956402592744));
#66049=CARTESIAN_POINT('Ctrl Pts',(-2.54919949508346,1.46865446387713,6.0946020513598));
#66050=CARTESIAN_POINT('Ctrl Pts',(-2.59583055206506,1.38771516206282,6.09964110297658));
#66051=CARTESIAN_POINT('Ctrl Pts',(-2.63859076000742,1.30457410237197,6.10468015459335));
#66052=CARTESIAN_POINT('Ctrl Pts',(-2.67728246142404,1.21964036574363,6.10971920621013));
#66053=CARTESIAN_POINT('Ctrl Pts',(-2.7160162988366,1.13461413466683,6.11476374544959));
#66054=CARTESIAN_POINT('Ctrl Pts',(-2.75067260205668,1.04779173411973,6.11980828468905));
#66055=CARTESIAN_POINT('Ctrl Pts',(-2.78110177929019,0.959602466247833,
6.12485282392852));
#66056=CARTESIAN_POINT('Ctrl Pts',(-2.81154981707233,0.871358537089423,
6.12990048986368));
#66057=CARTESIAN_POINT('Ctrl Pts',(-2.83776538832204,0.781746479188209,
6.13494815579885));
#66058=CARTESIAN_POINT('Ctrl Pts',(-2.85964932026176,0.691208915687925,
6.13999582173401));
#66059=CARTESIAN_POINT('Ctrl Pts',(-2.88156781018467,0.60052837990977,6.14505145868439));
#66060=CARTESIAN_POINT('Ctrl Pts',(-2.89914092304114,0.50891985594691,6.15010709563478));
#66061=CARTESIAN_POINT('Ctrl Pts',(-2.91232096194462,0.416834037259401,
6.15516273258516));
#66062=CARTESIAN_POINT('Ctrl Pts',(-2.9180893953109,0.376531355835743,6.15737540472414));
#66063=CARTESIAN_POINT('Ctrl Pts',(-2.92301700857039,0.336137285669298,
6.15958807686312));
#66064=CARTESIAN_POINT('Ctrl Pts',(-2.92710294302251,0.295689636187929,
6.1618007490021));
#66065=CARTESIAN_POINT('Ctrl Pts',(-2.93696575003513,0.198055333527562,
6.1671417936382));
#66066=CARTESIAN_POINT('Ctrl Pts',(-2.94194466883354,0.0999195090394462,
6.1724828382743));
#66067=CARTESIAN_POINT('Ctrl Pts',(-2.94199954141393,0.00164265645566952,
6.1778238829104));
#66068=CARTESIAN_POINT('',(-2.94171674527821,0.00106055427202949,7.17782383379665));
#66069=CARTESIAN_POINT('Ctrl Pts',(-2.94199954141428,0.00164265582640454,
6.1778238829446));
#66070=CARTESIAN_POINT('Ctrl Pts',(-2.94205080717708,-0.0901744176067026,
6.18281385845425));
#66071=CARTESIAN_POINT('Ctrl Pts',(-2.93779956711471,-0.182160903610382,
6.18780383396389));
#66072=CARTESIAN_POINT('Ctrl Pts',(-2.92922461152939,-0.273874378521423,
6.19279380947354));
#66073=CARTESIAN_POINT('Ctrl Pts',(-2.92066024317377,-0.365474617670936,
6.19777762401636));
#66074=CARTESIAN_POINT('Ctrl Pts',(-2.90778280444553,-0.456802064969237,
6.20276143855917));
#66075=CARTESIAN_POINT('Ctrl Pts',(-2.89062311501965,-0.547413926488978,
6.20774525310199));
#66076=CARTESIAN_POINT('Ctrl Pts',(-2.87347918866651,-0.637942550991512,
6.2127244894599));
#66077=CARTESIAN_POINT('Ctrl Pts',(-2.85206091248782,-0.727756450041725,
6.21770372581781));
#66078=CARTESIAN_POINT('Ctrl Pts',(-2.82645082215898,-0.816418856909155,
6.22268296217572));
#66079=CARTESIAN_POINT('Ctrl Pts',(-2.80085303484738,-0.905038670599187,
6.22765980652212));
#66080=CARTESIAN_POINT('Ctrl Pts',(-2.77106755726666,-0.992507653228784,
6.23263665086852));
#66081=CARTESIAN_POINT('Ctrl Pts',(-2.73722757790628,-1.07840121789125,
6.23761349521492));
#66082=CARTESIAN_POINT('Ctrl Pts',(-2.70339385391829,-1.16427890499577,
6.24258941958397));
#66083=CARTESIAN_POINT('Ctrl Pts',(-2.66550728414514,-1.24858132879256,
6.24756534395302));
#66084=CARTESIAN_POINT('Ctrl Pts',(-2.62374984100905,-1.33090223976256,
6.25254126832206));
#66085=CARTESIAN_POINT('Ctrl Pts',(-2.58198777541944,-1.41323226346925,
6.25751774351456));
#66086=CARTESIAN_POINT('Ctrl Pts',(-2.53635419345989,-1.4935799332287,6.26249421870706));
#66087=CARTESIAN_POINT('Ctrl Pts',(-2.48707721678308,-1.57156320832429,
6.26747069389957));
#66088=CARTESIAN_POINT('Ctrl Pts',(-2.43775032743971,-1.64962547270593,
6.27245220976549));
#66089=CARTESIAN_POINT('Ctrl Pts',(-2.3847729219904,-1.72531817690721,6.27743372563142));
#66090=CARTESIAN_POINT('Ctrl Pts',(-2.32841641952734,-1.79828834653274,
6.28241524149735));
#66091=CARTESIAN_POINT('Ctrl Pts',(-2.27202793949408,-1.87129992058581,
6.28739958395412));
#66092=CARTESIAN_POINT('Ctrl Pts',(-2.21225684298608,-1.94158553997426,
6.29238392641088));
#66093=CARTESIAN_POINT('Ctrl Pts',(-2.14941328097355,-2.00882715721749,
6.29736826886764));
#66094=CARTESIAN_POINT('Ctrl Pts',(-2.08647035740677,-2.07617508975199,
6.3023604920364));
#66095=CARTESIAN_POINT('Ctrl Pts',(-2.02044559977181,-2.1404690982592,6.30735271520517));
#66096=CARTESIAN_POINT('Ctrl Pts',(-1.95168397390846,-2.20142991393977,
6.31234493837394));
#66097=CARTESIAN_POINT('Ctrl Pts',(-1.91747594404155,-2.23175714046081,
6.31482850558334));
#66098=CARTESIAN_POINT('Ctrl Pts',(-1.88259104094524,-2.26126007576763,
6.31731207279274));
#66099=CARTESIAN_POINT('Ctrl Pts',(-1.84707437066062,-2.28990835389731,
6.31979564000214));
#66100=CARTESIAN_POINT('Ctrl Pts',(-1.77477066686261,-2.34822960416126,
6.3248516068603));
#66101=CARTESIAN_POINT('Ctrl Pts',(-1.69957457315796,-2.40322582802012,
6.32990757371846));
#66102=CARTESIAN_POINT('Ctrl Pts',(-1.62182459324367,-2.45459752072514,
6.33496354057661));
#66103=CARTESIAN_POINT('Ctrl Pts',(-1.54418060294483,-2.50589918298178,
6.34001261508594));
#66104=CARTESIAN_POINT('Ctrl Pts',(-1.46399001186172,-2.55358589060345,
6.34506168959526));
#66105=CARTESIAN_POINT('Ctrl Pts',(-1.38162424483441,-2.59739839956941,
6.35011076410459));
#66106=CARTESIAN_POINT('Ctrl Pts',(-1.29934542156755,-2.64116466087179,
6.35515450890547));
#66107=CARTESIAN_POINT('Ctrl Pts',(-1.21489637590213,-2.68106464535286,
6.36019825370634));
#66108=CARTESIAN_POINT('Ctrl Pts',(-1.12867643276995,-2.71688305050286,
6.36524199850721));
#66109=CARTESIAN_POINT('Ctrl Pts',(-1.042517365459,-2.75267616597218,6.3702821821586));
#66110=CARTESIAN_POINT('Ctrl Pts',(-0.954590294430732,-2.78439326068864,
6.37532236580998));
#66111=CARTESIAN_POINT('Ctrl Pts',(-0.86531706635547,-2.81186599514877,
6.38036254946136));
#66112=CARTESIAN_POINT('Ctrl Pts',(-0.776075385963216,-2.83932902119869,
6.38540095199516));
#66113=CARTESIAN_POINT('Ctrl Pts',(-0.685488917094498,-2.86255053659711,
6.39043935452896));
#66114=CARTESIAN_POINT('Ctrl Pts',(-0.593996331243704,-2.88141152188802,
6.39547775706276));
#66115=CARTESIAN_POINT('Ctrl Pts',(-0.5025105931954,-2.90027109552025,6.40051578249512));
#66116=CARTESIAN_POINT('Ctrl Pts',(-0.41011930741132,-2.91477069873775,
6.40555380792748));
#66117=CARTESIAN_POINT('Ctrl Pts',(-0.317271931378721,-2.92484230712687,
6.41059183335985));
#66118=CARTESIAN_POINT('Ctrl Pts',(-0.224405643466573,-2.93491596697994,
6.41563088497663));
#66119=CARTESIAN_POINT('Ctrl Pts',(-0.131083521679968,-2.94055979325709,
6.4206699365934));
#66120=CARTESIAN_POINT('Ctrl Pts',(-0.0377596101771619,-2.94175767388126,
6.42570898821018));
#66121=CARTESIAN_POINT('Ctrl Pts',(0.0556659328334915,-2.94295685902013,
6.43075352744964));
#66122=CARTESIAN_POINT('Ctrl Pts',(0.149092825385948,-2.9397004288215,6.43579806668911));
#66123=CARTESIAN_POINT('Ctrl Pts',(0.242067878670679,-2.93202441021828,
6.44084260592857));
#66124=CARTESIAN_POINT('Ctrl Pts',(0.335100559557109,-2.92434363388138,
6.44589027186372));
#66125=CARTESIAN_POINT('Ctrl Pts',(0.427680404283645,-2.912237872955,6.45093793779887));
#66126=CARTESIAN_POINT('Ctrl Pts',(0.519362342953723,-2.8957946675691,6.45598560373402));
#66127=CARTESIAN_POINT('Ctrl Pts',(0.61118906104042,-2.87932549591637,6.4610412406844));
#66128=CARTESIAN_POINT('Ctrl Pts',(0.70211461107622,-2.8585053059846,6.46609687763478));
#66129=CARTESIAN_POINT('Ctrl Pts',(0.791707273613052,-2.83347200319823,
6.47115251458516));
#66130=CARTESIAN_POINT('Ctrl Pts',(0.830918789432085,-2.82251581861328,
6.47336518672417));
#66131=CARTESIAN_POINT('Ctrl Pts',(0.869875227929949,-2.81075324335716,
6.47557785886319));
#66132=CARTESIAN_POINT('Ctrl Pts',(0.908541637458077,-2.79819872292963,
6.4777905310022));
#66133=CARTESIAN_POINT('Ctrl Pts',(0.996894575813124,-2.76951158122324,
6.48284649786035));
#66134=CARTESIAN_POINT('Ctrl Pts',(1.08404323289694,-2.73658516757626,6.4879024647185));
#66135=CARTESIAN_POINT('Ctrl Pts',(1.16955180473061,-2.69953932663545,6.49295843157666));
#66136=CARTESIAN_POINT('Ctrl Pts',(1.25494381035219,-2.66254398698661,6.49800750608598));
#66137=CARTESIAN_POINT('Ctrl Pts',(1.33869977024762,-2.62144055447741,6.5030565805953));
#66138=CARTESIAN_POINT('Ctrl Pts',(1.42039961040886,-2.57639844487423,6.50810565510463));
#66139=CARTESIAN_POINT('Ctrl Pts',(1.50201320975003,-2.53140388087777,6.51314939990553));
#66140=CARTESIAN_POINT('Ctrl Pts',(1.58157461725397,-2.48247911709228,6.51819314470643));
#66141=CARTESIAN_POINT('Ctrl Pts',(1.65868531518699,-2.4298409464784,6.52323688950733));
#66142=CARTESIAN_POINT('Ctrl Pts',(1.73574156890529,-2.37723994118581,6.52827707315871));
#66143=CARTESIAN_POINT('Ctrl Pts',(1.81035018721417,-2.32093098993557,6.53331725681009));
#66144=CARTESIAN_POINT('Ctrl Pts',(1.88213967803469,-2.26117540946461,6.53835744046147));
#66145=CARTESIAN_POINT('Ctrl Pts',(1.95390379963586,-2.20144094562801,6.54339584299526));
#66146=CARTESIAN_POINT('Ctrl Pts',(2.02285043250667,-2.13826255584747,6.54843424552905));
#66147=CARTESIAN_POINT('Ctrl Pts',(2.0886401971847,-2.07194259734778,6.55347264806285));
#66148=CARTESIAN_POINT('Ctrl Pts',(2.15442503779919,-2.00562760259421,6.55851067349521));
#66149=CARTESIAN_POINT('Ctrl Pts',(2.21705316792122,-1.93617182169925,6.56354869892758));
#66150=CARTESIAN_POINT('Ctrl Pts',(2.27622202327628,-1.86391451004386,6.56858672435995));
#66151=CARTESIAN_POINT('Ctrl Pts',(2.33540293060655,-1.79164248045412,6.57362577597674));
#66152=CARTESIAN_POINT('Ctrl Pts',(2.39112288311124,-1.71656813008922,6.57866482759353));
#66153=CARTESIAN_POINT('Ctrl Pts',(2.44312028738842,-1.63906292171812,6.58370387921032));
#66154=CARTESIAN_POINT('Ctrl Pts',(2.49517431782387,-1.56147330870688,6.58874841844977));
#66155=CARTESIAN_POINT('Ctrl Pts',(2.54349746104888,-1.48144792261921,6.59379295768923));
#66156=CARTESIAN_POINT('Ctrl Pts',(2.5878722580105,-1.39938599972261,6.59883749692869));
#66157=CARTESIAN_POINT('Ctrl Pts',(2.63227455926544,-1.31727321337756,6.60388516286385));
#66158=CARTESIAN_POINT('Ctrl Pts',(2.67272345017241,-1.23312177654122,6.608932828799));
#66159=CARTESIAN_POINT('Ctrl Pts',(2.70904905086834,-1.14735227371081,6.61398049473416));
#66160=CARTESIAN_POINT('Ctrl Pts',(2.74543201509027,-1.0614473280794,6.61903613168454));
#66161=CARTESIAN_POINT('Ctrl Pts',(2.77767853846176,-0.973919631385354,
6.62409176863493));
#66162=CARTESIAN_POINT('Ctrl Pts',(2.80566821755118,-0.885206107651309,
6.62914740558531));
#66163=CARTESIAN_POINT('Ctrl Pts',(2.81791830269533,-0.846379359559351,
6.63136007772429));
#66164=CARTESIAN_POINT('Ctrl Pts',(2.82935364752133,-0.807325612418335,
6.63357274986326));
#66165=CARTESIAN_POINT('Ctrl Pts',(2.83996725196405,-0.768082031928714,
6.63578542200224));
#66166=CARTESIAN_POINT('Ctrl Pts',(2.86421939097853,-0.678410255050615,
6.6408413888604));
#66167=CARTESIAN_POINT('Ctrl Pts',(2.88426305037514,-0.58743064818646,6.64589735571855));
#66168=CARTESIAN_POINT('Ctrl Pts',(2.89996046875691,-0.495573687403992,
6.6509533225767));
#66169=CARTESIAN_POINT('Ctrl Pts',(2.91563648824782,-0.403841947026036,
6.65600239708604));
#66170=CARTESIAN_POINT('Ctrl Pts',(2.92697796671261,-0.311235662961098,
6.66105147159537));
#66171=CARTESIAN_POINT('Ctrl Pts',(2.93389725427756,-0.218199223973404,
6.66610054610471));
#66172=CARTESIAN_POINT('Ctrl Pts',(2.94080923797221,-0.125260992507357,
6.6711442909056));
#66173=CARTESIAN_POINT('Ctrl Pts',(2.94330827688525,-0.0318939486430189,
6.6761880357065));
#66174=CARTESIAN_POINT('Ctrl Pts',(2.94135817884662,0.0614496845566321,
6.68123178050739));
#66175=CARTESIAN_POINT('Ctrl Pts',(2.93940945767992,0.154727412234268,6.68627196415877));
#66176=CARTESIAN_POINT('Ctrl Pts',(2.93301785288524,0.247981319954036,6.69131214781015));
#66177=CARTESIAN_POINT('Ctrl Pts',(2.92219922881418,0.340757490185938,6.69635233146153));
#66178=CARTESIAN_POINT('Ctrl Pts',(2.91138442786602,0.433500874852939,6.70139073399533));
#66179=CARTESIAN_POINT('Ctrl Pts',(2.89614576711634,0.525766417381258,6.70642913652912));
#66180=CARTESIAN_POINT('Ctrl Pts',(2.87655102977172,0.617104669500464,6.71146753906292));
#66181=CARTESIAN_POINT('Ctrl Pts',(2.8569577590038,0.708436085368164,6.71650556449527));
#66182=CARTESIAN_POINT('Ctrl Pts',(2.83300915322888,0.798839915285311,6.72154358992762));
#66183=CARTESIAN_POINT('Ctrl Pts',(2.80482401484709,0.88787738215198,6.72658161535997));
#66184=CARTESIAN_POINT('Ctrl Pts',(2.77663313549592,0.976932984866134,6.73162066697673));
#66185=CARTESIAN_POINT('Ctrl Pts',(2.74420414387257,1.06462124914391,6.7366597185935));
#66186=CARTESIAN_POINT('Ctrl Pts',(2.70770520375747,1.15052011262069,6.74169877021026));
#66187=CARTESIAN_POINT('Ctrl Pts',(2.67116651560502,1.23651252158737,6.74674330944972));
#66188=CARTESIAN_POINT('Ctrl Pts',(2.63054920594053,1.32071123146603,6.75178784868917));
#66189=CARTESIAN_POINT('Ctrl Pts',(2.58606881508641,1.40271596684346,6.75683238792862));
#66190=CARTESIAN_POINT('Ctrl Pts',(2.54156085448992,1.48477153022361,6.76188005386379));
#66191=CARTESIAN_POINT('Ctrl Pts',(2.4931852753493,1.56463003283944,6.76692771979894));
#66192=CARTESIAN_POINT('Ctrl Pts',(2.44120149563302,1.64191938222287,6.77197538573411));
#66193=CARTESIAN_POINT('Ctrl Pts',(2.38913562579732,1.71933078298377,6.77703102268449));
#66194=CARTESIAN_POINT('Ctrl Pts',(2.33345044580327,1.79416457673464,6.78208665963487));
#66195=CARTESIAN_POINT('Ctrl Pts',(2.27444609311608,1.86608117977462,6.78714229658525));
#66196=CARTESIAN_POINT('Ctrl Pts',(2.24862199052466,1.89755651422624,6.78935496872427));
#66197=CARTESIAN_POINT('Ctrl Pts',(2.22216258243794,1.92847353220668,6.79156764086329));
#66198=CARTESIAN_POINT('Ctrl Pts',(2.19509517053609,1.95880606296007,6.79378031300231));
#66199=CARTESIAN_POINT('Ctrl Pts',(2.13324599952761,2.02811604680667,6.79883627986046));
#66200=CARTESIAN_POINT('Ctrl Pts',(2.06800190455703,2.09461601085653,6.80389224671861));
#66201=CARTESIAN_POINT('Ctrl Pts',(1.99964813809884,2.15795535723004,6.80894821357677));
#66202=CARTESIAN_POINT('Ctrl Pts',(1.93138755223598,2.22120835872003,6.8139972880861));
#66203=CARTESIAN_POINT('Ctrl Pts',(1.86002604160601,2.281309005827,6.81904636259542));
#66204=CARTESIAN_POINT('Ctrl Pts',(1.78588789271304,2.33794106740546,6.82409543710475));
#66205=CARTESIAN_POINT('Ctrl Pts',(1.71182800266095,2.3945133492408,6.82913918190564));
#66206=CARTESIAN_POINT('Ctrl Pts',(1.63499765099952,2.44762405568488,6.83418292670652));
#66207=CARTESIAN_POINT('Ctrl Pts',(1.55575580312215,2.49699577113213,6.8392266715074));
#66208=CARTESIAN_POINT('Ctrl Pts',(1.4765699041633,2.54633262754772,6.84426685515878));
#66209=CARTESIAN_POINT('Ctrl Pts',(1.39497626872466,2.59193550654423,6.84930703881016));
#66210=CARTESIAN_POINT('Ctrl Pts',(1.31136372612226,2.63356966450685,6.85434722246154));
#66211=CARTESIAN_POINT('Ctrl Pts',(1.22778073081025,2.67518910964629,6.85938562499534));
#66212=CARTESIAN_POINT('Ctrl Pts',(1.14218064238477,2.71284242266176,6.86442402752913));
#66213=CARTESIAN_POINT('Ctrl Pts',(1.05497691667472,2.74634078462297,6.86946243006293));
#66214=CARTESIAN_POINT('Ctrl Pts',(0.967779717765627,2.77983663938464,6.87450045549528));
#66215=CARTESIAN_POINT('Ctrl Pts',(0.878979534310409,2.8091780026896,6.87953848092764));
#66216=CARTESIAN_POINT('Ctrl Pts',(0.7890087628912,2.83422461567197,6.88457650636));
#66217=CARTESIAN_POINT('Ctrl Pts',(0.699019665521892,2.85927633034428,6.88961555797676));
#66218=CARTESIAN_POINT('Ctrl Pts',(0.607859933921857,2.88003143873615,6.89465460959352));
#66219=CARTESIAN_POINT('Ctrl Pts',(0.515974938013121,2.89640015594226,6.89969366121029));
#66220=CARTESIAN_POINT('Ctrl Pts',(0.423989877602615,2.9127866989916,6.90473820044975));
#66221=CARTESIAN_POINT('Ctrl Pts',(0.331278413621512,2.92477723843429,6.90978273968921));
#66222=CARTESIAN_POINT('Ctrl Pts',(0.23829355673967,2.93233357256918,6.91482727892868));
#66223=CARTESIAN_POINT('Ctrl Pts',(0.145251066179789,2.93989459025518,6.91987494486382));
#66224=CARTESIAN_POINT('Ctrl Pts',(0.051935288190086,2.94301591615171,6.92492261079897));
#66225=CARTESIAN_POINT('Ctrl Pts',(-0.041200394394593,2.94171149630648,
6.92997027673411));
#66226=CARTESIAN_POINT('Ctrl Pts',(-0.134483152073845,2.94040501658832,
6.93502591368449));
#66227=CARTESIAN_POINT('Ctrl Pts',(-0.22758480473242,2.93465886741266,6.94008155063487));
#66228=CARTESIAN_POINT('Ctrl Pts',(-0.320056945971786,2.9245388613139,6.94513718758525));
#66229=CARTESIAN_POINT('Ctrl Pts',(-0.360528707011103,2.92010969526393,
6.94734985972429));
#66230=CARTESIAN_POINT('Ctrl Pts',(-0.400880016554807,2.91484337821709,
6.94956253186332));
#66231=CARTESIAN_POINT('Ctrl Pts',(-0.441074038102379,2.9087484753605,6.95177520400236));
#66232=CARTESIAN_POINT('Ctrl Pts',(-0.532917577529378,2.89482159197687,
6.95683117086051));
#66233=CARTESIAN_POINT('Ctrl Pts',(-0.624262754404763,2.87651596964992,
6.96188713771867));
#66234=CARTESIAN_POINT('Ctrl Pts',(-0.714660071314614,2.85387893619694,
6.96694310457682));
#66235=CARTESIAN_POINT('Ctrl Pts',(-0.80493415762276,2.8312727617932,6.97199217908619));
#66236=CARTESIAN_POINT('Ctrl Pts',(-0.894262525166504,2.80434701697255,
6.97704125359555));
#66237=CARTESIAN_POINT('Ctrl Pts',(-0.982203130010084,2.77320049967513,
6.98209032810491));
#66238=CARTESIAN_POINT('Ctrl Pts',(-1.07005090639836,2.74208686005798,6.98713407290579));
#66239=CARTESIAN_POINT('Ctrl Pts',(-1.15651341609533,2.70676145146423,6.99217781770668));
#66240=CARTESIAN_POINT('Ctrl Pts',(-1.24116217430607,2.66737332540307,6.99722156250756));
#66241=CARTESIAN_POINT('Ctrl Pts',(-1.32575116603479,2.62801300943361,7.00226174615894));
#66242=CARTESIAN_POINT('Ctrl Pts',(-1.40852855080163,2.58459586434057,7.00730192981032));
#66243=CARTESIAN_POINT('Ctrl Pts',(-1.48908526377058,2.53731926986363,7.01234211346171));
#66244=CARTESIAN_POINT('Ctrl Pts',(-1.56961350932878,2.49005938215369,7.0173805159955));
#66245=CARTESIAN_POINT('Ctrl Pts',(-1.64792226009275,2.43894297898139,7.02241891852929));
#66246=CARTESIAN_POINT('Ctrl Pts',(-1.72362745718247,2.38421315927219,7.02745732106309));
#66247=CARTESIAN_POINT('Ctrl Pts',(-1.79932698808367,2.32948743584025,7.03249534649545));
#66248=CARTESIAN_POINT('Ctrl Pts',(-1.87242299355824,2.27114909368057,7.03753337192781));
#66249=CARTESIAN_POINT('Ctrl Pts',(-1.94256173466028,2.20948362904857,7.04257139736016));
#66250=CARTESIAN_POINT('Ctrl Pts',(-2.01271476216936,2.14780560391272,7.04761044897692));
#66251=CARTESIAN_POINT('Ctrl Pts',(-2.07990899620287,2.08279940342091,7.05264950059368));
#66252=CARTESIAN_POINT('Ctrl Pts',(-2.14382588137846,2.01478896918061,7.05768855221044));
#66253=CARTESIAN_POINT('Ctrl Pts',(-2.20781237325329,1.94670447028857,7.0627330914499));
#66254=CARTESIAN_POINT('Ctrl Pts',(-2.26851408828369,1.87560953107339,7.06777763068936));
#66255=CARTESIAN_POINT('Ctrl Pts',(-2.32565149749558,1.80186267850704,7.07282216992883));
#66256=CARTESIAN_POINT('Ctrl Pts',(-2.38282432149591,1.72807011632212,7.07786983586396));
#66257=CARTESIAN_POINT('Ctrl Pts',(-2.43642818706021,1.65162273118897,7.08291750179909));
#66258=CARTESIAN_POINT('Ctrl Pts',(-2.48622703614279,1.57290785640883,7.08796516773422));
#66259=CARTESIAN_POINT('Ctrl Pts',(-2.53610452501461,1.49406867913423,7.0930208046846));
#66260=CARTESIAN_POINT('Ctrl Pts',(-2.58216478447112,1.41295524956243,7.09807644163498));
#66261=CARTESIAN_POINT('Ctrl Pts',(-2.62421791442431,1.32997907412655,7.10313207858535));
#66262=CARTESIAN_POINT('Ctrl Pts',(-2.64262307087035,1.29366335893743,7.10534475072438));
#66263=CARTESIAN_POINT('Ctrl Pts',(-2.66026128731189,1.25699108606173,7.1075574228634));
#66264=CARTESIAN_POINT('Ctrl Pts',(-2.67711960893711,1.21999778665553,7.10977009500242));
#66265=CARTESIAN_POINT('Ctrl Pts',(-2.72032798952284,1.12518285813541,7.11544123961691));
#66266=CARTESIAN_POINT('Ctrl Pts',(-2.75854574650834,1.02795888196169,7.1211123842314));
#66267=CARTESIAN_POINT('Ctrl Pts',(-2.79152320776205,0.928849923575334,
7.12678352884589));
#66268=CARTESIAN_POINT('Ctrl Pts',(-2.82342445984176,0.832975355168836,
7.13226959742272));
#66269=CARTESIAN_POINT('Ctrl Pts',(-2.85042193779947,0.735337238862226,
7.13775566599955));
#66270=CARTESIAN_POINT('Ctrl Pts',(-2.872336278233,0.636434053729535,7.14324173457637));
#66271=CARTESIAN_POINT('Ctrl Pts',(-2.89419608233716,0.537777000425265,
7.14871415044739));
#66272=CARTESIAN_POINT('Ctrl Pts',(-2.91099787708547,0.437861453721849,
7.15418656631841));
#66273=CARTESIAN_POINT('Ctrl Pts',(-2.92261169191948,0.337201569177166,
7.15965898218943));
#66274=CARTESIAN_POINT('Ctrl Pts',(-2.93418480596277,0.236894448728771,
7.1651122198958));
#66275=CARTESIAN_POINT('Ctrl Pts',(-2.94060613122474,0.135848499407986,
7.17056545760217));
#66276=CARTESIAN_POINT('Ctrl Pts',(-2.94179668125678,0.03458736975534,7.17601869530855));
#66277=CARTESIAN_POINT('Ctrl Pts',(-2.94192804686186,0.0234141899564756,
7.1766204069978));
#66278=CARTESIAN_POINT('Ctrl Pts',(-2.94199577873787,0.0122384025922069,
7.17722211868706));
#66279=CARTESIAN_POINT('Ctrl Pts',(-2.94199980878204,0.00106071977267785,
7.17782383037631));
#66280=CARTESIAN_POINT('',(-2.94179645842688,-0.00262223567938445,8.17782388291039));
#66281=CARTESIAN_POINT('Ctrl Pts',(-2.93765213932985,0.00105817779144944,
7.17782388291039));
#66282=CARTESIAN_POINT('Ctrl Pts',(-2.93583728528984,-0.555049110608679,
7.20780425060775));
#66283=CARTESIAN_POINT('Ctrl Pts',(-2.51737468444769,-2.09057369894412,
7.2904495819718));
#66284=CARTESIAN_POINT('Ctrl Pts',(-0.0450203642769795,-3.47131362076717,
7.42575987700252));
#66285=CARTESIAN_POINT('Ctrl Pts',(2.88266152300012,-1.93450449230245,7.58375476800256));
#66286=CARTESIAN_POINT('Ctrl Pts',(3.19531528460893,1.35720496568047,7.74174965900263));
#66287=CARTESIAN_POINT('Ctrl Pts',(0.609314704401834,3.41771571051832,7.89974455000268));
#66288=CARTESIAN_POINT('Ctrl Pts',(-2.27838582827551,2.4609932925897,8.04510262463861));
#66289=CARTESIAN_POINT('Ctrl Pts',(-2.93514585523751,0.737219387421443,
8.13779573560784));
#66290=CARTESIAN_POINT('Ctrl Pts',(-2.94179645842688,-0.00262223567938445,
8.17782388291039));
#66291=CARTESIAN_POINT('',(-2.94199962980641,0.00147587903620585,9.1778238829104));
#66292=CARTESIAN_POINT('Ctrl Pts',(-2.94179645842688,-0.00262223567938445,
8.17782388291039));
#66293=CARTESIAN_POINT('Ctrl Pts',(-2.94389604226671,-0.236188947098698,
8.19046069927452));
#66294=CARTESIAN_POINT('Ctrl Pts',(-2.81210260417286,-1.44082338645902,
8.25576247930533));
#66295=CARTESIAN_POINT('Ctrl Pts',(-1.15736505241686,-3.2730033947992,8.37372922300285));
#66296=CARTESIAN_POINT('Ctrl Pts',(2.10876587186763,-2.75774393020281,8.53172411400289));
#66297=CARTESIAN_POINT('Ctrl Pts',(3.46191394284634,0.259223724318882,8.68971900500295));
#66298=CARTESIAN_POINT('Ctrl Pts',(1.67456068997757,3.0410346236939,8.84771389600301));
#66299=CARTESIAN_POINT('Ctrl Pts',(-1.63188291307294,3.06414804553308,9.00570878700305));
#66300=CARTESIAN_POINT('Ctrl Pts',(-2.90366142307977,1.14432815538467,9.11574544930552));
#66301=CARTESIAN_POINT('Ctrl Pts',(-2.94630689264378,0.0881682471389342,
9.1731171479413));
#66302=CARTESIAN_POINT('Ctrl Pts',(-2.94577110767244,0.00147777103002609,
9.1778238829104));
#66303=CARTESIAN_POINT('',(-2.94199974257833,0.00123071890407352,10.177823882882));
#66304=CARTESIAN_POINT('Ctrl Pts',(-2.94199962980641,0.00147587903620585,
9.1778238829104));
#66305=CARTESIAN_POINT('Ctrl Pts',(-2.94204572414441,-0.090408023372339,
9.1828189994887));
#66306=CARTESIAN_POINT('Ctrl Pts',(-2.93778304636917,-0.182462980810345,
9.18781411606701));
#66307=CARTESIAN_POINT('Ctrl Pts',(-2.92918984160053,-0.274246006104506,
9.19280923264531));
#66308=CARTESIAN_POINT('Ctrl Pts',(-2.92060748250135,-0.365913190058677,
9.19779804477902));
#66309=CARTESIAN_POINT('Ctrl Pts',(-2.9077054945994,-0.457308674286831,
9.20278685691273));
#66310=CARTESIAN_POINT('Ctrl Pts',(-2.89051414762716,-0.547989016648372,
9.20777566904644));
#66311=CARTESIAN_POINT('Ctrl Pts',(-2.873339267682,-0.638582499285849,9.21275970256072));
#66312=CARTESIAN_POINT('Ctrl Pts',(-2.85188327766594,-0.728461756432582,
9.217743736075));
#66313=CARTESIAN_POINT('Ctrl Pts',(-2.82622816886955,-0.817189291099845,
9.22272776958929));
#66314=CARTESIAN_POINT('Ctrl Pts',(-2.80058607711949,-0.905871806646775,
9.2277092742741));
#66315=CARTESIAN_POINT('Ctrl Pts',(-2.77074922233177,-0.993403323725543,
9.23269077895892));
#66316=CARTESIAN_POINT('Ctrl Pts',(-2.73685027191682,-1.07935841549916,
9.23767228364374));
#66317=CARTESIAN_POINT('Ctrl Pts',(-2.70295853881579,-1.16529520685717,
9.24265272773279));
#66318=CARTESIAN_POINT('Ctrl Pts',(-2.66500659490321,-1.24965581662519,
9.24763317182184));
#66319=CARTESIAN_POINT('Ctrl Pts',(-2.62317593448274,-1.33203303891104,
9.25261361591089));
#66320=CARTESIAN_POINT('Ctrl Pts',(-2.58134186177172,-1.41441698102908,
9.25759446627424));
#66321=CARTESIAN_POINT('Ctrl Pts',(-2.53562865177555,-1.49481680959483,
9.2625753166376));
#66322=CARTESIAN_POINT('Ctrl Pts',(-2.48626401269523,-1.57284940766006,
9.26755616700095));
#66323=CARTESIAN_POINT('Ctrl Pts',(-2.43685013110183,-1.65095984527407,
9.27254198589226));
#66324=CARTESIAN_POINT('Ctrl Pts',(-2.38377779299346,-1.72669795348462,
9.27752780478357));
#66325=CARTESIAN_POINT('Ctrl Pts',(-2.32731810365292,-1.79970954445693,
9.28251362367488));
#66326=CARTESIAN_POINT('Ctrl Pts',(-2.2708279617166,-1.87276051560461,9.28750213176142));
#66327=CARTESIAN_POINT('Ctrl Pts',(-2.21094712780141,-1.94308169708971,
9.29249063984796));
#66328=CARTESIAN_POINT('Ctrl Pts',(-2.14798555653675,-2.01035371238733,
9.2974791479345));
#66329=CARTESIAN_POINT('Ctrl Pts',(-2.08492219063923,-2.07773449133175,
9.30247572131133));
#66330=CARTESIAN_POINT('Ctrl Pts',(-2.01876847020445,-2.14205594622441,
9.30747229468816));
#66331=CARTESIAN_POINT('Ctrl Pts',(-1.94986937444732,-2.20303731756692,
9.31246886806499));
#66332=CARTESIAN_POINT('Ctrl Pts',(-1.90744576391868,-2.24058570508794,
9.31554543504438));
#66333=CARTESIAN_POINT('Ctrl Pts',(-1.86398193743162,-2.27686857571756,
9.31862200202377));
#66334=CARTESIAN_POINT('Ctrl Pts',(-1.81956381119789,-2.3118286132365,9.32169856900316));
#66335=CARTESIAN_POINT('Ctrl Pts',(-1.74656797667083,-2.36928121941724,
9.32675453586132));
#66336=CARTESIAN_POINT('Ctrl Pts',(-1.67071971356128,-2.42337445495032,
9.33181050271948));
#66337=CARTESIAN_POINT('Ctrl Pts',(-1.5923610823007,-2.47381288370284,9.33686646957763));
#66338=CARTESIAN_POINT('Ctrl Pts',(-1.51410927037554,-2.5241825542426,9.34191554408697));
#66339=CARTESIAN_POINT('Ctrl Pts',(-1.43335426070549,-2.57090708094193,
9.3469646185963));
#66340=CARTESIAN_POINT('Ctrl Pts',(-1.35047055114782,-2.613731679129,9.35201369310564));
#66341=CARTESIAN_POINT('Ctrl Pts',(-1.26767433208128,-2.65651107247247,
9.35705743790651));
#66342=CARTESIAN_POINT('Ctrl Pts',(-1.18275427160391,-2.6953985177973,9.36210118270738));
#66343=CARTESIAN_POINT('Ctrl Pts',(-1.09611224029828,-2.73018350238007,
9.36714492750825));
#66344=CARTESIAN_POINT('Ctrl Pts',(-1.00953138283035,-2.76494392693152,
9.37218511115963));
#66345=CARTESIAN_POINT('Ctrl Pts',(-0.921231381617468,-2.79560748351997,
9.37722529481101));
#66346=CARTESIAN_POINT('Ctrl Pts',(-0.831636065873206,-2.82201088834521,
9.38226547846238));
#66347=CARTESIAN_POINT('Ctrl Pts',(-0.74207241163243,-2.84840496264367,
9.38730388099618));
#66348=CARTESIAN_POINT('Ctrl Pts',(-0.651214777262631,-2.87054175094294,
9.39234228352997));
#66349=CARTESIAN_POINT('Ctrl Pts',(-0.559503225919944,-2.88830748712549,
9.39738068606376));
#66350=CARTESIAN_POINT('Ctrl Pts',(-0.467798538768296,-2.90607189362377,
9.40241871149612));
#66351=CARTESIAN_POINT('Ctrl Pts',(-0.37524049715759,-2.91946581446411,
9.40745673692848));
#66352=CARTESIAN_POINT('Ctrl Pts',(-0.282279339760464,-2.92842660388551,
9.41249476236084));
#66353=CARTESIAN_POINT('Ctrl Pts',(-0.189299247307974,-2.93738921851055,
9.41753381397761));
#66354=CARTESIAN_POINT('Ctrl Pts',(-0.0959163174091777,-2.9419168661658,
9.42257286559438));
#66355=CARTESIAN_POINT('Ctrl Pts',(-0.00258475440709994,-2.9419988645553,
9.42761191721115));
#66356=CARTESIAN_POINT('Ctrl Pts',(0.0908484484355715,-2.94208095224259,
9.43265645645062));
#66357=CARTESIAN_POINT('Ctrl Pts',(0.184229728626193,-2.93770772693357,
9.43770099569008));
#66358=CARTESIAN_POINT('Ctrl Pts',(0.277106360492218,-2.92892063138876,
9.44274553492954));
#66359=CARTESIAN_POINT('Ctrl Pts',(0.370040558956836,-2.92012808944488,
9.4477932008647));
#66360=CARTESIAN_POINT('Ctrl Pts',(0.462469047758238,-2.90691629338502,
9.45284086679987));
#66361=CARTESIAN_POINT('Ctrl Pts',(0.553947835457103,-2.88937809841363,
9.45788853273503));
#66362=CARTESIAN_POINT('Ctrl Pts',(0.645571081766846,-2.87181220802404,
9.46294416968541));
#66363=CARTESIAN_POINT('Ctrl Pts',(0.736241202921866,-2.8499063848746,9.4679998066358));
#66364=CARTESIAN_POINT('Ctrl Pts',(0.825528159153147,-2.823803686244,9.47305544358618));
#66365=CARTESIAN_POINT('Ctrl Pts',(0.864605878215817,-2.81237946520524,
9.47526811572519));
#66366=CARTESIAN_POINT('Ctrl Pts',(0.903418896845142,-2.80015196088214,
9.4774807878642));
#66367=CARTESIAN_POINT('Ctrl Pts',(0.941932438603662,-2.78713603562979,
9.47969346000321));
#66368=CARTESIAN_POINT('Ctrl Pts',(1.02993607334383,-2.7573945816006,9.48474942686136));
#66369=CARTESIAN_POINT('Ctrl Pts',(1.11668482743304,-2.72342855723606,9.48980539371952));
#66370=CARTESIAN_POINT('Ctrl Pts',(1.20174436092563,-2.68536300916346,9.49486136057767));
#66371=CARTESIAN_POINT('Ctrl Pts',(1.28668794034038,-2.64734935245851,9.49991043508701));
#66372=CARTESIAN_POINT('Ctrl Pts',(1.36994647391018,-2.60524745737157,9.50495950959635));
#66373=CARTESIAN_POINT('Ctrl Pts',(1.45110194321668,-2.55923175003609,9.5100085841057));
#66374=CARTESIAN_POINT('Ctrl Pts',(1.53217174633044,-2.51326461601905,9.51505232890659));
#66375=CARTESIAN_POINT('Ctrl Pts',(1.61114251415322,-2.46339209948992,9.52009607370749));
#66376=CARTESIAN_POINT('Ctrl Pts',(1.68761834945002,-2.40983574265957,9.52513981850839));
#66377=CARTESIAN_POINT('Ctrl Pts',(1.76404018877863,-2.3563171994383,9.53018000215977));
#66378=CARTESIAN_POINT('Ctrl Pts',(1.83797023481414,-2.29912023964101,9.53522018581115));
#66379=CARTESIAN_POINT('Ctrl Pts',(1.90904014637848,-2.23851060294903,9.54026036946253));
#66380=CARTESIAN_POINT('Ctrl Pts',(1.98008494301095,-2.1779223847007,9.54529877199633));
#66381=CARTESIAN_POINT('Ctrl Pts',(2.04827127613392,-2.11392417304796,9.55033717453013));
#66382=CARTESIAN_POINT('Ctrl Pts',(2.11326340557759,-2.04682236128263,9.55537557706393));
#66383=CARTESIAN_POINT('Ctrl Pts',(2.17825067065679,-1.97972557178187,9.56041360249628));
#66384=CARTESIAN_POINT('Ctrl Pts',(2.24004389910237,-1.90952596280487,9.56545162792863));
#66385=CARTESIAN_POINT('Ctrl Pts',(2.29834460446165,-1.83656638299355,9.57048965336099));
#66386=CARTESIAN_POINT('Ctrl Pts',(2.35665718496453,-1.76359194220445,9.57552870497775));
#66387=CARTESIAN_POINT('Ctrl Pts',(2.41147555299702,-1.68785676070982,9.58056775659452));
#66388=CARTESIAN_POINT('Ctrl Pts',(2.46254257512752,-1.60973540238275,9.58560680821129));
#66389=CARTESIAN_POINT('Ctrl Pts',(2.51366521021272,-1.53152896841622,9.59065134745075));
#66390=CARTESIAN_POINT('Ctrl Pts',(2.5610281022436,-1.45093154260062,9.59569588669021));
#66391=CARTESIAN_POINT('Ctrl Pts',(2.6044185810476,-1.36834493264454,9.60074042592966));
#66392=CARTESIAN_POINT('Ctrl Pts',(2.64783595404679,-1.28570713402981,9.60578809186481));
#66393=CARTESIAN_POINT('Ctrl Pts',(2.68727582482498,-1.2010780982904,9.61083575779996));
#66394=CARTESIAN_POINT('Ctrl Pts',(2.72257335424169,-1.11488041097381,9.61588342373511));
#66395=CARTESIAN_POINT('Ctrl Pts',(2.75792662370707,-1.02854660468899,9.62093906068549));
#66396=CARTESIAN_POINT('Ctrl Pts',(2.78912434609606,-0.940639619324569,
9.62599469763587));
#66397=CARTESIAN_POINT('Ctrl Pts',(2.81605135052136,-0.851597787236908,
9.63105033458626));
#66398=CARTESIAN_POINT('Ctrl Pts',(2.82783634083285,-0.812627350277191,
9.63326300672526));
#66399=CARTESIAN_POINT('Ctrl Pts',(2.83880393502246,-0.773439671668044,
9.63547567886426));
#66400=CARTESIAN_POINT('Ctrl Pts',(2.84894757788484,-0.734071998147376,
9.63768835100327));
#66401=CARTESIAN_POINT('Ctrl Pts',(2.87212585234727,-0.644116668076289,
9.64274431786142));
#66402=CARTESIAN_POINT('Ctrl Pts',(2.89108031136519,-0.552903918800198,
9.64780028471957));
#66403=CARTESIAN_POINT('Ctrl Pts',(2.90567835023381,-0.460865842716244,
9.65285625157773));
#66404=CARTESIAN_POINT('Ctrl Pts',(2.92025648889761,-0.368953233935213,
9.65790532608706));
#66405=CARTESIAN_POINT('Ctrl Pts',(2.93048994016416,-0.276217968489724,
9.66295440059639));
#66406=CARTESIAN_POINT('Ctrl Pts',(2.93629637361263,-0.183105451337015,
9.66800347510572));
#66407=CARTESIAN_POINT('Ctrl Pts',(2.94209667789873,-0.0900912220130057,
9.67304721990659));
#66408=CARTESIAN_POINT('Ctrl Pts',(2.94347922587559,0.00329902713788016,
9.67809096470747));
#66409=CARTESIAN_POINT('Ctrl Pts',(2.94041323481618,0.0966126726567079,
9.68313470950834));
#66410=CARTESIAN_POINT('Ctrl Pts',(2.93734940850794,0.18986043382687,9.68817489315972));
#66411=CARTESIAN_POINT('Ctrl Pts',(2.9298433009337,0.283031256866857,9.6932150768111));
#66412=CARTESIAN_POINT('Ctrl Pts',(2.91791620242656,0.37567144636848,9.69825526046248));
#66413=CARTESIAN_POINT('Ctrl Pts',(2.90599331875885,0.468278898358642,9.70329366299628));
#66414=CARTESIAN_POINT('Ctrl Pts',(2.88965260465848,0.560355649942324,9.70833206553008));
#66415=CARTESIAN_POINT('Ctrl Pts',(2.86896721216729,0.651453095402149,9.71337046806389));
#66416=CARTESIAN_POINT('Ctrl Pts',(2.84828336788339,0.742543722633653,9.71840849349624));
#66417=CARTESIAN_POINT('Ctrl Pts',(2.82325559027714,0.832654757087544,9.72344651892859));
#66418=CARTESIAN_POINT('Ctrl Pts',(2.79400791935088,0.921348873448373,9.72848454436094));
#66419=CARTESIAN_POINT('Ctrl Pts',(2.7647542910301,1.01006105572096,9.73352359597774));
#66420=CARTESIAN_POINT('Ctrl Pts',(2.73127920149873,1.09735532569753,9.73856264759454));
#66421=CARTESIAN_POINT('Ctrl Pts',(2.6937558487669,1.18281166177633,9.74360169921134));
#66422=CARTESIAN_POINT('Ctrl Pts',(2.65619163239318,1.26836106142387,9.7486462384508));
#66423=CARTESIAN_POINT('Ctrl Pts',(2.61457053180976,1.35206812549773,9.75369077769027));
#66424=CARTESIAN_POINT('Ctrl Pts',(2.56911285769389,1.43353518423231,9.75873531692973));
#66425=CARTESIAN_POINT('Ctrl Pts',(2.52362700809808,1.51505273770784,9.76378298286489));
#66426=CARTESIAN_POINT('Ctrl Pts',(2.47430008483955,1.59432714555223,9.76883064880005));
#66427=CARTESIAN_POINT('Ctrl Pts',(2.42139593614525,1.67098944353914,9.77387831473521));
#66428=CARTESIAN_POINT('Ctrl Pts',(2.36840824393209,1.74777280269605,9.77893395168559));
#66429=CARTESIAN_POINT('Ctrl Pts',(2.31183231856937,1.82193546599406,9.78398958863597));
#66430=CARTESIAN_POINT('Ctrl Pts',(2.2519723361899,1.89314146249968,9.78904522558635));
#66431=CARTESIAN_POINT('Ctrl Pts',(2.22577375497221,1.92430578979287,9.79125789772534));
#66432=CARTESIAN_POINT('Ctrl Pts',(2.19894658899634,1.95490424470108,9.79347056986433));
#66433=CARTESIAN_POINT('Ctrl Pts',(2.17151845089302,1.98491098476259,9.79568324200333));
#66434=CARTESIAN_POINT('Ctrl Pts',(2.10884501871682,2.05347653525637,9.80073920886148));
#66435=CARTESIAN_POINT('Ctrl Pts',(2.04281050231568,2.1191916765165,9.80579517571964));
#66436=CARTESIAN_POINT('Ctrl Pts',(1.97370432558301,2.1817092462505,9.81085114257779));
#66437=CARTESIAN_POINT('Ctrl Pts',(1.90469235513961,2.24414159135571,9.81590021708712));
#66438=CARTESIAN_POINT('Ctrl Pts',(1.83261737166266,2.30338473221478,9.82094929159644));
#66439=CARTESIAN_POINT('Ctrl Pts',(1.7578074193906,2.35912633751043,9.82599836610577));
#66440=CARTESIAN_POINT('Ctrl Pts',(1.68307643510208,2.41480910301223,9.83104211090667));
#66441=CARTESIAN_POINT('Ctrl Pts',(1.6056165744162,2.46699741643588,9.83608585570757));
#66442=CARTESIAN_POINT('Ctrl Pts',(1.52579009389671,2.51541817385632,9.84112960050847));
#66443=CARTESIAN_POINT('Ctrl Pts',(1.44601997507753,2.56380474367134,9.84616978415985));
#66444=CARTESIAN_POINT('Ctrl Pts',(1.36388693594899,2.60842881565462,9.85120996781123));
#66445=CARTESIAN_POINT('Ctrl Pts',(1.27978258466925,2.64906031187991,9.85625015146261));
#66446=CARTESIAN_POINT('Ctrl Pts',(1.19570795447693,2.68967744960611,9.86128855399641));
#66447=CARTESIAN_POINT('Ctrl Pts',(1.1096637951006,2.72630462198829,9.86632695653021));
#66448=CARTESIAN_POINT('Ctrl Pts',(1.0220657903677,2.75875796694093,9.871365359064));
#66449=CARTESIAN_POINT('Ctrl Pts',(0.934474341945591,2.79120888290884,9.87640338449637));
#66450=CARTESIAN_POINT('Ctrl Pts',(0.845329695363665,2.81948643881613,9.88144140992873));
#66451=CARTESIAN_POINT('Ctrl Pts',(0.755065893256345,2.84345555562963,9.8864794353611));
#66452=CARTESIAN_POINT('Ctrl Pts',(0.664783705512163,2.86742955466022,9.89151848697787));
#66453=CARTESIAN_POINT('Ctrl Pts',(0.57338233816931,2.88709325821866,9.89655753859464));
#66454=CARTESIAN_POINT('Ctrl Pts',(0.481308202799502,2.90236221273602,9.90159659021141));
#66455=CARTESIAN_POINT('Ctrl Pts',(0.389133796951625,2.91764779543416,9.90664112945088));
#66456=CARTESIAN_POINT('Ctrl Pts',(0.296285598824076,2.92852900373624,9.91168566869033));
#66457=CARTESIAN_POINT('Ctrl Pts',(0.203217043452678,2.93497305494452,9.9167302079298));
#66458=CARTESIAN_POINT('Ctrl Pts',(0.110090802525321,2.94142110029105,9.92177787386495));
#66459=CARTESIAN_POINT('Ctrl Pts',(0.0167443754147969,2.94342650371529,
9.9268255398001));
#66460=CARTESIAN_POINT('Ctrl Pts',(-0.076369054192065,2.9410086309907,9.93187320573525));
#66461=CARTESIAN_POINT('Ctrl Pts',(-0.169629523752704,2.93858694008548,
9.93692884268563));
#66462=CARTESIAN_POINT('Ctrl Pts',(-0.262655819791868,2.93172806238203,
9.94198447963601));
#66463=CARTESIAN_POINT('Ctrl Pts',(-0.355000354827928,2.92050316693409,
9.94704011658639));
#66464=CARTESIAN_POINT('Ctrl Pts',(-0.395416267178388,2.91559043018805,
9.94925278872538));
#66465=CARTESIAN_POINT('Ctrl Pts',(-0.435701727522635,2.90984204242133,
9.95146546086437));
#66466=CARTESIAN_POINT('Ctrl Pts',(-0.475820004399961,2.90326700863231,
9.95367813300336));
#66467=CARTESIAN_POINT('Ctrl Pts',(-0.567490466880002,2.88824302367643,
9.95873409986152));
#66468=CARTESIAN_POINT('Ctrl Pts',(-0.658610249480061,2.86884657126655,
9.96379006671967));
#66469=CARTESIAN_POINT('Ctrl Pts',(-0.748730452774665,2.84513035010487,
9.96884603357783));
#66470=CARTESIAN_POINT('Ctrl Pts',(-0.838727803231509,2.82144645915288,
9.97389510808717));
#66471=CARTESIAN_POINT('Ctrl Pts',(-0.927727857000532,2.79345461371134,
9.97894418259651));
#66472=CARTESIAN_POINT('Ctrl Pts',(-1.01528978298722,2.76125888981127,9.98399325710585));
#66473=CARTESIAN_POINT('Ctrl Pts',(-1.1027592802453,2.72909715111417,9.98903700190674));
#66474=CARTESIAN_POINT('Ctrl Pts',(-1.18879325319887,2.69274050697242,9.99408074670762));
#66475=CARTESIAN_POINT('Ctrl Pts',(-1.27296502976534,2.65234312127872,9.9991244915085));
#66476=CARTESIAN_POINT('Ctrl Pts',(-1.35707737662388,2.61197425826721,10.0041646751599));
#66477=CARTESIAN_POINT('Ctrl Pts',(-1.43932974186841,2.56757051598641,10.0092048588113));
#66478=CARTESIAN_POINT('Ctrl Pts',(-1.51931544980777,2.51933415091675,10.0142450424626));
#66479=CARTESIAN_POINT('Ctrl Pts',(-1.59927289212015,2.47111483178113,10.0192834449964));
#66480=CARTESIAN_POINT('Ctrl Pts',(-1.67696488912535,2.41906580949601,10.0243218475302));
#66481=CARTESIAN_POINT('Ctrl Pts',(-1.75201031592716,2.36343475748429,10.029360250064));
#66482=CARTESIAN_POINT('Ctrl Pts',(-1.82705012592134,2.30780786920286,10.0343982754964));
#66483=CARTESIAN_POINT('Ctrl Pts',(-1.89944340349649,2.2485997486092,10.0394363009288));
#66484=CARTESIAN_POINT('Ctrl Pts',(-1.96883984843305,2.18610010091535,10.0444743263611));
#66485=CARTESIAN_POINT('Ctrl Pts',(-2.03825042858016,2.12358772280455,10.0495133779779));
#66486=CARTESIAN_POINT('Ctrl Pts',(-2.10466263450646,2.05778278306738,10.0545524295947));
#66487=CARTESIAN_POINT('Ctrl Pts',(-2.16776180670031,1.98901300885927,10.0595914812115));
#66488=CARTESIAN_POINT('Ctrl Pts',(-2.23092969508812,1.92016834306418,10.0646360204509));
#66489=CARTESIAN_POINT('Ctrl Pts',(-2.29077704808106,1.84835272547744,10.0696805596904));
#66490=CARTESIAN_POINT('Ctrl Pts',(-2.34702864329479,1.77392799954052,10.0747250989298));
#66491=CARTESIAN_POINT('Ctrl Pts',(-2.40331510425386,1.69945714382662,10.079772764865));
#66492=CARTESIAN_POINT('Ctrl Pts',(-2.45600112036106,1.62237432600091,10.0848204308001));
#66493=CARTESIAN_POINT('Ctrl Pts',(-2.50485528146661,1.54306967402927,10.0898680967353));
#66494=CARTESIAN_POINT('Ctrl Pts',(-2.55378659055836,1.46363978821765,10.0949237336857));
#66495=CARTESIAN_POINT('Ctrl Pts',(-2.59887375173245,1.38198145211319,10.0999793706361));
#66496=CARTESIAN_POINT('Ctrl Pts',(-2.63993179851563,1.29850841321343,10.1050350075864));
#66497=CARTESIAN_POINT('Ctrl Pts',(-2.65790144251704,1.26197523859199,10.1072476797254));
#66498=CARTESIAN_POINT('Ctrl Pts',(-2.67509993826843,1.22509470143544,10.1094603518644));
#66499=CARTESIAN_POINT('Ctrl Pts',(-2.69151475670051,1.18790248525012,10.1116730240034));
#66500=CARTESIAN_POINT('Ctrl Pts',(-2.73261802804903,1.09477189350805,10.117213631334));
#66501=CARTESIAN_POINT('Ctrl Pts',(-2.7689288940169,0.999403769174305,10.1227542386645));
#66502=CARTESIAN_POINT('Ctrl Pts',(-2.80022210883355,0.902286063950788,
10.1282948459951));
#66503=CARTESIAN_POINT('Ctrl Pts',(-2.83143484581624,0.805418119661116,
10.1338212043557));
#66504=CARTESIAN_POINT('Ctrl Pts',(-2.85765555046733,0.706809841115378,
10.1393475627163));
#66505=CARTESIAN_POINT('Ctrl Pts',(-2.87870681400129,0.606968762806256,
10.1448739210769));
#66506=CARTESIAN_POINT('Ctrl Pts',(-2.89966358194114,0.507575854365658,
10.150375472541));
#66507=CARTESIAN_POINT('Ctrl Pts',(-2.91549709249138,0.406961465818858,
10.1558770240051));
#66508=CARTESIAN_POINT('Ctrl Pts',(-2.92608011603149,0.305645472018067,
10.1613785754692));
#66509=CARTESIAN_POINT('Ctrl Pts',(-2.93662508542849,0.204693787463402,
10.1668603446068));
#66510=CARTESIAN_POINT('Ctrl Pts',(-2.94195715053947,0.103045818157862,
10.1723421137444));
#66511=CARTESIAN_POINT('Ctrl Pts',(-2.94199974257833,0.0012307189040667,
10.177823882882));
#66512=CARTESIAN_POINT('',(-2.94199883612238,-0.00261691699413304,11.1778238829104));
#66513=CARTESIAN_POINT('Ctrl Pts',(-2.94199974257855,0.00123071837608816,
10.1778238829104));
#66514=CARTESIAN_POINT('Ctrl Pts',(-2.9420396062843,-0.0940624163727975,
10.1829545066481));
#66515=CARTESIAN_POINT('Ctrl Pts',(-2.93744522033648,-0.189336333036378,
10.1880851303858));
#66516=CARTESIAN_POINT('Ctrl Pts',(-2.92824851849128,-0.284120773534126,
10.1932157541235));
#66517=CARTESIAN_POINT('Ctrl Pts',(-2.91904744884976,-0.378950230075376,
10.1983488145521));
#66518=CARTESIAN_POINT('Ctrl Pts',(-2.9052397544149,-0.473289329612877,
10.2034818749807));
#66519=CARTESIAN_POINT('Ctrl Pts',(-2.88690905912501,-0.566674584167986,
10.2086149354093));
#66520=CARTESIAN_POINT('Ctrl Pts',(-2.86855028875814,-0.660202866478942,
10.2137558575728));
#66521=CARTESIAN_POINT('Ctrl Pts',(-2.84565476095613,-0.752773972174129,
10.2188967797363));
#66522=CARTESIAN_POINT('Ctrl Pts',(-2.81835699241197,-0.843935935555881,
10.2240377018997));
#66523=CARTESIAN_POINT('Ctrl Pts',(-2.7910382169181,-0.935168052465979,
10.2291825802508));
#66524=CARTESIAN_POINT('Ctrl Pts',(-2.75931058979704,-1.02498846973067,
10.2343274586019));
#66525=CARTESIAN_POINT('Ctrl Pts',(-2.72335740126719,-1.11296382015015,
10.2394723369529));
#66526=CARTESIAN_POINT('Ctrl Pts',(-2.68732964970811,-1.20112162194304,
10.2446278852259));
#66527=CARTESIAN_POINT('Ctrl Pts',(-2.64705899886438,-1.28742632684711,
10.2497834334989));
#66528=CARTESIAN_POINT('Ctrl Pts',(-2.60277572787018,-1.37146728375482,
10.2549389817719));
#66529=CARTESIAN_POINT('Ctrl Pts',(-2.56060463327417,-1.45149974441383,
10.2598486261824));
#66530=CARTESIAN_POINT('Ctrl Pts',(-2.51479509137513,-1.52947919320769,
10.2647582705929));
#66531=CARTESIAN_POINT('Ctrl Pts',(-2.46558161295246,-1.60507673021285,
10.2696679150034));
#66532=CARTESIAN_POINT('Ctrl Pts',(-2.41490142207189,-1.68292730546819,
10.2747238818616));
#66533=CARTESIAN_POINT('Ctrl Pts',(-2.36044109596539,-1.75851242323328,
10.2797798487197));
#66534=CARTESIAN_POINT('Ctrl Pts',(-2.30242970610783,-1.83144245021027,
10.2848358155779));
#66535=CARTESIAN_POINT('Ctrl Pts',(-2.2444973980057,-1.90427305818402,10.2898848900872));
#66536=CARTESIAN_POINT('Ctrl Pts',(-2.18302391981014,-1.97445542392243,
10.2949339645966));
#66537=CARTESIAN_POINT('Ctrl Pts',(-2.11828211666327,-2.04162799604251,
10.2999830391059));
#66538=CARTESIAN_POINT('Ctrl Pts',(-2.05360865375081,-2.108729662054,10.3050267839068));
#66539=CARTESIAN_POINT('Ctrl Pts',(-1.98567402978589,-2.17282753208236,
10.3100705287077));
#66540=CARTESIAN_POINT('Ctrl Pts',(-1.91479122975435,-2.23359319180011,
10.3151142735086));
#66541=CARTESIAN_POINT('Ctrl Pts',(-1.84395847671322,-2.29431594776142,
10.32015445716));
#66542=CARTESIAN_POINT('Ctrl Pts',(-1.77018202094336,-2.35171088212786,
10.3251946408114));
#66543=CARTESIAN_POINT('Ctrl Pts',(-1.69381080949119,-2.40548725659705,
10.3302348244628));
#66544=CARTESIAN_POINT('Ctrl Pts',(-1.61746658636276,-2.4592446273844,10.3352732269966));
#66545=CARTESIAN_POINT('Ctrl Pts',(-1.53852979155112,-2.50938572374625,
10.3403116295304));
#66546=CARTESIAN_POINT('Ctrl Pts',(-1.4573806476547,-2.55566148929031,10.3453500320642));
#66547=CARTESIAN_POINT('Ctrl Pts',(-1.37623757740107,-2.60193379130467,
10.3503880574965));
#66548=CARTESIAN_POINT('Ctrl Pts',(-1.29288287268842,-2.64434111832053,
10.3554260829289));
#66549=CARTESIAN_POINT('Ctrl Pts',(-1.20772280877705,-2.68267955916462,
10.3604641083613));
#66550=CARTESIAN_POINT('Ctrl Pts',(-1.12254539879805,-2.72102580908208,
10.3655031599781));
#66551=CARTESIAN_POINT('Ctrl Pts',(-1.03556230377543,-2.75530134511192,
10.3705422115949));
#66552=CARTESIAN_POINT('Ctrl Pts',(-0.947200241424677,-2.78535019389753,
10.3755812632117));
#66553=CARTESIAN_POINT('Ctrl Pts',(-0.858741951113913,-2.81543176644879,
10.3806258024512));
#66554=CARTESIAN_POINT('Ctrl Pts',(-0.768902116520257,-2.84127732138304,
10.3856703416906));
#66555=CARTESIAN_POINT('Ctrl Pts',(-0.678122793716223,-2.86278072451288,
10.3907148809301));
#66556=CARTESIAN_POINT('Ctrl Pts',(-0.587287204263457,-2.88429745583678,
10.3957625468653));
#66557=CARTESIAN_POINT('Ctrl Pts',(-0.495511402822684,-2.90146659580192,
10.4008102128005));
#66558=CARTESIAN_POINT('Ctrl Pts',(-0.403245683702458,-2.91423350446997,
10.4058578787356));
#66559=CARTESIAN_POINT('Ctrl Pts',(-0.310834263289522,-2.92702057398557,
10.410913515686));
#66560=CARTESIAN_POINT('Ctrl Pts',(-0.217931821828598,-2.93539149560384,
10.4159691526364));
#66561=CARTESIAN_POINT('Ctrl Pts',(-0.124991562079888,-2.93934365282606,
10.4210247895868));
#66562=CARTESIAN_POINT('Ctrl Pts',(-0.0843149222526134,-2.94107337120971,
10.4232374617257));
#66563=CARTESIAN_POINT('Ctrl Pts',(-0.0436310082262822,-2.94195734882917,
10.4254501338646));
#66564=CARTESIAN_POINT('Ctrl Pts',(-0.0029775272444785,-2.94199849325786,
10.4276628060035));
#66565=CARTESIAN_POINT('Ctrl Pts',(0.0899158792836095,-2.94209250848234,
10.4327187728617));
#66566=CARTESIAN_POINT('Ctrl Pts',(0.182977487522895,-2.93778272669165,
10.4377747397198));
#66567=CARTESIAN_POINT('Ctrl Pts',(0.275755805977844,-2.92904809374471,
10.442830706578));
#66568=CARTESIAN_POINT('Ctrl Pts',(0.368407648023413,-2.92032536794407,
10.4478797810873));
#66569=CARTESIAN_POINT('Ctrl Pts',(0.460776529914912,-2.90718981922397,
10.4529288555966));
#66570=CARTESIAN_POINT('Ctrl Pts',(0.552410560194182,-2.88967239890371,
10.457977930106));
#66571=CARTESIAN_POINT('Ctrl Pts',(0.643947863307934,-2.87217346964415,
10.4630216749068));
#66572=CARTESIAN_POINT('Ctrl Pts',(0.734751423385491,-2.85030194586016,
10.4680654197077));
#66573=CARTESIAN_POINT('Ctrl Pts',(0.824375168337771,-2.82414050320236,
10.4731091645086));
#66574=CARTESIAN_POINT('Ctrl Pts',(0.91393563420547,-2.79799753190105,10.47814934816));
#66575=CARTESIAN_POINT('Ctrl Pts',(1.00231751621661,-2.76757078628082,10.4831895318114));
#66576=CARTESIAN_POINT('Ctrl Pts',(1.08908664591529,-2.73299364757567,10.4882297154627));
#66577=CARTESIAN_POINT('Ctrl Pts',(1.17582511283777,-2.6984287278598,10.4932681179965));
#66578=CARTESIAN_POINT('Ctrl Pts',(1.26095154817089,-2.65971649301147,10.4983065205303));
#66579=CARTESIAN_POINT('Ctrl Pts',(1.34404960287046,-2.61703929374852,10.5033449230641));
#66580=CARTESIAN_POINT('Ctrl Pts',(1.42714143805984,-2.57436528867919,10.5083829484965));
#66581=CARTESIAN_POINT('Ctrl Pts',(1.50820480013138,-2.52772711212906,10.5134209739288));
#66582=CARTESIAN_POINT('Ctrl Pts',(1.58684691390828,-2.47735360250001,10.5184589993612));
#66583=CARTESIAN_POINT('Ctrl Pts',(1.6655050461258,-2.42696983240066,10.5234980509779));
#66584=CARTESIAN_POINT('Ctrl Pts',(1.74174057736602,-2.37284945762111,10.5285371025947));
#66585=CARTESIAN_POINT('Ctrl Pts',(1.81518971068537,-2.31526463157496,10.5335761542115));
#66586=CARTESIAN_POINT('Ctrl Pts',(1.88871883150269,-2.25761709456208,10.5386206934509));
#66587=CARTESIAN_POINT('Ctrl Pts',(1.95945514821674,-2.19649784974213,10.5436652326904));
#66588=CARTESIAN_POINT('Ctrl Pts',(2.02706822350752,-2.13221912974395,10.5487097719299));
#66589=CARTESIAN_POINT('Ctrl Pts',(2.09472320659242,-2.06790056864475,10.553757437865));
#66590=CARTESIAN_POINT('Ctrl Pts',(2.15925078805762,-2.00041895390797,10.5588051038002));
#66591=CARTESIAN_POINT('Ctrl Pts',(2.22035915601031,-1.93012155532267,10.5638527697353));
#66592=CARTESIAN_POINT('Ctrl Pts',(2.28156402316422,-1.85971314669015,10.5689084066857));
#66593=CARTESIAN_POINT('Ctrl Pts',(2.33933862441082,-1.78648042580054,10.5739640436361));
#66594=CARTESIAN_POINT('Ctrl Pts',(2.39343312879448,-1.71080152501366,10.5790196805865));
#66595=CARTESIAN_POINT('Ctrl Pts',(2.4171083657428,-1.67767956690475,10.5812323527255));
#66596=CARTESIAN_POINT('Ctrl Pts',(2.44007926069762,-1.64408938586755,10.5834450248646));
#66597=CARTESIAN_POINT('Ctrl Pts',(2.46232764474373,-1.61006415087437,10.5856576970036));
#66598=CARTESIAN_POINT('Ctrl Pts',(2.51316531309907,-1.53231631944934,10.5907136638617));
#66599=CARTESIAN_POINT('Ctrl Pts',(2.56040666420099,-1.45202128913561,10.5957696307198));
#66600=CARTESIAN_POINT('Ctrl Pts',(2.60378736044614,-1.36954568437162,10.6008255975779));
#66601=CARTESIAN_POINT('Ctrl Pts',(2.64710891965606,-1.28718251124581,10.6058746720872));
#66602=CARTESIAN_POINT('Ctrl Pts',(2.68658007790076,-1.20264506008488,10.6109237465965));
#66603=CARTESIAN_POINT('Ctrl Pts',(2.72197983414798,-1.11632870718787,10.6159728211058));
#66604=CARTESIAN_POINT('Ctrl Pts',(2.75734222307558,-1.03010346821619,10.6210165659067));
#66605=CARTESIAN_POINT('Ctrl Pts',(2.78864158540353,-0.942103468255528,
10.6260603107075));
#66606=CARTESIAN_POINT('Ctrl Pts',(2.81570341959696,-0.85274747309505,10.6311040555083));
#66607=CARTESIAN_POINT('Ctrl Pts',(2.8427461467101,-0.763454567973511,10.6361442391596));
#66608=CARTESIAN_POINT('Ctrl Pts',(2.86555716460931,-0.672807993966921,
10.641184422811));
#66609=CARTESIAN_POINT('Ctrl Pts',(2.88401094261607,-0.581244254054003,
10.6462246064623));
#66610=CARTESIAN_POINT('Ctrl Pts',(2.90245819936272,-0.489712871253188,
10.6512630089961));
#66611=CARTESIAN_POINT('Ctrl Pts',(2.91655118785282,-0.39726540079145,10.6563014115298));
#66612=CARTESIAN_POINT('Ctrl Pts',(2.92621512676966,-0.304350179668779,
10.6613398140636));
#66613=CARTESIAN_POINT('Ctrl Pts',(2.93587834238477,-0.211441912826502,
10.6663778394959));
#66614=CARTESIAN_POINT('Ctrl Pts',(2.94111312198164,-0.118066406055722,
10.6714158649282));
#66615=CARTESIAN_POINT('Ctrl Pts',(2.94189649942872,-0.0246776548525677,
10.6764538903605));
#66616=CARTESIAN_POINT('Ctrl Pts',(2.94268003644025,0.0687301185018934,
10.6814929419773));
#66617=CARTESIAN_POINT('Ctrl Pts',(2.93901036718802,0.162150698232739,10.686531993594));
#66618=CARTESIAN_POINT('Ctrl Pts',(2.93091663663948,0.255130690176428,10.6915710452107));
#66619=CARTESIAN_POINT('Ctrl Pts',(2.92281409186503,0.348211939093015,10.6966155844502));
#66620=CARTESIAN_POINT('Ctrl Pts',(2.91027790789137,0.440851200105211,10.7016601236896));
#66621=CARTESIAN_POINT('Ctrl Pts',(2.89338902485617,0.532601117950279,10.706704662929));
#66622=CARTESIAN_POINT('Ctrl Pts',(2.87648967378904,0.624407904036254,10.7117523288641));
#66623=CARTESIAN_POINT('Ctrl Pts',(2.85523235344346,0.715323818093096,10.7167999947992));
#66624=CARTESIAN_POINT('Ctrl Pts',(2.82974845370013,0.804914709010681,10.7218476607343));
#66625=CARTESIAN_POINT('Ctrl Pts',(2.80422431108897,0.894647077269552,10.7269032976847));
#66626=CARTESIAN_POINT('Ctrl Pts',(2.77446040718515,0.983049825995977,10.731958934635));
#66627=CARTESIAN_POINT('Ctrl Pts',(2.74063691887184,1.0697070995916,10.7370145715854));
#66628=CARTESIAN_POINT('Ctrl Pts',(2.72583358331108,1.10763390027916,10.7392272437248));
#66629=CARTESIAN_POINT('Ctrl Pts',(2.71025323871163,1.14522665410072,10.7414399158642));
#66630=CARTESIAN_POINT('Ctrl Pts',(2.69391373655503,1.18245202016831,10.7436525880037));
#66631=CARTESIAN_POINT('Ctrl Pts',(2.65657789275248,1.26751216702421,10.7487085548619));
#66632=CARTESIAN_POINT('Ctrl Pts',(2.61514363903161,1.3509522039735,10.7537645217202));
#66633=CARTESIAN_POINT('Ctrl Pts',(2.56977358753034,1.4323504141206,10.7588204885784));
#66634=CARTESIAN_POINT('Ctrl Pts',(2.52446538497513,1.51363766134519,10.7638695630879));
#66635=CARTESIAN_POINT('Ctrl Pts',(2.47523226089738,1.59288822901452,10.7689186375973));
#66636=CARTESIAN_POINT('Ctrl Pts',(2.42228458744273,1.66970098443925,10.7739677121067));
#66637=CARTESIAN_POINT('Ctrl Pts',(2.3693928045601,1.74643265775859,10.7790114569077));
#66638=CARTESIAN_POINT('Ctrl Pts',(2.31279451671488,1.82073127072479,10.7840552017087));
#66639=CARTESIAN_POINT('Ctrl Pts',(2.25274509330889,1.89222185395178,10.7890989465096));
#66640=CARTESIAN_POINT('Ctrl Pts',(2.19273806795893,1.96366196106125,10.7941391301611));
#66641=CARTESIAN_POINT('Ctrl Pts',(2.12928503494304,2.03229764069085,10.7991793138126));
#66642=CARTESIAN_POINT('Ctrl Pts',(2.06268297746117,2.09778524508395,10.804219497464));
#66643=CARTESIAN_POINT('Ctrl Pts',(1.99610445604537,2.16324970724028,10.8092578999979));
#66644=CARTESIAN_POINT('Ctrl Pts',(1.92637943697039,2.22556799376019,10.8142963025318));
#66645=CARTESIAN_POINT('Ctrl Pts',(1.85384254508205,2.28443249364995,10.8193347050657));
#66646=CARTESIAN_POINT('Ctrl Pts',(1.78131108224913,2.34329258780045,10.8243727304982));
#66647=CARTESIAN_POINT('Ctrl Pts',(1.70596850960611,2.39869913010453,10.8294107559306));
#66648=CARTESIAN_POINT('Ctrl Pts',(1.62818250396606,2.45038481340764,10.834448781363));
#66649=CARTESIAN_POINT('Ctrl Pts',(1.55038065426389,2.50208102445504,10.8394878329799));
#66650=CARTESIAN_POINT('Ctrl Pts',(1.47013475263499,2.55005462617398,10.8445268845968));
#66651=CARTESIAN_POINT('Ctrl Pts',(1.38784044688097,2.5940822835834,10.8495659362137));
#66652=CARTESIAN_POINT('Ctrl Pts',(1.30545652106893,2.63815788794581,10.8546104754532));
#66653=CARTESIAN_POINT('Ctrl Pts',(1.22102013017517,2.67827876135069,10.8596550146928));
#66654=CARTESIAN_POINT('Ctrl Pts',(1.13495016633914,2.71426824759948,10.8646995539323));
#66655=CARTESIAN_POINT('Ctrl Pts',(1.04882685479923,2.75028004077591,10.8697472198676));
#66656=CARTESIAN_POINT('Ctrl Pts',(0.961068370996616,2.78215519753157,10.8747948858028));
#66657=CARTESIAN_POINT('Ctrl Pts',(0.872110115265059,2.80976652888676,10.8798425517381));
#66658=CARTESIAN_POINT('Ctrl Pts',(0.783011381217533,2.83742146264062,10.8848981886885));
#66659=CARTESIAN_POINT('Ctrl Pts',(0.692709521901368,2.86079901945179,10.889953825639));
#66660=CARTESIAN_POINT('Ctrl Pts',(0.601651273221105,2.8798228670235,10.8950094625895));
#66661=CARTESIAN_POINT('Ctrl Pts',(0.561798322589845,2.88814892720014,10.8972221347275));
#66662=CARTESIAN_POINT('Ctrl Pts',(0.521800565480502,2.89564170384939,10.8994348068656));
#66663=CARTESIAN_POINT('Ctrl Pts',(0.48169567966528,2.9022979296054,10.9016474790037));
#66664=CARTESIAN_POINT('Ctrl Pts',(0.390055815791504,2.91750743861646,10.9067034458618));
#66665=CARTESIAN_POINT('Ctrl Pts',(0.297533352779683,2.92839922383743,10.9117594127199));
#66666=CARTESIAN_POINT('Ctrl Pts',(0.204570337682543,2.93487903957564,10.916815379578));
#66667=CARTESIAN_POINT('Ctrl Pts',(0.111734050775317,2.94135002195881,10.9218644540873));
#66668=CARTESIAN_POINT('Ctrl Pts',(0.0184588439276381,2.94342095640441,
10.9269135285966));
#66669=CARTESIAN_POINT('Ctrl Pts',(-0.0748043782143797,2.94104884437507,
10.9319626031059));
#66670=CARTESIAN_POINT('Ctrl Pts',(-0.167969153446333,2.93867923630276,
10.9370063479067));
#66671=CARTESIAN_POINT('Ctrl Pts',(-0.261121528092837,2.93187591557138,
10.9420500927076));
#66672=CARTESIAN_POINT('Ctrl Pts',(-0.35380792209284,2.92064786550251,10.9470938375084));
#66673=CARTESIAN_POINT('Ctrl Pts',(-0.446428874616717,2.90942774302838,
10.9521340211597));
#66674=CARTESIAN_POINT('Ctrl Pts',(-0.538584061433512,2.89378915423348,
10.9571742048111));
#66675=CARTESIAN_POINT('Ctrl Pts',(-0.629823396012821,2.87379304923561,
10.9622143884624));
#66676=CARTESIAN_POINT('Ctrl Pts',(-0.721030488119714,2.85380401053064,
10.9672527909962));
#66677=CARTESIAN_POINT('Ctrl Pts',(-0.811321938223273,2.82946060983173,
10.9722911935299));
#66678=CARTESIAN_POINT('Ctrl Pts',(-0.900257272765933,2.80087501378267,
10.9773295960637));
#66679=CARTESIAN_POINT('Ctrl Pts',(-0.989185950904777,2.77229155723498,
10.982367621496));
#66680=CARTESIAN_POINT('Ctrl Pts',(-1.07675829319537,2.73946667265119,10.9874056469283));
#66681=CARTESIAN_POINT('Ctrl Pts',(-1.16254952067202,2.70256223091814,10.9924436723607));
#66682=CARTESIAN_POINT('Ctrl Pts',(-1.24835822277642,2.66565027219996,10.9974827239774));
#66683=CARTESIAN_POINT('Ctrl Pts',(-1.33238468234558,2.62465728155637,11.0025217755941));
#66684=CARTESIAN_POINT('Ctrl Pts',(-1.41422566362877,2.57979258320001,11.0075608272108));
#66685=CARTESIAN_POINT('Ctrl Pts',(-1.49615577129122,2.53487902633708,11.0126053664503));
#66686=CARTESIAN_POINT('Ctrl Pts',(-1.57589526075064,2.48608555945655,11.0176499056897));
#66687=CARTESIAN_POINT('Ctrl Pts',(-1.65306728902706,2.43366648042593,11.0226944449291));
#66688=CARTESIAN_POINT('Ctrl Pts',(-1.73028714990762,2.38121491111207,11.0277421108642));
#66689=CARTESIAN_POINT('Ctrl Pts',(-1.80493602719354,2.3251335218908,11.0327897767993));
#66690=CARTESIAN_POINT('Ctrl Pts',(-1.87666948679219,2.26571746635435,11.0378374427344));
#66691=CARTESIAN_POINT('Ctrl Pts',(-1.94851622419222,2.20620758402945,11.0428930796847));
#66692=CARTESIAN_POINT('Ctrl Pts',(-2.01743802668207,2.14335282208175,11.0479487166351));
#66693=CARTESIAN_POINT('Ctrl Pts',(-2.0831268591785,2.07748561693436,11.0530043535854));
#66694=CARTESIAN_POINT('Ctrl Pts',(-2.11187652039143,2.04865788836827,11.0552170257249));
#66695=CARTESIAN_POINT('Ctrl Pts',(-2.14000742323412,2.01925355904415,11.0574296978643));
#66696=CARTESIAN_POINT('Ctrl Pts',(-2.16749624331862,1.98930239913385,11.0596423700038));
#66697=CARTESIAN_POINT('Ctrl Pts',(-2.22958430090055,1.92165273881957,11.0646400568736));
#66698=CARTESIAN_POINT('Ctrl Pts',(-2.28862416138595,1.8509604081968,11.0696377437435));
#66699=CARTESIAN_POINT('Ctrl Pts',(-2.34429841515415,1.77753451181847,11.0746354306133));
#66700=CARTESIAN_POINT('Ctrl Pts',(-2.39990319760607,1.70420023756933,11.0796268812813));
#66701=CARTESIAN_POINT('Ctrl Pts',(-2.4521504371219,1.62813952602512,11.0846183319493));
#66702=CARTESIAN_POINT('Ctrl Pts',(-2.50076027439732,1.54969740594615,11.0896097826173));
#66703=CARTESIAN_POINT('Ctrl Pts',(-2.5493237596314,1.4713300845622,11.094596473674));
#66704=CARTESIAN_POINT('Ctrl Pts',(-2.5942564910186,1.39058624708043,11.0995831647308));
#66705=CARTESIAN_POINT('Ctrl Pts',(-2.63532034526617,1.30784199268343,11.1045698557875));
#66706=CARTESIAN_POINT('Ctrl Pts',(-2.67635712129754,1.22515230127989,11.1095532585339));
#66707=CARTESIAN_POINT('Ctrl Pts',(-2.71352988621776,1.14046521899455,11.1145366612802));
#66708=CARTESIAN_POINT('Ctrl Pts',(-2.74664579315571,1.05418256812566,11.1195200640266));
#66709=CARTESIAN_POINT('Ctrl Pts',(-2.77975901597079,0.967906910670452,
11.1245030628563));
#66710=CARTESIAN_POINT('Ctrl Pts',(-2.80881585622071,0.880036359803671,
11.1294860616861));
#66711=CARTESIAN_POINT('Ctrl Pts',(-2.83367146361466,0.790993069688948,
11.1344690605158));
#66712=CARTESIAN_POINT('Ctrl Pts',(-2.85852459050563,0.701958665784222,
11.1394515620596));
#66713=CARTESIAN_POINT('Ctrl Pts',(-2.87917720172363,0.611752195000438,
11.1444340636035));
#66714=CARTESIAN_POINT('Ctrl Pts',(-2.89553471140255,0.520809691790528,
11.1494165651473));
#66715=CARTESIAN_POINT('Ctrl Pts',(-2.91190491411364,0.429796619396097,
11.1544029329919));
#66716=CARTESIAN_POINT('Ctrl Pts',(-2.92397328119532,0.338046822642366,
11.1593893008365));
#66717=CARTESIAN_POINT('Ctrl Pts',(-2.93169672481608,0.246004702602807,
11.1643756686811));
#66718=CARTESIAN_POINT('Ctrl Pts',(-2.93864009038374,0.163258958807896,
11.1688584067575));
#66719=CARTESIAN_POINT('Ctrl Pts',(-2.94207257076881,0.0802772842537297,
11.173341144834));
#66720=CARTESIAN_POINT('Ctrl Pts',(-2.94199883612238,-0.00261691699413304,
11.1778238829104));
#66721=CARTESIAN_POINT('',(-2.94599368555865,0.00130075687149912,12.1778238829104));
#66722=CARTESIAN_POINT('Ctrl Pts',(-2.94145087575173,-0.00262142569101594,
11.1778241531392));
#66723=CARTESIAN_POINT('Ctrl Pts',(-2.94362752589749,-0.247984084398526,
11.1910951890941));
#66724=CARTESIAN_POINT('Ctrl Pts',(-2.80368830243438,-1.46459917676703,
11.2570311887159));
#66725=CARTESIAN_POINT('Ctrl Pts',(-1.11814973965556,-3.2866071025494,11.3756321520037));
#66726=CARTESIAN_POINT('Ctrl Pts',(2.14158719959913,-2.73233404879197,11.533627043004));
#66727=CARTESIAN_POINT('Ctrl Pts',(3.45856717040371,0.300596429689326,11.691621934004));
#66728=CARTESIAN_POINT('Ctrl Pts',(1.63808186784714,3.06083859111985,11.849616825004));
#66729=CARTESIAN_POINT('Ctrl Pts',(-1.66840174770122,3.04441795752147,12.0076117160041));
#66730=CARTESIAN_POINT('Ctrl Pts',(-2.90993729409171,1.12068341154196,12.1170140686395));
#66731=CARTESIAN_POINT('Ctrl Pts',(-2.94641083929854,0.0762932715455572,
12.1737514576083));
#66732=CARTESIAN_POINT('Ctrl Pts',(-2.94599368555865,0.00130075687149912,
12.1778238829104));
#66733=CARTESIAN_POINT('',(-2.94186551558604,0.00139596930223792,13.1778238494248));
#66734=CARTESIAN_POINT('Ctrl Pts',(-2.94599368555865,0.00130075687149912,
12.1778238829104));
#66735=CARTESIAN_POINT('Ctrl Pts',(-2.94101617029297,-0.893516551252978,
12.226416421275));
#66736=CARTESIAN_POINT('Ctrl Pts',(-2.03018396278169,-2.76692136029347,
12.3276739233063));
#66737=CARTESIAN_POINT('Ctrl Pts',(1.15073763387882,-3.27533937411075,12.4815963890041));
#66738=CARTESIAN_POINT('Ctrl Pts',(3.37191857800937,-0.825960120600501,
12.6395912800043));
#66739=CARTESIAN_POINT('Ctrl Pts',(2.53423820298509,2.37269506052472,12.7975861710044));
#66740=CARTESIAN_POINT('Ctrl Pts',(-0.60239551675097,3.41894207513383,12.9555810620044));
#66741=CARTESIAN_POINT('Ctrl Pts',(-2.68026052099427,1.77017590350058,13.0823266290105));
#66742=CARTESIAN_POINT('Ctrl Pts',(-2.93966479896272,0.398551205875977,
13.1564072323499));
#66743=CARTESIAN_POINT('Ctrl Pts',(-2.93794974228868,0.001412237267097,
13.1778228720226));
#66744=CARTESIAN_POINT('',(-2.94199885496721,-0.00259564473995637,14.1778238829374));
#66745=CARTESIAN_POINT('Ctrl Pts',(-2.94199966907297,0.0013954119655268,
13.1778238829104));
#66746=CARTESIAN_POINT('Ctrl Pts',(-2.94204471264643,-0.0935716525962874,
13.1829379245465));
#66747=CARTESIAN_POINT('Ctrl Pts',(-2.93748713814666,-0.188529989784559,
13.1880519661827));
#66748=CARTESIAN_POINT('Ctrl Pts',(-2.92835588116753,-0.28301207258969,
13.1931660078188));
#66749=CARTESIAN_POINT('Ctrl Pts',(-2.91922127699117,-0.377528789199093,
13.1982819240825));
#66750=CARTESIAN_POINT('Ctrl Pts',(-2.90550969590064,-0.471568481542718,
13.2033978403461));
#66751=CARTESIAN_POINT('Ctrl Pts',(-2.88730181220689,-0.564670032166427,
13.2085137566098));
#66752=CARTESIAN_POINT('Ctrl Pts',(-2.86859978416063,-0.660298268824794,
13.2137685138927));
#66753=CARTESIAN_POINT('Ctrl Pts',(-2.84515397675717,-0.754936240875184,
13.2190232711756));
#66754=CARTESIAN_POINT('Ctrl Pts',(-2.81710711756315,-0.848098749070564,
13.2242780284585));
#66755=CARTESIAN_POINT('Ctrl Pts',(-2.78974280920771,-0.938994046251209,
13.2294049055048));
#66756=CARTESIAN_POINT('Ctrl Pts',(-2.75799905007121,-1.02848449562343,
13.234531782551));
#66757=CARTESIAN_POINT('Ctrl Pts',(-2.72205758840463,-1.1161390976974,13.2396586595973));
#66758=CARTESIAN_POINT('Ctrl Pts',(-2.68477138921636,-1.20707326679207,
13.2449773569985));
#66759=CARTESIAN_POINT('Ctrl Pts',(-2.64296744073451,-1.29603105910162,
13.2502960543997));
#66760=CARTESIAN_POINT('Ctrl Pts',(-2.59690049794005,-1.38255987349508,
13.2556147518009));
#66761=CARTESIAN_POINT('Ctrl Pts',(-2.55083355514558,-1.46908868788855,
13.2609334492021));
#66762=CARTESIAN_POINT('Ctrl Pts',(-2.50050393867054,-1.55318813126393,
13.2662521466033));
#66763=CARTESIAN_POINT('Ctrl Pts',(-2.44621482673287,-1.63444088956201,
13.2715708440045));
#66764=CARTESIAN_POINT('Ctrl Pts',(-2.39460749082002,-1.71167992040394,
13.2766268081491));
#66765=CARTESIAN_POINT('Ctrl Pts',(-2.33924737933322,-1.78660846295203,
13.2816827722938));
#66766=CARTESIAN_POINT('Ctrl Pts',(-2.28036820549469,-1.85883965079533,
13.2867387364384));
#66767=CARTESIAN_POINT('Ctrl Pts',(-2.22156929641021,-1.93097237226847,
13.2917878082357));
#66768=CARTESIAN_POINT('Ctrl Pts',(-2.15926113603735,-2.00041470538282,
13.296836880033));
#66769=CARTESIAN_POINT('Ctrl Pts',(-2.09372087240025,-2.06680838697629,
13.3018859518303));
#66770=CARTESIAN_POINT('Ctrl Pts',(-2.02824979180801,-2.13313198467328,
13.3069296939243));
#66771=CARTESIAN_POINT('Ctrl Pts',(-1.95955369962162,-2.19641301369781,
13.3119734360183));
#66772=CARTESIAN_POINT('Ctrl Pts',(-1.88794948466174,-2.25632682547664,
13.3170171781123));
#66773=CARTESIAN_POINT('Ctrl Pts',(-1.81639582581118,-2.31619833514768,
13.3220573590754));
#66774=CARTESIAN_POINT('Ctrl Pts',(-1.74193846471106,-2.37270706943091,
13.3270975400386));
#66775=CARTESIAN_POINT('Ctrl Pts',(-1.66492979922436,-2.42556648304159,
13.3321377210018));
#66776=CARTESIAN_POINT('Ctrl Pts',(-1.58794834714745,-2.47840721713257,
13.33717612086));
#66777=CARTESIAN_POINT('Ctrl Pts',(-1.50841774718876,-2.52760094195155,
13.3422145207183));
#66778=CARTESIAN_POINT('Ctrl Pts',(-1.42672117217879,-2.57290316507574,
13.3472529205766));
#66779=CARTESIAN_POINT('Ctrl Pts',(-1.34503071152868,-2.61820199767721,
13.3522909433495));
#66780=CARTESIAN_POINT('Ctrl Pts',(-1.26117498613445,-2.65960969289675,
13.3573289661223));
#66781=CARTESIAN_POINT('Ctrl Pts',(-1.17556267986372,-2.69692721179338,
13.3623669888951));
#66782=CARTESIAN_POINT('Ctrl Pts',(-1.08993293507243,-2.73425233196077,
13.3674060378716));
#66783=CARTESIAN_POINT('Ctrl Pts',(-1.00254630542262,-2.76748544429363,
13.3724450868481));
#66784=CARTESIAN_POINT('Ctrl Pts',(-0.913831342618127,-2.79647568865684,
13.3774841358246));
#66785=CARTESIAN_POINT('Ctrl Pts',(-0.825019766700395,-2.82549750421924,
13.3825286724686));
#66786=CARTESIAN_POINT('Ctrl Pts',(-0.734877392389711,-2.85026709122484,
13.3875732091125));
#66787=CARTESIAN_POINT('Ctrl Pts',(-0.64384751275842,-2.87068360853557,
13.3926177457564));
#66788=CARTESIAN_POINT('Ctrl Pts',(-0.552761210754769,-2.89111278046418,
13.3976654091179));
#66789=CARTESIAN_POINT('Ctrl Pts',(-0.460786744733421,-2.9071834348439,
13.4027130724794));
#66790=CARTESIAN_POINT('Ctrl Pts',(-0.36837502971951,-2.91884631960628,
13.4077607358409));
#66791=CARTESIAN_POINT('Ctrl Pts',(-0.275817381732566,-2.93052762194102,
13.4128163702753));
#66792=CARTESIAN_POINT('Ctrl Pts',(-0.182821547841941,-2.93778722576749,
13.4178720047097));
#66793=CARTESIAN_POINT('Ctrl Pts',(-0.0898407292960799,-2.94062793351344,
13.4229276391442));
#66794=CARTESIAN_POINT('Ctrl Pts',(-0.0491458310464539,-2.94187122556536,
13.4251403377643));
#66795=CARTESIAN_POINT('Ctrl Pts',(-0.00845377089998635,-2.94226873013071,
13.4273530363844));
#66796=CARTESIAN_POINT('Ctrl Pts',(0.0321977799876051,-2.94182380556074,
13.4295657350046));
#66797=CARTESIAN_POINT('Ctrl Pts',(0.125085675168177,-2.94080716275335,
13.4346217024402));
#66798=CARTESIAN_POINT('Ctrl Pts',(0.218089107719228,-2.93538502623224,
13.4396776698758));
#66799=CARTESIAN_POINT('Ctrl Pts',(0.310756366649291,-2.92554174138516,
13.4447336373114));
#66800=CARTESIAN_POINT('Ctrl Pts',(0.403297300160726,-2.9157118750539,13.4497827123752));
#66801=CARTESIAN_POINT('Ctrl Pts',(0.495502533472043,-2.90147288387257,
13.454831787439));
#66802=CARTESIAN_POINT('Ctrl Pts',(0.586920577431533,-2.88286111975368,
13.4598808625028));
#66803=CARTESIAN_POINT('Ctrl Pts',(0.67824212180384,-2.86426900194833,13.4649246078347));
#66804=CARTESIAN_POINT('Ctrl Pts',(0.768777696246268,-2.84131337440413,
13.4699683531667));
#66805=CARTESIAN_POINT('Ctrl Pts',(0.858082248971938,-2.81408224009165,
13.4750120984986));
#66806=CARTESIAN_POINT('Ctrl Pts',(0.947323747340353,-2.78687033258923,
13.4800522826446));
#66807=CARTESIAN_POINT('Ctrl Pts',(1.0353355286556,-2.75538904777478,13.4850924667906));
#66808=CARTESIAN_POINT('Ctrl Pts',(1.12168505014706,-2.71977694825818,13.4901326509366));
#66809=CARTESIAN_POINT('Ctrl Pts',(1.20800405675712,-2.68417743362885,13.4951710539422));
#66810=CARTESIAN_POINT('Ctrl Pts',(1.29266156103043,-2.64445017345002,13.5002094569478));
#66811=CARTESIAN_POINT('Ctrl Pts',(1.37524342380712,-2.60078248326831,13.5052478599533));
#66812=CARTESIAN_POINT('Ctrl Pts',(1.45781910532763,-2.55711806161519,13.5102858858342));
#66813=CARTESIAN_POINT('Ctrl Pts',(1.53831906237339,-2.50951400397826,13.5153239117151));
#66814=CARTESIAN_POINT('Ctrl Pts',(1.61635328376672,-2.45820382841955,13.520361937596));
#66815=CARTESIAN_POINT('Ctrl Pts',(1.6944033994116,-2.4068832018456,13.5254009896376));
#66816=CARTESIAN_POINT('Ctrl Pts',(1.76998641163778,-2.35185520204692,13.5304400416792));
#66817=CARTESIAN_POINT('Ctrl Pts',(1.84274180329659,-2.29339631254243,13.5354790937207));
#66818=CARTESIAN_POINT('Ctrl Pts',(1.9155764264014,-2.23487376064481,13.5405236333471));
#66819=CARTESIAN_POINT('Ctrl Pts',(1.98557693649643,-2.17291313966353,13.5455681729735));
#66820=CARTESIAN_POINT('Ctrl Pts',(2.05241665285454,-2.10783061062443,13.5506127125998));
#66821=CARTESIAN_POINT('Ctrl Pts',(2.11929779738181,-2.04270774254487,13.5556603789007));
#66822=CARTESIAN_POINT('Ctrl Pts',(2.18301394551469,-1.97445943796929,13.5607080452017));
#66823=CARTESIAN_POINT('Ctrl Pts',(2.24327745808883,-1.90343643078264,13.5657557115026));
#66824=CARTESIAN_POINT('Ctrl Pts',(2.30363613528146,-1.83230126821215,13.5708113487832));
#66825=CARTESIAN_POINT('Ctrl Pts',(2.36053102339126,-1.75838300741313,13.5758669860639));
#66826=CARTESIAN_POINT('Ctrl Pts',(2.41371683017811,-1.68206274071894,13.5809226233446));
#66827=CARTESIAN_POINT('Ctrl Pts',(2.43699431280634,-1.64866015101536,13.5831352908979));
#66828=CARTESIAN_POINT('Ctrl Pts',(2.45956190856083,-1.6147977949142,13.5853479584512));
#66829=CARTESIAN_POINT('Ctrl Pts',(2.48140184649713,-1.58050905603247,13.5875606260046));
#66830=CARTESIAN_POINT('Ctrl Pts',(2.53130640275208,-1.50215881971651,13.5926166015623));
#66831=CARTESIAN_POINT('Ctrl Pts',(2.57758442902489,-1.42130455947248,13.5976725771201));
#66832=CARTESIAN_POINT('Ctrl Pts',(2.61997599008422,-1.33831603568897,13.6027285526779));
#66833=CARTESIAN_POINT('Ctrl Pts',(2.66230976296541,-1.25544064186519,13.6077776359295));
#66834=CARTESIAN_POINT('Ctrl Pts',(2.70076739903187,-1.17043715783292,13.6128267191811));
#66835=CARTESIAN_POINT('Ctrl Pts',(2.73513264036075,-1.08370357553771,13.6178758024328));
#66836=CARTESIAN_POINT('Ctrl Pts',(2.7694616066527,-0.997061546910688,13.6229195560061));
#66837=CARTESIAN_POINT('Ctrl Pts',(2.79970660248309,-0.908693460310509,
13.6279633095794));
#66838=CARTESIAN_POINT('Ctrl Pts',(2.82569814580013,-0.819020139448189,
13.6330070631527));
#66839=CARTESIAN_POINT('Ctrl Pts',(2.85167133779114,-0.729410132423238,
13.6380472555844));
#66840=CARTESIAN_POINT('Ctrl Pts',(2.87339692358576,-0.638497147704853,
13.6430874480162));
#66841=CARTESIAN_POINT('Ctrl Pts',(2.89075460058646,-0.546719159338895,
13.6481276404479));
#66842=CARTESIAN_POINT('Ctrl Pts',(2.90810614368617,-0.454973603716871,
13.6531660517633));
#66843=CARTESIAN_POINT('Ctrl Pts',(2.92109276231074,-0.362364087082582,
13.6582044630787));
#66844=CARTESIAN_POINT('Ctrl Pts',(2.92964504110006,-0.269339809827301,
13.6632428743942));
#66845=CARTESIAN_POINT('Ctrl Pts',(2.93819667977488,-0.176322495182945,
13.6682809085984));
#66846=CARTESIAN_POINT('Ctrl Pts',(2.94231459825068,-0.0828909232772339,
13.6733189428026));
#66847=CARTESIAN_POINT('Ctrl Pts',(2.9419812603063,0.010500666957926,13.6783569770068));
#66848=CARTESIAN_POINT('Ctrl Pts',(2.94164785446653,0.103911279503686,13.6833960373746));
#66849=CARTESIAN_POINT('Ctrl Pts',(2.93686139349325,0.197281450784621,13.6884350977425));
#66850=CARTESIAN_POINT('Ctrl Pts',(2.92765644134919,0.290158166224171,13.6934741581103));
#66851=CARTESIAN_POINT('Ctrl Pts',(2.91844146500886,0.383136024440997,13.6985187060167));
#66852=CARTESIAN_POINT('Ctrl Pts',(2.90479843715336,0.475618912294044,13.7035632539231));
#66853=CARTESIAN_POINT('Ctrl Pts',(2.88681364100954,0.567160472953867,13.7086078018296));
#66854=CARTESIAN_POINT('Ctrl Pts',(2.86881769771396,0.658758771964252,13.7136554763959));
#66855=CARTESIAN_POINT('Ctrl Pts',(2.84647473462245,0.749414152026579,13.7187031509622));
#66856=CARTESIAN_POINT('Ctrl Pts',(2.81992132323482,0.838694062674587,13.7237508255285));
#66857=CARTESIAN_POINT('Ctrl Pts',(2.79332598085164,0.928114956922829,13.7288064709735));
#66858=CARTESIAN_POINT('Ctrl Pts',(2.76250706438297,1.01615562814751,13.7338621164185));
#66859=CARTESIAN_POINT('Ctrl Pts',(2.72764971011007,1.10240240336115,13.7389177618635));
#66860=CARTESIAN_POINT('Ctrl Pts',(2.71239451437209,1.14014799435907,13.7411303469105));
#66861=CARTESIAN_POINT('Ctrl Pts',(2.69636642006694,1.1775502988612,13.7433429319576));
#66862=CARTESIAN_POINT('Ctrl Pts',(2.67958367377214,1.21457619573816,13.7455555170047));
#66863=CARTESIAN_POINT('Ctrl Pts',(2.64123365918508,1.29918354547628,13.7506114635905));
#66864=CARTESIAN_POINT('Ctrl Pts',(2.59880492609599,1.38212191993738,13.7556674101764));
#66865=CARTESIAN_POINT('Ctrl Pts',(2.55246511434818,1.46297157868345,13.7607233567623));
#66866=CARTESIAN_POINT('Ctrl Pts',(2.50618847383475,1.54371102177369,13.7657724109941));
#66867=CARTESIAN_POINT('Ctrl Pts',(2.45601156858285,1.62236702602864,13.770821465226));
#66868=CARTESIAN_POINT('Ctrl Pts',(2.40214954901253,1.69854100456212,13.7758705194578));
#66869=CARTESIAN_POINT('Ctrl Pts',(2.3483443851696,1.77463457528705,13.7809142440037));
#66870=CARTESIAN_POINT('Ctrl Pts',(2.29086209398443,1.84825096796688,13.7859579685496));
#66871=CARTESIAN_POINT('Ctrl Pts',(2.22996250719433,1.91901829499033,13.7910016930954));
#66872=CARTESIAN_POINT('Ctrl Pts',(2.16910591748539,1.98973565798833,13.7960418566084));
#66873=CARTESIAN_POINT('Ctrl Pts',(2.10483711646537,2.05760761848628,13.8010820201213));
#66874=CARTESIAN_POINT('Ctrl Pts',(2.03745717229748,2.12229410569166,13.8061221836343));
#66875=CARTESIAN_POINT('Ctrl Pts',(1.97010103810533,2.18695773470518,13.8111605661102));
#66876=CARTESIAN_POINT('Ctrl Pts',(1.89963626457905,2.2484378199862,13.8161989485862));
#66877=CARTESIAN_POINT('Ctrl Pts',(1.82640112802997,2.3064307749271,13.8212373310622));
#66878=CARTESIAN_POINT('Ctrl Pts',(1.75317147128809,2.36441939055458,13.826275336542));
#66879=CARTESIAN_POINT('Ctrl Pts',(1.67717221155185,2.41892111958122,13.8313133420219));
#66880=CARTESIAN_POINT('Ctrl Pts',(1.59877419287678,2.46967307152004,13.8363513475017));
#66881=CARTESIAN_POINT('Ctrl Pts',(1.52036020339346,2.52043536236418,13.841390379296));
#66882=CARTESIAN_POINT('Ctrl Pts',(1.43954685689406,2.56744611832926,13.8464294110903));
#66883=CARTESIAN_POINT('Ctrl Pts',(1.35673244065961,2.61048675240114,13.8514684428845));
#66884=CARTESIAN_POINT('Ctrl Pts',(1.27382783244256,2.65357426140488,13.8565129626154));
#66885=CARTESIAN_POINT('Ctrl Pts',(1.18891819863695,2.69268281348045,13.8615574823463));
#66886=CARTESIAN_POINT('Ctrl Pts',(1.10242451106388,2.72764077499321,13.8666020020773));
#66887=CARTESIAN_POINT('Ctrl Pts',(1.01587721034462,2.76262040521214,13.8716496486557));
#66888=CARTESIAN_POINT('Ctrl Pts',(0.927744319322681,2.79344417662816,13.8766972952341));
#66889=CARTESIAN_POINT('Ctrl Pts',(0.838462725260018,2.81999011671132,13.8817449418126));
#66890=CARTESIAN_POINT('Ctrl Pts',(0.749040134406092,2.84657797912363,13.8868005598209));
#66891=CARTESIAN_POINT('Ctrl Pts',(0.658465649250251,2.8688744188892,13.8918561778293));
#66892=CARTESIAN_POINT('Ctrl Pts',(0.567186883632633,2.88680845208599,13.8969117958377));
#66893=CARTESIAN_POINT('Ctrl Pts',(0.527233685493236,2.89465827320158,13.89912466656));
#66894=CARTESIAN_POINT('Ctrl Pts',(0.487145629108541,2.90167298955917,13.9013375372823));
#66895=CARTESIAN_POINT('Ctrl Pts',(0.446960438952583,2.90784978394884,13.9035504080047));
#66896=CARTESIAN_POINT('Ctrl Pts',(0.355145127557181,2.92196255281,13.9086063854347));
#66897=CARTESIAN_POINT('Ctrl Pts',(0.262498902156857,2.93174733982606,13.9136623628647));
#66898=CARTESIAN_POINT('Ctrl Pts',(0.169464906306277,2.93711519105578,13.9187183402947));
#66899=CARTESIAN_POINT('Ctrl Pts',(0.0765577378091241,2.94247572463393,
13.9237674252309));
#66900=CARTESIAN_POINT('Ctrl Pts',(-0.01673571162763,2.94343126289967,13.9288165101671));
#66901=CARTESIAN_POINT('Ctrl Pts',(-0.109964054207938,2.93994420130419,
13.9338655951033));
#66902=CARTESIAN_POINT('Ctrl Pts',(-0.203093984001307,2.93646082068641,
13.9389093501741));
#66903=CARTESIAN_POINT('Ctrl Pts',(-0.296158502692968,2.9285441786145,13.9439531052449));
#66904=CARTESIAN_POINT('Ctrl Pts',(-0.388704168742802,2.91620868066776,
13.9489968603157));
#66905=CARTESIAN_POINT('Ctrl Pts',(-0.481184487815518,2.9038818928804,13.9540370539648));
#66906=CARTESIAN_POINT('Ctrl Pts',(-0.573146244111906,2.88714250970049,
13.9590772476138));
#66907=CARTESIAN_POINT('Ctrl Pts',(-0.664140110676326,2.8660568580178,13.9641174412629));
#66908=CARTESIAN_POINT('Ctrl Pts',(-0.755101818452255,2.84497865836498,
13.9691558536213));
#66909=CARTESIAN_POINT('Ctrl Pts',(-0.845095884496893,2.81955734197982,
13.9741942659798));
#66910=CARTESIAN_POINT('Ctrl Pts',(-0.933683206420332,2.7899103336933,13.9792326783382));
#66911=CARTESIAN_POINT('Ctrl Pts',(-1.0222638947614,2.76026554542954,13.984270713411));
#66912=CARTESIAN_POINT('Ctrl Pts',(-1.10943762798828,2.72639583546516,13.9893087484838));
#66913=CARTESIAN_POINT('Ctrl Pts',(-1.19478159135926,2.68846814170245,13.9943467835566));
#66914=CARTESIAN_POINT('Ctrl Pts',(-1.28014293491138,2.6505327240169,13.9993858446184));
#66915=CARTESIAN_POINT('Ctrl Pts',(-1.36367336347592,2.60853786165571,14.0044249056801));
#66916=CARTESIAN_POINT('Ctrl Pts',(-1.44497217123477,2.56269768493224,14.0094639667418));
#66917=CARTESIAN_POINT('Ctrl Pts',(-1.52635950914418,2.5168075906533,14.0145085150776));
#66918=CARTESIAN_POINT('Ctrl Pts',(-1.60550998893169,2.46706404226412,14.0195530634133));
#66919=CARTESIAN_POINT('Ctrl Pts',(-1.6820498332811,2.41372582501804,14.0245976117491));
#66920=CARTESIAN_POINT('Ctrl Pts',(-1.75863711548155,2.36035454982122,14.0296452865941));
#66921=CARTESIAN_POINT('Ctrl Pts',(-1.83261018996262,2.30338444068044,14.0346929614391));
#66922=CARTESIAN_POINT('Ctrl Pts',(-1.90362817431552,2.24311474828021,14.0397406362841));
#66923=CARTESIAN_POINT('Ctrl Pts',(-1.97475830126131,2.18274988562641,14.044796281777));
#66924=CARTESIAN_POINT('Ctrl Pts',(-2.0429236998364,2.11907534138202,14.0498519272699));
#66925=CARTESIAN_POINT('Ctrl Pts',(-2.10782032968545,2.0524272113195,14.0549075727627));
#66926=CARTESIAN_POINT('Ctrl Pts',(-2.13622198242389,2.02325902415623,14.0571201481768));
#66927=CARTESIAN_POINT('Ctrl Pts',(-2.16399808150058,1.9935217248477,14.0593327235908));
#66928=CARTESIAN_POINT('Ctrl Pts',(-2.19112566304988,1.96324535622123,14.0615452990048));
#66929=CARTESIAN_POINT('Ctrl Pts',(-2.25247103055659,1.89477943135491,14.0665487399368));
#66930=CARTESIAN_POINT('Ctrl Pts',(-2.31072385919334,1.82330178025768,14.0715521808688));
#66931=CARTESIAN_POINT('Ctrl Pts',(-2.36557007798156,1.74912612642952,14.0765556218008));
#66932=CARTESIAN_POINT('Ctrl Pts',(-2.42034738467949,1.67504367135719,14.0815527761085));
#66933=CARTESIAN_POINT('Ctrl Pts',(-2.47172631103157,1.59827030322655,14.0865499304161));
#66934=CARTESIAN_POINT('Ctrl Pts',(-2.51943079147653,1.51915518857026,14.0915470847238));
#66935=CARTESIAN_POINT('Ctrl Pts',(-2.56708930283369,1.44011631098056,14.0965394236635));
#66936=CARTESIAN_POINT('Ctrl Pts',(-2.6110801661733,1.35874055337824,14.1015317626033));
#66937=CARTESIAN_POINT('Ctrl Pts',(-2.65116943561575,1.27540763038992,14.106524101543));
#66938=CARTESIAN_POINT('Ctrl Pts',(-2.69123180915622,1.19213061548275,14.1115130911212));
#66939=CARTESIAN_POINT('Ctrl Pts',(-2.72739759264673,1.10689945089866,14.1165020806993));
#66940=CARTESIAN_POINT('Ctrl Pts',(-2.75947842570916,1.0201190215096,14.1214910702775));
#66941=CARTESIAN_POINT('Ctrl Pts',(-2.79155519502114,0.933349584790464,
14.1264794278892));
#66942=CARTESIAN_POINT('Ctrl Pts',(-2.81954787202627,0.845031693356858,
14.131467785501));
#66943=CARTESIAN_POINT('Ctrl Pts',(-2.84331634284331,0.755589951309676,
14.1364561431128));
#66944=CARTESIAN_POINT('Ctrl Pts',(-2.86708219185211,0.666158075235707,
14.1414439504781));
#66945=CARTESIAN_POINT('Ctrl Pts',(-2.88662465035953,0.575603034936791,
14.1464317578433));
#66946=CARTESIAN_POINT('Ctrl Pts',(-2.90185401778846,0.484362735400811,
14.1514195652086));
#66947=CARTESIAN_POINT('Ctrl Pts',(-2.91709378833748,0.393060109980562,
14.1564107797252));
#66948=CARTESIAN_POINT('Ctrl Pts',(-2.92801451324544,0.301071739064547,
14.1614019942418));
#66949=CARTESIAN_POINT('Ctrl Pts',(-2.93457808096583,0.208843210842305,
14.1663932087584));
#66950=CARTESIAN_POINT('Ctrl Pts',(-2.93958861855725,0.13843721712899,14.1702034334757));
#66951=CARTESIAN_POINT('Ctrl Pts',(-2.94206104379116,0.0678914605600493,
14.1740136581931));
#66952=CARTESIAN_POINT('Ctrl Pts',(-2.94199885496765,-0.00259564423991444,
14.1778238829104));
#66953=CARTESIAN_POINT('',(-2.14520543675184,2.01332005258239,15.058));
#66954=CARTESIAN_POINT('Ctrl Pts',(-2.94199885496721,-0.00259564473995252,
14.1778238829374));
#66955=CARTESIAN_POINT('Ctrl Pts',(-2.94189565643288,-0.119564644835924,
14.1841467156966));
#66956=CARTESIAN_POINT('Ctrl Pts',(-2.93481305925187,-0.236228347809689,
14.1904695484559));
#66957=CARTESIAN_POINT('Ctrl Pts',(-2.92088173825648,-0.351871952732533,
14.1967923812151));
#66958=CARTESIAN_POINT('Ctrl Pts',(-2.90668755319215,-0.469697586807298,
14.2032345167703));
#66959=CARTESIAN_POINT('Ctrl Pts',(-2.88538377477223,-0.58646445157355,
14.2096766523255));
#66960=CARTESIAN_POINT('Ctrl Pts',(-2.85715701480589,-0.701439799801467,
14.2161187878807));
#66961=CARTESIAN_POINT('Ctrl Pts',(-2.85215996086937,-0.721794173351571,
14.2172592552554));
#66962=CARTESIAN_POINT('Ctrl Pts',(-2.84694605760728,-0.742092453460343,
14.2183997226302));
#66963=CARTESIAN_POINT('Ctrl Pts',(-2.84151649525502,-0.762330641646823,
14.2195401900049));
#66964=CARTESIAN_POINT('Ctrl Pts',(-2.81744663606155,-0.852048800933916,
14.2245960098561));
#66965=CARTESIAN_POINT('Ctrl Pts',(-2.78908102661924,-0.940784068631668,
14.2296518297074));
#66966=CARTESIAN_POINT('Ctrl Pts',(-2.75651675117941,-1.028095034745,14.2347076495587));
#66967=CARTESIAN_POINT('Ctrl Pts',(-2.72399686991963,-1.11528697168611,
14.2397565769189));
#66968=CARTESIAN_POINT('Ctrl Pts',(-2.68728985116877,-1.20105805364865,
14.2448055042791));
#66969=CARTESIAN_POINT('Ctrl Pts',(-2.6465430991831,-1.28498000924774,14.2498544316393));
#66970=CARTESIAN_POINT('Ctrl Pts',(-2.6058393594745,-1.36881337681881,14.2548980293511));
#66971=CARTESIAN_POINT('Ctrl Pts',(-2.56110455572065,-1.45080110112108,
14.2599416270629));
#66972=CARTESIAN_POINT('Ctrl Pts',(-2.5125345231665,-1.53053398194763,14.2649852247747));
#66973=CARTESIAN_POINT('Ctrl Pts',(-2.46399877791862,-1.61021057650958,
14.2700252620322));
#66974=CARTESIAN_POINT('Ctrl Pts',(-2.41163341555522,-1.68763511388406,
14.2750652992898));
#66975=CARTESIAN_POINT('Ctrl Pts',(-2.35568013616085,-1.76242307522831,
14.2801053365473));
#66976=CARTESIAN_POINT('Ctrl Pts',(-2.29974662484673,-1.83718461427098,
14.2851435931789));
#66977=CARTESIAN_POINT('Ctrl Pts',(-2.24022798033645,-1.90931107315869,
14.2901818498104));
#66978=CARTESIAN_POINT('Ctrl Pts',(-2.17740855236688,-1.9784478755023,14.295220106442));
#66979=CARTESIAN_POINT('Ctrl Pts',(-2.11459381790793,-2.04757951233699,
14.3002579866437));
#66980=CARTESIAN_POINT('Ctrl Pts',(-2.04847908882045,-2.11372160873315,
14.3052958668454));
#66981=CARTESIAN_POINT('Ctrl Pts',(-1.97938747119111,-2.17655444197743,
14.310333747047));
#66982=CARTESIAN_POINT('Ctrl Pts',(-1.91028176834968,-2.23940008450034,
14.3153726542852));
#66983=CARTESIAN_POINT('Ctrl Pts',(-1.83819829999229,-2.29893482591311,
14.3204115615233));
#66984=CARTESIAN_POINT('Ctrl Pts',(-1.76349445914154,-2.35487819060288,
14.3254504687615));
#66985=CARTESIAN_POINT('Ctrl Pts',(-1.6887092302608,-2.41088250423706,14.3304948657673));
#66986=CARTESIAN_POINT('Ctrl Pts',(-1.61129828619155,-2.46328736521615,
14.3355392627732));
#66987=CARTESIAN_POINT('Ctrl Pts',(-1.5316490427886,-2.51185493405267,14.340583659779));
#66988=CARTESIAN_POINT('Ctrl Pts',(-1.45195041378729,-2.56045261665231,
14.3456311845053));
#66989=CARTESIAN_POINT('Ctrl Pts',(-1.3700111113627,-2.60520805793399,14.3506787092316));
#66990=CARTESIAN_POINT('Ctrl Pts',(-1.28624233540467,-2.64592982798349,
14.3557262339578));
#66991=CARTESIAN_POINT('Ctrl Pts',(-1.20234122426813,-2.68671592895638,
14.3607817325989));
#66992=CARTESIAN_POINT('Ctrl Pts',(-1.1166052773998,-2.7234554642434,14.3658372312401));
#66993=CARTESIAN_POINT('Ctrl Pts',(-1.02946457505551,-2.75600556761153,
14.3708927298812));
#66994=CARTESIAN_POINT('Ctrl Pts',(-0.991300245927731,-2.7702612807819,
14.3731068469224));
#66995=CARTESIAN_POINT('Ctrl Pts',(-0.952866649820146,-2.78371406631994,
14.3753209639636));
#66996=CARTESIAN_POINT('Ctrl Pts',(-0.914200613338942,-2.79635499151497,
14.3775350810048));
#66997=CARTESIAN_POINT('Ctrl Pts',(-0.825904134260677,-2.82522138922698,
14.3825911652792));
#66998=CARTESIAN_POINT('Ctrl Pts',(-0.736083485315032,-2.84995255267627,
14.3876472495537));
#66999=CARTESIAN_POINT('Ctrl Pts',(-0.645161442640455,-2.8703885996377,
14.3927033338281));
#67000=CARTESIAN_POINT('Ctrl Pts',(-0.554363358769105,-2.89079678506138,
14.3977525248769));
#67001=CARTESIAN_POINT('Ctrl Pts',(-0.462467294202034,-2.90692139435603,
14.4028017159257));
#67002=CARTESIAN_POINT('Ctrl Pts',(-0.369912515066137,-2.91865186879104,
14.4078509069745));
#67003=CARTESIAN_POINT('Ctrl Pts',(-0.277455451504325,-2.93036995866791,
14.4128947672926));
#67004=CARTESIAN_POINT('Ctrl Pts',(-0.184341493399725,-2.937703079752,14.4179386276107));
#67005=CARTESIAN_POINT('Ctrl Pts',(-0.0910203966399159,-2.94059165600998,
14.4229824879288));
#67006=CARTESIAN_POINT('Ctrl Pts',(0.00223477549366748,-2.9434781916971,
14.4280227851232));
#67007=CARTESIAN_POINT('Ctrl Pts',(0.0956963534091555,-2.94192640984882,
14.4330630823177));
#67008=CARTESIAN_POINT('Ctrl Pts',(0.188910191959557,-2.93592863322217,
14.4381033795121));
#67009=CARTESIAN_POINT('Ctrl Pts',(0.282091067504582,-2.92993297757612,
14.4431418943174));
#67010=CARTESIAN_POINT('Ctrl Pts',(0.375023935629332,-2.91949447924339,
14.4481804091226));
#67011=CARTESIAN_POINT('Ctrl Pts',(0.467256423995743,-2.90465754164492,
14.4532189239278));
#67012=CARTESIAN_POINT('Ctrl Pts',(0.559481983632671,-2.88982171863339,
14.4582570602275));
#67013=CARTESIAN_POINT('Ctrl Pts',(0.651006830355907,-2.87058818408287,
14.4632951965272));
#67014=CARTESIAN_POINT('Ctrl Pts',(0.741386604551002,-2.84705284506493,
14.4683333328268));
#67015=CARTESIAN_POINT('Ctrl Pts',(0.831784760014276,-2.82351271947409,
14.4733724937732));
#67016=CARTESIAN_POINT('Ctrl Pts',(0.921036951425746,-2.79566916391259,
14.4784116547196));
#67017=CARTESIAN_POINT('Ctrl Pts',(1.00871295298068,-2.76366824682142,14.4834508156659));
#67018=CARTESIAN_POINT('Ctrl Pts',(1.0964843818845,-2.7316324996442,14.4884954612804));
#67019=CARTESIAN_POINT('Ctrl Pts',(1.18267577958268,-2.69543051155382,14.4935401068949));
#67020=CARTESIAN_POINT('Ctrl Pts',(1.2668762223947,-2.65525679306747,14.4985847525093));
#67021=CARTESIAN_POINT('Ctrl Pts',(1.35112882736926,-2.61505818696814,14.5036325232811));
#67022=CARTESIAN_POINT('Ctrl Pts',(1.43338763160374,-2.5708831616033,14.5086802940528));
#67023=CARTESIAN_POINT('Ctrl Pts',(1.51326758167948,-2.5229715072188,14.5137280648245));
#67024=CARTESIAN_POINT('Ctrl Pts',(1.59327361875479,-2.47498422638813,14.5187838032811));
#67025=CARTESIAN_POINT('Ctrl Pts',(1.6708929378474,-2.42324878851226,14.5238395417377));
#67026=CARTESIAN_POINT('Ctrl Pts',(1.74577083965426,-2.36804733386241,14.5288952801943));
#67027=CARTESIAN_POINT('Ctrl Pts',(1.77852515808371,-2.3439002092804,14.5311068441312));
#67028=CARTESIAN_POINT('Ctrl Pts',(1.81075535040236,-2.31909036610409,14.5333184080681));
#67029=CARTESIAN_POINT('Ctrl Pts',(1.84243390724532,-2.29364367272529,14.5355299720049));
#67030=CARTESIAN_POINT('Ctrl Pts',(1.91486001573722,-2.23546536035615,14.5405862304204));
#67031=CARTESIAN_POINT('Ctrl Pts',(1.98465534059067,-2.17375074658722,14.5456424888359));
#67032=CARTESIAN_POINT('Ctrl Pts',(2.05145495982987,-2.1087665939571,14.5506987472514));
#67033=CARTESIAN_POINT('Ctrl Pts',(2.11816355342989,-2.04387099308966,14.5557481156702));
#67034=CARTESIAN_POINT('Ctrl Pts',(2.1818842384775,-1.97571501370655,14.560797484089));
#67035=CARTESIAN_POINT('Ctrl Pts',(2.24228439509932,-1.90460617753227,14.5658468525078));
#67036=CARTESIAN_POINT('Ctrl Pts',(2.30262082108396,-1.83357237115413,14.5708908931347));
#67037=CARTESIAN_POINT('Ctrl Pts',(2.35964339746632,-1.75959223743332,14.5759349337616));
#67038=CARTESIAN_POINT('Ctrl Pts',(2.41305647398855,-1.68300993857492,14.5809789743885));
#67039=CARTESIAN_POINT('Ctrl Pts',(2.46643185705006,-1.60648168363351,14.5860194554499));
#67040=CARTESIAN_POINT('Ctrl Pts',(2.51620255046604,-1.52735527639034,14.5910599365112));
#67041=CARTESIAN_POINT('Ctrl Pts',(2.56211397344786,-1.44600691113951,14.5961004175726));
#67042=CARTESIAN_POINT('Ctrl Pts',(2.60800918087819,-1.36468727748791,14.6011391183759));
#67043=CARTESIAN_POINT('Ctrl Pts',(2.65004760823598,-1.28114763078779,14.6061778191791));
#67044=CARTESIAN_POINT('Ctrl Pts',(2.68801926317368,-1.19579113594609,14.6112165199824));
#67045=CARTESIAN_POINT('Ctrl Pts',(2.72598807988017,-1.11044102116521,14.6162548441628));
#67046=CARTESIAN_POINT('Ctrl Pts',(2.75989054863299,-1.02327473352243,14.6212931683431));
#67047=CARTESIAN_POINT('Ctrl Pts',(2.78956419132914,-0.934716867534871,
14.6263314925234));
#67048=CARTESIAN_POINT('Ctrl Pts',(2.81924387840178,-0.846140962741329,
14.6313708429858));
#67049=CARTESIAN_POINT('Ctrl Pts',(2.84469288811306,-0.756173337145417,
14.6364101934482));
#67050=CARTESIAN_POINT('Ctrl Pts',(2.86579847665913,-0.665254155325767,
14.6414495439106));
#67051=CARTESIAN_POINT('Ctrl Pts',(2.88692704124803,-0.574235996734604,
14.6464943803291));
#67052=CARTESIAN_POINT('Ctrl Pts',(2.90370264655347,-0.482264646847366,
14.6515392167476));
#67053=CARTESIAN_POINT('Ctrl Pts',(2.91606366689416,-0.38979057276928,14.6565840531661));
#67054=CARTESIAN_POINT('Ctrl Pts',(2.92843234706057,-0.297259194741166,
14.6616320157479));
#67055=CARTESIAN_POINT('Ctrl Pts',(2.93638095831432,-0.204224913726281,
14.6666799783297));
#67056=CARTESIAN_POINT('Ctrl Pts',(2.93989993331261,-0.111141270950566,
14.6717279409115));
#67057=CARTESIAN_POINT('Ctrl Pts',(2.9434244624339,-0.0179107109612863,
14.6767838708715));
#67058=CARTESIAN_POINT('Ctrl Pts',(2.94250540358311,0.075368923634541,14.6818398008316));
#67059=CARTESIAN_POINT('Ctrl Pts',(2.93718524404744,0.168246373363566,14.6868957307917));
#67060=CARTESIAN_POINT('Ctrl Pts',(2.93486005090881,0.20883876676735,14.6891054415295));
#67061=CARTESIAN_POINT('Ctrl Pts',(2.93169484525421,0.24935443342959,14.6913151522672));
#67062=CARTESIAN_POINT('Ctrl Pts',(2.92769624279459,0.289756294023833,14.693524863005));
#67063=CARTESIAN_POINT('Ctrl Pts',(2.91854904743635,0.382179513242121,14.6985797930731));
#67064=CARTESIAN_POINT('Ctrl Pts',(2.90500489782404,0.474332466220693,14.7036347231412));
#67065=CARTESIAN_POINT('Ctrl Pts',(2.88708765809673,0.565763956492032,14.7086896532093));
#67066=CARTESIAN_POINT('Ctrl Pts',(2.86919485437241,0.65707075009114,14.7137376892307));
#67067=CARTESIAN_POINT('Ctrl Pts',(2.84694089715092,0.747657604582368,14.7187857252522));
#67068=CARTESIAN_POINT('Ctrl Pts',(2.82040143879216,0.837078087193264,14.7238337612737));
#67069=CARTESIAN_POINT('Ctrl Pts',(2.79389000213786,0.926404155129092,14.728876467323));
#67070=CARTESIAN_POINT('Ctrl Pts',(2.76310218415545,1.01456587599627,14.7339191733723));
#67071=CARTESIAN_POINT('Ctrl Pts',(2.72816452790847,1.10112774402517,14.7389618794216));
#67072=CARTESIAN_POINT('Ctrl Pts',(2.69325151757845,1.18762854909678,14.7440010282171));
#67073=CARTESIAN_POINT('Ctrl Pts',(2.65419465335663,1.27253133430926,14.7490401770125));
#67074=CARTESIAN_POINT('Ctrl Pts',(2.61116975058343,1.35541747577565,14.7540793258079));
#67075=CARTESIAN_POINT('Ctrl Pts',(2.56816003098295,1.43827436733049,14.7591166963246));
#67076=CARTESIAN_POINT('Ctrl Pts',(2.52118525904805,1.51911563561082,14.7641540668414));
#67077=CARTESIAN_POINT('Ctrl Pts',(2.47046820581466,1.59754525571544,14.7691914373581));
#67078=CARTESIAN_POINT('Ctrl Pts',(2.4197549078974,1.67596906854225,14.7742284348856));
#67079=CARTESIAN_POINT('Ctrl Pts',(2.36530012081552,1.75198121585167,14.779265432413));
#67080=CARTESIAN_POINT('Ctrl Pts',(2.30737052829664,1.82521375327606,14.7843024299404));
#67081=CARTESIAN_POINT('Ctrl Pts',(2.2494290718373,1.89846128867344,14.7893404590415));
#67082=CARTESIAN_POINT('Ctrl Pts',(2.18801167210225,1.96892773589567,14.7943784881425));
#67083=CARTESIAN_POINT('Ctrl Pts',(2.12342522929933,2.0362782952178,14.7994165172436));
#67084=CARTESIAN_POINT('Ctrl Pts',(2.05876825398377,2.103702405644,14.8044600481935));
#67085=CARTESIAN_POINT('Ctrl Pts',(1.9909356354547,2.16800351568651,14.8095035791435));
#67086=CARTESIAN_POINT('Ctrl Pts',(1.92027083415288,2.22888400853472,14.8145471100935));
#67087=CARTESIAN_POINT('Ctrl Pts',(1.84956213092389,2.28980232461195,14.8195937744384));
#67088=CARTESIAN_POINT('Ctrl Pts',(1.77601809119875,2.34729551974612,14.8246404387832));
#67089=CARTESIAN_POINT('Ctrl Pts',(1.70001319058036,2.4011079009184,14.8296871031281));
#67090=CARTESIAN_POINT('Ctrl Pts',(1.62388794625745,2.45500548687679,14.8347417581983));
#67091=CARTESIAN_POINT('Ctrl Pts',(1.54529443642721,2.505210386688,14.8397964132685));
#67092=CARTESIAN_POINT('Ctrl Pts',(1.46463366396149,2.55151175391977,14.8448510683387));
#67093=CARTESIAN_POINT('Ctrl Pts',(1.42916132346781,2.57187379377584,14.8470739635608));
#67094=CARTESIAN_POINT('Ctrl Pts',(1.39328946144843,2.59148150978898,14.8492968587829));
#67095=CARTESIAN_POINT('Ctrl Pts',(1.35705338672014,2.61031992399235,14.8515197540051));
#67096=CARTESIAN_POINT('Ctrl Pts',(1.27461660312295,2.65317716740632,14.8565768230657));
#67097=CARTESIAN_POINT('Ctrl Pts',(1.19000253446716,2.69220084533978,14.8616338921263));
#67098=CARTESIAN_POINT('Ctrl Pts',(1.10360245323297,2.7271643927747,14.8666909611869));
#67099=CARTESIAN_POINT('Ctrl Pts',(1.01732021364868,2.76208025319291,14.8717411328771));
#67100=CARTESIAN_POINT('Ctrl Pts',(0.929257209804122,2.79294682294084,14.8767913045673));
#67101=CARTESIAN_POINT('Ctrl Pts',(0.839829004222327,2.81958352308757,14.8818414762576));
#67102=CARTESIAN_POINT('Ctrl Pts',(0.750495290970565,2.84619207815586,14.8868863117959));
#67103=CARTESIAN_POINT('Ctrl Pts',(0.659799665997159,2.86857952193179,14.8919311473342));
#67104=CARTESIAN_POINT('Ctrl Pts',(0.56817633346858,2.88661387339668,14.8969759828725));
#67105=CARTESIAN_POINT('Ctrl Pts',(0.47661793118525,2.90463544454862,14.9020172433126));
#67106=CARTESIAN_POINT('Ctrl Pts',(0.384133561889784,2.91830997004826,14.9070585037528));
#67107=CARTESIAN_POINT('Ctrl Pts',(0.291170202025931,2.92755596248,14.9120997641929));
#67108=CARTESIAN_POINT('Ctrl Pts',(0.198239854739045,2.93679867153173,14.9171392344116));
#67109=CARTESIAN_POINT('Ctrl Pts',(0.10483129549399,2.94161592817868,14.9221787046303));
#67110=CARTESIAN_POINT('Ctrl Pts',(0.0113982264469119,2.94197791977334,
14.927218174849));
#67111=CARTESIAN_POINT('Ctrl Pts',(-0.0820276584529391,2.94233988353416,
14.9322572575786));
#67112=CARTESIAN_POINT('Ctrl Pts',(-0.175477606146424,2.93824726198362,
14.9372963403083));
#67113=CARTESIAN_POINT('Ctrl Pts',(-0.268497436916809,2.92972236335956,
14.9423354230379));
#67114=CARTESIAN_POINT('Ctrl Pts',(-0.361535995095789,2.92119574844276,
14.9473755202712));
#67115=CARTESIAN_POINT('Ctrl Pts',(-0.454143823029988,2.90823512502494,
14.9524156175045));
#67116=CARTESIAN_POINT('Ctrl Pts',(-0.545872518920582,2.89091459456818,
14.9574557147378));
#67117=CARTESIAN_POINT('Ctrl Pts',(-0.637700656134728,2.87357528725587,
14.962501275844));
#67118=CARTESIAN_POINT('Ctrl Pts',(-0.72864732283676,2.85186672123159,14.9675468369502));
#67119=CARTESIAN_POINT('Ctrl Pts',(-0.818275274387837,2.82591393629132,
14.9725923980565));
#67120=CARTESIAN_POINT('Ctrl Pts',(-0.907958552103803,2.79994513103558,
14.9776410737218));
#67121=CARTESIAN_POINT('Ctrl Pts',(-0.996321074966273,2.76972703420609,
14.982689749387));
#67122=CARTESIAN_POINT('Ctrl Pts',(-1.08294374574899,2.73543357505591,14.9877384250523));
#67123=CARTESIAN_POINT('Ctrl Pts',(-1.16970269872328,2.70108616250383,14.9927950437258));
#67124=CARTESIAN_POINT('Ctrl Pts',(-1.25471593226287,2.66265077107231,14.9978516623992));
#67125=CARTESIAN_POINT('Ctrl Pts',(-1.33758739858879,2.62034805915865,15.0029082810727));
#67126=CARTESIAN_POINT('Ctrl Pts',(-1.37367733018883,2.60192553030587,15.0051104023835));
#67127=CARTESIAN_POINT('Ctrl Pts',(-1.40936142196231,2.58277011622747,15.0073125236943));
#67128=CARTESIAN_POINT('Ctrl Pts',(-1.44460872073146,2.56290258183697,15.0095146450051));
#67129=CARTESIAN_POINT('Ctrl Pts',(-1.54202772550784,2.50799126961531,15.0156010253516));
#67130=CARTESIAN_POINT('Ctrl Pts',(-1.63638431559853,2.44748194167846,15.021687405698));
#67131=CARTESIAN_POINT('Ctrl Pts',(-1.72710266414602,2.38169695542899,15.0277737860445));
#67132=CARTESIAN_POINT('Ctrl Pts',(-1.81676908628711,2.31667478028982,15.0337895916472));
#67133=CARTESIAN_POINT('Ctrl Pts',(-1.90288109881628,2.24649858300431,15.0398053972498));
#67134=CARTESIAN_POINT('Ctrl Pts',(-1.98490247403207,2.17152623023103,15.0458212028525));
#67135=CARTESIAN_POINT('Ctrl Pts',(-2.0402523172333,2.12093322371886,15.0498808019017));
#67136=CARTESIAN_POINT('Ctrl Pts',(-2.09373974757189,2.06815707469092,15.0539404009508));
#67137=CARTESIAN_POINT('Ctrl Pts',(-2.14520543675184,2.01332005258239,15.058));
#67138=CARTESIAN_POINT('',(0.261483065272176,2.93035673708439,15.0579981933191));
#67139=CARTESIAN_POINT('Origin',(0.,0.,15.058));
#67140=CARTESIAN_POINT('',(-2.94199899580993,-0.00243077217840307,14.3221761170896));
#67141=CARTESIAN_POINT('Ctrl Pts',(0.261483065272176,2.93035673708439,15.0579981933191));
#67142=CARTESIAN_POINT('Ctrl Pts',(0.359661773013358,2.92159600528688,15.0526990630625));
#67143=CARTESIAN_POINT('Ctrl Pts',(0.45728330298564,2.90790733319514,15.0473999328059));
#67144=CARTESIAN_POINT('Ctrl Pts',(0.553856556304756,2.88939559683998,15.0421008025493));
#67145=CARTESIAN_POINT('Ctrl Pts',(0.650732804101302,2.87082578069884,15.0367850464967));
#67146=CARTESIAN_POINT('Ctrl Pts',(0.74655383536055,2.84740271291704,15.0314692904441));
#67147=CARTESIAN_POINT('Ctrl Pts',(0.84084094592112,2.8192819127683,15.0261535343916));
#67148=CARTESIAN_POINT('Ctrl Pts',(0.935282325557894,2.79111510240846,15.020829080896));
#67149=CARTESIAN_POINT('Ctrl Pts',(1.02818443064924,2.75823534881844,15.0155046274004));
#67150=CARTESIAN_POINT('Ctrl Pts',(1.11908839081021,2.72084640756398,15.0101801739048));
#67151=CARTESIAN_POINT('Ctrl Pts',(1.210258016484,2.68334819766782,15.0048401597706));
#67152=CARTESIAN_POINT('Ctrl Pts',(1.29941748571425,2.64131460587378,14.9995001456364));
#67153=CARTESIAN_POINT('Ctrl Pts',(1.3861310604502,2.59499608540267,14.9941601315022));
#67154=CARTESIAN_POINT('Ctrl Pts',(1.44494860738031,2.56357837762349,14.9905380165923));
#67155=CARTESIAN_POINT('Ctrl Pts',(1.50264140027149,2.53019016395851,14.9869159016824));
#67156=CARTESIAN_POINT('Ctrl Pts',(1.55908161262863,2.49492054485976,14.9832937867725));
#67157=CARTESIAN_POINT('Ctrl Pts',(1.63799388701391,2.44560808228123,14.9782295016876));
#67158=CARTESIAN_POINT('Ctrl Pts',(1.71470044723877,2.39246299705959,14.9731652166027));
#67159=CARTESIAN_POINT('Ctrl Pts',(1.78880676794263,2.33570853210812,14.9681009315178));
#67160=CARTESIAN_POINT('Ctrl Pts',(1.86281259231978,2.27903103245727,14.9630435141609));
#67161=CARTESIAN_POINT('Ctrl Pts',(1.93422483739239,2.2187541473552,14.9579860968039));
#67162=CARTESIAN_POINT('Ctrl Pts',(2.00267634239024,2.15514534721685,14.952928679447));
#67163=CARTESIAN_POINT('Ctrl Pts',(2.07457810505856,2.08833038308557,14.9476163459559));
#67164=CARTESIAN_POINT('Ctrl Pts',(2.14321240660558,2.01783906022885,14.9423040124648));
#67165=CARTESIAN_POINT('Ctrl Pts',(2.20819115000048,1.94403082410222,14.9369916789738));
#67166=CARTESIAN_POINT('Ctrl Pts',(2.26994142235796,1.87388975265451,14.9319432889497));
#67167=CARTESIAN_POINT('Ctrl Pts',(2.32839034435918,1.80075383929931,14.9268948989257));
#67168=CARTESIAN_POINT('Ctrl Pts',(2.38324229469831,1.7249696127066,14.9218465089017));
#67169=CARTESIAN_POINT('Ctrl Pts',(2.43807549335941,1.64921129369617,14.9167998447194));
#67170=CARTESIAN_POINT('Ctrl Pts',(2.48931390495793,1.57080681794917,14.9117531805371));
#67171=CARTESIAN_POINT('Ctrl Pts',(2.53670323007296,1.49013446458278,14.9067065163548));
#67172=CARTESIAN_POINT('Ctrl Pts',(2.58408942671674,1.40946743691236,14.901660185335));
#67173=CARTESIAN_POINT('Ctrl Pts',(2.62762681880991,1.32653321046229,14.8966138543152));
#67174=CARTESIAN_POINT('Ctrl Pts',(2.66710593886766,1.24173665116919,14.8915675232953));
#67175=CARTESIAN_POINT('Ctrl Pts',(2.70659334242671,1.15692229987847,14.8865201334553));
#67176=CARTESIAN_POINT('Ctrl Pts',(2.74202059656648,1.07024524019156,14.8814727436153));
#67177=CARTESIAN_POINT('Ctrl Pts',(2.77322591465876,0.982131369148298,14.8764253537752));
#67178=CARTESIAN_POINT('Ctrl Pts',(2.8044646487814,0.893923141887225,14.8713725589676));
#67179=CARTESIAN_POINT('Ctrl Pts',(2.83147227578439,0.804275449368773,14.86631976416));
#67180=CARTESIAN_POINT('Ctrl Pts',(2.85413665238589,0.713630134949094,14.8612669693524));
#67181=CARTESIAN_POINT('Ctrl Pts',(2.87681511196177,0.622928496207644,14.8562110348873));
#67182=CARTESIAN_POINT('Ctrl Pts',(2.895144861223,0.531228434084276,14.8511551004222));
#67183=CARTESIAN_POINT('Ctrl Pts',(2.90906513108331,0.438980709274588,14.8460991659571));
#67184=CARTESIAN_POINT('Ctrl Pts',(2.92300664127415,0.346592227699102,14.8410355168629));
#67185=CARTESIAN_POINT('Ctrl Pts',(2.93252519769504,0.25365485410448,14.8359718677687));
#67186=CARTESIAN_POINT('Ctrl Pts',(2.93761200366519,0.160622899744075,14.8309082186745));
#67187=CARTESIAN_POINT('Ctrl Pts',(2.93944553151384,0.127089739616721,14.8290830376701));
#67188=CARTESIAN_POINT('Ctrl Pts',(2.94070376646984,0.0935442727577978,
14.8272578566656));
#67189=CARTESIAN_POINT('Ctrl Pts',(2.94138795159684,0.0600076511867527,
14.8254326756612));
#67190=CARTESIAN_POINT('Ctrl Pts',(2.94328660875558,-0.0330586025407972,
14.8203676825134));
#67191=CARTESIAN_POINT('Ctrl Pts',(2.94076720379232,-0.126372285094918,
14.8153026893656));
#67192=CARTESIAN_POINT('Ctrl Pts',(2.93380166489366,-0.21948073051458,14.8102376962178));
#67193=CARTESIAN_POINT('Ctrl Pts',(2.92684535599062,-0.312465798467389,
14.8051794146633));
#67194=CARTESIAN_POINT('Ctrl Pts',(2.91545465513211,-0.405245732896898,
14.8001211331089));
#67195=CARTESIAN_POINT('Ctrl Pts',(2.8996534899233,-0.497366704128502,14.7950628515544));
#67196=CARTESIAN_POINT('Ctrl Pts',(2.8830593259192,-0.59411086727295,14.7897507145959));
#67197=CARTESIAN_POINT('Ctrl Pts',(2.8616004292145,-0.690127704461536,14.7844385776374));
#67198=CARTESIAN_POINT('Ctrl Pts',(2.8353663274954,-0.784896037004432,14.7791264406789));
#67199=CARTESIAN_POINT('Ctrl Pts',(2.81042856039029,-0.874981477367452,
14.7740767982051));
#67200=CARTESIAN_POINT('Ctrl Pts',(2.78117639119523,-0.963938376115757,
14.7690271557314));
#67201=CARTESIAN_POINT('Ctrl Pts',(2.74773902194529,-1.05132976143509,14.7639775132576));
#67202=CARTESIAN_POINT('Ctrl Pts',(2.71431215219443,-1.13869370542782,14.7589294563965));
#67203=CARTESIAN_POINT('Ctrl Pts',(2.67670285138473,-1.22449270066437,14.7538813995354));
#67204=CARTESIAN_POINT('Ctrl Pts',(2.63508946894432,-1.3083071086938,14.7488333426744));
#67205=CARTESIAN_POINT('Ctrl Pts',(2.59347768630801,-1.39211829452341,14.7437854798831));
#67206=CARTESIAN_POINT('Ctrl Pts',(2.54786232501567,-1.47394464957085,14.7387376170918));
#67207=CARTESIAN_POINT('Ctrl Pts',(2.49846846617174,-1.55338962386951,14.7336897543006));
#67208=CARTESIAN_POINT('Ctrl Pts',(2.44906289559007,-1.63285343530146,14.7286406946147));
#67209=CARTESIAN_POINT('Ctrl Pts',(2.39587728115249,-1.70993436955877,14.7235916349288));
#67210=CARTESIAN_POINT('Ctrl Pts',(2.33918033139902,-1.78426437984844,14.7185425752429));
#67211=CARTESIAN_POINT('Ctrl Pts',(2.28242045583138,-1.85867688622363,14.7134879117954));
#67212=CARTESIAN_POINT('Ctrl Pts',(2.22214173515893,-1.93033202352542,14.7084332483478));
#67213=CARTESIAN_POINT('Ctrl Pts',(2.15865332432241,-1.9988946508988,14.7033785849003));
#67214=CARTESIAN_POINT('Ctrl Pts',(2.09512400695069,-2.06750145420118,14.6983206646573));
#67215=CARTESIAN_POINT('Ctrl Pts',(2.02838119685972,-2.13301147158374,14.6932627444143));
#67216=CARTESIAN_POINT('Ctrl Pts',(1.95876953423314,-2.19512776661407,14.6882048241713));
#67217=CARTESIAN_POINT('Ctrl Pts',(1.88904949279933,-2.25734077086971,14.6831390292225));
#67218=CARTESIAN_POINT('Ctrl Pts',(1.8164520263333,-2.31614922946661,14.6780732342738));
#67219=CARTESIAN_POINT('Ctrl Pts',(1.7413530971558,-2.37129782841083,14.673007439325));
#67220=CARTESIAN_POINT('Ctrl Pts',(1.71449134568613,-2.3910236484054,14.6711954810667));
#67221=CARTESIAN_POINT('Ctrl Pts',(1.68730980978028,-2.4102816484538,14.6693835228084));
#67222=CARTESIAN_POINT('Ctrl Pts',(1.65982647247631,-2.42906156391041,14.6675715645502));
#67223=CARTESIAN_POINT('Ctrl Pts',(1.58323294978353,-2.48139945376653,14.6625218042376));
#67224=CARTESIAN_POINT('Ctrl Pts',(1.50402331994656,-2.53020547805049,14.6574720439251));
#67225=CARTESIAN_POINT('Ctrl Pts',(1.42255732262935,-2.57520769333924,14.6524222836126));
#67226=CARTESIAN_POINT('Ctrl Pts',(1.34120382081709,-2.62014776556095,14.6473794964589));
#67227=CARTESIAN_POINT('Ctrl Pts',(1.25760052876846,-2.66129425305727,14.6423367093051));
#67228=CARTESIAN_POINT('Ctrl Pts',(1.17213692290193,-2.69841787608406,14.6372939221514));
#67229=CARTESIAN_POINT('Ctrl Pts',(1.08676485621621,-2.73550173638371,14.6322565362746));
#67230=CARTESIAN_POINT('Ctrl Pts',(0.999536841876472,-2.76857112030728,
14.6272191503979));
#67231=CARTESIAN_POINT('Ctrl Pts',(0.910866790340188,-2.79744270544642,
14.6221817645211));
#67232=CARTESIAN_POINT('Ctrl Pts',(0.822260869946003,-2.8262934090399,14.6171480219636));
#67233=CARTESIAN_POINT('Ctrl Pts',(0.732215407066378,-2.85095221122863,
14.6121142794061));
#67234=CARTESIAN_POINT('Ctrl Pts',(0.64116313067073,-2.87128435371151,14.6070805368487));
#67235=CARTESIAN_POINT('Ctrl Pts',(0.550143932939321,-2.89160910966721,
14.6020486230152));
#67236=CARTESIAN_POINT('Ctrl Pts',(0.45811908193511,-2.90761023173326,14.5970167091816));
#67237=CARTESIAN_POINT('Ctrl Pts',(0.365534253305122,-2.9192034375255,14.5919847953481));
#67238=CARTESIAN_POINT('Ctrl Pts',(0.272957092441749,-2.93079568318207,
14.5869532982518));
#67239=CARTESIAN_POINT('Ctrl Pts',(0.179820487475819,-2.93798068339455,
14.5819218011555));
#67240=CARTESIAN_POINT('Ctrl Pts',(0.0865768933064366,-2.94072583583465,
14.5768903040592));
#67241=CARTESIAN_POINT('Ctrl Pts',(-0.00668513067810722,-2.94347153086057,
14.5718578124756));
#67242=CARTESIAN_POINT('Ctrl Pts',(-0.100053741348647,-2.94177562272804,
14.5668253208921));
#67243=CARTESIAN_POINT('Ctrl Pts',(-0.193075973589511,-2.93565762111702,
14.5617928293086));
#67244=CARTESIAN_POINT('Ctrl Pts',(-0.286199262361645,-2.92953297309465,
14.5567548705788));
#67245=CARTESIAN_POINT('Ctrl Pts',(-0.378974977231565,-2.91897667224081,
14.5517169118491));
#67246=CARTESIAN_POINT('Ctrl Pts',(-0.470955102753805,-2.90406013904502,
14.5466789531194));
#67247=CARTESIAN_POINT('Ctrl Pts',(-0.56299205820675,-2.88913438966754,
14.5416378816863));
#67248=CARTESIAN_POINT('Ctrl Pts',(-0.654232011064526,-2.86984313698716,
14.5365968102532));
#67249=CARTESIAN_POINT('Ctrl Pts',(-0.744239103737049,-2.8463085139297,
14.5315557388201));
#67250=CARTESIAN_POINT('Ctrl Pts',(-0.834388722700486,-2.82273662378102,
14.5265066848471));
#67251=CARTESIAN_POINT('Ctrl Pts',(-0.923301160924991,-2.79490808336421,
14.521457630874));
#67252=CARTESIAN_POINT('Ctrl Pts',(-1.01055785568057,-2.7629941766718,14.516408576901));
#67253=CARTESIAN_POINT('Ctrl Pts',(-1.04914304526776,-2.74888174502809,
14.5141758690803));
#67254=CARTESIAN_POINT('Ctrl Pts',(-1.08740475570698,-2.73397106640143,
14.5119431612597));
#67255=CARTESIAN_POINT('Ctrl Pts',(-1.12530831193825,-2.71827982427908,
14.509710453439));
#67256=CARTESIAN_POINT('Ctrl Pts',(-1.21117629085882,-2.68273236167218,
14.5046524027667));
#67257=CARTESIAN_POINT('Ctrl Pts',(-1.29550855517803,-2.6430499600766,14.4995943520943));
#67258=CARTESIAN_POINT('Ctrl Pts',(-1.37787983046257,-2.59938669166487,
14.494536301422));
#67259=CARTESIAN_POINT('Ctrl Pts',(-1.46013917454961,-2.55578275561024,
14.4894851239426));
#67260=CARTESIAN_POINT('Ctrl Pts',(-1.54044243695998,-2.50820890864038,
14.4844339464632));
#67261=CARTESIAN_POINT('Ctrl Pts',(-1.61838395162,-2.45686739266466,14.4793827689838));
#67262=CARTESIAN_POINT('Ctrl Pts',(-1.6962434735779,-2.40557988679695,14.4743369052283));
#67263=CARTESIAN_POINT('Ctrl Pts',(-1.7717458184305,-2.35053283308713,14.4692910414728));
#67264=CARTESIAN_POINT('Ctrl Pts',(-1.8445105575821,-2.29197399700961,14.4642451777173));
#67265=CARTESIAN_POINT('Ctrl Pts',(-1.91722412050728,-2.23345634599354,
14.4592028627722));
#67266=CARTESIAN_POINT('Ctrl Pts',(-1.98720356076137,-2.17143209917494,
14.4541605478272));
#67267=CARTESIAN_POINT('Ctrl Pts',(-2.0540989090585,-2.10619127141974,14.4491182328822));
#67268=CARTESIAN_POINT('Ctrl Pts',(-2.12097073098796,-2.04097338815528,
14.4440776912645));
#67269=CARTESIAN_POINT('Ctrl Pts',(-2.18476029907851,-1.9725414805608,14.4390371496469));
#67270=CARTESIAN_POINT('Ctrl Pts',(-2.24515289510571,-1.90122394199065,
14.4339966080293));
#67271=CARTESIAN_POINT('Ctrl Pts',(-2.30554103308762,-1.82991166792041,
14.4289564384931));
#67272=CARTESIAN_POINT('Ctrl Pts',(-2.36253241155492,-1.75571452473796,
14.4239162689569));
#67273=CARTESIAN_POINT('Ctrl Pts',(-2.4158519204632,-1.67899478807835,14.4188760994207));
#67274=CARTESIAN_POINT('Ctrl Pts',(-2.46918230912261,-1.60225939689269,
14.4138349014468));
#67275=CARTESIAN_POINT('Ctrl Pts',(-2.51883908763949,-1.52300075389714,
14.4087937034729));
#67276=CARTESIAN_POINT('Ctrl Pts',(-2.56459052396015,-1.44161001814423,
14.4037525054991));
#67277=CARTESIAN_POINT('Ctrl Pts',(-2.61039156885869,-1.36013102989089,
14.3987058413217));
#67278=CARTESIAN_POINT('Ctrl Pts',(-2.65227860204805,-1.27651572125823,
14.3936591771443));
#67279=CARTESIAN_POINT('Ctrl Pts',(-2.69006607358686,-1.19117946579724,
14.388612512967));
#67280=CARTESIAN_POINT('Ctrl Pts',(-2.72787694116127,-1.10579037456846,
14.3835627241578));
#67281=CARTESIAN_POINT('Ctrl Pts',(-2.76158303393655,-1.01867862796998,
14.3785129353487));
#67282=CARTESIAN_POINT('Ctrl Pts',(-2.79104790841499,-0.930277148452167,
14.3734631465395));
#67283=CARTESIAN_POINT('Ctrl Pts',(-2.82055898625829,-0.841737048088894,
14.368405439243));
#67284=CARTESIAN_POINT('Ctrl Pts',(-2.84581545058168,-0.75190360359488,
14.3633477319465));
#67285=CARTESIAN_POINT('Ctrl Pts',(-2.86673146364986,-0.661222137651145,
14.3582900246501));
#67286=CARTESIAN_POINT('Ctrl Pts',(-2.87560988673235,-0.622729695627666,
14.3561431305427));
#67287=CARTESIAN_POINT('Ctrl Pts',(-2.88370687142123,-0.584084543517024,
14.3539962364353));
#67288=CARTESIAN_POINT('Ctrl Pts',(-2.89101867841434,-0.54532100735198,
14.351849342328));
#67289=CARTESIAN_POINT('Ctrl Pts',(-2.9162676760388,-0.411463476174145,
14.344435727025));
#67290=CARTESIAN_POINT('Ctrl Pts',(-2.93222540650343,-0.27580307450041,
14.337022111722));
#67291=CARTESIAN_POINT('Ctrl Pts',(-2.93869582950559,-0.13939448212346,
14.329608496419));
#67292=CARTESIAN_POINT('Ctrl Pts',(-2.94085809610147,-0.0938098669305718,
14.3271310366425));
#67293=CARTESIAN_POINT('Ctrl Pts',(-2.9419612278275,-0.0481419117786443,
14.3246535768661));
#67294=CARTESIAN_POINT('Ctrl Pts',(-2.94199899580993,-0.00243077217840307,
14.3221761170896));
#67295=CARTESIAN_POINT('',(-2.94154465770424,0.000354470811248017,13.3221761002206));
#67296=CARTESIAN_POINT('Ctrl Pts',(-2.94325255946896,-0.00241996395558216,
14.3221754754428));
#67297=CARTESIAN_POINT('Ctrl Pts',(-2.9361986618122,0.786308567410447,14.2794463940342));
#67298=CARTESIAN_POINT('Ctrl Pts',(-2.20502853201952,2.55780260563958,14.1840969422552));
#67299=CARTESIAN_POINT('Ctrl Pts',(0.779438885227077,3.38200690959716,14.0361271201057));
#67300=CARTESIAN_POINT('Ctrl Pts',(3.25729747472218,1.19795113049604,13.8782660089947));
#67301=CARTESIAN_POINT('Ctrl Pts',(2.78492903121012,-2.07109504482707,13.7204048978835));
#67302=CARTESIAN_POINT('Ctrl Pts',(-0.209925428309956,-3.4642751230223,
13.5625437867724));
#67303=CARTESIAN_POINT('Ctrl Pts',(-2.5683496391778,-1.99726696188011,13.4298008598411));
#67304=CARTESIAN_POINT('Ctrl Pts',(-2.9367843178467,-0.509922711901109,
13.3496783032802));
#67305=CARTESIAN_POINT('Ctrl Pts',(-2.93733773658367,0.000353650820144602,
13.3221761170896));
#67306=CARTESIAN_POINT('',(-2.94199923889461,0.0021162097116246,12.3221761170896));
#67307=CARTESIAN_POINT('Ctrl Pts',(-2.94199997863486,0.0003545595600269,
13.3221760983949));
#67308=CARTESIAN_POINT('Ctrl Pts',(-2.9419880493624,0.0993391119192297,
13.3168496162708));
#67309=CARTESIAN_POINT('Ctrl Pts',(-2.93697629515374,0.198210372559447,
13.3115231341467));
#67310=CARTESIAN_POINT('Ctrl Pts',(-2.92702446251479,0.296465505312221,
13.3061966520225));
#67311=CARTESIAN_POINT('Ctrl Pts',(-2.91704196021071,0.395023441792436,
13.3008537546884));
#67312=CARTESIAN_POINT('Ctrl Pts',(-2.90208897278557,0.492961091822583,
13.2955108573543));
#67313=CARTESIAN_POINT('Ctrl Pts',(-2.88227683628384,0.589783213580746,
13.2901679600201));
#67314=CARTESIAN_POINT('Ctrl Pts',(-2.86243333684518,0.686758606345156,
13.2848166047919));
#67315=CARTESIAN_POINT('Ctrl Pts',(-2.83771543063832,0.782614597196314,
13.2794652495637));
#67316=CARTESIAN_POINT('Ctrl Pts',(-2.808284369287,0.876871085860581,13.2741138943355));
#67317=CARTESIAN_POINT('Ctrl Pts',(-2.77877089374446,0.971391515814227,
13.2687475539999));
#67318=CARTESIAN_POINT('Ctrl Pts',(-2.74451799497217,1.06430314579817,13.2633812136644));
#67319=CARTESIAN_POINT('Ctrl Pts',(-2.70573563698505,1.15514443371775,13.2580148733288));
#67320=CARTESIAN_POINT('Ctrl Pts',(-2.67877108380303,1.21830445972866,13.2542837704026));
#67321=CARTESIAN_POINT('Ctrl Pts',(-2.64961792582727,1.28046412723049,13.2505526674764));
#67322=CARTESIAN_POINT('Ctrl Pts',(-2.61835946279969,1.34147594967906,13.2468215645502));
#67323=CARTESIAN_POINT('Ctrl Pts',(-2.5759972019918,1.42416071676599,13.2417650793634));
#67324=CARTESIAN_POINT('Ctrl Pts',(-2.52963999234658,1.50498226700905,13.2367085941766));
#67325=CARTESIAN_POINT('Ctrl Pts',(-2.47947552240893,1.58352932835959,13.2316521089898));
#67326=CARTESIAN_POINT('Ctrl Pts',(-2.42937932357179,1.6619694914547,13.2266025054029));
#67327=CARTESIAN_POINT('Ctrl Pts',(-2.37548639797535,1.73814094657396,13.2215529018159));
#67328=CARTESIAN_POINT('Ctrl Pts',(-2.31803087083851,1.81165583978847,13.2165032982289));
#67329=CARTESIAN_POINT('Ctrl Pts',(-2.2606358735758,1.88509328445355,13.2114590144412));
#67330=CARTESIAN_POINT('Ctrl Pts',(-2.19968600696845,1.9558793829046,13.2064147306535));
#67331=CARTESIAN_POINT('Ctrl Pts',(-2.13545874046757,2.02365510098946,13.2013704468658));
#67332=CARTESIAN_POINT('Ctrl Pts',(-2.07127668804704,2.09138310698987,13.1963297141035));
#67333=CARTESIAN_POINT('Ctrl Pts',(-2.00382212594782,2.15610462414014,13.1912889813411));
#67334=CARTESIAN_POINT('Ctrl Pts',(-1.93341218163038,2.21749438238821,13.1862482485788));
#67335=CARTESIAN_POINT('Ctrl Pts',(-1.86302701698762,2.27886253547449,13.1812092898232));
#67336=CARTESIAN_POINT('Ctrl Pts',(-1.78968887043984,2.33690096819232,13.1761703310676));
#67337=CARTESIAN_POINT('Ctrl Pts',(-1.71375027989472,2.39132264200396,13.171131372312));
#67338=CARTESIAN_POINT('Ctrl Pts',(-1.63781727600902,2.4457403121153,13.1660927842632));
#67339=CARTESIAN_POINT('Ctrl Pts',(-1.55928456908114,2.49654149438389,13.1610541962143));
#67340=CARTESIAN_POINT('Ctrl Pts',(-1.47853527103567,2.5434813646464,13.1560156081655));
#67341=CARTESIAN_POINT('Ctrl Pts',(-1.39776943609134,2.59043084787032,13.1509759882486));
#67342=CARTESIAN_POINT('Ctrl Pts',(-1.31478649191079,2.63351722608229,13.1459363683317));
#67343=CARTESIAN_POINT('Ctrl Pts',(-1.22999483376291,2.67254124550334,13.1408967484148));
#67344=CARTESIAN_POINT('Ctrl Pts',(-1.14511095785756,2.71160770668856,13.1358516475053));
#67345=CARTESIAN_POINT('Ctrl Pts',(-1.05841484500098,2.74660280501691,13.1308065465959));
#67346=CARTESIAN_POINT('Ctrl Pts',(-0.970335291761442,2.77737527560865,
13.1257614456864));
#67347=CARTESIAN_POINT('Ctrl Pts',(-0.882201077622042,2.80816684315164,
13.1207132138601));
#67348=CARTESIAN_POINT('Ctrl Pts',(-0.792682138512077,2.8347304398849,13.1156649820338));
#67349=CARTESIAN_POINT('Ctrl Pts',(-0.702220785372583,2.85696516754943,
13.1106167502075));
#67350=CARTESIAN_POINT('Ctrl Pts',(-0.611617100800494,2.87923487922128,
13.105560575519));
#67351=CARTESIAN_POINT('Ctrl Pts',(-0.520068476729443,2.89716204108954,
13.1005044008304));
#67352=CARTESIAN_POINT('Ctrl Pts',(-0.428025485042737,2.91069719898067,
13.0954482261419));
#67353=CARTESIAN_POINT('Ctrl Pts',(-0.3886575144761,2.91648635997716,13.0932856352409));
#67354=CARTESIAN_POINT('Ctrl Pts',(-0.349199142779485,2.92147270529838,
13.09112304434));
#67355=CARTESIAN_POINT('Ctrl Pts',(-0.309685661186744,2.92565527553321,
13.088960453439));
#67356=CARTESIAN_POINT('Ctrl Pts',(-0.217296290305112,2.93543484992374,
13.0839039409587));
#67357=CARTESIAN_POINT('Ctrl Pts',(-0.124280802336355,2.94085098155313,
13.0788474284784));
#67358=CARTESIAN_POINT('Ctrl Pts',(-0.0310861472398973,2.94183576214747,
13.0737909159981));
#67359=CARTESIAN_POINT('Ctrl Pts',(0.0619816830295821,2.94281920259383,
13.0687412847206));
#67360=CARTESIAN_POINT('Ctrl Pts',(0.155227756270759,2.93938327137785,13.0636916534431));
#67361=CARTESIAN_POINT('Ctrl Pts',(0.248199318647507,2.93151174280829,13.0586420221656));
#67362=CARTESIAN_POINT('Ctrl Pts',(0.34107294178894,2.92364850636021,13.0535977103322));
#67363=CARTESIAN_POINT('Ctrl Pts',(0.433672189396265,2.91135899786555,13.0485533984987));
#67364=CARTESIAN_POINT('Ctrl Pts',(0.525544717101477,2.89467904098654,13.0435090866653));
#67365=CARTESIAN_POINT('Ctrl Pts',(0.617352577095301,2.8780108248821,13.0384683254482));
#67366=CARTESIAN_POINT('Ctrl Pts',(0.708434298944026,2.85695838221765,13.0334275642312));
#67367=CARTESIAN_POINT('Ctrl Pts',(0.798344103119171,2.83160920556048,13.0283868030141));
#67368=CARTESIAN_POINT('Ctrl Pts',(0.888222269458715,2.80626894887695,13.023347815561));
#67369=CARTESIAN_POINT('Ctrl Pts',(0.976928911119476,2.7766350823183,13.018308828108));
#67370=CARTESIAN_POINT('Ctrl Pts',(1.06403087676328,2.74284565611964,13.0132698406549));
#67371=CARTESIAN_POINT('Ctrl Pts',(1.15112643808778,2.70905871434567,13.008231223702));
#67372=CARTESIAN_POINT('Ctrl Pts',(1.23661714477252,2.671116981117,13.003192606749));
#67373=CARTESIAN_POINT('Ctrl Pts',(1.32008845357155,2.62920719509647,12.998153989796));
#67374=CARTESIAN_POINT('Ctrl Pts',(1.40357685944841,2.58728882487039,12.9931143408043));
#67375=CARTESIAN_POINT('Ctrl Pts',(1.48504464993766,2.54140098688932,12.9880746918125));
#67376=CARTESIAN_POINT('Ctrl Pts',(1.564101593611,2.49177651583434,12.9830350428208));
#67377=CARTESIAN_POINT('Ctrl Pts',(1.64324451888058,2.44209807366645,12.9779899127537));
#67378=CARTESIAN_POINT('Ctrl Pts',(1.71997098785871,2.38867512301693,12.9729447826866));
#67379=CARTESIAN_POINT('Ctrl Pts',(1.79391977637422,2.33178383130458,12.9678996526195));
#67380=CARTESIAN_POINT('Ctrl Pts',(1.8679144574754,2.27485723288158,12.9628513915469));
#67381=CARTESIAN_POINT('Ctrl Pts',(1.93912768839629,2.21445829466963,12.9578031304743));
#67382=CARTESIAN_POINT('Ctrl Pts',(2.00723301042557,2.15090205306004,12.9527548694018));
#67383=CARTESIAN_POINT('Ctrl Pts',(2.07544548651093,2.08724581472664,12.947698665607));
#67384=CARTESIAN_POINT('Ctrl Pts',(2.14053998407788,2.02042267413597,12.9426424618123));
#67385=CARTESIAN_POINT('Ctrl Pts',(2.20222858602172,1.95078272878063,12.9375862580175));
#67386=CARTESIAN_POINT('Ctrl Pts',(2.22860995671424,1.92100093513422,12.9354239527877));
#67387=CARTESIAN_POINT('Ctrl Pts',(2.25436895385661,1.89070436916235,12.9332616475578));
#67388=CARTESIAN_POINT('Ctrl Pts',(2.27948547368887,1.8599220347212,12.9310993423279));
#67389=CARTESIAN_POINT('Ctrl Pts',(2.33821991426747,1.78793820873022,12.9260428381273));
#67390=CARTESIAN_POINT('Ctrl Pts',(2.39364451016909,1.71304294853357,12.9209863339267));
#67391=CARTESIAN_POINT('Ctrl Pts',(2.44545788122685,1.63557321791031,12.9159298297262));
#67392=CARTESIAN_POINT('Ctrl Pts',(2.49720074076032,1.55820891391113,12.910880206796));
#67393=CARTESIAN_POINT('Ctrl Pts',(2.54534189723609,1.47827746733343,12.9058305838658));
#67394=CARTESIAN_POINT('Ctrl Pts',(2.58962005589505,1.39614897704582,12.9007809609357));
#67395=CARTESIAN_POINT('Ctrl Pts',(2.63385156995547,1.31410700459398,12.8957366575048));
#67396=CARTESIAN_POINT('Ctrl Pts',(2.67422796606321,1.22987297731259,12.890692354074));
#67397=CARTESIAN_POINT('Ctrl Pts',(2.71053174137645,1.14384512893607,12.8856480506432));
#67398=CARTESIAN_POINT('Ctrl Pts',(2.74680996262532,1.05787783517558,12.8806072978748));
#67399=CARTESIAN_POINT('Ctrl Pts',(2.77902108941892,0.970119637511359,12.8755665451065));
#67400=CARTESIAN_POINT('Ctrl Pts',(2.8069944601598,0.880991544018547,12.8705257923382));
#67401=CARTESIAN_POINT('Ctrl Pts',(2.83495798735894,0.791894813786075,12.865486813359));
#67402=CARTESIAN_POINT('Ctrl Pts',(2.85868658860374,0.70142956806775,12.8604478343798));
#67403=CARTESIAN_POINT('Ctrl Pts',(2.87805883080864,0.610033905946551,12.8554088554006));
#67404=CARTESIAN_POINT('Ctrl Pts',(2.89742964857949,0.518644964115729,12.8503702469357));
#67405=CARTESIAN_POINT('Ctrl Pts',(2.9124446526143,0.426326175699014,12.8453316384708));
#67406=CARTESIAN_POINT('Ctrl Pts',(2.92303334545943,0.333526702577529,12.8402930300059));
#67407=CARTESIAN_POINT('Ctrl Pts',(2.93362420713858,0.240708221760124,12.8352533895056));
#67408=CARTESIAN_POINT('Ctrl Pts',(2.9397869071143,0.147409301188208,12.8302137490054));
#67409=CARTESIAN_POINT('Ctrl Pts',(2.9415028342468,0.0540839728388559,12.8251741085052));
#67410=CARTESIAN_POINT('Ctrl Pts',(2.94322062762461,-0.0393428562980931,
12.8201289868832));
#67411=CARTESIAN_POINT('Ctrl Pts',(2.94048198688949,-0.132795706635729,
12.8150838652613));
#67412=CARTESIAN_POINT('Ctrl Pts',(2.93332044320623,-0.225821118295903,
12.8100387436394));
#67413=CARTESIAN_POINT('Ctrl Pts',(2.92615445504389,-0.318904261852187,
12.8049904909973));
#67414=CARTESIAN_POINT('Ctrl Pts',(2.91456015427157,-0.41155899908982,12.7999422383553));
#67415=CARTESIAN_POINT('Ctrl Pts',(2.89862262841597,-0.503339704409327,
12.7948939857132));
#67416=CARTESIAN_POINT('Ctrl Pts',(2.88266002676136,-0.595264815738986,
12.7898377902468));
#67417=CARTESIAN_POINT('Ctrl Pts',(2.86234065578813,-0.686312718114918,
12.7847815947804));
#67418=CARTESIAN_POINT('Ctrl Pts',(2.83780003802596,-0.77605086442827,12.7797253993139));
#67419=CARTESIAN_POINT('Ctrl Pts',(2.82730472168999,-0.814429288398268,
12.7775630099482));
#67420=CARTESIAN_POINT('Ctrl Pts',(2.8160379383468,-0.852568380814664,12.7754006205825));
#67421=CARTESIAN_POINT('Ctrl Pts',(2.80401296805785,-0.890435441210312,
12.7732382312168));
#67422=CARTESIAN_POINT('Ctrl Pts',(2.7758939434078,-0.978983252897487,12.7681817297523));
#67423=CARTESIAN_POINT('Ctrl Pts',(2.74352700603293,-1.06635347859154,12.7631252282878));
#67424=CARTESIAN_POINT('Ctrl Pts',(2.70702931838185,-1.1521094867334,12.7580687268232));
#67425=CARTESIAN_POINT('Ctrl Pts',(2.67058130005601,-1.23774879041166,12.7530191066992));
#67426=CARTESIAN_POINT('Ctrl Pts',(2.63001387495199,-1.32177783754301,12.7479694865751));
#67427=CARTESIAN_POINT('Ctrl Pts',(2.58549387302857,-1.40377542097436,12.7429198664511));
#67428=CARTESIAN_POINT('Ctrl Pts',(2.54102077107732,-1.48568662335865,12.737875565892));
#67429=CARTESIAN_POINT('Ctrl Pts',(2.49260357962393,-1.56557022839382,12.7328312653329));
#67430=CARTESIAN_POINT('Ctrl Pts',(2.44045663862699,-1.64302629162818,12.7277869647739));
#67431=CARTESIAN_POINT('Ctrl Pts',(2.3883464045338,-1.72042783254151,12.722746214963));
#67432=CARTESIAN_POINT('Ctrl Pts',(2.33251188645847,-1.79540486148966,12.7177054651521));
#67433=CARTESIAN_POINT('Ctrl Pts',(2.27321211569137,-1.86758418205819,12.7126647153412));
#67434=CARTESIAN_POINT('Ctrl Pts',(2.21393321252999,-1.93973810270386,12.7076257393715));
#67435=CARTESIAN_POINT('Ctrl Pts',(2.15119176058289,-2.00909592874094,12.7025867634019));
#67436=CARTESIAN_POINT('Ctrl Pts',(2.08528803137386,-2.07531631955443,12.6975477874323));
#67437=CARTESIAN_POINT('Ctrl Pts',(2.01938914867922,-2.14153184056644,12.6925091820254));
#67438=CARTESIAN_POINT('Ctrl Pts',(1.95032876409864,-2.20461007109985,12.6874705766185));
#67439=CARTESIAN_POINT('Ctrl Pts',(1.8784442774801,-2.26424625348089,12.6824319712117));
#67440=CARTESIAN_POINT('Ctrl Pts',(1.80654506771829,-2.32389465034797,12.6773923338143));
#67441=CARTESIAN_POINT('Ctrl Pts',(1.73182094854209,-2.38009931613171,12.6723526964169));
#67442=CARTESIAN_POINT('Ctrl Pts',(1.65464178465762,-2.43259626006147,12.6673130590195));
#67443=CARTESIAN_POINT('Ctrl Pts',(1.57737868128386,-2.48515029928017,12.6622679405497));
#67444=CARTESIAN_POINT('Ctrl Pts',(1.49765557091017,-2.53398831824227,12.6572228220798));
#67445=CARTESIAN_POINT('Ctrl Pts',(1.41587036776032,-2.57889028492843,12.65217770361));
#67446=CARTESIAN_POINT('Ctrl Pts',(1.33403440892513,-2.62382011765888,12.6471294541527));
#67447=CARTESIAN_POINT('Ctrl Pts',(1.25013420754304,-2.66480884058395,12.6420812046954));
#67448=CARTESIAN_POINT('Ctrl Pts',(1.16458932795676,-2.70168386329882,12.6370329552381));
#67449=CARTESIAN_POINT('Ctrl Pts',(1.07890985394616,-2.73861690436005,12.6319767629766));
#67450=CARTESIAN_POINT('Ctrl Pts',(0.991580950691239,-2.77142316980094,
12.626920570715));
#67451=CARTESIAN_POINT('Ctrl Pts',(0.90303882945407,-2.79997944144207,12.6218643784535));
#67452=CARTESIAN_POINT('Ctrl Pts',(0.865171360192689,-2.81219231508323,
12.6197019590043));
#67453=CARTESIAN_POINT('Ctrl Pts',(0.827082128135142,-2.82362846559316,
12.617539539555));
#67454=CARTESIAN_POINT('Ctrl Pts',(0.788805772570232,-2.8342811175252,12.6153771201057));
#67455=CARTESIAN_POINT('Ctrl Pts',(0.69930204799943,-2.8591908042078,12.6103206148053));
#67456=CARTESIAN_POINT('Ctrl Pts',(0.60845988395492,-2.8799004770425,12.605264109505));
#67457=CARTESIAN_POINT('Ctrl Pts',(0.516708866610124,-2.89626931537219,
12.6002076042046));
#67458=CARTESIAN_POINT('Ctrl Pts',(0.425082711115756,-2.91261587772606,
12.595157980186));
#67459=CARTESIAN_POINT('Ctrl Pts',(0.332550593042832,-2.92463326773718,
12.5901083561675));
#67460=CARTESIAN_POINT('Ctrl Pts',(0.239556361801636,-2.93223067808799,
12.5850587321489));
#67461=CARTESIAN_POINT('Ctrl Pts',(0.146660095071974,-2.93982008496823,
12.5800144276426));
#67462=CARTESIAN_POINT('Ctrl Pts',(0.0533031224500042,-2.94299873179844,
12.5749701231362));
#67463=CARTESIAN_POINT('Ctrl Pts',(-0.0400625107877926,-2.9417272129192,
12.5699258186299));
#67464=CARTESIAN_POINT('Ctrl Pts',(-0.133362423946594,-2.94045658906224,
12.56488506481));
#67465=CARTESIAN_POINT('Ctrl Pts',(-0.226670543507126,-2.93474203204424,
12.5598443109902));
#67466=CARTESIAN_POINT('Ctrl Pts',(-0.319532761982364,-2.92459617964941,
12.5548035571703));
#67467=CARTESIAN_POINT('Ctrl Pts',(-0.4123623029202,-2.91445389750604,12.549764577155));
#67468=CARTESIAN_POINT('Ctrl Pts',(-0.504745814202936,-2.89988346616527,
12.5447255971396));
#67469=CARTESIAN_POINT('Ctrl Pts',(-0.596233289766803,-2.88094947268671,
12.5396866171243));
#67470=CARTESIAN_POINT('Ctrl Pts',(-0.687714037985619,-2.86201687148078,
12.53464800764));
#67471=CARTESIAN_POINT('Ctrl Pts',(-0.778298447406953,-2.83872143630571,
12.5296093981558));
#67472=CARTESIAN_POINT('Ctrl Pts',(-0.86754681996549,-2.81117884795112,
12.5245707886716));
#67473=CARTESIAN_POINT('Ctrl Pts',(-0.956813472537783,-2.78363061827356,
12.5195311471702));
#67474=CARTESIAN_POINT('Ctrl Pts',(-1.04474312126971,-2.75183363878216,
12.5144915056688));
#67475=CARTESIAN_POINT('Ctrl Pts',(-1.13091242977066,-2.71595306958538,
12.5094518641674));
#67476=CARTESIAN_POINT('Ctrl Pts',(-1.21717545556445,-2.6800334768677,12.5044067415781));
#67477=CARTESIAN_POINT('Ctrl Pts',(-1.30167390991871,-2.64002160046159,
12.4993616189888));
#67478=CARTESIAN_POINT('Ctrl Pts',(-1.38400590558996,-2.5961301302693,12.4943164963995));
#67479=CARTESIAN_POINT('Ctrl Pts',(-1.46638899648283,-2.55221142103855,
12.489268242808));
#67480=CARTESIAN_POINT('Ctrl Pts',(-1.54660257146044,-2.50440855142868,
12.4842199892165));
#67481=CARTESIAN_POINT('Ctrl Pts',(-1.62427260901957,-2.45297829007694,
12.479171735625));
#67482=CARTESIAN_POINT('Ctrl Pts',(-1.70206485054719,-2.40146710972174,
12.4741155392457));
#67483=CARTESIAN_POINT('Ctrl Pts',(-1.77730520929182,-2.34631740689808,
12.4690593428665));
#67484=CARTESIAN_POINT('Ctrl Pts',(-1.84965188288115,-2.28782689733166,
12.4640031464873));
#67485=CARTESIAN_POINT('Ctrl Pts',(-1.88059232265756,-2.2628123113259,12.4618407673231));
#67486=CARTESIAN_POINT('Ctrl Pts',(-1.91100395709612,-2.23718715700358,
12.4596783881588));
#67487=CARTESIAN_POINT('Ctrl Pts',(-1.94086216417454,-2.21097672074487,
12.4575160089946));
#67488=CARTESIAN_POINT('Ctrl Pts',(-2.00967785375516,-2.15056822935034,
12.4525322665707));
#67489=CARTESIAN_POINT('Ctrl Pts',(-2.07580853770669,-2.08682247606317,
12.4475485241467));
#67490=CARTESIAN_POINT('Ctrl Pts',(-2.1389063411806,-2.02001080780708,12.4425647817228));
#67491=CARTESIAN_POINT('Ctrl Pts',(-2.20241500976163,-1.95276409139205,
12.4375485873631));
#67492=CARTESIAN_POINT('Ctrl Pts',(-2.26285075439455,-1.8824116313411,12.4325323930033));
#67493=CARTESIAN_POINT('Ctrl Pts',(-2.31989191581895,-1.80927209090227,
12.4275161986436));
#67494=CARTESIAN_POINT('Ctrl Pts',(-2.37642201481953,-1.73678784691744,
12.4225449470653));
#67495=CARTESIAN_POINT('Ctrl Pts',(-2.42961780913018,-1.66156661640815,
12.417573695487));
#67496=CARTESIAN_POINT('Ctrl Pts',(-2.47920362591192,-1.58395498082022,
12.4126024439086));
#67497=CARTESIAN_POINT('Ctrl Pts',(-2.52875950177525,-1.50639020870657,
12.4076341940725));
#67498=CARTESIAN_POINT('Ctrl Pts',(-2.57470948191501,-1.4264382813823,12.4026659442363));
#67499=CARTESIAN_POINT('Ctrl Pts',(-2.6168201469361,-1.34447622462776,12.3976976944002));
#67500=CARTESIAN_POINT('Ctrl Pts',(-2.65891791987531,-1.26253926036575,
12.3927309655822));
#67501=CARTESIAN_POINT('Ctrl Pts',(-2.69717850398541,-1.17859379583,12.3877642367641));
#67502=CARTESIAN_POINT('Ctrl Pts',(-2.73141419640922,-1.09304185082464,
12.3827975079461));
#67503=CARTESIAN_POINT('Ctrl Pts',(-2.76623616488011,-1.00602485421419,
12.3777457253747));
#67504=CARTESIAN_POINT('Ctrl Pts',(-2.79689388932123,-0.91734627984373,
12.3726939428033));
#67505=CARTESIAN_POINT('Ctrl Pts',(-2.82324129385255,-0.827449452646961,
12.3676421602319));
#67506=CARTESIAN_POINT('Ctrl Pts',(-2.84916408591644,-0.739001394856118,
12.3626717917467));
#67507=CARTESIAN_POINT('Ctrl Pts',(-2.87091440004144,-0.649374526423084,
12.3577014232615));
#67508=CARTESIAN_POINT('Ctrl Pts',(-2.88840419500333,-0.559003762319318,
12.3527310547763));
#67509=CARTESIAN_POINT('Ctrl Pts',(-2.90632371132637,-0.466412603531484,
12.3476385651619));
#67510=CARTESIAN_POINT('Ctrl Pts',(-2.91977050802025,-0.373041016470945,
12.3425460755474));
#67511=CARTESIAN_POINT('Ctrl Pts',(-2.92870625322799,-0.279362993797054,
12.337453585933));
#67512=CARTESIAN_POINT('Ctrl Pts',(-2.93764199843573,-0.185684971123177,
12.3323610963185));
#67513=CARTESIAN_POINT('Ctrl Pts',(-2.94206672257804,-0.0917010259822679,
12.3272686067041));
#67514=CARTESIAN_POINT('Ctrl Pts',(-2.94199923889461,0.0021162097116246,
12.3221761170896));
#67515=CARTESIAN_POINT('',(-2.94199894961115,-0.00248605850196559,11.3221761170896));
#67516=CARTESIAN_POINT('Ctrl Pts',(-2.9445363666432,0.00211803469319205,
12.3221761170896));
#67517=CARTESIAN_POINT('Ctrl Pts',(-2.9456637214079,0.140538485345201,12.3146690440209));
#67518=CARTESIAN_POINT('Ctrl Pts',(-2.87416309229677,1.24803879024156,12.2545416005818));
#67519=CARTESIAN_POINT('Ctrl Pts',(-1.4701722548823,3.14385641459552,12.1417937867725));
#67520=CARTESIAN_POINT('Ctrl Pts',(1.82719979676511,2.95069151525937,11.9839326756612));
#67521=CARTESIAN_POINT('Ctrl Pts',(3.46958573405994,0.0849379149032947,
11.8260715645502));
#67522=CARTESIAN_POINT('Ctrl Pts',(1.96939451380668,-2.85774821044887,11.668210453439));
#67523=CARTESIAN_POINT('Ctrl Pts',(-1.31457570167652,-3.21202900045203,
11.5103493423279));
#67524=CARTESIAN_POINT('Ctrl Pts',(-2.84408765266999,-1.34515018134913,
11.3950045635448));
#67525=CARTESIAN_POINT('Ctrl Pts',(-2.94485546023631,-0.189014750280763,
11.332280155132));
#67526=CARTESIAN_POINT('Ctrl Pts',(-2.94318142996902,-0.00248705772575741,
11.3221761170896));
#67527=CARTESIAN_POINT('',(-2.94199997051088,0.000416550106448989,10.3221761170469));
#67528=CARTESIAN_POINT('Ctrl Pts',(-2.94199894961115,-0.00248605850196559,
11.3221761170896));
#67529=CARTESIAN_POINT('Ctrl Pts',(-2.94207652581505,0.089317537506325,
11.3172011584662));
#67530=CARTESIAN_POINT('Ctrl Pts',(-2.93785286391276,0.181261441456098,
11.3122261998427));
#67531=CARTESIAN_POINT('Ctrl Pts',(-2.92931522269092,0.272903510624668,
11.3072512412193));
#67532=CARTESIAN_POINT('Ctrl Pts',(-2.92078590003141,0.36445628929195,11.3022811298953));
#67533=CARTESIAN_POINT('Ctrl Pts',(-2.90795099198411,0.455707364124172,
11.2973110185713));
#67534=CARTESIAN_POINT('Ctrl Pts',(-2.89084981018168,0.546215502318019,
11.2923409072473));
#67535=CARTESIAN_POINT('Ctrl Pts',(-2.87375744361081,0.63667698583005,11.2873733578914));
#67536=CARTESIAN_POINT('Ctrl Pts',(-2.85240325316874,0.726395844222927,
11.2824058085355));
#67537=CARTESIAN_POINT('Ctrl Pts',(-2.82687815151478,0.81493798321612,11.2774382591796));
#67538=CARTESIAN_POINT('Ctrl Pts',(-2.80135860763729,0.903460843249249,
11.2724717914464));
#67539=CARTESIAN_POINT('Ctrl Pts',(-2.77167008307933,0.990807053319003,
11.2675053237131));
#67540=CARTESIAN_POINT('Ctrl Pts',(-2.73795383302997,1.07655599399032,11.2625388559799));
#67541=CARTESIAN_POINT('Ctrl Pts',(-2.70423488576364,1.16231179436574,11.2575719909415));
#67542=CARTESIAN_POINT('Ctrl Pts',(-2.66648774252331,1.246469646557,11.2526051259031));
#67543=CARTESIAN_POINT('Ctrl Pts',(-2.62490194595386,1.32862853127864,11.2476382608647));
#67544=CARTESIAN_POINT('Ctrl Pts',(-2.58327509075301,1.41086853339232,11.242666491924));
#67545=CARTESIAN_POINT('Ctrl Pts',(-2.53780222461493,1.49110521992984,11.2376947229834));
#67546=CARTESIAN_POINT('Ctrl Pts',(-2.48871880318195,1.56896230633135,11.2327229540427));
#67547=CARTESIAN_POINT('Ctrl Pts',(-2.43960868296054,1.64686174287508,11.2277484807224));
#67548=CARTESIAN_POINT('Ctrl Pts',(-2.38688436221856,1.72237862948383,11.2227740074021));
#67549=CARTESIAN_POINT('Ctrl Pts',(-2.33082322136789,1.79516771103209,11.2177995340818));
#67550=CARTESIAN_POINT('Ctrl Pts',(-2.27467308627105,1.86807234159245,11.2128171640349));
#67551=CARTESIAN_POINT('Ctrl Pts',(-2.21517585487161,1.93824017657899,11.2078347939879));
#67552=CARTESIAN_POINT('Ctrl Pts',(-2.15264731424576,2.0053611995026,11.202852423941));
#67553=CARTESIAN_POINT('Ctrl Pts',(-2.11823823849968,2.04229749033582,11.2001106559959));
#67554=CARTESIAN_POINT('Ctrl Pts',(-2.08291183600716,2.07831181353667,11.1973688880508));
#67555=CARTESIAN_POINT('Ctrl Pts',(-2.04672493224266,2.11335776709394,11.1946271201058));
#67556=CARTESIAN_POINT('Ctrl Pts',(-1.97998725583821,2.17799124673651,11.1895706161538));
#67557=CARTESIAN_POINT('Ctrl Pts',(-1.91006766593611,2.2395739985057,11.1845141122018));
#67558=CARTESIAN_POINT('Ctrl Pts',(-1.83727632392557,2.29777712355715,11.1794576082499));
#67559=CARTESIAN_POINT('Ctrl Pts',(-1.76458404224229,2.35590104110318,11.1744079855962));
#67560=CARTESIAN_POINT('Ctrl Pts',(-1.68902811823042,2.41065419727838,11.1693583629425));
#67561=CARTESIAN_POINT('Ctrl Pts',(-1.61095513182416,2.46174482090436,11.1643087402888));
#67562=CARTESIAN_POINT('Ctrl Pts',(-1.53296439143067,2.51278162309634,11.1592644371618));
#67563=CARTESIAN_POINT('Ctrl Pts',(-1.45246222850332,2.56016332066176,11.1542201340347));
#67564=CARTESIAN_POINT('Ctrl Pts',(-1.36982697401538,2.60363938771479,11.1491758309076));
#67565=CARTESIAN_POINT('Ctrl Pts',(-1.28724988676171,2.64708485181763,11.1441350784826));
#67566=CARTESIAN_POINT('Ctrl Pts',(-1.20254308380114,2.68662994420094,11.1390943260575));
#67567=CARTESIAN_POINT('Ctrl Pts',(-1.1161115648444,2.72206887767753,11.1340535736324));
#67568=CARTESIAN_POINT('Ctrl Pts',(-1.02971046067275,2.75749534038466,11.1290145950209));
#67569=CARTESIAN_POINT('Ctrl Pts',(-0.941586256143343,2.7888183469212,11.1239756164094));
#67570=CARTESIAN_POINT('Ctrl Pts',(-0.852165159560519,2.81587970993635,
11.1189366377978));
#67571=CARTESIAN_POINT('Ctrl Pts',(-0.762750638506969,2.84293908300962,
11.1138980297247));
#67572=CARTESIAN_POINT('Ctrl Pts',(-0.672039839466033,2.86573730756244,
11.1088594216516));
#67573=CARTESIAN_POINT('Ctrl Pts',(-0.580474317815216,2.88416600880687,
11.1038208135785));
#67574=CARTESIAN_POINT('Ctrl Pts',(-0.488890041643242,2.90259848463219,
11.0987811734938));
#67575=CARTESIAN_POINT('Ctrl Pts',(-0.396451129835384,2.91665957256184,
11.0937415334091));
#67576=CARTESIAN_POINT('Ctrl Pts',(-0.303608395204779,2.92629218335442,
11.0887018933244));
#67577=CARTESIAN_POINT('Ctrl Pts',(-0.2106646852654,2.93593527052787,11.0836567721515));
#67578=CARTESIAN_POINT('Ctrl Pts',(-0.117316717492807,2.94114022141322,
11.0786116509787));
#67579=CARTESIAN_POINT('Ctrl Pts',(-0.0240191613170752,2.94190194940104,
11.0735665298058));
#67580=CARTESIAN_POINT('Ctrl Pts',(0.0693362952866036,2.94266415011696,
11.0685182776326));
#67581=CARTESIAN_POINT('Ctrl Pts',(0.162640835401097,2.93897765568961,11.0634700254595));
#67582=CARTESIAN_POINT('Ctrl Pts',(0.255443218682719,2.93088941484134,11.0584217732863));
#67583=CARTESIAN_POINT('Ctrl Pts',(0.348391614996983,2.9227884481499,11.0533655783149));
#67584=CARTESIAN_POINT('Ctrl Pts',(0.440835838760165,2.91027197002818,11.0483093833435));
#67585=CARTESIAN_POINT('Ctrl Pts',(0.532333399195466,2.89343829243013,11.0432531883721));
#67586=CARTESIAN_POINT('Ctrl Pts',(0.571464345852351,2.88623899949823,11.0410907952462));
#67587=CARTESIAN_POINT('Ctrl Pts',(0.610422318321621,2.87825070366841,11.0389284021204));
#67588=CARTESIAN_POINT('Ctrl Pts',(0.64917360658853,2.86948386099466,11.0367660089946));
#67589=CARTESIAN_POINT('Ctrl Pts',(0.739788971436703,2.84898362260321,11.0317095050485));
#67590=CARTESIAN_POINT('Ctrl Pts',(0.829591626257177,2.82415083111023,11.0266530011023));
#67591=CARTESIAN_POINT('Ctrl Pts',(0.918136568920149,2.79506515859855,11.0215964971561));
#67592=CARTESIAN_POINT('Ctrl Pts',(1.00656101248464,2.76601906821557,11.0165468745083));
#67593=CARTESIAN_POINT('Ctrl Pts',(1.09373072757481,2.73273173556562,11.0114972518605));
#67594=CARTESIAN_POINT('Ctrl Pts',(1.17921186430988,2.69533363038248,11.0064476292127));
#67595=CARTESIAN_POINT('Ctrl Pts',(1.2646029509125,2.65797492224592,11.0014033260916));
#67596=CARTESIAN_POINT('Ctrl Pts',(1.34830859100062,2.61651422642895,10.9963590229704));
#67597=CARTESIAN_POINT('Ctrl Pts',(1.42991208731481,2.5711311562328,10.9913147198493));
#67598=CARTESIAN_POINT('Ctrl Pts',(1.51145814265147,2.52578003133352,10.9862739674302));
#67599=CARTESIAN_POINT('Ctrl Pts',(1.59090460907757,2.47651223503371,10.9812332150111));
#67600=CARTESIAN_POINT('Ctrl Pts',(1.66785764676815,2.42355418138671,10.9761924625921));
#67601=CARTESIAN_POINT('Ctrl Pts',(1.74478360509921,2.37061476339358,10.9711534839866));
#67602=CARTESIAN_POINT('Ctrl Pts',(1.81921751306633,2.31398791915949,10.9661145053812));
#67603=CARTESIAN_POINT('Ctrl Pts',(1.89079377057828,2.25394385847172,10.9610755267757));
#67604=CARTESIAN_POINT('Ctrl Pts',(1.96236476477056,2.19390421309003,10.9560369187087));
#67605=CARTESIAN_POINT('Ctrl Pts',(2.03107818687781,2.13044813608663,10.9509983106418));
#67606=CARTESIAN_POINT('Ctrl Pts',(2.09660173569173,2.06388593722968,10.9459597025748));
#67607=CARTESIAN_POINT('Ctrl Pts',(2.16213870508923,1.99731010505205,10.9409200624962));
#67608=CARTESIAN_POINT('Ctrl Pts',(2.22448419285335,1.92762720366024,10.9358804224176));
#67609=CARTESIAN_POINT('Ctrl Pts',(2.28334376141409,1.85518335137295,10.930840782339));
#67610=CARTESIAN_POINT('Ctrl Pts',(2.34226734535684,1.7826607095024,10.9257956611723));
#67611=CARTESIAN_POINT('Ctrl Pts',(2.39769716290024,1.70737146784726,10.9207505400056));
#67612=CARTESIAN_POINT('Ctrl Pts',(2.44938019527269,1.62969342485203,10.9157054188388));
#67613=CARTESIAN_POINT('Ctrl Pts',(2.5010953021154,1.5519671748928,10.9106571666718));
#67614=CARTESIAN_POINT('Ctrl Pts',(2.54905876699972,1.4718495522115,10.9056089145048));
#67615=CARTESIAN_POINT('Ctrl Pts',(2.59306300351438,1.38974395476468,10.9005606623378));
#67616=CARTESIAN_POINT('Ctrl Pts',(2.63713647523431,1.30750917434951,10.8955044673724));
#67617=CARTESIAN_POINT('Ctrl Pts',(2.67723809372118,1.22328057524653,10.8904482724071));
#67618=CARTESIAN_POINT('Ctrl Pts',(2.71320805331004,1.13748233368854,10.8853920774418));
#67619=CARTESIAN_POINT('Ctrl Pts',(2.72859139909721,1.10078882519136,10.8832296842557));
#67620=CARTESIAN_POINT('Ctrl Pts',(2.74321967074903,1.06380842165138,10.8810672910696));
#67621=CARTESIAN_POINT('Ctrl Pts',(2.75708317692166,1.02657506083851,10.8789048978835));
#67622=CARTESIAN_POINT('Ctrl Pts',(2.78950136716245,0.939509194591843,10.8738483939365));
#67623=CARTESIAN_POINT('Ctrl Pts',(2.81784833592938,0.85075315980588,10.8687918899894));
#67624=CARTESIAN_POINT('Ctrl Pts',(2.84194730101225,0.760723036504873,10.8637353860424));
#67625=CARTESIAN_POINT('Ctrl Pts',(2.86601347028002,0.670815433455974,10.8586857633936));
#67626=CARTESIAN_POINT('Ctrl Pts',(2.88584301053909,0.579637612249602,10.8536361407449));
#67627=CARTESIAN_POINT('Ctrl Pts',(2.90130776147331,0.4876241105757,10.8485865180962));
#67628=CARTESIAN_POINT('Ctrl Pts',(2.91675622106045,0.395707540556076,10.8435422149742));
#67629=CARTESIAN_POINT('Ctrl Pts',(2.92784895820001,0.30295747497166,10.8384979118521));
#67630=CARTESIAN_POINT('Ctrl Pts',(2.93450833287159,0.209820981570504,10.8334536087301));
#67631=CARTESIAN_POINT('Ctrl Pts',(2.94116301998676,0.116750047262867,10.8284128563101));
#67632=CARTESIAN_POINT('Ctrl Pts',(2.94339051614705,0.0232936668301138,
10.8233721038901));
#67633=CARTESIAN_POINT('Ctrl Pts',(2.94116486181815,-0.0700946189534286,
10.8183313514702));
#67634=CARTESIAN_POINT('Ctrl Pts',(2.93893999068502,-0.163450041902257,
10.8132923728638));
#67635=CARTESIAN_POINT('Ctrl Pts',(2.93226509298428,-0.256736974999994,
10.8082533942575));
#67636=CARTESIAN_POINT('Ctrl Pts',(2.92116631910506,-0.34950155382513,10.8032144156511));
#67637=CARTESIAN_POINT('Ctrl Pts',(2.91006836136792,-0.442259311259358,
10.7981758075832));
#67638=CARTESIAN_POINT('Ctrl Pts',(2.89454722727486,-0.534494350619572,
10.7931371995153));
#67639=CARTESIAN_POINT('Ctrl Pts',(2.8746808515922,-0.625758740641423,10.7880985914474));
#67640=CARTESIAN_POINT('Ctrl Pts',(2.85481040686323,-0.717041823505658,
10.783058951368));
#67641=CARTESIAN_POINT('Ctrl Pts',(2.8305930475925,-0.807353429093737,10.7780193112885));
#67642=CARTESIAN_POINT('Ctrl Pts',(2.8021573982697,-0.896257728179997,10.772979671209));
#67643=CARTESIAN_POINT('Ctrl Pts',(2.77369082247245,-0.98525871915126,10.7679345500414));
#67644=CARTESIAN_POINT('Ctrl Pts',(2.74099693481821,-1.07284892576681,10.7628894288738));
#67645=CARTESIAN_POINT('Ctrl Pts',(2.7042535389354,-1.1586098554541,10.7578443077062));
#67646=CARTESIAN_POINT('Ctrl Pts',(2.66748734011517,-1.24442400834152,10.7527960555383));
#67647=CARTESIAN_POINT('Ctrl Pts',(2.62666682341887,-1.32840622578979,10.7477478033704));
#67648=CARTESIAN_POINT('Ctrl Pts',(2.58201607775066,-1.41016203829102,10.7426995512026));
#67649=CARTESIAN_POINT('Ctrl Pts',(2.5372950796754,-1.49204648341714,10.7376433562364));
#67650=CARTESIAN_POINT('Ctrl Pts',(2.48873205358918,-1.57169715329904,10.7325871612703));
#67651=CARTESIAN_POINT('Ctrl Pts',(2.43659462291282,-1.64874820503082,10.7275309663041));
#67652=CARTESIAN_POINT('Ctrl Pts',(2.41429690197303,-1.68170078492101,10.7253685731269));
#67653=CARTESIAN_POINT('Ctrl Pts',(2.39134591533303,-1.71417829678479,10.7232061799497));
#67654=CARTESIAN_POINT('Ctrl Pts',(2.36776476825675,-1.74615406027134,10.7210437867724));
#67655=CARTESIAN_POINT('Ctrl Pts',(2.31262300932557,-1.82092564946127,10.7159872828243));
#67656=CARTESIAN_POINT('Ctrl Pts',(2.25383902616345,-1.89321415253696,10.7109307788762));
#67657=CARTESIAN_POINT('Ctrl Pts',(2.19166437696011,-1.96264394599837,10.705874274928));
#67658=CARTESIAN_POINT('Ctrl Pts',(2.12957434003321,-2.03197925379797,10.7008246522782));
#67659=CARTESIAN_POINT('Ctrl Pts',(2.06410310012087,-2.09846325559609,10.6957750296284));
#67660=CARTESIAN_POINT('Ctrl Pts',(1.99554426767324,-2.16175092824231,10.6907254069786));
#67661=CARTESIAN_POINT('Ctrl Pts',(1.92705765855026,-2.22497193046889,10.6856811038554));
#67662=CARTESIAN_POINT('Ctrl Pts',(1.85549024648217,-2.28500299756638,10.6806368007323));
#67663=CARTESIAN_POINT('Ctrl Pts',(1.78117377113338,-2.3415345389352,10.6755924976091));
#67664=CARTESIAN_POINT('Ctrl Pts',(1.70690960740335,-2.39802628756054,10.670551745188));
#67665=CARTESIAN_POINT('Ctrl Pts',(1.6299005787077,-2.45102313921977,10.6655109927669));
#67666=CARTESIAN_POINT('Ctrl Pts',(1.55051211865024,-2.5002552209562,10.6604702403458));
#67667=CARTESIAN_POINT('Ctrl Pts',(1.47115159496399,-2.54946997818842,10.6554312617383));
#67668=CARTESIAN_POINT('Ctrl Pts',(1.38941367989568,-2.59492236415437,10.6503922831308));
#67669=CARTESIAN_POINT('Ctrl Pts',(1.30569258860119,-2.63638594748036,10.6453533045233));
#67670=CARTESIAN_POINT('Ctrl Pts',(1.22197765368996,-2.67784648180512,10.6403146964543));
#67671=CARTESIAN_POINT('Ctrl Pts',(1.13628022996328,-2.71531860023218,10.6352760883852));
#67672=CARTESIAN_POINT('Ctrl Pts',(1.04901789875083,-2.74862246372622,10.6302374803162));
#67673=CARTESIAN_POINT('Ctrl Pts',(0.961737694400502,-2.78193314854322,
10.6251978402355));
#67674=CARTESIAN_POINT('Ctrl Pts',(0.872892360276499,-2.81107372509559,
10.6201582001549));
#67675=CARTESIAN_POINT('Ctrl Pts',(0.782917081301991,-2.83591340555483,
10.6151185600743));
#67676=CARTESIAN_POINT('Ctrl Pts',(0.692843945649627,-2.86078010153029,
10.6100734389055));
#67677=CARTESIAN_POINT('Ctrl Pts',(0.601638840232294,-2.88133644688177,
10.6050283177367));
#67678=CARTESIAN_POINT('Ctrl Pts',(0.509749345449273,-2.8975023045399,10.5999831965679));
#67679=CARTESIAN_POINT('Ctrl Pts',(0.417802824080872,-2.91367819472313,
10.5949349443989));
#67680=CARTESIAN_POINT('Ctrl Pts',(0.325171507177231,-2.9254581167554,10.5898866922298));
#67681=CARTESIAN_POINT('Ctrl Pts',(0.232308190442077,-2.9328138203189,10.5848384400608));
#67682=CARTESIAN_POINT('Ctrl Pts',(0.139298764802533,-2.9401810971691,10.5797822450934));
#67683=CARTESIAN_POINT('Ctrl Pts',(0.046057053095913,-2.94311024668023,
10.5747260501261));
#67684=CARTESIAN_POINT('Ctrl Pts',(-0.0469642920738009,-2.94162512147112,
10.5696698551587));
#67685=CARTESIAN_POINT('Ctrl Pts',(-0.0867469195964879,-2.94098997495813,
10.5675074619929));
#67686=CARTESIAN_POINT('Ctrl Pts',(-0.12648930900846,-2.93954809020669,
10.5653450688271));
#67687=CARTESIAN_POINT('Ctrl Pts',(-0.166156486030579,-2.93730421001128,
10.5631826756613));
#67688=CARTESIAN_POINT('Ctrl Pts',(-0.258913548142371,-2.93205715815928,
10.558126171714));
#67689=CARTESIAN_POINT('Ctrl Pts',(-0.351584892786728,-2.92240282069134,
10.5530696677668));
#67690=CARTESIAN_POINT('Ctrl Pts',(-0.443718470194708,-2.90834625160211,
10.5480131638195));
#67691=CARTESIAN_POINT('Ctrl Pts',(-0.53572666480091,-2.89430881182563,
10.5429635411705));
#67692=CARTESIAN_POINT('Ctrl Pts',(-0.627198111896935,-2.87588111218902,
10.5379139185216));
#67693=CARTESIAN_POINT('Ctrl Pts',(-0.717683367920239,-2.85312014878635,
10.5328642958726));
#67694=CARTESIAN_POINT('Ctrl Pts',(-0.808073302220233,-2.83038316292822,
10.5278199927503));
#67695=CARTESIAN_POINT('Ctrl Pts',(-0.897478682815411,-2.80332209486652,
10.522775689628));
#67696=CARTESIAN_POINT('Ctrl Pts',(-0.9854588635448,-2.77204524282361,10.5177313865058));
#67697=CARTESIAN_POINT('Ctrl Pts',(-1.07337711472662,-2.74079040666291,
10.5126906340856));
#67698=CARTESIAN_POINT('Ctrl Pts',(-1.15987174354931,-2.70532583323625,
10.5076498816653));
#67699=CARTESIAN_POINT('Ctrl Pts',(-1.2445169147434,-2.66580975482452,10.5026091292451));
#67700=CARTESIAN_POINT('Ctrl Pts',(-1.32913229975777,-2.62630758190789,
10.4975701506385));
#67701=CARTESIAN_POINT('Ctrl Pts',(-1.41189911881721,-2.58275692393808,
10.492531172032));
#67702=CARTESIAN_POINT('Ctrl Pts',(-1.49241215236125,-2.53536387279705,
10.4874921934254));
#67703=CARTESIAN_POINT('Ctrl Pts',(-1.57291926542495,-2.48797430667721,
10.4824535853572));
#67704=CARTESIAN_POINT('Ctrl Pts',(-1.65117254059657,-2.43674313438026,
10.4774149772891));
#67705=CARTESIAN_POINT('Ctrl Pts',(-1.72679297425622,-2.38192149829909,
10.4723763692209));
#67706=CARTESIAN_POINT('Ctrl Pts',(-1.80242889655112,-2.32708863360833,
10.4673367291412));
#67707=CARTESIAN_POINT('Ctrl Pts',(-1.87543054762043,-2.26866410506297,
10.4622970890615));
#67708=CARTESIAN_POINT('Ctrl Pts',(-1.94545035083473,-2.2069406273022,10.4572574489818));
#67709=CARTESIAN_POINT('Ctrl Pts',(-2.01554630724814,-2.14515001938573,
10.4522123278139));
#67710=CARTESIAN_POINT('Ctrl Pts',(-2.08265360976431,-2.08005359448698,
10.447167206646));
#67711=CARTESIAN_POINT('Ctrl Pts',(-2.14646029714233,-2.01198215518719,
10.4421220854781));
#67712=CARTESIAN_POINT('Ctrl Pts',(-2.21030658292621,-1.94386847077812,
10.43707383331));
#67713=CARTESIAN_POINT('Ctrl Pts',(-2.27084788837547,-1.87277643348794,
10.4320255811418));
#67714=CARTESIAN_POINT('Ctrl Pts',(-2.32781283067783,-1.79906959991315,
10.4269773289737));
#67715=CARTESIAN_POINT('Ctrl Pts',(-2.38486740024746,-1.72524679778287,
10.4219211340072));
#67716=CARTESIAN_POINT('Ctrl Pts',(-2.43833412084441,-1.64880134988332,
10.4168649390408));
#67717=CARTESIAN_POINT('Ctrl Pts',(-2.48798530075998,-1.57012519984944,
10.4118087440743));
#67718=CARTESIAN_POINT('Ctrl Pts',(-2.50921972175825,-1.53647761090627,
10.4096463508996));
#67719=CARTESIAN_POINT('Ctrl Pts',(-2.52975684650336,-1.50242231663193,
10.4074839577249));
#67720=CARTESIAN_POINT('Ctrl Pts',(-2.54958150965234,-1.46799118718026,
10.4053215645501));
#67721=CARTESIAN_POINT('Ctrl Pts',(-2.59775504666128,-1.38432422767455,
10.4000669921598));
#67722=CARTESIAN_POINT('Ctrl Pts',(-2.64187647244433,-1.29816218218148,
10.3948124197694));
#67723=CARTESIAN_POINT('Ctrl Pts',(-2.68169059492538,-1.20991716786265,
10.389557847379));
#67724=CARTESIAN_POINT('Ctrl Pts',(-2.72143509013441,-1.12182647716651,
10.384312464229));
#67725=CARTESIAN_POINT('Ctrl Pts',(-2.75688711194816,-1.0316604243227,10.379067081079));
#67726=CARTESIAN_POINT('Ctrl Pts',(-2.78783665101677,-0.939856801458403,
10.373821697929));
#67727=CARTESIAN_POINT('Ctrl Pts',(-2.81872219219728,-0.848243011404531,
10.3685871612554));
#67728=CARTESIAN_POINT('Ctrl Pts',(-2.84512367388878,-0.75499876941976,
10.3633526245818));
#67729=CARTESIAN_POINT('Ctrl Pts',(-2.86687908403034,-0.66058180231471,
10.3581180879081));
#67730=CARTESIAN_POINT('Ctrl Pts',(-2.88860740729712,-0.566282390362534,
10.3528900685669));
#67731=CARTESIAN_POINT('Ctrl Pts',(-2.90570108032047,-0.470813540940017,
10.3476620492256));
#67732=CARTESIAN_POINT('Ctrl Pts',(-2.91804772344475,-0.374648480176971,
10.3424340298844));
#67733=CARTESIAN_POINT('Ctrl Pts',(-2.93037738695065,-0.278615669614791,
10.3372132003333));
#67734=CARTESIAN_POINT('Ctrl Pts',(-2.93797297421279,-0.181888944945489,
10.3319923707823));
#67735=CARTESIAN_POINT('Ctrl Pts',(-2.94077325018523,-0.0849511094394904,
10.3267715412312));
#67736=CARTESIAN_POINT('Ctrl Pts',(-2.94159486008975,-0.0565092392245919,
10.325239733184));
#67737=CARTESIAN_POINT('Ctrl Pts',(-2.94200400090166,-0.0280492502006135,
10.3237079251368));
#67738=CARTESIAN_POINT('Ctrl Pts',(-2.94199997051099,0.000416549312712471,
10.3221761170896));
#67739=CARTESIAN_POINT('',(-2.94199926785449,0.00207555863534859,9.3221761170896));
#67740=CARTESIAN_POINT('Ctrl Pts',(-2.94199997051088,0.000416550106449056,
10.3221761170469));
#67741=CARTESIAN_POINT('Ctrl Pts',(-2.94198593005877,0.0995811140799426,
10.3168398510825));
#67742=CARTESIAN_POINT('Ctrl Pts',(-2.93695388461969,0.198628671924865,
10.3115035851181));
#67743=CARTESIAN_POINT('Ctrl Pts',(-2.9269647239196,0.297054717064461,10.3061673191537));
#67744=CARTESIAN_POINT('Ctrl Pts',(-2.91694385381805,0.395793203967011,
10.3008141138483));
#67745=CARTESIAN_POINT('Ctrl Pts',(-2.90193443700809,0.493905874428624,
10.2954609085429));
#67746=CARTESIAN_POINT('Ctrl Pts',(-2.88204893916369,0.59089585568477,10.2901077032374));
#67747=CARTESIAN_POINT('Ctrl Pts',(-2.86213087062913,0.688044697968832,
10.2847457298542));
#67748=CARTESIAN_POINT('Ctrl Pts',(-2.83732087392621,0.784066834855588,
10.279383756471));
#67749=CARTESIAN_POINT('Ctrl Pts',(-2.80778130463142,0.878480589064014,
10.2740217830878));
#67750=CARTESIAN_POINT('Ctrl Pts',(-2.77815835592025,0.973160838821047,
10.268644674812));
#67751=CARTESIAN_POINT('Ctrl Pts',(-2.74377926182703,1.06622328964424,10.2632675665361));
#67752=CARTESIAN_POINT('Ctrl Pts',(-2.70485505981839,1.15720486750395,10.2578904582602));
#67753=CARTESIAN_POINT('Ctrl Pts',(-2.67968790095532,1.2160306803774,10.2544137899865));
#67754=CARTESIAN_POINT('Ctrl Pts',(-2.65262161242553,1.27398705792399,10.2509371217127));
#67755=CARTESIAN_POINT('Ctrl Pts',(-2.62372318127054,1.33095479564996,10.247460453439));
#67756=CARTESIAN_POINT('Ctrl Pts',(-2.58169299037788,1.41380928967087,10.2424039494914));
#67757=CARTESIAN_POINT('Ctrl Pts',(-2.53566037629418,1.49481659052653,10.2373474455438));
#67758=CARTESIAN_POINT('Ctrl Pts',(-2.48581137957154,1.57356467461387,10.2322909415962));
#67759=CARTESIAN_POINT('Ctrl Pts',(-2.43603022138356,1.65220559195798,10.227241318947));
#67760=CARTESIAN_POINT('Ctrl Pts',(-2.38244323678257,1.72859303091348,10.2221916962977));
#67761=CARTESIAN_POINT('Ctrl Pts',(-2.32528299642955,1.8023381998159,10.2171420736484));
#67762=CARTESIAN_POINT('Ctrl Pts',(-2.26818297155094,1.87600568184535,10.2120977705259));
#67763=CARTESIAN_POINT('Ctrl Pts',(-2.2075174436185,1.94703607819576,10.2070534674033));
#67764=CARTESIAN_POINT('Ctrl Pts',(-2.14356244264622,2.01506924309726,10.2020091642807));
#67765=CARTESIAN_POINT('Ctrl Pts',(-2.07965245981562,2.08305451922369,10.1969684118602));
#67766=CARTESIAN_POINT('Ctrl Pts',(-2.01245790932483,2.14804643540509,10.1919276594396));
#67767=CARTESIAN_POINT('Ctrl Pts',(-1.94229461420281,2.20971845076217,10.1868869070191));
#67768=CARTESIAN_POINT('Ctrl Pts',(-1.87215600916627,2.27136876406936,10.1818479284122));
#67769=CARTESIAN_POINT('Ctrl Pts',(-1.79905106774777,2.32970120519855,10.1768089498053));
#67770=CARTESIAN_POINT('Ctrl Pts',(-1.72333117638428,2.3844273225456,10.1717699711983));
#67771=CARTESIAN_POINT('Ctrl Pts',(-1.64761685304031,2.43914941563846,10.1667313631299));
#67772=CARTESIAN_POINT('Ctrl Pts',(-1.5692883216123,2.49026545280252,10.1616927550614));
#67773=CARTESIAN_POINT('Ctrl Pts',(-1.48872771155874,2.53752907389001,10.1566541469929));
#67774=CARTESIAN_POINT('Ctrl Pts',(-1.40815060101888,2.58480237554883,10.1516145069129));
#67775=CARTESIAN_POINT('Ctrl Pts',(-1.32534088641352,2.62822146999654,10.1465748668328));
#67776=CARTESIAN_POINT('Ctrl Pts',(-1.24070616309238,2.6675854657095,10.1415352267527));
#67777=CARTESIAN_POINT('Ctrl Pts',(-1.15597939145598,2.7069922735136,10.1364901055845));
#67778=CARTESIAN_POINT('Ctrl Pts',(-1.06942405194301,2.74233499254364,10.1314449844163));
#67779=CARTESIAN_POINT('Ctrl Pts',(-0.981468333530933,2.77346063795324,
10.1263998632481));
#67780=CARTESIAN_POINT('Ctrl Pts',(-0.893458029833515,2.80460559992653,
10.1213516110796));
#67781=CARTESIAN_POINT('Ctrl Pts',(-0.804046041169711,2.83152815024812,
10.1163033589111));
#67782=CARTESIAN_POINT('Ctrl Pts',(-0.713674272862074,2.85412561606086,
10.1112551067427));
#67783=CARTESIAN_POINT('Ctrl Pts',(-0.623160315792424,2.87675863618165,
10.1061989117759));
#67784=CARTESIAN_POINT('Ctrl Pts',(-0.531683998757212,2.89505290136774,
10.1011427168091));
#67785=CARTESIAN_POINT('Ctrl Pts',(-0.439695694379682,2.90895714927944,
10.0960865218424));
#67786=CARTESIAN_POINT('Ctrl Pts',(-0.400354869401907,2.91490360722584,
10.0939241286709));
#67787=CARTESIAN_POINT('Ctrl Pts',(-0.360920440448954,2.92004776598015,
10.0917617354994));
#67788=CARTESIAN_POINT('Ctrl Pts',(-0.321427684744325,2.92438852471417,
10.0895993423279));
#67789=CARTESIAN_POINT('Ctrl Pts',(-0.229078486757704,2.93453888218069,
10.0845428383805));
#67790=CARTESIAN_POINT('Ctrl Pts',(-0.136085657609308,2.94032836210759,
10.079486334433));
#67791=CARTESIAN_POINT('Ctrl Pts',(-0.0428958694685178,2.9416872614849,
10.0744298304855));
#67792=CARTESIAN_POINT('Ctrl Pts',(0.0501670984936496,2.94304431156236,
10.0693802078364));
#67793=CARTESIAN_POINT('Ctrl Pts',(0.143426053188793,2.93998275679977,10.0643305851872));
#67794=CARTESIAN_POINT('Ctrl Pts',(0.236428310975977,2.93248455303162,10.0592809625381));
#67795=CARTESIAN_POINT('Ctrl Pts',(0.329332595503363,2.92499424824876,10.0542366594156));
#67796=CARTESIAN_POINT('Ctrl Pts',(0.421980281012603,2.91307662036411,10.0491923562932));
#67797=CARTESIAN_POINT('Ctrl Pts',(0.513918884235275,2.89676567578849,10.0441480531707));
#67798=CARTESIAN_POINT('Ctrl Pts',(0.605792771563805,2.88046621254199,10.0391073007503));
#67799=CARTESIAN_POINT('Ctrl Pts',(0.696958133395661,2.85977965685362,10.0340665483299));
#67800=CARTESIAN_POINT('Ctrl Pts',(0.786968843712302,2.83479170998966,10.0290257959095));
#67801=CARTESIAN_POINT('Ctrl Pts',(0.876947879744954,2.80981255624957,10.0239868173027));
#67802=CARTESIAN_POINT('Ctrl Pts',(0.965772644729208,2.78053513708429,10.0189478386959));
#67803=CARTESIAN_POINT('Ctrl Pts',(1.05300943767834,2.74709576173827,10.0139088600891));
#67804=CARTESIAN_POINT('Ctrl Pts',(1.14023981571905,2.71365884533787,10.0088702520208));
#67805=CARTESIAN_POINT('Ctrl Pts',(1.22588204004082,2.6760607402814,10.0038316439524));
#67806=CARTESIAN_POINT('Ctrl Pts',(1.30952082207223,2.63448651857611,9.99879303588408));
#67807=CARTESIAN_POINT('Ctrl Pts',(1.3931767350635,2.59290378160665,9.99375339580415));
#67808=CARTESIAN_POINT('Ctrl Pts',(1.47482799397496,2.54734350819388,9.98871375572421));
#67809=CARTESIAN_POINT('Ctrl Pts',(1.55408343676181,2.49803696361415,9.98367411564428));
#67810=CARTESIAN_POINT('Ctrl Pts',(1.63342507738448,2.44867679347527,9.9786289944762));
#67811=CARTESIAN_POINT('Ctrl Pts',(1.71036532406792,2.39556245429527,9.97358387330812));
#67812=CARTESIAN_POINT('Ctrl Pts',(1.78454184780575,2.33896866020689,9.96853875214004));
#67813=CARTESIAN_POINT('Ctrl Pts',(1.85876440546589,2.28233974403151,9.96349049997169));
#67814=CARTESIAN_POINT('Ctrl Pts',(1.93021948655862,2.22222735913253,9.95844224780333));
#67815=CARTESIAN_POINT('Ctrl Pts',(1.99857937121796,2.15894522786986,9.95339399563498));
#67816=CARTESIAN_POINT('Ctrl Pts',(2.06704681167218,2.0955635300271,9.94833780066834));
#67817=CARTESIAN_POINT('Ctrl Pts',(2.1324090246093,2.02900244652801,9.9432816057017));
#67818=CARTESIAN_POINT('Ctrl Pts',(2.19437669071125,1.95961091527454,9.93822541073506));
#67819=CARTESIAN_POINT('Ctrl Pts',(2.22087852835673,1.92993409813857,9.93606301756232));
#67820=CARTESIAN_POINT('Ctrl Pts',(2.24676001381569,1.89973997174884,9.93390062438958));
#67821=CARTESIAN_POINT('Ctrl Pts',(2.27200092458726,1.86905746264652,9.93173823121683));
#67822=CARTESIAN_POINT('Ctrl Pts',(2.33102384722868,1.79730999768455,9.92668172726932));
#67823=CARTESIAN_POINT('Ctrl Pts',(2.38674864010326,1.72263783546821,9.92162522332181));
#67824=CARTESIAN_POINT('Ctrl Pts',(2.43887257272417,1.64537672707918,9.9165687193743));
#67825=CARTESIAN_POINT('Ctrl Pts',(2.49092557089423,1.56822076183687,9.91151909672512));
#67826=CARTESIAN_POINT('Ctrl Pts',(2.53938720114163,1.4884832164628,9.90646947407594));
#67827=CARTESIAN_POINT('Ctrl Pts',(2.58399468503541,1.40653313779261,9.90141985142676));
#67828=CARTESIAN_POINT('Ctrl Pts',(2.62855517716029,1.32466938946035,9.89637554830426));
#67829=CARTESIAN_POINT('Ctrl Pts',(2.66926938274567,1.24059812832851,9.89133124518176));
#67830=CARTESIAN_POINT('Ctrl Pts',(2.70591820197124,1.15471671168331,9.88628694205926));
#67831=CARTESIAN_POINT('Ctrl Pts',(2.74254122396885,1.06889574725815,9.88124618963881));
#67832=CARTESIAN_POINT('Ctrl Pts',(2.77510437425366,0.981267566700582,9.87620543721836));
#67833=CARTESIAN_POINT('Ctrl Pts',(2.80343530244129,0.892252489503912,9.87116468479791));
#67834=CARTESIAN_POINT('Ctrl Pts',(2.83175626112793,0.803268736233301,9.86612570619108));
#67835=CARTESIAN_POINT('Ctrl Pts',(2.85584782229247,0.712899478029739,9.86108672758425));
#67836=CARTESIAN_POINT('Ctrl Pts',(2.87558679505007,0.621582322893509,9.85604774897742));
#67837=CARTESIAN_POINT('Ctrl Pts',(2.89532431631343,0.530271882712828,9.85100914090904));
#67838=CARTESIAN_POINT('Ctrl Pts',(2.91070979222329,0.43801411761001,9.84597053284066));
#67839=CARTESIAN_POINT('Ctrl Pts',(2.92167092270248,0.345257902784065,9.84093192477228));
#67840=CARTESIAN_POINT('Ctrl Pts',(2.93263429824887,0.252482689558648,9.83589228469231));
#67841=CARTESIAN_POINT('Ctrl Pts',(2.939171476924,0.159209264134449,9.83085264461234));
#67842=CARTESIAN_POINT('Ctrl Pts',(2.94126202499463,0.0658915800728639,
9.82581300453237));
#67843=CARTESIAN_POINT('Ctrl Pts',(2.94335484673521,-0.0275275958500429,
9.82076788336426));
#67844=CARTESIAN_POINT('Ctrl Pts',(2.94099137518667,-0.120990682620149,
9.81572276219614));
#67845=CARTESIAN_POINT('Ctrl Pts',(2.93420332079691,-0.214044089440471,
9.81067764102802));
#67846=CARTESIAN_POINT('Ctrl Pts',(2.92741105374318,-0.307155245169547,
9.80562938885963));
#67847=CARTESIAN_POINT('Ctrl Pts',(2.91618879038018,-0.399855775035067,
9.80058113669124));
#67848=CARTESIAN_POINT('Ctrl Pts',(2.90061982855417,-0.491699715475195,
9.79553288452285));
#67849=CARTESIAN_POINT('Ctrl Pts',(2.88502637089887,-0.583688160957556,
9.79047668955618));
#67850=CARTESIAN_POINT('Ctrl Pts',(2.86507265794508,-0.674816894385031,
9.7854204945895));
#67851=CARTESIAN_POINT('Ctrl Pts',(2.84089247464087,-0.76465282810494,9.78036429962283));
#67852=CARTESIAN_POINT('Ctrl Pts',(2.83055128652842,-0.803073144368351,
9.77820190645046));
#67853=CARTESIAN_POINT('Ctrl Pts',(2.81943767403642,-0.84125722711009,9.77603951327809));
#67854=CARTESIAN_POINT('Ctrl Pts',(2.80756478591604,-0.879172322633171,
9.77387712010573));
#67855=CARTESIAN_POINT('Ctrl Pts',(2.77980142335258,-0.967832346459148,
9.7688206161582));
#67856=CARTESIAN_POINT('Ctrl Pts',(2.74778545100014,-1.05533184283114,9.76376411221068));
#67857=CARTESIAN_POINT('Ctrl Pts',(2.71163227818096,-1.14123371310486,9.75870760826316));
#67858=CARTESIAN_POINT('Ctrl Pts',(2.6755283055148,-1.22701868118629,9.75365798561397));
#67859=CARTESIAN_POINT('Ctrl Pts',(2.6352984916249,-1.31120993858839,9.74860836296478));
#67860=CARTESIAN_POINT('Ctrl Pts',(2.59110797484379,-1.39338561163122,9.74355874031559));
#67861=CARTESIAN_POINT('Ctrl Pts',(2.54696401057743,-1.47547471668369,9.73851443719307));
#67862=CARTESIAN_POINT('Ctrl Pts',(2.49886784613195,-1.55555206960214,9.73347013407056));
#67863=CARTESIAN_POINT('Ctrl Pts',(2.44703221478881,-1.63321686857128,9.72842583094805));
#67864=CARTESIAN_POINT('Ctrl Pts',(2.39523307072211,-1.71082699902541,9.72338507852758));
#67865=CARTESIAN_POINT('Ctrl Pts',(2.33969993737056,-1.78602758336162,9.71834432610713));
#67866=CARTESIAN_POINT('Ctrl Pts',(2.28069034633778,-1.85844438822411,9.71330357368666));
#67867=CARTESIAN_POINT('Ctrl Pts',(2.22170152046214,-1.93083571000313,9.70826459507982));
#67868=CARTESIAN_POINT('Ctrl Pts',(2.15923894722988,-2.00044485518431,9.70322561647297));
#67869=CARTESIAN_POINT('Ctrl Pts',(2.09360152599711,-2.06692928044057,9.69818663786613));
#67870=CARTESIAN_POINT('Ctrl Pts',(2.02796893137513,-2.13340881680208,9.69314802979773));
#67871=CARTESIAN_POINT('Ctrl Pts',(1.95916226467271,-2.19676377484079,9.68810942172934));
#67872=CARTESIAN_POINT('Ctrl Pts',(1.88751770009901,-2.25668804485975,9.68307081366095));
#67873=CARTESIAN_POINT('Ctrl Pts',(1.81585846123038,-2.31662458861389,9.67803117358097));
#67874=CARTESIAN_POINT('Ctrl Pts',(1.74136051034097,-2.37312876464277,9.67299153350099));
#67875=CARTESIAN_POINT('Ctrl Pts',(1.66439264986219,-2.42593509952033,9.66795189342101));
#67876=CARTESIAN_POINT('Ctrl Pts',(1.58734107951099,-2.47879886631205,9.66290677225287));
#67877=CARTESIAN_POINT('Ctrl Pts',(1.50781460399198,-2.52795651350885,9.65786165108474));
#67878=CARTESIAN_POINT('Ctrl Pts',(1.42621025147046,-2.57318641349603,9.65281652991661));
#67879=CARTESIAN_POINT('Ctrl Pts',(1.34455525531888,-2.6184443831419,9.64776827774821));
#67880=CARTESIAN_POINT('Ctrl Pts',(1.26082021209893,-2.65976955669674,9.6427200255798));
#67881=CARTESIAN_POINT('Ctrl Pts',(1.17542399034816,-2.69698766087537,9.63767177341139));
#67882=CARTESIAN_POINT('Ctrl Pts',(1.08989340824036,-2.73426432312207,9.6326155784447));
#67883=CARTESIAN_POINT('Ctrl Pts',(1.0026968441177,-2.76742085976246,9.62755938347801));
#67884=CARTESIAN_POINT('Ctrl Pts',(0.914270011482932,-2.79633230251753,
9.62250318851132));
#67885=CARTESIAN_POINT('Ctrl Pts',(0.876452328345462,-2.80869691796943,
9.62034079533908));
#67886=CARTESIAN_POINT('Ctrl Pts',(0.838409771986596,-2.82028572562746,
9.61817840216685));
#67887=CARTESIAN_POINT('Ctrl Pts',(0.800176952928685,-2.83109181129856,
9.61601600899462));
#67888=CARTESIAN_POINT('Ctrl Pts',(0.710773969709414,-2.8563605808982,9.61095950504711));
#67889=CARTESIAN_POINT('Ctrl Pts',(0.620015697827995,-2.8774347460313,9.60590300109961));
#67890=CARTESIAN_POINT('Ctrl Pts',(0.528331154426677,-2.8941717625708,9.6008464971521));
#67891=CARTESIAN_POINT('Ctrl Pts',(0.4367713827455,-2.91088600202851,9.59579687450293));
#67892=CARTESIAN_POINT('Ctrl Pts',(0.344288277065512,-2.9232747433809,9.59074725185375));
#67893=CARTESIAN_POINT('Ctrl Pts',(0.251325318444532,-2.93124539817272,
9.58569762920458));
#67894=CARTESIAN_POINT('Ctrl Pts',(0.158460291683603,-2.93920765627557,
9.58065332608208));
#67895=CARTESIAN_POINT('Ctrl Pts',(0.0651168562606086,-2.94276104172703,
9.57560902295958));
#67896=CARTESIAN_POINT('Ctrl Pts',(-0.0282531046025607,-2.94186433441114,
9.57056471983709));
#67897=CARTESIAN_POINT('Ctrl Pts',(-0.121557342034083,-2.94096825829058,
9.56552396741664));
#67898=CARTESIAN_POINT('Ctrl Pts',(-0.214887625674755,-2.93562832010324,
9.56048321499619));
#67899=CARTESIAN_POINT('Ctrl Pts',(-0.307789801172765,-2.92585533447811,
9.55544246257575));
#67900=CARTESIAN_POINT('Ctrl Pts',(-0.400659284895781,-2.91608578791397,
9.55040348396892));
#67901=CARTESIAN_POINT('Ctrl Pts',(-0.493100519278439,-2.90188633956518,
9.54536450536209));
#67902=CARTESIAN_POINT('Ctrl Pts',(-0.584663242803674,-2.88331976938291,
9.54032552675526));
#67903=CARTESIAN_POINT('Ctrl Pts',(-0.676219233315614,-2.86475456448291,
9.53528691868688));
#67904=CARTESIAN_POINT('Ctrl Pts',(-0.76689640697302,-2.84182296470806,
9.53024831061851));
#67905=CARTESIAN_POINT('Ctrl Pts',(-0.856254605057123,-2.81463888470945,
9.52520970255013));
#67906=CARTESIAN_POINT('Ctrl Pts',(-0.945631105556222,-2.78744923684664,
9.52017006247016));
#67907=CARTESIAN_POINT('Ctrl Pts',(-1.03368766992456,-2.75600550826659,
9.51513042239021));
#67908=CARTESIAN_POINT('Ctrl Pts',(-1.12000030235379,-2.72047115822378,
9.51009078231024));
#67909=CARTESIAN_POINT('Ctrl Pts',(-1.20640680798421,-2.68489816119388,
9.50504566114213));
#67910=CARTESIAN_POINT('Ctrl Pts',(-1.29106518540278,-2.64522583180418,
9.500000539974));
#67911=CARTESIAN_POINT('Ctrl Pts',(-1.37357269697196,-2.60166524482555,
9.49495541880589));
#67912=CARTESIAN_POINT('Ctrl Pts',(-1.45613141267132,-2.55807762416326,
9.4899071666375));
#67913=CARTESIAN_POINT('Ctrl Pts',(-1.53653622364786,-2.51059716708712,
9.48485891446911));
#67914=CARTESIAN_POINT('Ctrl Pts',(-1.61441208083413,-2.45947913860981,
9.47981066230072));
#67915=CARTESIAN_POINT('Ctrl Pts',(-1.69241046601709,-2.40828068225855,
9.47475446733405));
#67916=CARTESIAN_POINT('Ctrl Pts',(-1.76787159678691,-2.35343349035532,
9.46969827236737));
#67917=CARTESIAN_POINT('Ctrl Pts',(-1.84045247857413,-2.29523390400855,
9.4646420774007));
#67918=CARTESIAN_POINT('Ctrl Pts',(-1.87149329172669,-2.27034356869074,
9.4624796842283));
#67919=CARTESIAN_POINT('Ctrl Pts',(-1.90200774803109,-2.24484053918549,
9.4603172910559));
#67920=CARTESIAN_POINT('Ctrl Pts',(-1.93197112367303,-2.21875000333376,
9.4581548978835));
#67921=CARTESIAN_POINT('Ctrl Pts',(-2.00103674140832,-2.15861128608182,
9.45317057895952));
#67922=CARTESIAN_POINT('Ctrl Pts',(-2.0674300095447,-2.09512390774132,9.44818626003554));
#67923=CARTESIAN_POINT('Ctrl Pts',(-2.13080192571592,-2.02855789992924,
9.44320194111156));
#67924=CARTESIAN_POINT('Ctrl Pts',(-2.19491665642982,-1.96121163799769,
9.43815919844398));
#67925=CARTESIAN_POINT('Ctrl Pts',(-2.25593833618249,-1.89071434632796,
9.4331164557764));
#67926=CARTESIAN_POINT('Ctrl Pts',(-2.31353904436894,-1.81738853583389,
9.42807371310882));
#67927=CARTESIAN_POINT('Ctrl Pts',(-2.37032961360863,-1.74509403375171,
9.42310189530244));
#67928=CARTESIAN_POINT('Ctrl Pts',(-2.42379451678455,-1.67005042725981,
9.41813007749606));
#67929=CARTESIAN_POINT('Ctrl Pts',(-2.4736568633579,-1.59260344165218,9.41315825968969));
#67930=CARTESIAN_POINT('Ctrl Pts',(-2.52348920478088,-1.51520306051883,
9.40818943372287));
#67931=CARTESIAN_POINT('Ctrl Pts',(-2.56972304646865,-1.4354025549002,9.40322060775605));
#67932=CARTESIAN_POINT('Ctrl Pts',(-2.61212364897492,-1.35357823655153,
9.39825178178923));
#67933=CARTESIAN_POINT('Ctrl Pts',(-2.65451135241786,-1.27177881070444,
9.39328446743303));
#67934=CARTESIAN_POINT('Ctrl Pts',(-2.69306792318456,-1.18795720101285,
9.38831715307682));
#67935=CARTESIAN_POINT('Ctrl Pts',(-2.72760425371636,-1.10251486842963,
9.38334983872062));
#67936=CARTESIAN_POINT('Ctrl Pts',(-2.76304788446274,-1.01482788954229,
9.3782520285847));
#67937=CARTESIAN_POINT('Ctrl Pts',(-2.79425685906639,-0.925434289069423,
9.37315421844878));
#67938=CARTESIAN_POINT('Ctrl Pts',(-2.82107978309542,-0.834789109542235,
9.36805640831286));
#67939=CARTESIAN_POINT('Ctrl Pts',(-2.847235644682,-0.746398195612121,9.36308537621489));
#67940=CARTESIAN_POINT('Ctrl Pts',(-2.86922100535572,-0.656817697940494,
9.35811434411692));
#67941=CARTESIAN_POINT('Ctrl Pts',(-2.88694677326747,-0.56648241660315,
9.35314331201895));
#67942=CARTESIAN_POINT('Ctrl Pts',(-2.90535064122947,-0.472691355007414,
9.34798211286406));
#67943=CARTESIAN_POINT('Ctrl Pts',(-2.91916237285942,-0.378087135627378,
9.34282091370917));
#67944=CARTESIAN_POINT('Ctrl Pts',(-2.92834128938451,-0.283163014685617,
9.33765971455428));
#67945=CARTESIAN_POINT('Ctrl Pts',(-2.93752020590961,-0.188238893743857,
9.33249851539938));
#67946=CARTESIAN_POINT('Ctrl Pts',(-2.94206633972349,-0.0929954194237398,
9.32733731624449));
#67947=CARTESIAN_POINT('Ctrl Pts',(-2.94199926785449,0.00207555863534859,
9.3221761170896));
#67948=CARTESIAN_POINT('',(-2.94199893297947,-0.00250566312373982,8.3221761170896));
#67949=CARTESIAN_POINT('Ctrl Pts',(-2.94464008512449,0.00207742171232136,
9.3221761170896));
#67950=CARTESIAN_POINT('Ctrl Pts',(-2.94572064417758,0.136558752036829,
9.31488200698387));
#67951=CARTESIAN_POINT('Ctrl Pts',(-2.87651233014906,1.2400826680256,9.25496752650772));
#67952=CARTESIAN_POINT('Ctrl Pts',(-1.48278064012933,3.13792943795001,9.14243267566131));
#67953=CARTESIAN_POINT('Ctrl Pts',(1.81534028008774,2.95800257805624,8.98457156455015));
#67954=CARTESIAN_POINT('Ctrl Pts',(3.46921681308081,0.0988649995372459,
8.82671045343907));
#67955=CARTESIAN_POINT('Ctrl Pts',(1.98085035420067,-2.84981954842035,8.66884934232795));
#67956=CARTESIAN_POINT('Ctrl Pts',(-1.30167123501552,-3.2172801525869,8.51098823121684));
#67957=CARTESIAN_POINT('Ctrl Pts',(-2.8415027498017,-1.35312072688065,8.39543048947073));
#67958=CARTESIAN_POINT('Ctrl Pts',(-2.94478032747652,-0.192985093804385,
8.33249311809497));
#67959=CARTESIAN_POINT('Ctrl Pts',(-2.94306537549688,-0.00250657139928612,
8.3221761170896));
#67960=CARTESIAN_POINT('',(-2.94199996099939,0.000479040305267797,7.32217611704064));
#67961=CARTESIAN_POINT('Ctrl Pts',(-2.94199893297947,-0.00250566312373982,
8.3221761170896));
#67962=CARTESIAN_POINT('Ctrl Pts',(-2.94207713595497,0.0893155670756921,
8.31720090487355));
#67963=CARTESIAN_POINT('Ctrl Pts',(-2.93785244836421,0.181275223426796,
8.31222569265751));
#67964=CARTESIAN_POINT('Ctrl Pts',(-2.92931265872361,0.272931030558297,
8.30725048044146));
#67965=CARTESIAN_POINT('Ctrl Pts',(-2.92078100783252,0.364499486163972,
8.3022800097949));
#67966=CARTESIAN_POINT('Ctrl Pts',(-2.90794246826347,0.455764214554573,
8.29730953914834));
#67967=CARTESIAN_POINT('Ctrl Pts',(-2.89083688222758,0.546283919178212,
8.29233906850178));
#67968=CARTESIAN_POINT('Ctrl Pts',(-2.87373987349475,0.636758234246803,
8.28737109021257));
#67969=CARTESIAN_POINT('Ctrl Pts',(-2.85238015013863,0.726487818501757,
8.28240311192336));
#67970=CARTESIAN_POINT('Ctrl Pts',(-2.82684914637299,0.815038590282867,
8.27743513363415));
#67971=CARTESIAN_POINT('Ctrl Pts',(-2.80132334617133,0.903571314218693,
8.27246816788612));
#67972=CARTESIAN_POINT('Ctrl Pts',(-2.77162808100322,0.990925263531778,
8.2675012021381));
#67973=CARTESIAN_POINT('Ctrl Pts',(-2.73790510853684,1.07667990445066,8.26253423639008));
#67974=CARTESIAN_POINT('Ctrl Pts',(-2.70417897265835,1.16244258965657,8.25756680471161));
#67975=CARTESIAN_POINT('Ctrl Pts',(-2.66642454858315,1.24660524362766,8.25259937303314));
#67976=CARTESIAN_POINT('Ctrl Pts',(-2.62483185301556,1.32876700116871,8.24763194135467));
#67977=CARTESIAN_POINT('Ctrl Pts',(-2.58319772789434,1.41101059819852,8.24265956172862));
#67978=CARTESIAN_POINT('Ctrl Pts',(-2.53771790793819,1.49124891238343,8.23768718210257));
#67979=CARTESIAN_POINT('Ctrl Pts',(-2.48862828313252,1.56910588182981,8.23271480247653));
#67980=CARTESIAN_POINT('Ctrl Pts',(-2.43951135879074,1.64700614879897,8.22773965762957));
#67981=CARTESIAN_POINT('Ctrl Pts',(-2.38678089793278,1.72252206200371,8.22276451278261));
#67982=CARTESIAN_POINT('Ctrl Pts',(-2.3307146686714,1.79530864567627,8.21778936793565));
#67983=CARTESIAN_POINT('Ctrl Pts',(-2.27456009386465,1.8682099217495,8.21280638357656));
#67984=CARTESIAN_POINT('Ctrl Pts',(-2.21505955674095,1.93837293788326,8.20782339921746));
#67985=CARTESIAN_POINT('Ctrl Pts',(-2.15252915667446,2.00548802780429,8.20284041485836));
#67986=CARTESIAN_POINT('Ctrl Pts',(-2.12084595943131,2.03949421726892,8.20031561290378));
#67987=CARTESIAN_POINT('Ctrl Pts',(-2.08838546529636,2.0727185323238,8.1977908109492));
#67988=CARTESIAN_POINT('Ctrl Pts',(-2.05519198062807,2.10512468104909,8.19526600899461));
#67989=CARTESIAN_POINT('Ctrl Pts',(-1.98871429672409,2.17002554135448,8.1902095050471));
#67990=CARTESIAN_POINT('Ctrl Pts',(-1.91904247858982,2.2318884713599,8.18515300109959));
#67991=CARTESIAN_POINT('Ctrl Pts',(-1.84648536483333,2.29038332980668,8.18009649715207));
#67992=CARTESIAN_POINT('Ctrl Pts',(-1.77402699264839,2.34879858373294,8.1750468745029));
#67993=CARTESIAN_POINT('Ctrl Pts',(-1.69869147014349,2.40385459882147,8.16999725185372));
#67994=CARTESIAN_POINT('Ctrl Pts',(-1.62082420321798,2.45525821498734,8.16494762920454));
#67995=CARTESIAN_POINT('Ctrl Pts',(-1.54303896559086,2.50660767999656,8.15990332608204));
#67996=CARTESIAN_POINT('Ctrl Pts',(-1.46272765317577,2.55431215130621,8.15485902295953));
#67997=CARTESIAN_POINT('Ctrl Pts',(-1.38026758822414,2.59811958633507,8.14981471983702));
#67998=CARTESIAN_POINT('Ctrl Pts',(-1.2978655671916,2.641896185162,8.14477396741658));
#67999=CARTESIAN_POINT('Ctrl Pts',(-1.21331819055915,2.68178099290725,8.13973321499613));
#68000=CARTESIAN_POINT('Ctrl Pts',(-1.12702962869304,2.71756659827281,8.13469246257568));
#68001=CARTESIAN_POINT('Ctrl Pts',(-1.04077143130685,2.75333961087668,8.12965348396884));
#68002=CARTESIAN_POINT('Ctrl Pts',(-0.952773675161863,2.78501611732971,
8.124614505362));
#68003=CARTESIAN_POINT('Ctrl Pts',(-0.863461930124583,2.81243622065026,
8.11957552675517));
#68004=CARTESIAN_POINT('Ctrl Pts',(-0.774156752576108,2.83985430764898,
8.11453691868678));
#68005=CARTESIAN_POINT('Ctrl Pts',(-0.683538202183492,2.8630164840472,8.1094983106184));
#68006=CARTESIAN_POINT('Ctrl Pts',(-0.592047395722709,2.88181260341785,
8.10445970255001));
#68007=CARTESIAN_POINT('Ctrl Pts',(-0.50053785004424,2.90061257262419,8.09942006247003));
#68008=CARTESIAN_POINT('Ctrl Pts',(-0.408156127785994,2.9150446198816,8.09438042239004));
#68009=CARTESIAN_POINT('Ctrl Pts',(-0.315352808957852,2.92504984673465,
8.08934078231006));
#68010=CARTESIAN_POINT('Ctrl Pts',(-0.222448557689706,2.93506595522396,
8.08429566114194));
#68011=CARTESIAN_POINT('Ctrl Pts',(-0.129122236070494,2.940645585982,8.07925053997382));
#68012=CARTESIAN_POINT('Ctrl Pts',(-0.0358284894473728,2.94178182728494,
8.07420541880569));
#68013=CARTESIAN_POINT('Ctrl Pts',(0.0575231552393617,2.9429187737388,8.0691571666373));
#68014=CARTESIAN_POINT('Ctrl Pts',(0.150841742008688,2.93960685650917,8.0641089144689));
#68015=CARTESIAN_POINT('Ctrl Pts',(0.243675845689539,2.93189121254993,8.0590606623005));
#68016=CARTESIAN_POINT('Ctrl Pts',(0.336656012311531,2.92416342898245,8.05400446733382));
#68017=CARTESIAN_POINT('Ctrl Pts',(0.429149735399227,2.91201814569531,8.04894827236714));
#68018=CARTESIAN_POINT('Ctrl Pts',(0.52071413309325,2.89555189758307,8.04389207740046));
#68019=CARTESIAN_POINT('Ctrl Pts',(0.559873665054721,2.88850974380414,8.04172968422814));
#68020=CARTESIAN_POINT('Ctrl Pts',(0.598863391467464,2.88067789908918,8.03956729105582));
#68021=CARTESIAN_POINT('Ctrl Pts',(0.637649560612953,2.87206668408833,8.0374048978835));
#68022=CARTESIAN_POINT('Ctrl Pts',(0.72834648839811,2.85193036327393,8.03234839393599));
#68023=CARTESIAN_POINT('Ctrl Pts',(0.818248104638546,2.82745826184522,8.02729188998847));
#68024=CARTESIAN_POINT('Ctrl Pts',(0.906909090966337,2.79872826489508,8.02223538604096));
#68025=CARTESIAN_POINT('Ctrl Pts',(0.99544942027428,2.77003736604158,8.01718576339178));
#68026=CARTESIAN_POINT('Ctrl Pts',(1.08275205660791,2.73710022230183,8.0121361407426));
#68027=CARTESIAN_POINT('Ctrl Pts',(1.16838262984417,2.70004556077827,8.00708651809342));
#68028=CARTESIAN_POINT('Ctrl Pts',(1.2539229955243,2.66302993450033,8.00204221497091));
#68029=CARTESIAN_POINT('Ctrl Pts',(1.33779439465786,2.62190558779252,7.99699791184841));
#68030=CARTESIAN_POINT('Ctrl Pts',(1.41957941233063,2.57685045978361,7.9919536087259));
#68031=CARTESIAN_POINT('Ctrl Pts',(1.5013068612524,2.53182704623194,7.98691285630545));
#68032=CARTESIAN_POINT('Ctrl Pts',(1.58095046066298,2.48287856456771,7.981872103885));
#68033=CARTESIAN_POINT('Ctrl Pts',(1.65811546502868,2.43022984605011,7.97683135146455));
#68034=CARTESIAN_POINT('Ctrl Pts',(1.73525331544513,2.37759965433286,7.97179237285772));
#68035=CARTESIAN_POINT('Ctrl Pts',(1.80991393781239,2.32127206237876,7.96675339425089));
#68036=CARTESIAN_POINT('Ctrl Pts',(1.88173065029614,2.26151581018928,7.96171441564405));
#68037=CARTESIAN_POINT('Ctrl Pts',(1.95354208177837,2.20176395214216,7.95667580757567));
#68038=CARTESIAN_POINT('Ctrl Pts',(2.02250967859608,2.1385842189999,7.9516371995073));
#68039=CARTESIAN_POINT('Ctrl Pts',(2.08829989655837,2.0722855840917,7.94659859143892));
#68040=CARTESIAN_POINT('Ctrl Pts',(2.15410358972397,2.00597336984585,7.94155895135894));
#68041=CARTESIAN_POINT('Ctrl Pts',(2.21672829950995,1.93654130002476,7.93651931127896));
#68042=CARTESIAN_POINT('Ctrl Pts',(2.27587820131431,1.86433430821361,7.93147967119898));
#68043=CARTESIAN_POINT('Ctrl Pts',(2.33509243426537,1.79204878442792,7.92643455003086));
#68044=CARTESIAN_POINT('Ctrl Pts',(2.39082403477812,1.71698265830804,7.92138942886275));
#68045=CARTESIAN_POINT('Ctrl Pts',(2.44281846954338,1.63951270957494,7.91634430769463));
#68046=CARTESIAN_POINT('Ctrl Pts',(2.49484517203511,1.56199468302106,7.91129605552623));
#68047=CARTESIAN_POINT('Ctrl Pts',(2.5431298623532,1.48207024299637,7.90624780335782));
#68048=CARTESIAN_POINT('Ctrl Pts',(2.58746333642,1.40014195090436,7.90119955118942));
#68049=CARTESIAN_POINT('Ctrl Pts',(2.63186656370626,1.31808475481242,7.89614335622274));
#68050=CARTESIAN_POINT('Ctrl Pts',(2.67230597343853,1.23401781209865,7.89108716125607));
#68051=CARTESIAN_POINT('Ctrl Pts',(2.70862005849138,1.14836465407908,7.88603096628939));
#68052=CARTESIAN_POINT('Ctrl Pts',(2.7241505770128,1.11173319399672,7.88386857311706));
#68053=CARTESIAN_POINT('Ctrl Pts',(2.73892717915958,1.07481181013318,7.88170617994472));
#68054=CARTESIAN_POINT('Ctrl Pts',(2.75294003743155,1.03763440108083,7.87954378677239));
#68055=CARTESIAN_POINT('Ctrl Pts',(2.78570747032704,0.9506993709316,7.87448728282488));
#68056=CARTESIAN_POINT('Ctrl Pts',(2.81441049930312,0.86205784297445,7.86943077887736));
#68057=CARTESIAN_POINT('Ctrl Pts',(2.83887067332622,0.772125184233966,7.86437427492985));
#68058=CARTESIAN_POINT('Ctrl Pts',(2.863297559972,0.682314913107818,7.85932465228068));
#68059=CARTESIAN_POINT('Ctrl Pts',(2.88349295071196,0.591217427185472,7.8542750296315));
#68060=CARTESIAN_POINT('Ctrl Pts',(2.89932694192119,0.499266746188751,7.84922540698233));
#68061=CARTESIAN_POINT('Ctrl Pts',(2.91514425280701,0.407412930668159,7.84418110385985));
#68062=CARTESIAN_POINT('Ctrl Pts',(2.92660922219562,0.314708141355005,7.83913680073737));
#68063=CARTESIAN_POINT('Ctrl Pts',(2.93364241605211,0.221599130729175,7.83409249761489));
#68064=CARTESIAN_POINT('Ctrl Pts',(2.94067065921967,0.128555659850846,7.82905174519444));
#68065=CARTESIAN_POINT('Ctrl Pts',(2.94327329437766,0.0351089741175195,
7.82401099277399));
#68066=CARTESIAN_POINT('Ctrl Pts',(2.94142254157655,-0.0582874935586067,
7.81897024035353));
#68067=CARTESIAN_POINT('Ctrl Pts',(2.93957244004538,-0.151651095520984,
7.8139312617467));
#68068=CARTESIAN_POINT('Ctrl Pts',(2.93327207286506,-0.24496407168727,7.80889228313987));
#68069=CARTESIAN_POINT('Ctrl Pts',(2.92254576829046,-0.337772456318622,
7.80385330453303));
#68070=CARTESIAN_POINT('Ctrl Pts',(2.9118202524686,-0.430574016337872,7.79881469646464));
#68071=CARTESIAN_POINT('Ctrl Pts',(2.89666949760899,-0.522870618214443,
7.79377608839625));
#68072=CARTESIAN_POINT('Ctrl Pts',(2.87716963974356,-0.614214021443608,
7.78873748032786));
#68073=CARTESIAN_POINT('Ctrl Pts',(2.85766578790226,-0.705576133698785,
7.78369784024789));
#68074=CARTESIAN_POINT('Ctrl Pts',(2.83381115679292,-0.795984226091077,
7.77865820016793));
#68075=CARTESIAN_POINT('Ctrl Pts',(2.80573262034301,-0.885001956575884,
7.77361856008796));
#68076=CARTESIAN_POINT('Ctrl Pts',(2.77762354581281,-0.974116502313364,
7.76857343891985));
#68077=CARTESIAN_POINT('Ctrl Pts',(2.74528153024882,-1.06183724453324,7.76352831775173));
#68078=CARTESIAN_POINT('Ctrl Pts',(2.70888269591461,-1.14774498028716,7.75848319658362));
#68079=CARTESIAN_POINT('Ctrl Pts',(2.67246127247764,-1.23370603034926,7.75343494441522));
#68080=CARTESIAN_POINT('Ctrl Pts',(2.63197820998977,-1.31785143476304,7.74838669224683));
#68081=CARTESIAN_POINT('Ctrl Pts',(2.58765601205185,-1.39978582765077,7.74333844007843));
#68082=CARTESIAN_POINT('Ctrl Pts',(2.543264078636,-1.48184913413737,7.73828224511175));
#68083=CARTESIAN_POINT('Ctrl Pts',(2.49502118123996,-1.56169410622437,7.73322605014507));
#68084=CARTESIAN_POINT('Ctrl Pts',(2.44319347254472,-1.63895382964709,7.7281698551784));
#68085=CARTESIAN_POINT('Ctrl Pts',(2.4210282110861,-1.6719956525059,7.72600746200602));
#68086=CARTESIAN_POINT('Ctrl Pts',(2.39820778215354,-1.70456503353761,7.72384506883365));
#68087=CARTESIAN_POINT('Ctrl Pts',(2.37475518372315,-1.73663519985633,7.72168267566128));
#68088=CARTESIAN_POINT('Ctrl Pts',(2.31991402067386,-1.81162753920514,7.71662617171377));
#68089=CARTESIAN_POINT('Ctrl Pts',(2.26142069502047,-1.88415143323315,7.71156966776626));
#68090=CARTESIAN_POINT('Ctrl Pts',(2.1995252550804,-1.95383025165021,7.70651316381875));
#68091=CARTESIAN_POINT('Ctrl Pts',(2.13771404744642,-2.02341424551207,7.70146354116958));
#68092=CARTESIAN_POINT('Ctrl Pts',(2.07251021822523,-2.09016052932911,7.69641391852041));
#68093=CARTESIAN_POINT('Ctrl Pts',(2.00420599049321,-2.15372290410608,7.69136429587124));
#68094=CARTESIAN_POINT('Ctrl Pts',(1.9359737178726,-2.21721831907821,7.68631999274873));
#68095=CARTESIAN_POINT('Ctrl Pts',(1.86464786194383,-2.27753619172648,7.68127568962622));
#68096=CARTESIAN_POINT('Ctrl Pts',(1.79055891692532,-2.33436560226097,7.67623138650371));
#68097=CARTESIAN_POINT('Ctrl Pts',(1.71652212336627,-2.39115501038081,7.67119063408326));
#68098=CARTESIAN_POINT('Ctrl Pts',(1.63972645757972,-2.44446056825905,7.66614988166281));
#68099=CARTESIAN_POINT('Ctrl Pts',(1.56053626688848,-2.49401093817284,7.66110912924236));
#68100=CARTESIAN_POINT('Ctrl Pts',(1.48137394279865,-2.54354387157844,7.65607015063552));
#68101=CARTESIAN_POINT('Ctrl Pts',(1.39981914339623,-2.58932400746781,7.65103117202868));
#68102=CARTESIAN_POINT('Ctrl Pts',(1.31626517170938,-2.63112333381483,7.64599219342185));
#68103=CARTESIAN_POINT('Ctrl Pts',(1.23271734411695,-2.67291958647185,7.64095358535348));
#68104=CARTESIAN_POINT('Ctrl Pts',(1.14717103319778,-2.71073541356624,7.63591497728511));
#68105=CARTESIAN_POINT('Ctrl Pts',(1.06004309499874,-2.74438930123725,7.63087636921674));
#68106=CARTESIAN_POINT('Ctrl Pts',(0.972897311187784,-2.77805008192365,
7.62583672913675));
#68107=CARTESIAN_POINT('Ctrl Pts',(0.884169670371078,-2.80754707076227,
7.62079708905677));
#68108=CARTESIAN_POINT('Ctrl Pts',(0.794294828950772,-2.83274773403882,
7.61575744897678));
#68109=CARTESIAN_POINT('Ctrl Pts',(0.704322240088413,-2.85797580543464,
7.61071232780866));
#68110=CARTESIAN_POINT('Ctrl Pts',(0.613200387771495,-2.87889810494226,
7.60566720664055));
#68111=CARTESIAN_POINT('Ctrl Pts',(0.521376527103044,-2.89543269943992,
7.60062208547243));
#68112=CARTESIAN_POINT('Ctrl Pts',(0.429495680581492,-2.91197755530066,
7.59557383330403));
#68113=CARTESIAN_POINT('Ctrl Pts',(0.336912397542223,-2.92412922736843,
7.59052558113563));
#68114=CARTESIAN_POINT('Ctrl Pts',(0.244079356636889,-2.93185764791944,
7.58547732896723));
#68115=CARTESIAN_POINT('Ctrl Pts',(0.151100254462614,-2.93959822818106,
7.58042113400055));
#68116=CARTESIAN_POINT('Ctrl Pts',(0.0578710523553916,-2.94290164931675,
7.57536493903387));
#68117=CARTESIAN_POINT('Ctrl Pts',(-0.0351555049776785,-2.94178994669398,
7.57030874406719));
#68118=CARTESIAN_POINT('Ctrl Pts',(-0.0749403617224944,-2.94131450257503,
7.56814635089485));
#68119=CARTESIAN_POINT('Ctrl Pts',(-0.114688219126788,-2.94003216518703,
7.56598395772251));
#68120=CARTESIAN_POINT('Ctrl Pts',(-0.154364084154138,-2.93794753689089,
7.56382156455017));
#68121=CARTESIAN_POINT('Ctrl Pts',(-0.247141461875206,-2.93307287702638,
7.55876506060266));
#68122=CARTESIAN_POINT('Ctrl Pts',(-0.339850814750179,-2.92379062296448,
7.55370855665515));
#68123=CARTESIAN_POINT('Ctrl Pts',(-0.432040076364305,-2.91010401401997,
7.54865205270765));
#68124=CARTESIAN_POINT('Ctrl Pts',(-0.524103879397204,-2.89643603091658,
7.54360243005846));
#68125=CARTESIAN_POINT('Ctrl Pts',(-0.615648562829644,-2.87837566868871,
7.53855280740927));
#68126=CARTESIAN_POINT('Ctrl Pts',(-0.706224457923897,-2.855978118794,7.53350318476009));
#68127=CARTESIAN_POINT('Ctrl Pts',(-0.796704935811239,-2.83360416360569,
7.52845888163757));
#68128=CARTESIAN_POINT('Ctrl Pts',(-0.886218225858062,-2.80690220881182,
7.52341457851505));
#68129=CARTESIAN_POINT('Ctrl Pts',(-0.974323250717918,-2.77597878289991,
7.51837027539253));
#68130=CARTESIAN_POINT('Ctrl Pts',(-1.06236625815215,-2.74507712409231,
7.51332952297207));
#68131=CARTESIAN_POINT('Ctrl Pts',(-1.14900255362035,-2.70996004716568,
7.50828877055162));
#68132=CARTESIAN_POINT('Ctrl Pts',(-1.23380567010069,-2.67078407371831,
7.50324801813116));
#68133=CARTESIAN_POINT('Ctrl Pts',(-1.31857894482114,-2.63162188608497,
7.49820903952433));
#68134=CARTESIAN_POINT('Ctrl Pts',(-1.40151992009744,-2.58840382541785,
7.4931700609175));
#68135=CARTESIAN_POINT('Ctrl Pts',(-1.48222255233038,-2.54133435528724,
7.48813108231067));
#68136=CARTESIAN_POINT('Ctrl Pts',(-1.56291925014091,-2.49426834638349,
7.48309247424227));
#68137=CARTESIAN_POINT('Ctrl Pts',(-1.64137754937265,-2.44335171479377,
7.47805386617388));
#68138=CARTESIAN_POINT('Ctrl Pts',(-1.71721744131187,-2.38883407947357,
7.47301525810549));
#68139=CARTESIAN_POINT('Ctrl Pts',(-1.7930728668365,-2.33430527780906,7.46797561802549));
#68140=CARTESIAN_POINT('Ctrl Pts',(-1.86630846018385,-2.27617426661408,
7.4629359779455));
#68141=CARTESIAN_POINT('Ctrl Pts',(-1.93657547249624,-2.21473236291114,
7.4578963378655));
#68142=CARTESIAN_POINT('Ctrl Pts',(-2.00691890687062,-2.15322363529156,
7.45285121669738));
#68143=CARTESIAN_POINT('Ctrl Pts',(-2.0742869817916,-2.08839712013141,7.44780609552925));
#68144=CARTESIAN_POINT('Ctrl Pts',(-2.13836641060864,-2.02058236505734,
7.44276097436113));
#68145=CARTESIAN_POINT('Ctrl Pts',(-2.20248560709479,-1.95272552417211,
7.43771272219273));
#68146=CARTESIAN_POINT('Ctrl Pts',(-2.2633118057172,-1.88187708739681,7.43266447002434));
#68147=CARTESIAN_POINT('Ctrl Pts',(-2.32057216644433,-1.80839951900123,
7.42761621785594));
#68148=CARTESIAN_POINT('Ctrl Pts',(-2.37792261924285,-1.7348063427706,7.42256002288926));
#68149=CARTESIAN_POINT('Ctrl Pts',(-2.43169577992265,-1.65857613939135,
7.41750382792259));
#68150=CARTESIAN_POINT('Ctrl Pts',(-2.48166238525116,-1.58009993532989,
7.41244763295591));
#68151=CARTESIAN_POINT('Ctrl Pts',(-2.50303170485151,-1.54653785772654,
7.41028523978362));
#68152=CARTESIAN_POINT('Ctrl Pts',(-2.52370537044815,-1.51256527895886,
7.40812284661134));
#68153=CARTESIAN_POINT('Ctrl Pts',(-2.54366808888571,-1.47821400804637,
7.40596045343906));
#68154=CARTESIAN_POINT('Ctrl Pts',(-2.59210151914144,-1.39487115626297,
7.40071406782164));
#68155=CARTESIAN_POINT('Ctrl Pts',(-2.63650617799513,-1.3090235510266,7.39546768220423));
#68156=CARTESIAN_POINT('Ctrl Pts',(-2.67662574138782,-1.22108093119993,
7.39022129658682));
#68157=CARTESIAN_POINT('Ctrl Pts',(-2.71667599687629,-1.13329023522677,
7.38498397427821));
#68158=CARTESIAN_POINT('Ctrl Pts',(-2.75245572483854,-1.04341208544652,
7.37974665196959));
#68159=CARTESIAN_POINT('Ctrl Pts',(-2.78375366163325,-0.951882110002848,
7.37450932966098));
#68160=CARTESIAN_POINT('Ctrl Pts',(-2.81498817722214,-0.860537608171982,
7.36928262010612));
#68161=CARTESIAN_POINT('Ctrl Pts',(-2.8417588666175,-0.767548322398948,
7.36405591055125));
#68162=CARTESIAN_POINT('Ctrl Pts',(-2.86390237024338,-0.673370042186563,
7.35882920099639));
#68163=CARTESIAN_POINT('Ctrl Pts',(-2.88601895663896,-0.579306243336356,
7.35360884493225));
#68164=CARTESIAN_POINT('Ctrl Pts',(-2.90351945760502,-0.484056709901852,
7.3483884888681));
#68165=CARTESIAN_POINT('Ctrl Pts',(-2.91629009012335,-0.388092914452626,
7.34316813280396));
#68166=CARTESIAN_POINT('Ctrl Pts',(-2.92904377630873,-0.292256460732716,
7.33795470403115));
#68167=CARTESIAN_POINT('Ctrl Pts',(-2.93708004351147,-0.195708024943747,
7.33274127525835));
#68168=CARTESIAN_POINT('Ctrl Pts',(-2.94033621960299,-0.098928841551814,
7.32752784648554));
#68169=CARTESIAN_POINT('Ctrl Pts',(-2.94145040466026,-0.0658133352158173,
7.32574393668689));
#68170=CARTESIAN_POINT('Ctrl Pts',(-2.94200535872909,-0.0326708858341013,
7.32396002688824));
#68171=CARTESIAN_POINT('Ctrl Pts',(-2.94199996099953,0.000479039395695414,
7.32217611708959));
#68172=CARTESIAN_POINT('',(-2.94199929728077,0.0020334206256296,6.3221761170896));
#68173=CARTESIAN_POINT('Ctrl Pts',(-2.94199996099939,0.000479040305269824,
7.32217611704064));
#68174=CARTESIAN_POINT('Ctrl Pts',(-2.94198378421545,0.0998278783730615,
7.31682981944008));
#68175=CARTESIAN_POINT('Ctrl Pts',(-2.93693095783807,0.199055979289579,
7.31148352183952));
#68176=CARTESIAN_POINT('Ctrl Pts',(-2.92690352421262,0.297657118093517,
7.30613722423896));
#68177=CARTESIAN_POINT('Ctrl Pts',(-2.91684329563174,0.39658073422059,7.30077344144746));
#68178=CARTESIAN_POINT('Ctrl Pts',(-2.90177595852271,0.494872932518549,
7.29540965865596));
#68179=CARTESIAN_POINT('Ctrl Pts',(-2.88181511798122,0.592035155860621,
7.29004587586446));
#68180=CARTESIAN_POINT('Ctrl Pts',(-2.86182045155733,0.689362031484373,
7.28467300354161));
#68181=CARTESIAN_POINT('Ctrl Pts',(-2.83691582196706,0.785554767436168,
7.27930013121876));
#68182=CARTESIAN_POINT('Ctrl Pts',(-2.80726469917522,0.880130052188105,
7.27392725889591));
#68183=CARTESIAN_POINT('Ctrl Pts',(-2.77752918840202,0.974974501026125,
7.2685390952179));
#68184=CARTESIAN_POINT('Ctrl Pts',(-2.74302029293948,1.06819195891079,7.26315093153989));
#68185=CARTESIAN_POINT('Ctrl Pts',(-2.70395013541805,1.15931775849967,7.25776276786188));
#68186=CARTESIAN_POINT('Ctrl Pts',(-2.6805932875586,1.21379441209139,7.25454162601724));
#68187=CARTESIAN_POINT('Ctrl Pts',(-2.65560720026491,1.26752399495668,7.25132048417259));
#68188=CARTESIAN_POINT('Ctrl Pts',(-2.62904482224712,1.32041180039244,7.24809934232795));
#68189=CARTESIAN_POINT('Ctrl Pts',(-2.58734756836014,1.40343434638977,7.24304283838044));
#68190=CARTESIAN_POINT('Ctrl Pts',(-2.54164050844154,1.48462578081831,7.23798633443293));
#68191=CARTESIAN_POINT('Ctrl Pts',(-2.49210802758016,1.56357333658211,7.23292983048542));
#68192=CARTESIAN_POINT('Ctrl Pts',(-2.44264295451304,1.64241345414569,7.22788020783624));
#68193=CARTESIAN_POINT('Ctrl Pts',(-2.38936303967928,1.71901538900267,7.22283058518707));
#68194=CARTESIAN_POINT('Ctrl Pts',(-2.33249929116039,1.79298941902519,7.21778096253789));
#68195=CARTESIAN_POINT('Ctrl Pts',(-2.27569544577662,1.86688552108075,7.21273665941539));
#68196=CARTESIAN_POINT('Ctrl Pts',(-2.21531554015483,1.93815887151289,7.2076923562929));
#68197=CARTESIAN_POINT('Ctrl Pts',(-2.1516341563711,2.00644821940094,7.20264805317041));
#68198=CARTESIAN_POINT('Ctrl Pts',(-2.08799759812901,2.07468949818583,7.19760730074996));
#68199=CARTESIAN_POINT('Ctrl Pts',(-2.02106448260628,2.13995062620793,7.19256654832952));
#68200=CARTESIAN_POINT('Ctrl Pts',(-1.95114931947164,2.20190379742743,7.18752579590907));
#68201=CARTESIAN_POINT('Ctrl Pts',(-1.88125875910622,2.26383516765978,7.18248681730224));
#68202=CARTESIAN_POINT('Ctrl Pts',(-1.80838856750224,2.32246060005221,7.17744783869541));
#68203=CARTESIAN_POINT('Ctrl Pts',(-1.73288897034967,2.37749023477289,7.17240886008858));
#68204=CARTESIAN_POINT('Ctrl Pts',(-1.65739492501744,2.43251582292039,7.1673702520202));
#68205=CARTESIAN_POINT('Ctrl Pts',(-1.57927221706682,2.4839458782693,7.16233164395183));
#68206=CARTESIAN_POINT('Ctrl Pts',(-1.49890198392706,2.53153250869498,7.15729303588345));
#68207=CARTESIAN_POINT('Ctrl Pts',(-1.41851528929414,2.57912888585102,7.15225339580348));
#68208=CARTESIAN_POINT('Ctrl Pts',(-1.33588053684632,2.62288004907297,7.14721375572351));
#68209=CARTESIAN_POINT('Ctrl Pts',(-1.25140451222114,2.6625834722676,7.14217411564354));
#68210=CARTESIAN_POINT('Ctrl Pts',(-1.16683661188062,2.70233007671304,7.13712899447543));
#68211=CARTESIAN_POINT('Ctrl Pts',(-1.08042384414241,2.73801996545164,7.13208387330731));
#68212=CARTESIAN_POINT('Ctrl Pts',(-0.99259378041509,2.76949843601351,7.12703875213919));
#68213=CARTESIAN_POINT('Ctrl Pts',(-0.90470920938366,2.80099644210223,7.1219904999708));
#68214=CARTESIAN_POINT('Ctrl Pts',(-0.815406014878199,2.82827769726885,
7.1169422478024));
#68215=CARTESIAN_POINT('Ctrl Pts',(-0.725125686506602,2.85123775556658,
7.11189399563401));
#68216=CARTESIAN_POINT('Ctrl Pts',(-0.634703313242367,2.87423393866663,
7.10683780066733));
#68217=CARTESIAN_POINT('Ctrl Pts',(-0.543301170934598,2.89289526494013,
7.10178160570066));
#68218=CARTESIAN_POINT('Ctrl Pts',(-0.451369422798152,2.90716866455369,
7.09672541073398));
#68219=CARTESIAN_POINT('Ctrl Pts',(-0.412052785325619,2.91327299836091,
7.0945630175616));
#68220=CARTESIAN_POINT('Ctrl Pts',(-0.372639324005275,2.91857541518902,
7.09240062438922));
#68221=CARTESIAN_POINT('Ctrl Pts',(-0.333164311357436,2.92307467260721,
7.09023823121684));
#68222=CARTESIAN_POINT('Ctrl Pts',(-0.24085660347553,2.93359566073579,7.08518172726933));
#68223=CARTESIAN_POINT('Ctrl Pts',(-0.147887763980285,2.93975839015493,
7.08012522332181));
#68224=CARTESIAN_POINT('Ctrl Pts',(-0.0547041816371323,2.94149136536408,
7.0750687193743));
#68225=CARTESIAN_POINT('Ctrl Pts',(0.038352588972679,2.94322198220081,7.07001909672512));
#68226=CARTESIAN_POINT('Ctrl Pts',(0.131623082105364,2.94053481653771,7.06496947407595));
#68227=CARTESIAN_POINT('Ctrl Pts',(0.224654690201034,2.93341000717095,7.05991985142677));
#68228=CARTESIAN_POINT('Ctrl Pts',(0.317588294117885,2.92629270343701,7.05487554830427));
#68229=CARTESIAN_POINT('Ctrl Pts',(0.410283073450271,2.914747082221,7.04983124518177));
#68230=CARTESIAN_POINT('Ctrl Pts',(0.50228641206536,2.89880533328033,7.04478694205927));
#68231=CARTESIAN_POINT('Ctrl Pts',(0.594224989218892,2.88287480579073,7.03974618963882));
#68232=CARTESIAN_POINT('Ctrl Pts',(0.685472657454865,2.86255437701052,7.03470543721837));
#68233=CARTESIAN_POINT('Ctrl Pts',(0.775582950323216,2.83792795665569,7.02966468479792));
#68234=CARTESIAN_POINT('Ctrl Pts',(0.865661533865007,2.8133102022055,7.02462570619108));
#68235=CARTESIAN_POINT('Ctrl Pts',(0.954603109955396,2.78438958343318,7.01958672758425));
#68236=CARTESIAN_POINT('Ctrl Pts',(1.04197343392313,2.75130066750227,7.01454774897741));
#68237=CARTESIAN_POINT('Ctrl Pts',(1.12933733316328,2.71821418474617,7.00950914090904));
#68238=CARTESIAN_POINT('Ctrl Pts',(1.2151297955174,2.68096017162062,7.00447053284066));
#68239=CARTESIAN_POINT('Ctrl Pts',(1.29893479283542,2.63972203157105,6.99943192477228));
#68240=CARTESIAN_POINT('Ctrl Pts',(1.38275695515762,2.59847544509384,6.99439228469231));
#68241=CARTESIAN_POINT('Ctrl Pts',(1.46459044636346,2.55324330704513,6.98935264461233));
#68242=CARTESIAN_POINT('Ctrl Pts',(1.54404317920392,2.50425531061708,6.98431300453236));
#68243=CARTESIAN_POINT('Ctrl Pts',(1.62358232445195,2.45521403508129,6.97926788336424));
#68244=CARTESIAN_POINT('Ctrl Pts',(1.70073516526895,2.40240898096491,6.97422276219612));
#68245=CARTESIAN_POINT('Ctrl Pts',(1.77513827279761,2.34611340570935,6.969177641028));
#68246=CARTESIAN_POINT('Ctrl Pts',(1.84958755486642,2.28978289344125,6.96412938885961));
#68247=CARTESIAN_POINT('Ctrl Pts',(1.92128336616778,2.22995783118312,6.95908113669121));
#68248=CARTESIAN_POINT('Ctrl Pts',(1.9898967301173,2.16695062321883,6.95403288452282));
#68249=CARTESIAN_POINT('Ctrl Pts',(2.05861804867987,2.10384428123219,6.94897668955614));
#68250=CARTESIAN_POINT('Ctrl Pts',(2.12424692758221,2.03754611405718,6.94392049458946));
#68251=CARTESIAN_POINT('Ctrl Pts',(2.18649264911458,1.96840389538527,6.93886429962278));
#68252=CARTESIAN_POINT('Ctrl Pts',(2.21311340328578,1.93883370227314,6.93670190645043));
#68253=CARTESIAN_POINT('Ctrl Pts',(2.2391158868758,1.90874371382886,6.93453951327808));
#68254=CARTESIAN_POINT('Ctrl Pts',(2.26447976142844,1.87816277518243,6.93237712010573));
#68255=CARTESIAN_POINT('Ctrl Pts',(2.32379022052512,1.8066528208589,6.92732061615821));
#68256=CARTESIAN_POINT('Ctrl Pts',(2.3798143168841,1.73220495333977,6.9222641122107));
#68257=CARTESIAN_POINT('Ctrl Pts',(2.43224797467008,1.65515370576672,6.91720760826319));
#68258=CARTESIAN_POINT('Ctrl Pts',(2.48461027650623,1.57820731574487,6.91215798561401));
#68259=CARTESIAN_POINT('Ctrl Pts',(2.5333916024548,1.49866494975525,6.90710836296483));
#68260=CARTESIAN_POINT('Ctrl Pts',(2.5783276947571,1.41689459680265,6.90205874031565));
#68261=CARTESIAN_POINT('Ctrl Pts',(2.62321644911784,1.33521038485588,6.89701443719315));
#68262=CARTESIAN_POINT('Ctrl Pts',(2.66426780942961,1.25130323795345,6.89197013407064));
#68263=CARTESIAN_POINT('Ctrl Pts',(2.7012610825473,1.16556963065935,6.88692583094814));
#68264=CARTESIAN_POINT('Ctrl Pts',(2.73822831597478,1.07989637154176,6.88188507852769));
#68265=CARTESIAN_POINT('Ctrl Pts',(2.77114296501136,0.992399613526902,6.87684432610724));
#68266=CARTESIAN_POINT('Ctrl Pts',(2.79983099339525,0.903498980864605,6.87180357368678));
#68267=CARTESIAN_POINT('Ctrl Pts',(2.82850892661651,0.814629631855959,6.86676459507995));
#68268=CARTESIAN_POINT('Ctrl Pts',(2.85296305815076,0.72435781123335,6.86172561647312));
#68269=CARTESIAN_POINT('Ctrl Pts',(2.87306844143933,0.633120628952623,6.85668663786628));
#68270=CARTESIAN_POINT('Ctrl Pts',(2.89317234628988,0.541890155746658,6.8516480297979));
#68271=CARTESIAN_POINT('Ctrl Pts',(2.90892804364763,0.449694895068448,6.84660942172951));
#68272=CARTESIAN_POINT('Ctrl Pts',(2.92026143212223,0.35698342827003,6.84157081366113));
#68273=CARTESIAN_POINT('Ctrl Pts',(2.9315971419102,0.264252972237484,6.83653117358116));
#68274=CARTESIAN_POINT('Ctrl Pts',(2.93850869043589,0.171006540175025,6.83149153350119));
#68275=CARTESIAN_POINT('Ctrl Pts',(2.94097382184918,0.0776979999604444,
6.82645189342121));
#68276=CARTESIAN_POINT('Ctrl Pts',(2.94344163432745,-0.0157120221706676,
6.82140677225309));
#68277=CARTESIAN_POINT('Ctrl Pts',(2.94145336569045,-0.109183843454912,
6.81636165108497));
#68278=CARTESIAN_POINT('Ctrl Pts',(2.93503890530532,-0.202263749456388,
6.81131652991685));
#68279=CARTESIAN_POINT('Ctrl Pts',(2.92862046410852,-0.295401420811999,
6.80626827774845));
#68280=CARTESIAN_POINT('Ctrl Pts',(2.91777041394201,-0.388146252709685,
6.80122002558006));
#68281=CARTESIAN_POINT('Ctrl Pts',(2.90257026177326,-0.480051950802704,
6.79617177341167));
#68282=CARTESIAN_POINT('Ctrl Pts',(2.88734619405146,-0.572102251105938,
6.79111557844499));
#68283=CARTESIAN_POINT('Ctrl Pts',(2.86775845506615,-0.663310349420649,
6.78605938347831));
#68284=CARTESIAN_POINT('Ctrl Pts',(2.8439390901669,-0.753242624537838,6.78100318851163));
#68285=CARTESIAN_POINT('Ctrl Pts',(2.83375221399479,-0.791704143321829,
6.77884079533929));
#68286=CARTESIAN_POINT('Ctrl Pts',(2.82279197136707,-0.829932531189377,
6.77667840216695));
#68287=CARTESIAN_POINT('Ctrl Pts',(2.81107137944757,-0.867894981925068,
6.77451600899461));
#68288=CARTESIAN_POINT('Ctrl Pts',(2.78366414376714,-0.956665740387302,
6.7694595050471));
#68289=CARTESIAN_POINT('Ctrl Pts',(2.75199967391826,-1.04429305177003,6.76440300109959));
#68290=CARTESIAN_POINT('Ctrl Pts',(2.71619162367162,-1.13033935766926,6.75934649715208));
#68291=CARTESIAN_POINT('Ctrl Pts',(2.68043230390734,-1.21626856481658,6.7542968745029));
#68292=CARTESIAN_POINT('Ctrl Pts',(2.64054077861423,-1.30062063626899,6.74924725185372));
#68293=CARTESIAN_POINT('Ctrl Pts',(2.59668049128932,-1.38297303883968,6.74419762920454));
#68294=CARTESIAN_POINT('Ctrl Pts',(2.55286640859885,-1.46523868724418,6.73915332608204));
#68295=CARTESIAN_POINT('Ctrl Pts',(2.50509208190367,-1.54550846482934,6.73410902295954));
#68296=CARTESIAN_POINT('Ctrl Pts',(2.45356863385393,-1.62338071904534,6.72906471983704));
#68297=CARTESIAN_POINT('Ctrl Pts',(2.40208145333375,-1.70119815871788,6.72402396741659));
#68298=CARTESIAN_POINT('Ctrl Pts',(2.34685064110187,-1.77662106083995,6.71898321499614));
#68299=CARTESIAN_POINT('Ctrl Pts',(2.28813222442199,-1.84927416127562,6.71394246257569));
#68300=CARTESIAN_POINT('Ctrl Pts',(2.22943447043659,-1.92190169547669,6.70890348396885));
#68301=CARTESIAN_POINT('Ctrl Pts',(2.16725182874029,-1.99176101997443,6.70386450536202));
#68302=CARTESIAN_POINT('Ctrl Pts',(2.10188182122762,-2.05850839434598,6.69882552675519));
#68303=CARTESIAN_POINT('Ctrl Pts',(2.03651662066159,-2.12525086048699,6.69378691868681));
#68304=CARTESIAN_POINT('Ctrl Pts',(1.96796483076143,-2.18888151498805,6.68874831061843));
#68305=CARTESIAN_POINT('Ctrl Pts',(1.89656139422789,-2.24909290113245,6.68370970255004));
#68306=CARTESIAN_POINT('Ctrl Pts',(1.82514333278744,-2.30931661981936,6.67867006247007));
#68307=CARTESIAN_POINT('Ctrl Pts',(1.75087280382795,-2.36611939372584,6.6736304223901));
#68308=CARTESIAN_POINT('Ctrl Pts',(1.67411754113354,-2.41923427110087,6.66859078231013));
#68309=CARTESIAN_POINT('Ctrl Pts',(1.59727879978707,-2.47240691595937,6.66354566114201));
#68310=CARTESIAN_POINT('Ctrl Pts',(1.51795029593581,-2.52188340596303,6.65850053997389));
#68311=CARTESIAN_POINT('Ctrl Pts',(1.43652816487824,-2.5674405215139,6.65345541880577));
#68312=CARTESIAN_POINT('Ctrl Pts',(1.35505550327721,-2.6130259097933,6.64840716663738));
#68313=CARTESIAN_POINT('Ctrl Pts',(1.27148702415407,-2.65468688349036,6.64335891446899));
#68314=CARTESIAN_POINT('Ctrl Pts',(1.18624089309556,-2.69224748928248,6.6383106623006));
#68315=CARTESIAN_POINT('Ctrl Pts',(1.1008606378291,-2.72986719202646,6.63325446733392));
#68316=CARTESIAN_POINT('Ctrl Pts',(1.01379787477102,-2.76337349002297,6.62819827236724));
#68317=CARTESIAN_POINT('Ctrl Pts',(0.925487812259978,-2.79263966693848,
6.62314207740057));
#68318=CARTESIAN_POINT('Ctrl Pts',(0.88772006843628,-2.8051559922701,6.62097968422821));
#68319=CARTESIAN_POINT('Ctrl Pts',(0.849724338919268,-2.81689741875508,
6.61881729105586));
#68320=CARTESIAN_POINT('Ctrl Pts',(0.811535206197165,-2.8278568933209,6.6166548978835));
#68321=CARTESIAN_POINT('Ctrl Pts',(0.722234378378193,-2.85348434493941,
6.61159839393599));
#68322=CARTESIAN_POINT('Ctrl Pts',(0.631561434640505,-2.87492266635056,
6.60654188998847));
#68323=CARTESIAN_POINT('Ctrl Pts',(0.539944816462444,-2.89202759239523,
6.60148538604096));
#68324=CARTESIAN_POINT('Ctrl Pts',(0.448452877566457,-2.90910924067718,
6.59643576339178));
#68325=CARTESIAN_POINT('Ctrl Pts',(0.356020248495451,-2.92186913219511,
6.5913861407426));
#68326=CARTESIAN_POINT('Ctrl Pts',(0.263090035061182,-2.93021289899753,
6.58633651809342));
#68327=CARTESIAN_POINT('Ctrl Pts',(0.170257718991431,-2.93854787605601,
6.58129221497091));
#68328=CARTESIAN_POINT('Ctrl Pts',(0.0769292998126101,-2.94247593643618,
6.57624791184841));
#68329=CARTESIAN_POINT('Ctrl Pts',(-0.0164435083619719,-2.94195404638359,
6.5712036087259));
#68330=CARTESIAN_POINT('Ctrl Pts',(-0.109750591100613,-2.94143252369117,
6.56616285630545));
#68331=CARTESIAN_POINT('Ctrl Pts',(-0.20310155859628,-2.9364672792926,6.561122103885));
#68332=CARTESIAN_POINT('Ctrl Pts',(-0.296042216743756,-2.92706730464222,
6.55608135146455));
#68333=CARTESIAN_POINT('Ctrl Pts',(-0.388950169574352,-2.91767063779227,
6.55104237285771));
#68334=CARTESIAN_POINT('Ctrl Pts',(-0.48144765923277,-2.9038423857515,6.54600339425088));
#68335=CARTESIAN_POINT('Ctrl Pts',(-0.573084175815556,-2.88564352050453,
6.54096441564405));
#68336=CARTESIAN_POINT('Ctrl Pts',(-0.664713953958702,-2.86744599350087,
6.53592580757567));
#68337=CARTESIAN_POINT('Ctrl Pts',(-0.755482450113381,-2.84487857901544,
6.53088719950729));
#68338=CARTESIAN_POINT('Ctrl Pts',(-0.844949051825742,-2.81805342387592,
6.52584859143891));
#68339=CARTESIAN_POINT('Ctrl Pts',(-0.934433978156555,-2.79122277438741,
6.52080895135893));
#68340=CARTESIAN_POINT('Ctrl Pts',(-1.0226160559201,-2.76013277990829,6.51576931127896));
#68341=CARTESIAN_POINT('Ctrl Pts',(-1.10907063655849,-2.72494519635235,
6.51072967119899));
#68342=CARTESIAN_POINT('Ctrl Pts',(-1.19561924478017,-2.68971934295091,
6.50568455003086));
#68343=CARTESIAN_POINT('Ctrl Pts',(-1.28043619460545,-2.65038717280091,
6.50063942886274));
#68344=CARTESIAN_POINT('Ctrl Pts',(-1.36311790433551,-2.60715814228442,
6.49559430769461));
#68345=CARTESIAN_POINT('Ctrl Pts',(-1.44585092630306,-2.5639022838481,6.49054605552622));
#68346=CARTESIAN_POINT('Ctrl Pts',(-1.52644568770699,-2.51674497405849,
6.48549780335783));
#68347=CARTESIAN_POINT('Ctrl Pts',(-1.60452611780499,-2.46593997033213,
6.48044955118943));
#68348=CARTESIAN_POINT('Ctrl Pts',(-1.68272939776976,-2.41505503123745,
6.47539335622275));
#68349=CARTESIAN_POINT('Ctrl Pts',(-1.75841009068825,-2.36051120082445,
6.47033716125607));
#68350=CARTESIAN_POINT('Ctrl Pts',(-1.8312240151683,-2.30260344094916,6.46528096628939));
#68351=CARTESIAN_POINT('Ctrl Pts',(-1.86236449416172,-2.27783791165198,
6.46311857311706));
#68352=CARTESIAN_POINT('Ctrl Pts',(-1.89298108005343,-2.25245758017783,
6.46095617994473));
#68353=CARTESIAN_POINT('Ctrl Pts',(-1.92304894811814,-2.22648753491721,
6.45879378677239));
#68354=CARTESIAN_POINT('Ctrl Pts',(-1.99236460879073,-2.16661861301485,
6.4538088070907));
#68355=CARTESIAN_POINT('Ctrl Pts',(-2.05902051282149,-2.10338958358544,
6.44882382740901));
#68356=CARTESIAN_POINT('Ctrl Pts',(-2.12266652911026,-2.03706917069475,
6.44383884772732));
#68357=CARTESIAN_POINT('Ctrl Pts',(-2.18738886024589,-1.96962721635957,
6.43876956728409));
#68358=CARTESIAN_POINT('Ctrl Pts',(-2.24899815107245,-1.89898859804056,
6.43370028684085));
#68359=CARTESIAN_POINT('Ctrl Pts',(-2.3071601469075,-1.82547967847406,6.42863100639761));
#68360=CARTESIAN_POINT('Ctrl Pts',(-2.36421136770326,-1.75337462876876,
6.42365853883197));
#68361=CARTESIAN_POINT('Ctrl Pts',(-2.41794548947623,-1.67850830759329,
6.41868607126633));
#68362=CARTESIAN_POINT('Ctrl Pts',(-2.46808440048347,-1.60122559063055,
6.41371360370068));
#68363=CARTESIAN_POINT('Ctrl Pts',(-2.51819323891477,-1.52398922669638,
6.40874411854741));
#68364=CARTESIAN_POINT('Ctrl Pts',(-2.56471089929148,-1.44433972671108,
6.40377463339414));
#68365=CARTESIAN_POINT('Ctrl Pts',(-2.60740131820889,-1.36265269449062,
6.39880514824087));
#68366=CARTESIAN_POINT('Ctrl Pts',(-2.650078827755,-1.28099036402424,6.3938371658353));
#68367=CARTESIAN_POINT('Ctrl Pts',(-2.68893118346864,-1.19729213026207,
6.38886918342974));
#68368=CARTESIAN_POINT('Ctrl Pts',(-2.72376786861293,-1.11195890117926,
6.38390120102417));
#68369=CARTESIAN_POINT('Ctrl Pts',(-2.75983712736816,-1.02360645583439,
6.37875744402963));
#68370=CARTESIAN_POINT('Ctrl Pts',(-2.79160102499696,-0.933501625967505,
6.37361368703508));
#68371=CARTESIAN_POINT('Ctrl Pts',(-2.81890271353629,-0.842111329705131,
6.36846993004053));
#68372=CARTESIAN_POINT('Ctrl Pts',(-2.84529157772194,-0.753776642549063,
6.36349815312872));
#68373=CARTESIAN_POINT('Ctrl Pts',(-2.86751181411504,-0.664241554947752,
6.35852637621692));
#68374=CARTESIAN_POINT('Ctrl Pts',(-2.88547327196091,-0.573940760705475,
6.35355459930512));
#68375=CARTESIAN_POINT('Ctrl Pts',(-2.90436669429192,-0.47895453758905,
6.3483248522692));
#68376=CARTESIAN_POINT('Ctrl Pts',(-2.91854736623395,-0.383121572191401,
6.34309510523328));
#68377=CARTESIAN_POINT('Ctrl Pts',(-2.9279721520141,-0.286954834477387,
6.33786535819736));
#68378=CARTESIAN_POINT('Ctrl Pts',(-2.93739693779424,-0.190788096763381,
6.33263561116144));
#68379=CARTESIAN_POINT('Ctrl Pts',(-2.94206587184204,-0.0942881716709648,
6.32740586412552));
#68380=CARTESIAN_POINT('Ctrl Pts',(-2.94199929728077,0.0020334206256296,
6.3221761170896));
#68381=CARTESIAN_POINT('',(-2.94199891764675,-0.00252360166277677,5.3221761170896));
#68382=CARTESIAN_POINT('Ctrl Pts',(-2.94474230559933,0.0020353165097306,
6.3221761170896));
#68383=CARTESIAN_POINT('Ctrl Pts',(-2.94577608567865,0.132578411608025,
6.31509496994683));
#68384=CARTESIAN_POINT('Ctrl Pts',(-2.87884406698728,1.23212772485676,6.25539345243361));
#68385=CARTESIAN_POINT('Ctrl Pts',(-1.49536511544646,3.13195190828347,6.14307156455023));
#68386=CARTESIAN_POINT('Ctrl Pts',(1.803451502182,2.96526596843762,5.98521045343903));
#68387=CARTESIAN_POINT('Ctrl Pts',(3.46879199270658,0.112790494414378,5.82734934232797));
#68388=CARTESIAN_POINT('Ctrl Pts',(1.99227427239527,-2.84184496548413,5.66948823121683));
#68389=CARTESIAN_POINT('Ctrl Pts',(-1.28874579170721,-3.22247945977241,
5.51162712010572));
#68390=CARTESIAN_POINT('Ctrl Pts',(-2.83889964018183,-1.36109225107598,
5.39585641539665));
#68391=CARTESIAN_POINT('Ctrl Pts',(-2.94470393564848,-0.196954622309047,
5.33270608105794));
#68392=CARTESIAN_POINT('Ctrl Pts',(-2.94294893056736,-0.00252441656932667,
5.3221761170896));
#68393=CARTESIAN_POINT('',(-2.94157989262999,0.000541900692576724,4.32217607813505));
#68394=CARTESIAN_POINT('Ctrl Pts',(-2.94199891764675,-0.00252360166277676,
5.3221761170896));
#68395=CARTESIAN_POINT('Ctrl Pts',(-2.94207769696413,0.0893168301654653,
5.31720056856825));
#68396=CARTESIAN_POINT('Ctrl Pts',(-2.93785178601327,0.181293760433016,
5.3122250200469));
#68397=CARTESIAN_POINT('Ctrl Pts',(-2.92930951506285,0.272964768719746,
5.30724947152555));
#68398=CARTESIAN_POINT('Ctrl Pts',(-2.92077520090699,0.364550389012694,
5.30227855753494));
#68399=CARTESIAN_POINT('Ctrl Pts',(-2.9079325573502,0.455830200173258,5.29730764354433));
#68400=CARTESIAN_POINT('Ctrl Pts',(-2.89082196906571,0.546362831062912,
5.29233672955373));
#68401=CARTESIAN_POINT('Ctrl Pts',(-2.87371971674413,0.636851356125155,
5.2873682373007));
#68402=CARTESIAN_POINT('Ctrl Pts',(-2.85235373180398,0.726592974961472,
5.28239974504768));
#68403=CARTESIAN_POINT('Ctrl Pts',(-2.8268159815655,0.815153609061427,5.27743125279465));
#68404=CARTESIAN_POINT('Ctrl Pts',(-2.80128307582474,0.903697443255923,
5.27246370306198));
#68405=CARTESIAN_POINT('Ctrl Pts',(-2.77158010358642,0.991060298465522,
5.2674961533293));
#68406=CARTESIAN_POINT('Ctrl Pts',(-2.73784933610354,1.07682171820474,5.26252860359663));
#68407=CARTESIAN_POINT('Ctrl Pts',(-2.70411493295863,1.16259238171637,5.2575605184379));
#68408=CARTESIAN_POINT('Ctrl Pts',(-2.66635204186074,1.24676084220454,5.25259243327916));
#68409=CARTESIAN_POINT('Ctrl Pts',(-2.62475116418239,1.32892638100205,5.24762434812043));
#68410=CARTESIAN_POINT('Ctrl Pts',(-2.58310848034422,1.41117449078935,5.24265127036121));
#68411=CARTESIAN_POINT('Ctrl Pts',(-2.53762031987618,1.49141525350977,5.23767819260199));
#68412=CARTESIAN_POINT('Ctrl Pts',(-2.48852301719977,1.56927282295557,5.23270511484277));
#68413=CARTESIAN_POINT('Ctrl Pts',(-2.43939780754102,1.64717464676357,5.22772921037851));
#68414=CARTESIAN_POINT('Ctrl Pts',(-2.38665963665628,1.7226902083042,5.22275330591424));
#68415=CARTESIAN_POINT('Ctrl Pts',(-2.33058667000846,1.79547480449571,5.21777740144998));
#68416=CARTESIAN_POINT('Ctrl Pts',(-2.27442599553133,1.86837324839887,5.21279371380952));
#68417=CARTESIAN_POINT('Ctrl Pts',(-2.21492041233414,1.93853185555798,5.20781002616905));
#68418=CARTESIAN_POINT('Ctrl Pts',(-2.15238634144226,2.0056413032177,5.20282633852859));
#68419=CARTESIAN_POINT('Ctrl Pts',(-2.12343683716622,2.03670893106088,5.20051919164689));
#68420=CARTESIAN_POINT('Ctrl Pts',(-2.093838775635,2.06712363248387,5.1982120447652));
#68421=CARTESIAN_POINT('Ctrl Pts',(-2.0636259110797,2.096857672595,5.1959048978835));
#68422=CARTESIAN_POINT('Ctrl Pts',(-1.99740929084564,2.16202486779619,5.19084839393599));
#68423=CARTESIAN_POINT('Ctrl Pts',(-1.92798636711574,2.22416697921654,5.18579188998848));
#68424=CARTESIAN_POINT('Ctrl Pts',(-1.85566465074133,2.28295262850306,5.18073538604096));
#68425=CARTESIAN_POINT('Ctrl Pts',(-1.78344135559066,2.3416582775375,5.17568576339178));
#68426=CARTESIAN_POINT('Ctrl Pts',(-1.70832744848884,2.39701626439059,5.17063614074261));
#68427=CARTESIAN_POINT('Ctrl Pts',(-1.63066715573537,2.448732044795,5.16558651809343));
#68428=CARTESIAN_POINT('Ctrl Pts',(-1.5530886742435,2.50039334519311,5.16054221497093));
#68429=CARTESIAN_POINT('Ctrl Pts',(-1.47296950641336,2.54841982154668,5.15549791184844));
#68430=CARTESIAN_POINT('Ctrl Pts',(-1.3906859596952,2.59255791864071,5.15045360872594));
#68431=CARTESIAN_POINT('Ctrl Pts',(-1.30846033264412,2.63666494677878,5.14541285630549));
#68432=CARTESIAN_POINT('Ctrl Pts',(-1.22407374466982,2.67688882717798,5.14037210388503));
#68433=CARTESIAN_POINT('Ctrl Pts',(-1.13792953028198,2.713020527772,5.13533135146458));
#68434=CARTESIAN_POINT('Ctrl Pts',(-1.05181562957913,2.74913951381521,5.13029237285775));
#68435=CARTESIAN_POINT('Ctrl Pts',(-0.963945739747836,2.78116900973128,
5.12525339425093));
#68436=CARTESIAN_POINT('Ctrl Pts',(-0.874744785359857,2.80894741148455,
5.1202144156441));
#68437=CARTESIAN_POINT('Ctrl Pts',(-0.785550390313629,2.83672377056874,
5.11517580757571));
#68438=CARTESIAN_POINT('Ctrl Pts',(-0.695025548731039,2.86024952554517,
5.11013719950733));
#68439=CARTESIAN_POINT('Ctrl Pts',(-0.603610931679016,2.87941276012273,
5.10509859143894));
#68440=CARTESIAN_POINT('Ctrl Pts',(-0.512177591014646,2.89857991972877,
5.10005895135896));
#68441=CARTESIAN_POINT('Ctrl Pts',(-0.41985454688234,2.91338269371054,5.09501931127899));
#68442=CARTESIAN_POINT('Ctrl Pts',(-0.32709213922869,2.92376037534795,5.08997967119902));
#68443=CARTESIAN_POINT('Ctrl Pts',(-0.234228843629678,2.93414934370166,
5.08493455003089));
#68444=CARTESIAN_POINT('Ctrl Pts',(-0.140925671965079,2.94010356436376,
5.07988942886277));
#68445=CARTESIAN_POINT('Ctrl Pts',(-0.0476372381735444,2.94161430060761,
5.07484430769465));
#68446=CARTESIAN_POINT('Ctrl Pts',(0.0457090903843088,2.9431259744138,5.06979605552626));
#68447=CARTESIAN_POINT('Ctrl Pts',(0.139040220126571,2.94018868767891,5.06474780335787));
#68448=CARTESIAN_POINT('Ctrl Pts',(0.231904548328501,2.93284576486125,5.05969955118948));
#68449=CARTESIAN_POINT('Ctrl Pts',(0.32491498702623,2.9254912888658,5.0546433562228));
#68450=CARTESIAN_POINT('Ctrl Pts',(0.417456719041778,2.91371739603875,5.04958716125613));
#68451=CARTESIAN_POINT('Ctrl Pts',(0.509086478569261,2.89761884265994,5.04453096628945));
#68452=CARTESIAN_POINT('Ctrl Pts',(0.548273963959443,2.89073394163447,5.04236857311709));
#68453=CARTESIAN_POINT('Ctrl Pts',(0.587294815183116,2.88305867439424,5.04020617994474));
#68454=CARTESIAN_POINT('Ctrl Pts',(0.62611523936405,2.87460322601852,5.03804378677239));
#68455=CARTESIAN_POINT('Ctrl Pts',(0.716892268547699,2.85483114726983,5.03298728282492));
#68456=CARTESIAN_POINT('Ctrl Pts',(0.80689139748673,2.83072013026423,5.02793077887745));
#68457=CARTESIAN_POINT('Ctrl Pts',(0.895666998751246,2.80234627184935,5.02287427492999));
#68458=CARTESIAN_POINT('Ctrl Pts',(0.984321787018764,2.77401102686904,5.01782465228084));
#68459=CARTESIAN_POINT('Ctrl Pts',(1.0717559377579,2.74142460281036,5.0127750296317));
#68460=CARTESIAN_POINT('Ctrl Pts',(1.15753456760308,2.70471398206981,5.00772540698256));
#68461=CARTESIAN_POINT('Ctrl Pts',(1.24322283392177,2.66804203414504,5.00268110386009));
#68462=CARTESIAN_POINT('Ctrl Pts',(1.3272586405576,2.6272546992518,4.99763680073763));
#68463=CARTESIAN_POINT('Ctrl Pts',(1.40922386166798,2.58252823947882,4.99259249761517));
#68464=CARTESIAN_POINT('Ctrl Pts',(1.49113138718159,2.53783326281237,4.98755174519476));
#68465=CARTESIAN_POINT('Ctrl Pts',(1.5709708361648,2.48920488457255,4.98251099277435));
#68466=CARTESIAN_POINT('Ctrl Pts',(1.64834656373636,2.43686634960117,4.97747024035394));
#68467=CARTESIAN_POINT('Ctrl Pts',(1.72569506320627,2.38454623227826,4.97243126174715));
#68468=CARTESIAN_POINT('Ctrl Pts',(1.80058119686232,2.32851880030492,4.96739228314035));
#68469=CARTESIAN_POINT('Ctrl Pts',(1.87263720703598,2.26905131956606,4.96235330453356));
#68470=CARTESIAN_POINT('Ctrl Pts',(1.94468791861156,2.20958821173488,4.95731469646522));
#68471=CARTESIAN_POINT('Ctrl Pts',(2.01390857877139,2.14668584057405,4.95227608839688));
#68472=CARTESIAN_POINT('Ctrl Pts',(2.07996440571687,2.08065183799474,4.94723748032854));
#68473=CARTESIAN_POINT('Ctrl Pts',(2.14603376226782,2.01460431028003,4.94219784024861));
#68474=CARTESIAN_POINT('Ctrl Pts',(2.20893668492199,1.94542419090428,4.93715820016867));
#68475=CARTESIAN_POINT('Ctrl Pts',(2.26837596681243,1.87345522316061,4.93211856008874));
#68476=CARTESIAN_POINT('Ctrl Pts',(2.32787989457801,1.80140798231614,4.92707343892066));
#68477=CARTESIAN_POINT('Ctrl Pts',(2.3839123799885,1.72656618139609,4.92202831775258));
#68478=CARTESIAN_POINT('Ctrl Pts',(2.43621737929887,1.64930557532622,4.91698319658449));
#68479=CARTESIAN_POINT('Ctrl Pts',(2.48855483907183,1.57199702135372,4.91193494441614));
#68480=CARTESIAN_POINT('Ctrl Pts',(2.53715997675792,1.49226705193994,4.90688669224779));
#68481=CARTESIAN_POINT('Ctrl Pts',(2.58182197398437,1.41051738544814,4.90183844007944));
#68482=CARTESIAN_POINT('Ctrl Pts',(2.62655424132081,1.32863909600141,4.8967822451128));
#68483=CARTESIAN_POINT('Ctrl Pts',(2.66733079065861,1.2447351643849,4.89172605014616));
#68484=CARTESIAN_POINT('Ctrl Pts',(2.70398841601454,1.1592284701728,4.88666985517952));
#68485=CARTESIAN_POINT('Ctrl Pts',(2.71966585711833,1.12265964855726,4.88450746200678));
#68486=CARTESIAN_POINT('Ctrl Pts',(2.73459055174711,1.08579787909022,4.88234506883403));
#68487=CARTESIAN_POINT('Ctrl Pts',(2.74875253640259,1.04867702064093,4.88018267566128));
#68488=CARTESIAN_POINT('Ctrl Pts',(2.78186868392787,0.961874227488885,4.87512617171368));
#68489=CARTESIAN_POINT('Ctrl Pts',(2.81092731058382,0.873348634759145,4.87006966776607));
#68490=CARTESIAN_POINT('Ctrl Pts',(2.83574829938907,0.783514889783219,4.86501316381847));
#68491=CARTESIAN_POINT('Ctrl Pts',(2.86053550979112,0.693803397811868,4.85996354116921));
#68492=CARTESIAN_POINT('Ctrl Pts',(2.88109642557836,0.602787715147935,4.85491391851994));
#68493=CARTESIAN_POINT('Ctrl Pts',(2.89729940191038,0.510901336551127,4.84986429587068));
#68494=CARTESIAN_POINT('Ctrl Pts',(2.91348530921158,0.419111755690579,4.84481999274808));
#68495=CARTESIAN_POINT('Ctrl Pts',(2.92532232610127,0.326453736522251,4.83977568962548));
#68496=CARTESIAN_POINT('Ctrl Pts',(2.93272922581001,0.233373709058706,4.83473138650289));
#68497=CARTESIAN_POINT('Ctrl Pts',(2.94013091177696,0.140359200941705,4.82969063408234));
#68498=CARTESIAN_POINT('Ctrl Pts',(2.94310864399567,0.0469237157370147,
4.8246498816618));
#68499=CARTESIAN_POINT('Ctrl Pts',(2.94163282254895,-0.0464794288120706,
4.81960912924125));
#68500=CARTESIAN_POINT('Ctrl Pts',(2.94015752043585,-0.139849705297845,
4.81457015063433));
#68501=CARTESIAN_POINT('Ctrl Pts',(2.93423178530535,-0.233187220858687,
4.8095311720274));
#68502=CARTESIAN_POINT('Ctrl Pts',(2.92387812288593,-0.326037915753797,
4.80449219342047));
#68503=CARTESIAN_POINT('Ctrl Pts',(2.91352522181726,-0.418881782925141,
4.79945358535201));
#68504=CARTESIAN_POINT('Ctrl Pts',(2.89874509033896,-0.511238460022593,
4.79441497728354));
#68505=CARTESIAN_POINT('Ctrl Pts',(2.87961206452165,-0.602659404524128,
4.78937636921508));
#68506=CARTESIAN_POINT('Ctrl Pts',(2.8604751198631,-0.694099073934688,4.78433672913499));
#68507=CARTESIAN_POINT('Ctrl Pts',(2.83698360132016,-0.784602196269378,
4.7792970890549));
#68508=CARTESIAN_POINT('Ctrl Pts',(2.80926263021356,-0.873731923696038,
4.77425744897481));
#68509=CARTESIAN_POINT('Ctrl Pts',(2.7815115099132,-0.962958588182086,4.7692123278066));
#68510=CARTESIAN_POINT('Ctrl Pts',(2.74952188761334,-1.05080845244922,4.7641672066384));
#68511=CARTESIAN_POINT('Ctrl Pts',(2.71346820137455,-1.13686160992847,4.75912208547019));
#68512=CARTESIAN_POINT('Ctrl Pts',(2.67739214023187,-1.22296817196435,4.75407383330172));
#68513=CARTESIAN_POINT('Ctrl Pts',(2.6372471843141,-1.30727540740105,4.74902558113325));
#68514=CARTESIAN_POINT('Ctrl Pts',(2.59325424833327,-1.38938706036202,4.74397732896477));
#68515=CARTESIAN_POINT('Ctrl Pts',(2.5491920949273,-1.47162790581872,4.73892113399801));
#68516=CARTESIAN_POINT('Ctrl Pts',(2.50127010362758,-1.55166589346778,4.73386493903125));
#68517=CARTESIAN_POINT('Ctrl Pts',(2.44975295208641,-1.62913304359832,4.72880874406449));
#68518=CARTESIAN_POINT('Ctrl Pts',(2.42772050724658,-1.66226357704378,4.72664635089305));
#68519=CARTESIAN_POINT('Ctrl Pts',(2.4050310037142,-1.69492430247281,4.72448395772161));
#68520=CARTESIAN_POINT('Ctrl Pts',(2.38170733180708,-1.72708835489572,4.72232156455017));
#68521=CARTESIAN_POINT('Ctrl Pts',(2.32716764835563,-1.80230023596858,4.7172650606027));
#68522=CARTESIAN_POINT('Ctrl Pts',(2.26896592277806,-1.87505835229019,4.71220855665523));
#68523=CARTESIAN_POINT('Ctrl Pts',(2.20735068949027,-1.94498507284936,4.70715205270776));
#68524=CARTESIAN_POINT('Ctrl Pts',(2.14581930718074,-2.01481663148815,4.70210243005863));
#68525=CARTESIAN_POINT('Ctrl Pts',(2.08088393935117,-2.08182412176524,4.6970528074095));
#68526=CARTESIAN_POINT('Ctrl Pts',(2.01283541699537,-2.1456601744193,4.69200318476036));
#68527=CARTESIAN_POINT('Ctrl Pts',(1.94485858037865,-2.20942897896193,4.68695888163793));
#68528=CARTESIAN_POINT('Ctrl Pts',(1.87377542994107,-2.2700326851886,4.6819145785155));
#68529=CARTESIAN_POINT('Ctrl Pts',(1.79991520912955,-2.32715904912924,4.67687027539307));
#68530=CARTESIAN_POINT('Ctrl Pts',(1.72610697877716,-2.38424520162919,4.67182952297266));
#68531=CARTESIAN_POINT('Ctrl Pts',(1.64952591339223,-2.43785860675055,4.66678877055225));
#68532=CARTESIAN_POINT('Ctrl Pts',(1.57053526814548,-2.48772646637672,4.66174801813184));
#68533=CARTESIAN_POINT('Ctrl Pts',(1.49157241928116,-2.5375767777718,4.65670903952505));
#68534=CARTESIAN_POINT('Ctrl Pts',(1.41020204972646,-2.58368392587307,4.65167006091826));
#68535=CARTESIAN_POINT('Ctrl Pts',(1.32681654404416,-2.62581832167626,4.64663108231146));
#68536=CARTESIAN_POINT('Ctrl Pts',(1.24343717006805,-2.66794961915038,4.64159247424312));
#68537=CARTESIAN_POINT('Ctrl Pts',(1.15804335045787,-2.70610854553738,4.63655386617478));
#68538=CARTESIAN_POINT('Ctrl Pts',(1.07105120926042,-2.74011191507606,4.63151525810644));
#68539=CARTESIAN_POINT('Ctrl Pts',(0.984041250265262,-2.77412224921122,
4.6264756180265));
#68540=CARTESIAN_POINT('Ctrl Pts',(0.895432732522731,-2.80397517501077,
4.62143597794655));
#68541=CARTESIAN_POINT('Ctrl Pts',(0.805659776909909,-2.82953641501032,
4.6163963378666));
#68542=CARTESIAN_POINT('Ctrl Pts',(0.715789184665435,-2.85512545529068,
4.61135121669852));
#68543=CARTESIAN_POINT('Ctrl Pts',(0.624752053796445,-2.87641337180181,
4.60630609553044));
#68544=CARTESIAN_POINT('Ctrl Pts',(0.532995306902624,-2.89331643668987,
4.60126097436235));
#68545=CARTESIAN_POINT('Ctrl Pts',(0.441181615806447,-2.9102299916136,4.59621272219398));
#68546=CARTESIAN_POINT('Ctrl Pts',(0.348647858529523,-2.92275321789415,
4.59116447002561));
#68547=CARTESIAN_POINT('Ctrl Pts',(0.25584658937695,-2.93085423088631,4.58611621785724));
#68548=CARTESIAN_POINT('Ctrl Pts',(0.162899308944509,-2.93896798981703,
4.5810600228906));
#68549=CARTESIAN_POINT('Ctrl Pts',(0.0696841187437275,-2.9426456293354,
4.57600382792396));
#68550=CARTESIAN_POINT('Ctrl Pts',(-0.0233461517107244,-2.94190736720249,
4.57094763295732));
#68551=CARTESIAN_POINT('Ctrl Pts',(-0.0631325964616277,-2.94159163313638,
4.56878523978457));
#68552=CARTESIAN_POINT('Ctrl Pts',(-0.102885281238585,-2.94046886377766,
4.56662284661181));
#68553=CARTESIAN_POINT('Ctrl Pts',(-0.142569194812085,-2.93854352097951,
4.56446045343906));
#68554=CARTESIAN_POINT('Ctrl Pts',(-0.235365393096446,-2.93404133165457,
4.55940394949179));
#68555=CARTESIAN_POINT('Ctrl Pts',(-0.328111260252495,-2.92513131057668,
4.55434744554452));
#68556=CARTESIAN_POINT('Ctrl Pts',(-0.420354720504467,-2.91181488232848,
4.54929094159725));
#68557=CARTESIAN_POINT('Ctrl Pts',(-0.512472648416987,-2.8985165761497,
4.54424131894832));
#68558=CARTESIAN_POINT('Ctrl Pts',(-0.604089093004346,-2.88082384236276,
4.53919169629939));
#68559=CARTESIAN_POINT('Ctrl Pts',(-0.69475416759977,-2.85879006689941,
4.53414207365046));
#68560=CARTESIAN_POINT('Ctrl Pts',(-0.785323731042124,-2.83677950292417,
4.5290977705282));
#68561=CARTESIAN_POINT('Ctrl Pts',(-0.874943488094165,-2.81043709168458,
4.52405346740593));
#68562=CARTESIAN_POINT('Ctrl Pts',(-0.9631719373317,-2.77986759021661,4.51900916428366));
#68563=CARTESIAN_POINT('Ctrl Pts',(-1.0513382822649,-2.74931960672429,4.51396841186346));
#68564=CARTESIAN_POINT('Ctrl Pts',(-1.13811484829377,-2.71455059218884,
4.50892765944325));
#68565=CARTESIAN_POINT('Ctrl Pts',(-1.22307454351632,-2.67571535500366,
4.50388690702304));
#68566=CARTESIAN_POINT('Ctrl Pts',(-1.30800434187964,-2.63689378372931,
4.49884792841646));
#68567=CARTESIAN_POINT('Ctrl Pts',(-1.39111813683626,-2.59400901679853,
4.49380894980989));
#68568=CARTESIAN_POINT('Ctrl Pts',(-1.47200906729136,-2.54726388617513,
4.48876997120331));
#68569=CARTESIAN_POINT('Ctrl Pts',(-1.5528940494777,-2.50052219292843,4.48373136313517));
#68570=CARTESIAN_POINT('Ctrl Pts',(-1.63155610846921,-2.44992092253735,
4.47869275506703));
#68571=CARTESIAN_POINT('Ctrl Pts',(-1.70761423658196,-2.39570816649746,
4.47365414699889));
#68572=CARTESIAN_POINT('Ctrl Pts',(-1.783687942979,-2.34148430655918,4.46861450691918));
#68573=CARTESIAN_POINT('Ctrl Pts',(-1.85715629846442,-2.28364774946203,
4.46357486683946));
#68574=CARTESIAN_POINT('Ctrl Pts',(-1.92766938757211,-2.22248840991744,
4.45853522675974));
#68575=CARTESIAN_POINT('Ctrl Pts',(-1.99825916637435,-2.16126255377108,
4.45349010559186));
#68576=CARTESIAN_POINT('Ctrl Pts',(-2.06588692811334,-2.09670699298994,
4.44844498442397));
#68577=CARTESIAN_POINT('Ctrl Pts',(-2.1302380657774,-2.02915001493555,4.44339986325609));
#68578=CARTESIAN_POINT('Ctrl Pts',(-2.1946291397329,-1.9615511110464,4.43835161108794));
#68579=CARTESIAN_POINT('Ctrl Pts',(-2.25573925136043,-1.89094741646589,
4.43330335891978));
#68580=CARTESIAN_POINT('Ctrl Pts',(-2.31329410780585,-1.81770029729621,
4.42825510675163));
#68581=CARTESIAN_POINT('Ctrl Pts',(-2.37093951967525,-1.74433793287459,
4.42319891178519));
#68582=CARTESIAN_POINT('Ctrl Pts',(-2.42501825392597,-1.668324202419,4.41814271681874));
#68583=CARTESIAN_POINT('Ctrl Pts',(-2.47529947949604,-1.59004920892613,
4.4130865218523));
#68584=CARTESIAN_POINT('Ctrl Pts',(-2.49680335340005,-1.55657318341515,
4.41092412867752));
#68585=CARTESIAN_POINT('Ctrl Pts',(-2.51761322675657,-1.52268386751969,
4.40876173550273));
#68586=CARTESIAN_POINT('Ctrl Pts',(-2.53771367884418,-1.48841300861257,
4.40659934232795));
#68587=CARTESIAN_POINT('Ctrl Pts',(-2.58640672226634,-1.40539236740483,
4.40136097732518));
#68588=CARTESIAN_POINT('Ctrl Pts',(-2.63109406438861,-1.3198572950255,4.39612261232242));
#68589=CARTESIAN_POINT('Ctrl Pts',(-2.67151824800373,-1.23221518030865,
4.39088424731965));
#68590=CARTESIAN_POINT('Ctrl Pts',(-2.71187342478902,-1.14472267664032,
4.3856548245621));
#68591=CARTESIAN_POINT('Ctrl Pts',(-2.74797975873238,-1.05513064776356,
4.38042540180455));
#68592=CARTESIAN_POINT('Ctrl Pts',(-2.77962473008703,-0.963872584882775,
4.37519597904699));
#68593=CARTESIAN_POINT('Ctrl Pts',(-2.81120685140212,-0.872795769530967,
4.36997694243969));
#68594=CARTESIAN_POINT('Ctrl Pts',(-2.83834513170718,-0.780059886798695,
4.36475790583239));
#68595=CARTESIAN_POINT('Ctrl Pts',(-2.86087486123827,-0.68611881502761,
4.35953886922509));
#68596=CARTESIAN_POINT('Ctrl Pts',(-2.88337783884318,-0.592289289407769,
4.35432602973089));
#68597=CARTESIAN_POINT('Ctrl Pts',(-2.90128305986531,-0.497257807785013,
4.34911319023669));
#68598=CARTESIAN_POINT('Ctrl Pts',(-2.91447533446412,-0.401494115523807,
4.34390035074249));
#68599=CARTESIAN_POINT('Ctrl Pts',(-2.92765073378575,-0.30585292214167,
4.33869417940174));
#68600=CARTESIAN_POINT('Ctrl Pts',(-2.9361251402031,-0.209481777646127,
4.33348800806098));
#68601=CARTESIAN_POINT('Ctrl Pts',(-2.93983444014366,-0.112860376329525,
4.32828183672023));
#68602=CARTESIAN_POINT('Ctrl Pts',(-2.94128451058126,-0.0750883331045788,
4.32624659684335));
#68603=CARTESIAN_POINT('Ctrl Pts',(-2.94200690804472,-0.0372781398498132,
4.32421135696648));
#68604=CARTESIAN_POINT('Ctrl Pts',(-2.94199995021121,0.000541255242094748,
4.3221761170896));
#68605=CARTESIAN_POINT('',(-2.94484294150901,0.00199174253909633,3.3221761170896));
#68606=CARTESIAN_POINT('Ctrl Pts',(-2.93739244246854,0.000548335028833932,
4.32217568980677));
#68607=CARTESIAN_POINT('Ctrl Pts',(-2.93814515251413,0.454714538465635,
4.29769653694346));
#68608=CARTESIAN_POINT('Ctrl Pts',(-2.62620581469539,1.88417429984043,4.22059701370977));
#68609=CARTESIAN_POINT('Ctrl Pts',(-0.406867188726433,3.44669387613551,
4.09087712010572));
#68610=CARTESIAN_POINT('Ctrl Pts',(2.66245099976357,2.22634100195606,3.93301600899463));
#68611=CARTESIAN_POINT('Ctrl Pts',(3.32025430017048,-1.01052014634335,3.77515489788349));
#68612=CARTESIAN_POINT('Ctrl Pts',(0.970737398643962,-3.33210271331847,
3.6172937867724));
#68613=CARTESIAN_POINT('Ctrl Pts',(-2.11754863214004,-2.66593520061748,
3.46630085984108));
#68614=CARTESIAN_POINT('Ctrl Pts',(-2.93826750108625,-0.841388295482023,
3.36792830328016));
#68615=CARTESIAN_POINT('Ctrl Pts',(-2.94484294150901,0.00199174253909633,
3.3221761170896));
#68616=CARTESIAN_POINT('',(-2.9419989036421,-0.00253987572311715,2.3221761170896));
#68617=CARTESIAN_POINT('Ctrl Pts',(-2.94484294150901,0.00199174253909633,
3.3221761170896));
#68618=CARTESIAN_POINT('Ctrl Pts',(-2.94583002736539,0.128597483532049,
3.31530793290979));
#68619=CARTESIAN_POINT('Ctrl Pts',(-2.88115833278038,1.22417398585304,3.25581937835959));
#68620=CARTESIAN_POINT('Ctrl Pts',(-1.50792549309295,3.12592391504645,3.14371045343908));
#68621=CARTESIAN_POINT('Ctrl Pts',(1.79153366111829,2.97248156539303,2.98584934232795));
#68622=CARTESIAN_POINT('Ctrl Pts',(3.46831127903085,0.126714191662369,2.82798823121682));
#68623=CARTESIAN_POINT('Ctrl Pts',(2.00366607964191,-2.83382462640087,2.67012712010574));
#68624=CARTESIAN_POINT('Ctrl Pts',(-1.2757995679391,-3.22762676650926,2.5122660089946));
#68625=CARTESIAN_POINT('Ctrl Pts',(-2.83627828908289,-1.36906481860164,
2.39628234132257));
#68626=CARTESIAN_POINT('Ctrl Pts',(-2.94462630681883,-0.200923340849699,
2.3329190440209));
#68627=CARTESIAN_POINT('Ctrl Pts',(-2.94283216929169,-0.00254059509496668,
2.3221761170896));
#68628=CARTESIAN_POINT('',(-2.94155351776559,0.000606762388042248,1.32217607092416));
#68629=CARTESIAN_POINT('Ctrl Pts',(-2.9419989036421,-0.00253987572311715,
2.3221761170896));
#68630=CARTESIAN_POINT('Ctrl Pts',(-2.94208233219418,0.0940974150397186,
2.31694143665972));
#68631=CARTESIAN_POINT('Ctrl Pts',(-2.93739914386076,0.190883610583203,
2.31170675622983));
#68632=CARTESIAN_POINT('Ctrl Pts',(-2.92793797328572,0.287303366829364,
2.30647207579995));
#68633=CARTESIAN_POINT('Ctrl Pts',(-2.91895287204066,0.378871451880253,
2.30150079520893));
#68634=CARTESIAN_POINT('Ctrl Pts',(-2.90565898929855,0.470108555172867,
2.2965295146179));
#68635=CARTESIAN_POINT('Ctrl Pts',(-2.88809996570594,0.560573445758306,
2.29155823402688));
#68636=CARTESIAN_POINT('Ctrl Pts',(-2.87054897094082,0.650996971458291,
2.28658922654369));
#68637=CARTESIAN_POINT('Ctrl Pts',(-2.84873679368341,0.740648537302737,
2.28162021906051));
#68638=CARTESIAN_POINT('Ctrl Pts',(-2.82275860045843,0.829094616758536,
2.27665121157733));
#68639=CARTESIAN_POINT('Ctrl Pts',(-2.79678456174355,0.917526551653617,
2.27168299875264));
#68640=CARTESIAN_POINT('Ctrl Pts',(-2.7666459596833,1.00475294463453,2.26671478592795));
#68641=CARTESIAN_POINT('Ctrl Pts',(-2.73248815572983,1.09035429049287,2.26174657310326));
#68642=CARTESIAN_POINT('Ctrl Pts',(-2.69832565821172,1.17596739868377,2.25677767760505));
#68643=CARTESIAN_POINT('Ctrl Pts',(-2.66014303362448,1.25995459257028,2.25180878210685));
#68644=CARTESIAN_POINT('Ctrl Pts',(-2.61813371460277,1.34191648490519,2.24683988660865));
#68645=CARTESIAN_POINT('Ctrl Pts',(-2.5760814180424,1.42396222816838,2.24186590769316));
#68646=CARTESIAN_POINT('Ctrl Pts',(-2.53019482458214,1.50397812834879,2.23689192877767));
#68647=CARTESIAN_POINT('Ctrl Pts',(-2.48071299062712,1.58159004110859,2.23191794986219));
#68648=CARTESIAN_POINT('Ctrl Pts',(-2.43120173070495,1.6592481082934,2.22694101300985));
#68649=CARTESIAN_POINT('Ctrl Pts',(-2.37809124117542,1.73449897176268,2.22196407615751));
#68650=CARTESIAN_POINT('Ctrl Pts',(-2.32166215487591,1.80699995534503,2.21698713930517));
#68651=CARTESIAN_POINT('Ctrl Pts',(-2.26514624234863,1.87961249463965,2.21200254454658));
#68652=CARTESIAN_POINT('Ctrl Pts',(-2.20530184332275,1.94946636739178,2.20701794978799));
#68653=CARTESIAN_POINT('Ctrl Pts',(-2.14244750736819,2.01625461640435,2.2020333550294));
#68654=CARTESIAN_POINT('Ctrl Pts',(-2.1193735375216,2.04077273469195,2.20020349894373));
#68655=CARTESIAN_POINT('Ctrl Pts',(-2.09589426644895,2.06487810247725,2.19837364285806));
#68656=CARTESIAN_POINT('Ctrl Pts',(-2.07202654684849,2.08855691546942,2.19654378677239));
#68657=CARTESIAN_POINT('Ctrl Pts',(-2.00607205389579,2.15398939627457,2.19148728232508));
#68658=CARTESIAN_POINT('Ctrl Pts',(-1.93689913945909,2.21640968854567,2.18643077787778));
#68659=CARTESIAN_POINT('Ctrl Pts',(-1.86481398163189,2.27548518208979,2.18137427343047));
#68660=CARTESIAN_POINT('Ctrl Pts',(-1.79282692342056,2.33448028067608,2.17632465030463));
#68661=CARTESIAN_POINT('Ctrl Pts',(-1.71793583779818,2.39013934760752,2.17127502717879));
#68662=CARTESIAN_POINT('Ctrl Pts',(-1.64048376588073,2.44216645908541,2.16622540405295));
#68663=CARTESIAN_POINT('Ctrl Pts',(-1.56311328622637,2.49413876234885,2.16118110047724));
#68664=CARTESIAN_POINT('Ctrl Pts',(-1.48318754920317,2.54248646965816,2.15613679690152));
#68665=CARTESIAN_POINT('Ctrl Pts',(-1.40108184137037,2.58695451714602,2.1510924933258));
#68666=CARTESIAN_POINT('Ctrl Pts',(-1.3190339286073,2.63139126310842,2.14605174048833));
#68667=CARTESIAN_POINT('Ctrl Pts',(-1.23480948400394,2.67195356706271,2.14101098765085));
#68668=CARTESIAN_POINT('Ctrl Pts',(-1.14881099969759,2.70843077943185,2.13597023481338));
#68669=CARTESIAN_POINT('Ctrl Pts',(-1.06284277817821,2.74489515550375,2.13093125581216));
#68670=CARTESIAN_POINT('Ctrl Pts',(-0.975102165040744,2.77727712311088,
2.12589227681094));
#68671=CARTESIAN_POINT('Ctrl Pts',(-0.886013432712717,2.80541337364971,
2.12085329780972));
#68672=CARTESIAN_POINT('Ctrl Pts',(-0.796931251880015,2.83354755507711,
2.11581468936992));
#68673=CARTESIAN_POINT('Ctrl Pts',(-0.706501571851507,2.85743650704494,
2.11077608093013));
#68674=CARTESIAN_POINT('Ctrl Pts',(-0.615164610897789,2.87696654507816,
2.10573747249033));
#68675=CARTESIAN_POINT('Ctrl Pts',(-0.523808942661735,2.89650058317808,
2.10069783206228));
#68676=CARTESIAN_POINT('Ctrl Pts',(-0.431546058022076,2.91167384188408,
2.09565819163423));
#68677=CARTESIAN_POINT('Ctrl Pts',(-0.338826049636303,2.92242380706287,
2.09061855120618));
#68678=CARTESIAN_POINT('Ctrl Pts',(-0.246005200103549,2.9331854637723,2.08557342972685));
#68679=CARTESIAN_POINT('Ctrl Pts',(-0.152726675531535,2.93951417380657,
2.08052830824751));
#68680=CARTESIAN_POINT('Ctrl Pts',(-0.0594450511706656,2.94139937544892,
2.07548318676818));
#68681=CARTESIAN_POINT('Ctrl Pts',(0.0338944633452301,2.94328574703891,
2.07043493430923));
#68682=CARTESIAN_POINT('Ctrl Pts',(0.127236638694068,2.94072313234364,2.06538668185028));
#68683=CARTESIAN_POINT('Ctrl Pts',(0.220129701808395,2.93375304250064,2.06033842939132));
#68684=CARTESIAN_POINT('Ctrl Pts',(0.313168919995696,2.92677198613381,2.05528223416806));
#68685=CARTESIAN_POINT('Ctrl Pts',(0.405757176148202,2.91536966639149,2.0502260389448));
#68686=CARTESIAN_POINT('Ctrl Pts',(0.497450827572616,2.89963905928778,2.04516984372153));
#68687=CARTESIAN_POINT('Ctrl Pts',(0.536665566494046,2.89291153081591,2.04300745436812));
#68688=CARTESIAN_POINT('Ctrl Pts',(0.575716845939192,2.8853929763205,2.0408450650147));
#68689=CARTESIAN_POINT('Ctrl Pts',(0.614570832594503,2.87709344508031,2.03868267566128));
#68690=CARTESIAN_POINT('Ctrl Pts',(0.705426662090724,2.85768589233814,2.03362616292447));
#68691=CARTESIAN_POINT('Ctrl Pts',(0.795522008345901,2.8339362990504,2.02856965018766));
#68692=CARTESIAN_POINT('Ctrl Pts',(0.884410940870408,2.80591897382457,2.02351313745085));
#68693=CARTESIAN_POINT('Ctrl Pts',(0.973178907124536,2.77793977653258,2.01846350596989));
#68694=CARTESIAN_POINT('Ctrl Pts',(1.0607433029531,2.74570452108668,2.01341387448892));
#68695=CARTESIAN_POINT('Ctrl Pts',(1.14666873770656,2.70933844433774,2.00836424300796));
#68696=CARTESIAN_POINT('Ctrl Pts',(1.2325036549473,2.67301067716296,2.00331993102388));
#68697=CARTESIAN_POINT('Ctrl Pts',(1.31670263693068,2.63256091057823,1.99827561903979));
#68698=CARTESIAN_POINT('Ctrl Pts',(1.3988468526778,2.58816372796495,1.99323130705571));
#68699=CARTESIAN_POINT('Ctrl Pts',(1.48093324704763,2.543797796563,1.98819054576675));
#68700=CARTESIAN_POINT('Ctrl Pts',(1.56096736118657,2.49549018245944,1.98314978447779));
#68701=CARTESIAN_POINT('Ctrl Pts',(1.63855265637552,2.44346254161686,1.97810902318883));
#68702=CARTESIAN_POINT('Ctrl Pts',(1.7161106497743,2.39145320898243,1.97307003571289));
#68703=CARTESIAN_POINT('Ctrl Pts',(1.79122116840698,2.33572669710995,1.96803104823695));
#68704=CARTESIAN_POINT('Ctrl Pts',(1.8635153838847,2.27654879456274,1.96299206076102));
#68705=CARTESIAN_POINT('Ctrl Pts',(1.93580428310543,2.21737524374596,1.95795344383412));
#68706=CARTESIAN_POINT('Ctrl Pts',(2.00527694809872,2.15475108798733,1.95291482690723));
#68707=CARTESIAN_POINT('Ctrl Pts',(2.07159736407132,2.08898261389911,1.94787620998034));
#68708=CARTESIAN_POINT('Ctrl Pts',(2.13793136353176,2.02320066936963,1.94283656106366));
#68709=CARTESIAN_POINT('Ctrl Pts',(2.20111151718236,1.9542734398753,1.93779691214698));
#68710=CARTESIAN_POINT('Ctrl Pts',(2.26083923990971,1.88254347394277,1.9327572632303));
#68711=CARTESIAN_POINT('Ctrl Pts',(2.32063192108609,1.81073549620727,1.92771213331147));
#68712=CARTESIAN_POINT('Ctrl Pts',(2.37696439284234,1.73611903914493,1.92266700339263));
#68713=CARTESIAN_POINT('Ctrl Pts',(2.42957910435542,1.65906882789097,1.91762187347379));
#68714=CARTESIAN_POINT('Ctrl Pts',(2.48222646809696,1.58197079995174,1.91257361259158));
#68715=CARTESIAN_POINT('Ctrl Pts',(2.53115124617158,1.50243638816991,1.90752535170937));
#68716=CARTESIAN_POINT('Ctrl Pts',(2.57614100852258,1.42086646248276,1.90247709082716));
#68717=CARTESIAN_POINT('Ctrl Pts',(2.6212015553242,1.33916819910108,1.89742088728523));
#68718=CARTESIAN_POINT('Ctrl Pts',(2.66231453302157,1.25542842638829,1.8923646837433));
#68719=CARTESIAN_POINT('Ctrl Pts',(2.69931503860233,1.17006936648016,1.88730848020137));
#68720=CARTESIAN_POINT('Ctrl Pts',(2.71513844950498,1.13356523071256,1.8851461749843));
#68721=CARTESIAN_POINT('Ctrl Pts',(2.73021035688101,1.0967651522541,1.88298386976724));
#68722=CARTESIAN_POINT('Ctrl Pts',(2.74452066257809,1.05970294549083,1.88082156455017));
#68723=CARTESIAN_POINT('Ctrl Pts',(2.77798486904029,0.973034123361867,1.87576508079993));
#68724=CARTESIAN_POINT('Ctrl Pts',(2.80739853700098,0.884626233625418,1.8707085970497));
#68725=CARTESIAN_POINT('Ctrl Pts',(2.83257988597991,0.794893193795283,1.86565211329946));
#68726=CARTESIAN_POINT('Ctrl Pts',(2.85772696598989,0.705282270487064,1.86060251085192));
#68727=CARTESIAN_POINT('Ctrl Pts',(2.87865305421882,0.614350204153821,1.85555290840438));
#68728=CARTESIAN_POINT('Ctrl Pts',(2.89522476619359,0.522529954375151,1.85050330595683));
#68729=CARTESIAN_POINT('Ctrl Pts',(2.91177902069943,0.430806432632733,1.84545902301267));
#68730=CARTESIAN_POINT('Ctrl Pts',(2.92398793878408,0.338197021380879,1.8404147400685));
#68731=CARTESIAN_POINT('Ctrl Pts',(2.93176850166836,0.245147817908464,1.83537045712433));
#68732=CARTESIAN_POINT('Ctrl Pts',(2.93954358794746,0.152164110179341,1.83032972476468));
#68733=CARTESIAN_POINT('Ctrl Pts',(2.94289647804148,0.0587416661613416,
1.82528899240502));
#68734=CARTESIAN_POINT('Ctrl Pts',(2.94179575194014,-0.0346663217969656,
1.82024826004537));
#68735=CARTESIAN_POINT('Ctrl Pts',(2.94069541316216,-0.128041441364473,
1.81520930141797));
#68736=CARTESIAN_POINT('Ctrl Pts',(2.93514457697084,-0.221401672070292,
1.81017034279057));
#68737=CARTESIAN_POINT('Ctrl Pts',(2.92516392560423,-0.3142928703354,1.80513138416317));
#68738=CARTESIAN_POINT('Ctrl Pts',(2.91518400795212,-0.40717723982588,1.8000927959682));
#68739=CARTESIAN_POINT('Ctrl Pts',(2.90077497032774,-0.499592204648292,
1.79505420777324));
#68740=CARTESIAN_POINT('Ctrl Pts',(2.88200934704536,-0.591088930316898,
1.79001561957828));
#68741=CARTESIAN_POINT('Ctrl Pts',(2.86323987967138,-0.682604398863855,
1.78497599924096));
#68742=CARTESIAN_POINT('Ctrl Pts',(2.84011214361872,-0.77320082047799,1.77993637890365));
#68743=CARTESIAN_POINT('Ctrl Pts',(2.81274950498193,-0.862440851434997,
1.77489675856633));
#68744=CARTESIAN_POINT('Ctrl Pts',(2.78535710504907,-0.951777945362338,
1.76985165682662));
#68745=CARTESIAN_POINT('Ctrl Pts',(2.75372073900004,-1.03975527952438,1.76480655508691));
#68746=CARTESIAN_POINT('Ctrl Pts',(2.71801315726655,-1.1259522533953,1.7597614533472));
#68747=CARTESIAN_POINT('Ctrl Pts',(2.68228341425677,-1.2122027238868,1.75471322045472));
#68748=CARTESIAN_POINT('Ctrl Pts',(2.64247761402116,-1.29667023359253,1.74966498756224));
#68749=CARTESIAN_POINT('Ctrl Pts',(2.59881507814656,-1.37895764604939,1.74461675466976));
#68750=CARTESIAN_POINT('Ctrl Pts',(2.55508384085064,-1.46137453477417,1.73956057856537));
#68751=CARTESIAN_POINT('Ctrl Pts',(2.50748398038528,-1.5416040982564,1.73450440246099));
#68752=CARTESIAN_POINT('Ctrl Pts',(2.45627869436139,-1.61927730041099,1.7294482263566));
#68753=CARTESIAN_POINT('Ctrl Pts',(2.4343775407991,-1.65249911909723,1.72728563538409));
#68754=CARTESIAN_POINT('Ctrl Pts',(2.41181732711787,-1.68525368649539,1.72512304441157));
#68755=CARTESIAN_POINT('Ctrl Pts',(2.38862084210658,-1.71751403856098,1.72296045343906));
#68756=CARTESIAN_POINT('Ctrl Pts',(2.33438342280857,-1.79294435659545,1.71790393934698));
#68757=CARTESIAN_POINT('Ctrl Pts',(2.27647413028142,-1.86593562161687,1.7128474252549));
#68758=CARTESIAN_POINT('Ctrl Pts',(2.21513998173545,-1.93610920697079,1.70779091116282));
#68759=CARTESIAN_POINT('Ctrl Pts',(2.1538893032477,-2.00618729261706,1.70274127851502));
#68760=CARTESIAN_POINT('Ctrl Pts',(2.08922332047284,-2.0734549878868,1.69769164586722));
#68761=CARTESIAN_POINT('Ctrl Pts',(2.02143146833816,-2.13756375783559,1.69264201321942));
#68762=CARTESIAN_POINT('Ctrl Pts',(1.95371103352441,-2.20160499051474,1.68759770025568));
#68763=CARTESIAN_POINT('Ctrl Pts',(1.88287159564746,-2.26249360987447,1.68255338729194));
#68764=CARTESIAN_POINT('Ctrl Pts',(1.80924114279776,-2.31991605175874,1.6775090743282));
#68765=CARTESIAN_POINT('Ctrl Pts',(1.73566252252895,-2.37729807078468,1.6724683123376));
#68766=CARTESIAN_POINT('Ctrl Pts',(1.65929714134141,-2.43121849058279,1.66742755034699));
#68767=CARTESIAN_POINT('Ctrl Pts',(1.58050715713632,-2.48140305598282,1.66238678835638));
#68768=CARTESIAN_POINT('Ctrl Pts',(1.50174490134216,-2.53156996002315,1.65734780035166));
#68769=CARTESIAN_POINT('Ctrl Pts',(1.42056011141324,-2.57800338384005,1.65230881234694));
#68770=CARTESIAN_POINT('Ctrl Pts',(1.33734424792106,-2.62047216404839,1.64726982434222));
#68771=CARTESIAN_POINT('Ctrl Pts',(1.25413450667023,-2.66293781980292,1.64223120705889));
#68772=CARTESIAN_POINT('Ctrl Pts',(1.16889438401989,-2.70143921067305,1.63719258977556));
#68773=CARTESIAN_POINT('Ctrl Pts',(1.08203926619567,-2.7357914807987,1.63215397249223));
#68774=CARTESIAN_POINT('Ctrl Pts',(0.995166362011864,-2.77015078564889,
1.62711432339107));
#68775=CARTESIAN_POINT('Ctrl Pts',(0.906678218184794,-2.80035911955002,
1.62207467428992));
#68776=CARTESIAN_POINT('Ctrl Pts',(0.817008414070304,-2.82628046225748,
1.61703502518876));
#68777=CARTESIAN_POINT('Ctrl Pts',(0.727241091791453,-2.85222999507624,
1.61198989534262));
#68778=CARTESIAN_POINT('Ctrl Pts',(0.636289970756585,-2.87388310780977,
1.60694476549647));
#68779=CARTESIAN_POINT('Ctrl Pts',(0.544601634966138,-2.89115427799905,
1.60189963565033));
#68780=CARTESIAN_POINT('Ctrl Pts',(0.452856400874139,-2.9084361660211,1.59685137498807));
#68781=CARTESIAN_POINT('Ctrl Pts',(0.360373479938316,-2.92133063663873,
1.59180311432582));
#68782=CARTESIAN_POINT('Ctrl Pts',(0.267605296108074,-2.9298039875553,1.58675485366356));
#68783=CARTESIAN_POINT('Ctrl Pts',(0.174691159895797,-2.93829066961298,
1.581698650562));
#68784=CARTESIAN_POINT('Ctrl Pts',(0.0814913071132577,-2.94234232815569,
1.57664244746044));
#68785=CARTESIAN_POINT('Ctrl Pts',(-0.0115413537709718,-2.94197736176761,
1.57158624435889));
#68786=CARTESIAN_POINT('Ctrl Pts',(-0.0513270549326549,-2.94182128277867,
1.56942394368191));
#68787=CARTESIAN_POINT('Ctrl Pts',(-0.0910822387100624,-2.94085810811356,
1.56726164300493));
#68788=CARTESIAN_POINT('Ctrl Pts',(-0.130771880773216,-2.93909215833717,
1.56509934232795));
#68789=CARTESIAN_POINT('Ctrl Pts',(-0.22358640832019,-2.93496247145547,
1.56004278587352));
#68790=CARTESIAN_POINT('Ctrl Pts',(-0.3163682720864,-2.92642469220872,1.55498622941909));
#68791=CARTESIAN_POINT('Ctrl Pts',(-0.408665385939188,-2.91347843690925,
1.54992967296466));
#68792=CARTESIAN_POINT('Ctrl Pts',(-0.500836901600221,-2.90054979891316,
1.54487999748755));
#68793=CARTESIAN_POINT('Ctrl Pts',(-0.592524542861914,-2.88322466760058,
1.53983032201044));
#68794=CARTESIAN_POINT('Ctrl Pts',(-0.683278204939454,-2.86155462898312,
1.53478064653333));
#68795=CARTESIAN_POINT('Ctrl Pts',(-0.773936267927405,-2.83990741738901,
1.52973629033885));
#68796=CARTESIAN_POINT('Ctrl Pts',(-0.863661878402266,-2.81392449876672,
1.52469193414437));
#68797=CARTESIAN_POINT('Ctrl Pts',(-0.952013111233592,-2.78370886337622,
1.51964757794989));
#68798=CARTESIAN_POINT('Ctrl Pts',(-1.04030215639899,-2.75351449582522,
1.51460677231977));
#68799=CARTESIAN_POINT('Ctrl Pts',(-1.12721832848165,-2.71909347659518,
1.50956596668964));
#68800=CARTESIAN_POINT('Ctrl Pts',(-1.21233391138896,-2.68059890459135,
1.50452516105951));
#68801=CARTESIAN_POINT('Ctrl Pts',(-1.29741954396359,-2.64211787799482,
1.49948612917986));
#68802=CARTESIAN_POINT('Ctrl Pts',(-1.38070544259646,-2.59956632899173,
1.49444709730021));
#68803=CARTESIAN_POINT('Ctrl Pts',(-1.46178392945742,-2.55314546071704,
1.48940806542056));
#68804=CARTESIAN_POINT('Ctrl Pts',(-1.5428564542476,-2.50672800598043,1.4843694040839));
#68805=CARTESIAN_POINT('Ctrl Pts',(-1.6217215054357,-2.45644201828579,1.47933074274723));
#68806=CARTESIAN_POINT('Ctrl Pts',(-1.69799707696022,-2.40253406357424,
1.47429208141057));
#68807=CARTESIAN_POINT('Ctrl Pts',(-1.77428827004858,-2.34861506828261,
1.46925238813448));
#68808=CARTESIAN_POINT('Ctrl Pts',(-1.84798856838221,-2.29107288886368,
1.46421269485838));
#68809=CARTESIAN_POINT('Ctrl Pts',(-1.91874689009342,-2.23019603886224,
1.45917300158229));
#68810=CARTESIAN_POINT('Ctrl Pts',(-1.98958216136788,-2.16925298538245,
1.45412782764771));
#68811=CARTESIAN_POINT('Ctrl Pts',(-2.05746873359588,-2.10496831261553,
1.44908265371313));
#68812=CARTESIAN_POINT('Ctrl Pts',(-2.12209067909298,-2.03766904812992,
1.44403747977855));
#68813=CARTESIAN_POINT('Ctrl Pts',(-2.18675272632632,-1.9703280204734,1.43898917501538));
#68814=CARTESIAN_POINT('Ctrl Pts',(-2.24814582232597,-1.89996901047082,
1.43394087025221));
#68815=CARTESIAN_POINT('Ctrl Pts',(-2.30599422035143,-1.82695228610542,
1.42889256548904));
#68816=CARTESIAN_POINT('Ctrl Pts',(-2.36393362600364,-1.75382069116408,
1.42383631868683));
#68817=CARTESIAN_POINT('Ctrl Pts',(-2.41831694414293,-1.67802339537995,
1.41878007188462));
#68818=CARTESIAN_POINT('Ctrl Pts',(-2.46891177401681,-1.59994957799338,
1.4137238250824));
#68819=CARTESIAN_POINT('Ctrl Pts',(-2.49054425696941,-1.56656809360318,
1.41156196046055));
#68820=CARTESIAN_POINT('Ctrl Pts',(-2.51148474069642,-1.53277074223601,
1.4094000958387));
#68821=CARTESIAN_POINT('Ctrl Pts',(-2.5317176883814,-1.49858918531289,1.40723823121684));
#68822=CARTESIAN_POINT('Ctrl Pts',(-2.58066863291028,-1.41589142308336,
1.40200788530626));
#68823=CARTESIAN_POINT('Ctrl Pts',(-2.62563695420144,-1.33066964034243,
1.39677753939567));
#68824=CARTESIAN_POINT('Ctrl Pts',(-2.66636406248024,-1.2433288729511,1.39154719348508));
#68825=CARTESIAN_POINT('Ctrl Pts',(-2.70702244659364,-1.15613548703612,
1.3863256734198));
#68826=CARTESIAN_POINT('Ctrl Pts',(-2.74345368984489,-1.06683059212917,
1.38110415335452));
#68827=CARTESIAN_POINT('Ctrl Pts',(-2.77544401528677,-0.975845540036365,
1.37588263328924));
#68828=CARTESIAN_POINT('Ctrl Pts',(-2.80737206235508,-0.885037616528062,
1.37067127841524));
#68829=CARTESIAN_POINT('Ctrl Pts',(-2.83487628148681,-0.792556427915325,
1.36545992354124));
#68830=CARTESIAN_POINT('Ctrl Pts',(-2.85779061008119,-0.698853939626707,
1.36024856866724));
#68831=CARTESIAN_POINT('Ctrl Pts',(-2.88067835069349,-0.605260176325145,
1.35504326063897));
#68832=CARTESIAN_POINT('Ctrl Pts',(-2.89898670081184,-0.510448320170043,
1.3498379526107));
#68833=CARTESIAN_POINT('Ctrl Pts',(-2.91259906001162,-0.414886388809551,
1.34463264458243));
#68834=CARTESIAN_POINT('Ctrl Pts',(-2.92619465701788,-0.319442131950787,
1.33943374634538));
#68835=CARTESIAN_POINT('Ctrl Pts',(-2.93510572388532,-0.223250035343443,
1.33423484810833));
#68836=CARTESIAN_POINT('Ctrl Pts',(-2.93926670076444,-0.126788255675884,
1.32903594987128));
#68837=CARTESIAN_POINT('Ctrl Pts',(-2.94109680683036,-0.0843618511973775,
1.32674933894406));
#68838=CARTESIAN_POINT('Ctrl Pts',(-2.94200868962107,-0.0418833966442406,
1.32446272801683));
#68839=CARTESIAN_POINT('Ctrl Pts',(-2.9419999375878,0.000605997841190852,
1.3221761170896));
#68840=CARTESIAN_POINT('Ctrl Pts',(-2.93741502701325,0.00061385004391417,
1.322175642952));
#68841=CARTESIAN_POINT('Ctrl Pts',(-2.93824669003836,0.450821023061646,
1.29790946866991));
#68842=CARTESIAN_POINT('Ctrl Pts',(-2.63011361001259,1.87620303645204,1.22102292401743));
#68843=CARTESIAN_POINT('Ctrl Pts',(-0.420704297245342,3.44500822120456,
1.09151600899461));
#68844=CARTESIAN_POINT('Ctrl Pts',(2.6535010782834,2.23705783115148,0.933654897883501));
#68845=CARTESIAN_POINT('Ctrl Pts',(3.3242675736315,-0.997273536182898,0.775793786772391));
#68846=CARTESIAN_POINT('Ctrl Pts',(0.984136888139677,-3.32800743087111,
0.61793267566128));
#68847=CARTESIAN_POINT('Ctrl Pts',(-2.11124554144075,-2.67379892134876,
0.466726785767013));
#68848=CARTESIAN_POINT('Ctrl Pts',(-2.93840347440061,-0.845052391620324,
0.368141266243119));
#68849=CARTESIAN_POINT('Ctrl Pts',(-2.94490570994055,0.00214417779480537,
0.322176117089595));
#68850=CARTESIAN_POINT('Origin',(0.,0.,-1.84858989190501));
#68851=CARTESIAN_POINT('',(-2.3717491904533,-0.00195961326026947,14.6514101080561));
#68852=CARTESIAN_POINT('Ctrl Pts',(-2.36544101854889,0.172878137039876,
14.63965844111));
#68853=CARTESIAN_POINT('Ctrl Pts',(-2.36969704386767,0.114644186597092,
14.6435756634253));
#68854=CARTESIAN_POINT('Ctrl Pts',(-2.37179733216257,0.0563070163347199,
14.6474928857407));
#68855=CARTESIAN_POINT('Ctrl Pts',(-2.3717491904533,-0.00195961326026254,
14.6514101080561));
#68856=CARTESIAN_POINT('',(-2.34668236863853,0.343918483395512,15.62825));
#68857=CARTESIAN_POINT('Ctrl Pts',(-2.37174919045282,-0.00195961383911467,
14.651410108095));
#68858=CARTESIAN_POINT('Ctrl Pts',(-2.37165303655356,-0.118336079531962,
14.6592340116152));
#68859=CARTESIAN_POINT('Ctrl Pts',(-2.36298799025286,-0.234362805409626,
14.6670579151354));
#68860=CARTESIAN_POINT('Ctrl Pts',(-2.34592725613449,-0.349032049281036,
14.6748818186556));
#68861=CARTESIAN_POINT('Ctrl Pts',(-2.34141960030033,-0.379329074165719,
14.6769489902149));
#68862=CARTESIAN_POINT('Ctrl Pts',(-2.33632609141068,-0.409531501361688,
14.6790161617741));
#68863=CARTESIAN_POINT('Ctrl Pts',(-2.33065042506097,-0.439621039832174,
14.6810833333333));
#68864=CARTESIAN_POINT('Ctrl Pts',(-2.31599449587478,-0.517319431156899,
14.6864212651497));
#68865=CARTESIAN_POINT('Ctrl Pts',(-2.29742185661224,-0.59442755062193,
14.6917591969661));
#68866=CARTESIAN_POINT('Ctrl Pts',(-2.27499436621545,-0.670521212332572,
14.6970971287826));
#68867=CARTESIAN_POINT('Ctrl Pts',(-2.2525987969661,-0.746506569594014,
14.7024274630968));
#68868=CARTESIAN_POINT('Ctrl Pts',(-2.22635940435725,-0.821479891836962,
14.707757797411));
#68869=CARTESIAN_POINT('Ctrl Pts',(-2.19638914799177,-0.895026688475827,
14.7130881317251));
#68870=CARTESIAN_POINT('Ctrl Pts',(-2.16645305795681,-0.968489641181807,
14.7184123894158));
#68871=CARTESIAN_POINT('Ctrl Pts',(-2.13279473239622,-1.04052886937477,
14.7237366471065));
#68872=CARTESIAN_POINT('Ctrl Pts',(-2.09557661492103,-1.11074601664652,
14.7290609047972));
#68873=CARTESIAN_POINT('Ctrl Pts',(-2.05838165286002,-1.18091947801374,
14.7343818499777));
#68874=CARTESIAN_POINT('Ctrl Pts',(-2.01763151364378,-1.24927269667142,
14.7397027951583));
#68875=CARTESIAN_POINT('Ctrl Pts',(-1.9735358295509,-1.315429356514,14.7450237403388));
#68876=CARTESIAN_POINT('Ctrl Pts',(-1.92945393263375,-1.38156533148656,
14.7503430218462));
#68877=CARTESIAN_POINT('Ctrl Pts',(-1.88202882737253,-1.4455057228044,14.7556623033536));
#68878=CARTESIAN_POINT('Ctrl Pts',(-1.83151419094341,-1.50690206412789,
14.7609815848609));
#68879=CARTESIAN_POINT('Ctrl Pts',(-1.78099971538943,-1.56829820992104,
14.7663008494279));
#68880=CARTESIAN_POINT('Ctrl Pts',(-1.72739602646039,-1.62714996174261,
14.7716201139948));
#68881=CARTESIAN_POINT('Ctrl Pts',(-1.67099697324794,-1.68314205517426,
14.7769393785617));
#68882=CARTESIAN_POINT('Ctrl Pts',(-1.614542210969,-1.73918945569137,14.7822638973173));
#68883=CARTESIAN_POINT('Ctrl Pts',(-1.55528690171925,-1.79237122556598,
14.7875884160728));
#68884=CARTESIAN_POINT('Ctrl Pts',(-1.49356121586978,-1.84240955190467,
14.7929129348284));
#68885=CARTESIAN_POINT('Ctrl Pts',(-1.43180550260319,-1.89247222016321,
14.7982400437787));
#68886=CARTESIAN_POINT('Ctrl Pts',(-1.36757739662557,-1.93938812234721,
14.8035671527289));
#68887=CARTESIAN_POINT('Ctrl Pts',(-1.30123752244291,-1.9829218271749,14.8088942616792));
#68888=CARTESIAN_POINT('Ctrl Pts',(-1.23478023064405,-2.02653258406077,
14.8142307992942));
#68889=CARTESIAN_POINT('Ctrl Pts',(-1.1662041068135,-2.06674894578569,14.8195673369093));
#68890=CARTESIAN_POINT('Ctrl Pts',(-1.09589570948668,-2.10338076829391,
14.8249038745243));
#68891=CARTESIAN_POINT('Ctrl Pts',(-1.03423463259541,-2.13550719572259,
14.8295840644977));
#68892=CARTESIAN_POINT('Ctrl Pts',(-0.971241734419387,-2.16487723257753,
14.8342642544711));
#68893=CARTESIAN_POINT('Ctrl Pts',(-0.907188983289324,-2.19139366867263,
14.8389444444445));
#68894=CARTESIAN_POINT('Ctrl Pts',(-0.834258870232282,-2.22158513817499,
14.8442732832198));
#68895=CARTESIAN_POINT('Ctrl Pts',(-0.759682288760601,-2.24818891298128,
14.8496021219951));
#68896=CARTESIAN_POINT('Ctrl Pts',(-0.683846636270297,-2.27102440333912,
14.8549309607704));
#68897=CARTESIAN_POINT('Ctrl Pts',(-0.608119617639673,-2.29382718207157,
14.8602521660343));
#68898=CARTESIAN_POINT('Ctrl Pts',(-0.531137555331562,-2.31287226173924,
14.8655733712981));
#68899=CARTESIAN_POINT('Ctrl Pts',(-0.453307800790021,-2.32802708322797,
14.870894576562));
#68900=CARTESIAN_POINT('Ctrl Pts',(-0.375567090829125,-2.34316456617141,
14.876209693865));
#68901=CARTESIAN_POINT('Ctrl Pts',(-0.296981074207135,-2.35442054610887,
14.8815248111681));
#68902=CARTESIAN_POINT('Ctrl Pts',(-0.217970767376855,-2.36171268512263,
14.8868399284712));
#68903=CARTESIAN_POINT('Ctrl Pts',(-0.139009742111534,-2.36900027576749,
14.8921517305448));
#68904=CARTESIAN_POINT('Ctrl Pts',(-0.0596254180553557,-2.37232888966095,
14.8974635326184));
#68905=CARTESIAN_POINT('Ctrl Pts',(0.0197537452978395,-2.371667736435,14.902775334692));
#68906=CARTESIAN_POINT('Ctrl Pts',(0.0991081939534888,-2.37100678905906,
14.9080854829364));
#68907=CARTESIAN_POINT('Ctrl Pts',(0.178457016093407,-2.36635854517191,
14.9133956311807));
#68908=CARTESIAN_POINT('Ctrl Pts',(0.257370915444152,-2.35774431912865,
14.9187057794251));
#68909=CARTESIAN_POINT('Ctrl Pts',(0.33628489608205,-2.34913008421211,14.9240159331393));
#68910=CARTESIAN_POINT('Ctrl Pts',(0.414763486632712,-2.33654991148123,
14.9293260868535));
#68911=CARTESIAN_POINT('Ctrl Pts',(0.492383177521609,-2.32007691014624,
14.9346362405677));
#68912=CARTESIAN_POINT('Ctrl Pts',(0.570081103006483,-2.3035873053104,14.9399517465028));
#68913=CARTESIAN_POINT('Ctrl Pts',(0.646917939504538,-2.283197132457,14.9452672524379));
#68914=CARTESIAN_POINT('Ctrl Pts',(0.722481638564208,-2.25903039918403,
14.950582758373));
#68915=CARTESIAN_POINT('Ctrl Pts',(0.798082721014159,-2.23485170997941,
14.9559008940315));
#68916=CARTESIAN_POINT('Ctrl Pts',(0.872408971671045,-2.2068929043621,14.9612190296901));
#68917=CARTESIAN_POINT('Ctrl Pts',(0.945067178850849,-2.17532666281616,
14.9665371653487));
#68918=CARTESIAN_POINT('Ctrl Pts',(1.01785652619065,-2.1437034476381,14.9718648996636));
#68919=CARTESIAN_POINT('Ctrl Pts',(1.08897139349092,-2.10845999664893,14.9771926339784));
#68920=CARTESIAN_POINT('Ctrl Pts',(1.15804230830806,-2.06981546874801,14.9825203682933));
#68921=CARTESIAN_POINT('Ctrl Pts',(1.2197753011225,-2.03527643926591,14.9872820973808));
#68922=CARTESIAN_POINT('Ctrl Pts',(1.27987573716285,-1.99802135198414,14.9920438264682));
#68923=CARTESIAN_POINT('Ctrl Pts',(1.3381010999646,-1.95823479408715,14.9968055555556));
#68924=CARTESIAN_POINT('Ctrl Pts',(1.40347453969688,-1.91356381189524,15.0021518616074));
#68925=CARTESIAN_POINT('Ctrl Pts',(1.46672801140548,-1.86553405579549,15.0074981676593));
#68926=CARTESIAN_POINT('Ctrl Pts',(1.52749715228343,-1.8143733111645,15.0128444737111));
#68927=CARTESIAN_POINT('Ctrl Pts',(1.58817937416269,-1.76328574250129,15.0181831328625));
#68928=CARTESIAN_POINT('Ctrl Pts',(1.64638396926533,-1.70907637782963,15.0235217920139));
#68929=CARTESIAN_POINT('Ctrl Pts',(1.70177600406537,-1.65201588808562,15.0288604511653));
#68930=CARTESIAN_POINT('Ctrl Pts',(1.7571038186477,-1.59502155292659,15.0341929208014));
#68931=CARTESIAN_POINT('Ctrl Pts',(1.80962523111407,-1.53518299546105,15.0395253904374));
#68932=CARTESIAN_POINT('Ctrl Pts',(1.8590399755671,-1.47280970656208,15.0448578600734));
#68933=CARTESIAN_POINT('Ctrl Pts',(1.90842334678594,-1.41047601822811,15.0501869441446));
#68934=CARTESIAN_POINT('Ctrl Pts',(1.95470367709152,-1.34561115761927,15.0555160282158));
#68935=CARTESIAN_POINT('Ctrl Pts',(1.99761983056691,-1.27855898378833,15.060845112287));
#68936=CARTESIAN_POINT('Ctrl Pts',(2.04052190853373,-1.21152880152399,15.0661724485416));
#68937=CARTESIAN_POINT('Ctrl Pts',(2.08006175013366,-1.14231312308764,15.0714997847961));
#68938=CARTESIAN_POINT('Ctrl Pts',(2.11602139654005,-1.07128498163873,15.0768271210507));
#68939=CARTESIAN_POINT('Ctrl Pts',(2.1519802852596,-1.0002583367865,15.0821543450557));
#68940=CARTESIAN_POINT('Ctrl Pts',(2.18435891954638,-0.927419721225917,
15.0874815690608));
#68941=CARTESIAN_POINT('Ctrl Pts',(2.21298585799553,-0.853165666686019,
15.0928087930658));
#68942=CARTESIAN_POINT('Ctrl Pts',(2.2416399377268,-0.778841211664881,15.0981410678272));
#68943=CARTESIAN_POINT('Ctrl Pts',(2.26653504833346,-0.703099072749055,
15.1034733425885));
#68944=CARTESIAN_POINT('Ctrl Pts',(2.28754861581706,-0.626354047463135,
15.1088056173499));
#68945=CARTESIAN_POINT('Ctrl Pts',(2.30857199613196,-0.549573184093736,
15.1141403821554));
#68946=CARTESIAN_POINT('Ctrl Pts',(2.32571012093138,-0.471788956798449,
15.119475146961));
#68947=CARTESIAN_POINT('Ctrl Pts',(2.33889143828093,-0.393427124682763,
15.1248099117666));
#68948=CARTESIAN_POINT('Ctrl Pts',(2.35209542360752,-0.314930533334536,
15.1301538507938));
#68949=CARTESIAN_POINT('Ctrl Pts',(2.36132895093892,-0.235854816316838,
15.1354977898209));
#68950=CARTESIAN_POINT('Ctrl Pts',(2.36657234708878,-0.156631377746257,
15.1408417288481));
#68951=CARTESIAN_POINT('Ctrl Pts',(2.37109395716964,-0.0883135378878964,
15.1454500414543));
#68952=CARTESIAN_POINT('Ctrl Pts',(2.37264921575342,-0.0198860738465293,
15.1500583540605));
#68953=CARTESIAN_POINT('Ctrl Pts',(2.37125658538404,0.0483763245071093,
15.1546666666666));
#68954=CARTESIAN_POINT('Ctrl Pts',(2.36964161779268,0.127537000213953,15.1600107089003));
#68955=CARTESIAN_POINT('Ctrl Pts',(2.36405545103476,0.206759138475579,15.165354751134));
#68956=CARTESIAN_POINT('Ctrl Pts',(2.35449000539771,0.285613159679849,15.1706987933677));
#68957=CARTESIAN_POINT('Ctrl Pts',(2.34493796483008,0.364356674414422,15.1760353464305));
#68958=CARTESIAN_POINT('Ctrl Pts',(2.33141777735698,0.442732637510022,15.1813718994932));
#68959=CARTESIAN_POINT('Ctrl Pts',(2.31397336310136,0.520312730343378,15.186708452556));
#68960=CARTESIAN_POINT('Ctrl Pts',(2.2965483857409,0.59780638197503,15.1920390595308));
#68961=CARTESIAN_POINT('Ctrl Pts',(2.27520797345393,0.674505473075603,15.1973696665055));
#68962=CARTESIAN_POINT('Ctrl Pts',(2.25004750123224,0.749989536392724,15.2027002734803));
#68963=CARTESIAN_POINT('Ctrl Pts',(2.22490230563315,0.825427768235062,15.2080276438834));
#68964=CARTESIAN_POINT('Ctrl Pts',(2.19594180171421,0.899651995628935,15.2133550142866));
#68965=CARTESIAN_POINT('Ctrl Pts',(2.16331151907301,0.972255796560776,15.2186823846897));
#68966=CARTESIAN_POINT('Ctrl Pts',(2.13069102338093,1.0448378211043,15.2240081572304));
#68967=CARTESIAN_POINT('Ctrl Pts',(2.09440312610934,1.11579995955118,15.229333929771));
#68968=CARTESIAN_POINT('Ctrl Pts',(2.05464136394079,1.1847560626912,15.2346597023117));
#68969=CARTESIAN_POINT('Ctrl Pts',(2.01487931203249,1.25371266830701,15.2399855136607));
#68970=CARTESIAN_POINT('Ctrl Pts',(1.9716435791553,1.32066280648512,15.2453113250098));
#68971=CARTESIAN_POINT('Ctrl Pts',(1.9251727719285,1.38524649818187,15.2506371363588));
#68972=CARTESIAN_POINT('Ctrl Pts',(1.87865577596628,1.44989438155564,15.2559682411922));
#68973=CARTESIAN_POINT('Ctrl Pts',(1.82889755604729,1.51217074113547,15.2612993460255));
#68974=CARTESIAN_POINT('Ctrl Pts',(1.77617869626716,1.57174657671861,15.2666304508589));
#68975=CARTESIAN_POINT('Ctrl Pts',(1.72343391037242,1.63135171054433,15.2719641774264));
#68976=CARTESIAN_POINT('Ctrl Pts',(1.66772591038729,1.6882533409391,15.277297903994));
#68977=CARTESIAN_POINT('Ctrl Pts',(1.60937229223899,1.74215926007739,15.2826316305615));
#68978=CARTESIAN_POINT('Ctrl Pts',(1.5509157973428,1.79616021472213,15.2879747604267));
#68979=CARTESIAN_POINT('Ctrl Pts',(1.4898047237546,1.84715460629835,15.293317890292));
#68980=CARTESIAN_POINT('Ctrl Pts',(1.42638970436655,1.89489062316987,15.2986610201572));
#68981=CARTESIAN_POINT('Ctrl Pts',(1.37153042865215,1.93618625528247,15.3032832726974));
#68982=CARTESIAN_POINT('Ctrl Pts',(1.31494760601248,1.97504400532842,15.3079055252376));
#68983=CARTESIAN_POINT('Ctrl Pts',(1.25688368958199,2.01132828085392,15.3125277777778));
#68984=CARTESIAN_POINT('Ctrl Pts',(1.19056964084797,2.0527680831166,15.3178067926817));
#68985=CARTESIAN_POINT('Ctrl Pts',(1.12206547864385,2.09101114118911,15.3230858075856));
#68986=CARTESIAN_POINT('Ctrl Pts',(1.05171556453074,2.12581571022132,15.3283648224894));
#68987=CARTESIAN_POINT('Ctrl Pts',(0.981467658141026,2.1605698124563,15.3336361827956));
#68988=CARTESIAN_POINT('Ctrl Pts',(0.909379736706693,2.19189511070529,15.3389075431017));
#68989=CARTESIAN_POINT('Ctrl Pts',(0.83582423970175,2.2195936346158,15.3441789034078));
#68990=CARTESIAN_POINT('Ctrl Pts',(0.762351145219771,2.24726112851027,15.3494443583309));
#68991=CARTESIAN_POINT('Ctrl Pts',(0.687414185600126,2.27130974851289,15.3547098132539));
#68992=CARTESIAN_POINT('Ctrl Pts',(0.611407990096484,2.29158860447205,15.359975268177));
#68993=CARTESIAN_POINT('Ctrl Pts',(0.535447891305022,2.311855161584,15.365237529674));
#68994=CARTESIAN_POINT('Ctrl Pts',(0.458420304264606,2.32835636625989,15.3704997911711));
#68995=CARTESIAN_POINT('Ctrl Pts',(0.380736000933961,2.34099085006602,15.3757620526681));
#68996=CARTESIAN_POINT('Ctrl Pts',(0.303073462940556,2.35362179398327,15.3810228398018));
#68997=CARTESIAN_POINT('Ctrl Pts',(0.224755046136807,2.36238808998572,15.3862836269354));
#68998=CARTESIAN_POINT('Ctrl Pts',(0.14620112273661,2.3672395937485,15.391544414069));
#68999=CARTESIAN_POINT('Ctrl Pts',(0.0676435753024226,2.37209132133224,
15.3968054439056));
#69000=CARTESIAN_POINT('Ctrl Pts',(-0.0111490222247413,2.37302787014035,
15.4020664737422));
#69001=CARTESIAN_POINT('Ctrl Pts',(-0.0897534095969474,2.37005113614996,
15.4073275035788));
#69002=CARTESIAN_POINT('Ctrl Pts',(-0.168448232980228,2.36707097736413,
15.4125945863416));
#69003=CARTESIAN_POINT('Ctrl Pts',(-0.246953934046379,2.36016856275869,
15.4178616691043));
#69004=CARTESIAN_POINT('Ctrl Pts',(-0.32485014880416,2.3493978895287,15.4231287518671));
#69005=CARTESIAN_POINT('Ctrl Pts',(-0.402789595570061,2.33862123862914,
15.4283987578343));
#69006=CARTESIAN_POINT('Ctrl Pts',(-0.480118412252643,2.32397214703836,
15.4336687638016));
#69007=CARTESIAN_POINT('Ctrl Pts',(-0.556427007255923,2.30555569182274,
15.4389387697688));
#69008=CARTESIAN_POINT('Ctrl Pts',(-0.632890005094257,2.28710197274586,
15.4442194390678));
#69009=CARTESIAN_POINT('Ctrl Pts',(-0.708328197589392,2.26486579866246,
15.4495001083668));
#69010=CARTESIAN_POINT('Ctrl Pts',(-0.782347930230338,2.23900196037527,
15.4547807776658));
#69011=CARTESIAN_POINT('Ctrl Pts',(-0.855274810918575,2.21351998439923,
15.4599834814068));
#69012=CARTESIAN_POINT('Ctrl Pts',(-0.926824476841342,2.18451701900297,
15.4651861851478));
#69013=CARTESIAN_POINT('Ctrl Pts',(-0.996644042858746,2.15218463760296,
15.4703888888888));
#69014=CARTESIAN_POINT('Ctrl Pts',(-1.07023465554323,2.11810594172304,15.4758725975075));
#69015=CARTESIAN_POINT('Ctrl Pts',(-1.14218689897926,2.08019728947419,15.4813563061261));
#69016=CARTESIAN_POINT('Ctrl Pts',(-1.21208900263023,2.03863638547998,15.4868400147447));
#69017=CARTESIAN_POINT('Ctrl Pts',(-1.28188065229525,1.99714115286424,15.4923150584242));
#69018=CARTESIAN_POINT('Ctrl Pts',(-1.34962823191753,1.95200536686404,15.4977901021036));
#69019=CARTESIAN_POINT('Ctrl Pts',(-1.41494265277655,1.90345353288533,15.5032651457831));
#69020=CARTESIAN_POINT('Ctrl Pts',(-1.48015447212883,1.85497796830098,15.5087315887933));
#69021=CARTESIAN_POINT('Ctrl Pts',(-1.5429403935587,1.80309729790061,15.5141980318035));
#69022=CARTESIAN_POINT('Ctrl Pts',(-1.60293970151325,1.74807962513514,15.5196644748137));
#69023=CARTESIAN_POINT('Ctrl Pts',(-1.66288342070942,1.69311292569291,15.5251258532192));
#69024=CARTESIAN_POINT('Ctrl Pts',(-1.72004533954628,1.63501529660287,15.5305872316247));
#69025=CARTESIAN_POINT('Ctrl Pts',(-1.77409770341292,1.5740951055273,15.5360486100302));
#69026=CARTESIAN_POINT('Ctrl Pts',(-1.82811319668854,1.51321646977493,15.5415062630805));
#69027=CARTESIAN_POINT('Ctrl Pts',(-1.87902306477552,1.44951942710436,15.5469639161309));
#69028=CARTESIAN_POINT('Ctrl Pts',(-1.92653709979407,1.38334842524111,15.5524215691813));
#69029=CARTESIAN_POINT('Ctrl Pts',(-1.97403032342431,1.31720640661226,15.5578768317519));
#69030=CARTESIAN_POINT('Ctrl Pts',(-2.01813041946052,1.24859293908361,15.5633320943226));
#69031=CARTESIAN_POINT('Ctrl Pts',(-2.05858877012042,1.17788383893918,15.5687873568932));
#69032=CARTESIAN_POINT('Ctrl Pts',(-2.09905065068051,1.10716856958462,15.5742430954233));
#69033=CARTESIAN_POINT('Ctrl Pts',(-2.13586992630258,1.03435767661531,15.5796988339534));
#69034=CARTESIAN_POINT('Ctrl Pts',(-2.1688428443841,0.959853519482995,15.5851545724834));
#69035=CARTESIAN_POINT('Ctrl Pts',(-2.20181578264016,0.885349316765168,
15.5906103143516));
#69036=CARTESIAN_POINT('Ctrl Pts',(-2.23094218778358,0.809152249651672,
15.5960660562197));
#69037=CARTESIAN_POINT('Ctrl Pts',(-2.2560662000637,0.731685289882293,15.6015217980879));
#69038=CARTESIAN_POINT('Ctrl Pts',(-2.28120754002064,0.654164902243658,
15.6069813027043));
#69039=CARTESIAN_POINT('Ctrl Pts',(-2.30234084338011,0.575373289754166,
15.6124408073206));
#69040=CARTESIAN_POINT('Ctrl Pts',(-2.31936008877542,0.495748768123185,
15.617900311937));
#69041=CARTESIAN_POINT('Ctrl Pts',(-2.33011465921646,0.445433521658159,
15.621350207958));
#69042=CARTESIAN_POINT('Ctrl Pts',(-2.33922747603912,0.394785958881003,
15.624800103979));
#69043=CARTESIAN_POINT('Ctrl Pts',(-2.34668236863853,0.343918483395496,
15.62825));
#69044=CARTESIAN_POINT('',(-0.439445221994505,2.33068358199182,15.62825));
#69045=CARTESIAN_POINT('Origin',(0.,0.,15.62825));
#69046=CARTESIAN_POINT('',(-2.37181912929798,0.000927365841751814,14.8485899293694));
#69047=CARTESIAN_POINT('Ctrl Pts',(-2.37174981871279,0.00092732725788483,
14.8485899301431));
#69048=CARTESIAN_POINT('Ctrl Pts',(-2.3717804010031,-0.0772905196480431,
14.8538670087384));
#69049=CARTESIAN_POINT('Ctrl Pts',(-2.36793742071335,-0.155665441830004,
14.8591440873337));
#69050=CARTESIAN_POINT('Ctrl Pts',(-2.36020048238129,-0.233777127767286,
14.864421165929));
#69051=CARTESIAN_POINT('Ctrl Pts',(-2.35214591793149,-0.315095548783754,
14.8699148855153));
#69052=CARTESIAN_POINT('Ctrl Pts',(-2.33987067538355,-0.396128138407514,
14.8754086051016));
#69053=CARTESIAN_POINT('Ctrl Pts',(-2.32341183915449,-0.476398455262787,
14.8809023246879));
#69054=CARTESIAN_POINT('Ctrl Pts',(-2.3076405835705,-0.553315417392622,
14.8861665398788));
#69055=CARTESIAN_POINT('Ctrl Pts',(-2.28802840003837,-0.629531996772985,
14.8914307550697));
#69056=CARTESIAN_POINT('Ctrl Pts',(-2.26466074652353,-0.704634490821663,
14.8966949702607));
#69057=CARTESIAN_POINT('Ctrl Pts',(-2.24130539769904,-0.779697438198127,
14.9019564134772));
#69058=CARTESIAN_POINT('Ctrl Pts',(-2.21419864424466,-0.853647007499199,
14.9072178566937));
#69059=CARTESIAN_POINT('Ctrl Pts',(-2.18347633982578,-0.926082683091,14.9124792999102));
#69060=CARTESIAN_POINT('Ctrl Pts',(-2.15276017382182,-0.998503885802566,
14.9177396918735));
#69061=CARTESIAN_POINT('Ctrl Pts',(-2.11843007850108,-1.06941135454287,
14.9230000838367));
#69062=CARTESIAN_POINT('Ctrl Pts',(-2.08067018877933,-1.1384241863317,14.9282604758));
#69063=CARTESIAN_POINT('Ctrl Pts',(-2.04290550487823,-1.20744578032549,
14.9335215356483));
#69064=CARTESIAN_POINT('Ctrl Pts',(-2.00171039456691,-1.27457184092691,
14.9387825954965));
#69065=CARTESIAN_POINT('Ctrl Pts',(-1.95731432203941,-1.33944716478084,
14.9440436553447));
#69066=CARTESIAN_POINT('Ctrl Pts',(-1.91287075215952,-1.40439189581299,
14.9493103437632));
#69067=CARTESIAN_POINT('Ctrl Pts',(-1.86521965965363,-1.46708069074338,
14.9545770321817));
#69068=CARTESIAN_POINT('Ctrl Pts',(-1.81463261526301,-1.52718909573232,
14.9598437206002));
#69069=CARTESIAN_POINT('Ctrl Pts',(-1.76401351139897,-1.58733559434456,
14.9651137467757));
#69070=CARTESIAN_POINT('Ctrl Pts',(-1.71045508175997,-1.64489810102531,
14.9703837729511));
#69071=CARTESIAN_POINT('Ctrl Pts',(-1.65426598936552,-1.69958880289573,
14.9756537991265));
#69072=CARTESIAN_POINT('Ctrl Pts',(-1.59798611215559,-1.75436786862941,
14.9809323400925));
#69073=CARTESIAN_POINT('Ctrl Pts',(-1.53906745394361,-1.80626556029958,
14.9862108810585));
#69074=CARTESIAN_POINT('Ctrl Pts',(-1.47785131589474,-1.85503464943601,
14.9914894220245));
#69075=CARTESIAN_POINT('Ctrl Pts',(-1.45936923827676,-1.8697587747975,14.9930830933496));
#69076=CARTESIAN_POINT('Ctrl Pts',(-1.44067793128034,-1.88419802432291,
14.9946767646747));
#69077=CARTESIAN_POINT('Ctrl Pts',(-1.42178725865968,-1.89834639979457,
14.9962704359998));
#69078=CARTESIAN_POINT('Ctrl Pts',(-1.35842070635087,-1.94580547086168,
15.0016162201026));
#69079=CARTESIAN_POINT('Ctrl Pts',(-1.29255927181258,-1.99017524410936,
15.0069620042054));
#69080=CARTESIAN_POINT('Ctrl Pts',(-1.22453598376717,-2.03118430649692,
15.0123077883082));
#69081=CARTESIAN_POINT('Ctrl Pts',(-1.15661015585879,-2.07213461328835,
15.0176459132567));
#69082=CARTESIAN_POINT('Ctrl Pts',(-1.08652902241226,-2.10973353404438,
15.0229840382053));
#69083=CARTESIAN_POINT('Ctrl Pts',(-1.01465672105759,-2.14375133840487,
15.0283221631539));
#69084=CARTESIAN_POINT('Ctrl Pts',(-0.942867940345527,-2.17772961169669,
15.0336540848279));
#69085=CARTESIAN_POINT('Ctrl Pts',(-0.869292548025791,-2.2081348415054,
15.0389860065018));
#69086=CARTESIAN_POINT('Ctrl Pts',(-0.794320251626988,-2.23478262933003,
15.0443179281757));
#69087=CARTESIAN_POINT('Ctrl Pts',(-0.719395684358074,-2.26141345254523,
15.0496464554227));
#69088=CARTESIAN_POINT('Ctrl Pts',(-0.643076416527853,-2.28429142689331,
15.0549749826697));
#69089=CARTESIAN_POINT('Ctrl Pts',(-0.565772072374481,-2.30328027487344,
15.0603035099167));
#69090=CARTESIAN_POINT('Ctrl Pts',(-0.488493200923583,-2.32226286580191,
15.0656302813505));
#69091=CARTESIAN_POINT('Ctrl Pts',(-0.410230350154702,-2.33735876452577,
15.0709570527843));
#69092=CARTESIAN_POINT('Ctrl Pts',(-0.331406838044755,-2.34848197144393,
15.076283824218));
#69093=CARTESIAN_POINT('Ctrl Pts',(-0.252585092592087,-2.35960492905965,
15.0816104762638));
#69094=CARTESIAN_POINT('Ctrl Pts',(-0.173203172501378,-2.36675530813906,
15.0869371283096));
#69095=CARTESIAN_POINT('Ctrl Pts',(-0.0936916385221681,-2.3698987192222,
15.0922637803554));
#69096=CARTESIAN_POINT('Ctrl Pts',(-0.0141046307164287,-2.37304511408959,
15.0975954885584));
#69097=CARTESIAN_POINT('Ctrl Pts',(0.0656117699587432,-2.37217692473355,
15.1029271967614));
#69098=CARTESIAN_POINT('Ctrl Pts',(0.14502546978225,-2.36731190923681,15.1082589049644));
#69099=CARTESIAN_POINT('Ctrl Pts',(0.224476179236341,-2.36244462646847,
15.1135930979345));
#69100=CARTESIAN_POINT('Ctrl Pts',(0.303623442888271,-2.35357685774052,
15.1189272909046));
#69101=CARTESIAN_POINT('Ctrl Pts',(0.382041247237252,-2.34077819280457,
15.1242614838747));
#69102=CARTESIAN_POINT('Ctrl Pts',(0.460594386535239,-2.32795743968748,
15.1296048826972));
#69103=CARTESIAN_POINT('Ctrl Pts',(0.538415094286813,-2.31119233319851,
15.1349482815197));
#69104=CARTESIAN_POINT('Ctrl Pts',(0.615088739328564,-2.29060339326807,
15.1402916803422));
#69105=CARTESIAN_POINT('Ctrl Pts',(0.681925750711367,-2.2726558545572,15.1449495625614));
#69106=CARTESIAN_POINT('Ctrl Pts',(0.747891177234452,-2.25180353856829,
15.1496074447807));
#69107=CARTESIAN_POINT('Ctrl Pts',(0.812722713330219,-2.22815615559978,
15.1542653269999));
#69108=CARTESIAN_POINT('Ctrl Pts',(0.887095955506878,-2.20102842353797,
15.1596087419979));
#69109=CARTESIAN_POINT('Ctrl Pts',(0.960243664981093,-2.17012395952759,
15.164952156996));
#69110=CARTESIAN_POINT('Ctrl Pts',(1.03175679799573,-2.13557392105485,15.170295571994));
#69111=CARTESIAN_POINT('Ctrl Pts',(1.10316953615153,-2.1010723862078,15.1756314855533));
#69112=CARTESIAN_POINT('Ctrl Pts',(1.17295183897759,-2.06293564331141,15.1809673991125));
#69113=CARTESIAN_POINT('Ctrl Pts',(1.24071265927342,-2.02134365203413,15.1863033126717));
#69114=CARTESIAN_POINT('Ctrl Pts',(1.30839780260162,-1.97979811172607,15.19163326695));
#69115=CARTESIAN_POINT('Ctrl Pts',(1.37406555478731,-1.9348052351937,15.1969632212284));
#69116=CARTESIAN_POINT('Ctrl Pts',(1.4373489279239,-1.8865911379777,15.2022931755067));
#69117=CARTESIAN_POINT('Ctrl Pts',(1.50059377146843,-1.83840639554173,15.2076198846837));
#69118=CARTESIAN_POINT('Ctrl Pts',(1.56145674785138,-1.78700460774479,15.2129465938606));
#69119=CARTESIAN_POINT('Ctrl Pts',(1.61960037055053,-1.73265481334644,15.2182733030376));
#69120=CARTESIAN_POINT('Ctrl Pts',(1.6777264696894,-1.67832139910905,15.2235984068294));
#69121=CARTESIAN_POINT('Ctrl Pts',(1.73313450246579,-1.62104206115198,15.2289235106211));
#69122=CARTESIAN_POINT('Ctrl Pts',(1.78552168443477,-1.56112471536172,15.2342486144129));
#69123=CARTESIAN_POINT('Ctrl Pts',(1.83790918402227,-1.50120700629828,15.2395737504903));
#69124=CARTESIAN_POINT('Ctrl Pts',(1.88727549062441,-1.43865160970255,15.2448988865677));
#69125=CARTESIAN_POINT('Ctrl Pts',(1.93335715456253,-1.37380063160631,15.2502240226451));
#69126=CARTESIAN_POINT('Ctrl Pts',(1.97948468935904,-1.30888509919976,15.2555544594981));
#69127=CARTESIAN_POINT('Ctrl Pts',(2.0223207799605,-1.24166980202093,15.2608848963512));
#69128=CARTESIAN_POINT('Ctrl Pts',(2.06164486190368,-1.17252655658034,15.2662153332042));
#69129=CARTESIAN_POINT('Ctrl Pts',(2.10098825176765,-1.10334936216396,15.2715483872742));
#69130=CARTESIAN_POINT('Ctrl Pts',(2.13681598740719,-1.03224275051682,15.2768814413441));
#69131=CARTESIAN_POINT('Ctrl Pts',(2.16895428834543,-0.959601666092737,
15.2822144954141));
#69132=CARTESIAN_POINT('Ctrl Pts',(2.20114946393685,-0.886832029867145,
15.2875569873072));
#69133=CARTESIAN_POINT('Ctrl Pts',(2.2296419918257,-0.812522931436238,15.2928994792003));
#69134=CARTESIAN_POINT('Ctrl Pts',(2.25430699883861,-0.737087523627462,
15.2982419710934));
#69135=CARTESIAN_POINT('Ctrl Pts',(2.27587996298933,-0.671108813485499,
15.3029147200623));
#69136=CARTESIAN_POINT('Ctrl Pts',(2.29452563020474,-0.604268919533596,
15.3075874690311));
#69137=CARTESIAN_POINT('Ctrl Pts',(2.31019260680153,-0.536850241668533,
15.3122602179999));
#69138=CARTESIAN_POINT('Ctrl Pts',(2.3278902754598,-0.460693019190823,15.3175386303638));
#69139=CARTESIAN_POINT('Ctrl Pts',(2.34185491885702,-0.383500328117279,
15.3228170427277));
#69140=CARTESIAN_POINT('Ctrl Pts',(2.35196941557815,-0.305676185995863,
15.3280954550917));
#69141=CARTESIAN_POINT('Ctrl Pts',(2.36206922168904,-0.227965078083739,
15.333366200925));
#69142=CARTESIAN_POINT('Ctrl Pts',(2.3683299184671,-0.149624809785199,15.3386369467583));
#69143=CARTESIAN_POINT('Ctrl Pts',(2.37068489347443,-0.071071783093953,
15.3439076925916));
#69144=CARTESIAN_POINT('Ctrl Pts',(2.37303722400934,0.0073930340362505,
15.3491725197455));
#69145=CARTESIAN_POINT('Ctrl Pts',(2.37149252781999,0.0860696590820804,
15.3544373468995));
#69146=CARTESIAN_POINT('Ctrl Pts',(2.3660359219475,0.164535949123724,15.3597021740534));
#69147=CARTESIAN_POINT('Ctrl Pts',(2.36058263520585,0.242954509882856,15.3649637987312));
#69148=CARTESIAN_POINT('Ctrl Pts',(2.3512221914708,0.321162512866807,15.370225423409));
#69149=CARTESIAN_POINT('Ctrl Pts',(2.33799178822351,0.39873858692059,15.3754870480869));
#69150=CARTESIAN_POINT('Ctrl Pts',(2.324765113418,0.476292799367432,15.3807471899934));
#69151=CARTESIAN_POINT('Ctrl Pts',(2.30767072365399,0.553214964383808,15.3860073319));
#69152=CARTESIAN_POINT('Ctrl Pts',(2.28679738776715,0.629091225341251,15.3912674738066));
#69153=CARTESIAN_POINT('Ctrl Pts',(2.26592311963945,0.704970875069427,15.3965278506406));
#69154=CARTESIAN_POINT('Ctrl Pts',(2.24126969884978,0.779804066555513,15.4017882274746));
#69155=CARTESIAN_POINT('Ctrl Pts',(2.21297606265564,0.85319107391789,15.4070486043086));
#69156=CARTESIAN_POINT('Ctrl Pts',(2.18464568023134,0.926673392319267,15.4123158130329));
#69157=CARTESIAN_POINT('Ctrl Pts',(2.15266580974587,0.998705325762675,15.4175830217572));
#69158=CARTESIAN_POINT('Ctrl Pts',(2.11722382701338,1.06890660435176,15.4228502304815));
#69159=CARTESIAN_POINT('Ctrl Pts',(2.08176741572692,1.13913646212462,15.4281195835047));
#69160=CARTESIAN_POINT('Ctrl Pts',(2.04284633207388,1.20753376939129,15.4333889365279));
#69161=CARTESIAN_POINT('Ctrl Pts',(2.00069270464125,1.27374517235406,15.4386582895511));
#69162=CARTESIAN_POINT('Ctrl Pts',(1.95845349473204,1.3400910011347,15.4439383406876));
#69163=CARTESIAN_POINT('Ctrl Pts',(1.91296890876711,1.40424166909597,15.449218391824));
#69164=CARTESIAN_POINT('Ctrl Pts',(1.86451294622471,1.46587500690217,15.4544984429605));
#69165=CARTESIAN_POINT('Ctrl Pts',(1.81631237646607,1.52718349903638,15.4597506649737));
#69166=CARTESIAN_POINT('Ctrl Pts',(1.76517206266093,1.58600085819359,15.4650028869868));
#69167=CARTESIAN_POINT('Ctrl Pts',(1.71139636532063,1.64204766778171,15.470255109));
#69168=CARTESIAN_POINT('Ctrl Pts',(1.65525380497527,1.70056130024199,15.4757385003069));
#69169=CARTESIAN_POINT('Ctrl Pts',(1.59602203841579,1.75628138880867,15.4812218916139));
#69170=CARTESIAN_POINT('Ctrl Pts',(1.53400284422592,1.80887626343174,15.4867052829208));
#69171=CARTESIAN_POINT('Ctrl Pts',(1.47208183857198,1.86138787006329,15.4921799929449));
#69172=CARTESIAN_POINT('Ctrl Pts',(1.40738251214331,1.910783822024,15.497654702969));
#69173=CARTESIAN_POINT('Ctrl Pts',(1.34024353999736,1.9567691013493,15.5031294129932));
#69174=CARTESIAN_POINT('Ctrl Pts',(1.2732102974973,2.00268196360976,15.5085955015098));
#69175=CARTESIAN_POINT('Ctrl Pts',(1.20374541608499,2.04519460060527,15.5140615900264));
#69176=CARTESIAN_POINT('Ctrl Pts',(1.13221958775623,2.08405299059336,15.5195276785431));
#69177=CARTESIAN_POINT('Ctrl Pts',(1.06076018696158,2.12287529198119,15.5249886905888));
#69178=CARTESIAN_POINT('Ctrl Pts',(0.98724402702801,2.15804988681664,15.5304497026346));
#69179=CARTESIAN_POINT('Ctrl Pts',(0.912069174297032,2.18936700527735,15.5359107146804));
#69180=CARTESIAN_POINT('Ctrl Pts',(0.836945750303487,2.22066269902217,15.5413679907301));
#69181=CARTESIAN_POINT('Ctrl Pts',(0.760166292428859,2.248105997647,15.5468252667799));
#69182=CARTESIAN_POINT('Ctrl Pts',(0.682150793644788,2.27153436188621,15.5522825428296));
#69183=CARTESIAN_POINT('Ctrl Pts',(0.604169603162241,2.29495242320616,15.5577374189732));
#69184=CARTESIAN_POINT('Ctrl Pts',(0.524953870931903,2.3143589380584,15.5631922951168));
#69185=CARTESIAN_POINT('Ctrl Pts',(0.444939746137389,2.32964089181298,15.5686471712604));
#69186=CARTESIAN_POINT('Ctrl Pts',(0.364918690462446,2.34492416930128,15.5741025199093));
#69187=CARTESIAN_POINT('Ctrl Pts',(0.284099531150378,2.35608208087988,15.5795578685581));
#69188=CARTESIAN_POINT('Ctrl Pts',(0.202928946101218,2.3630526666442,15.585013217207));
#69189=CARTESIAN_POINT('Ctrl Pts',(0.121758408129459,2.37002324836571,15.5904685626919));
#69190=CARTESIAN_POINT('Ctrl Pts',(0.0402368804729099,2.37280647805828,
15.5959239081767));
#69191=CARTESIAN_POINT('Ctrl Pts',(-0.0411850251413373,2.37139238764995,
15.6013792536616));
#69192=CARTESIAN_POINT('Ctrl Pts',(-0.122663307909011,2.36997731811454,
15.6068383764696));
#69193=CARTESIAN_POINT('Ctrl Pts',(-0.204041393925436,2.36435913591515,
15.6122974992776));
#69194=CARTESIAN_POINT('Ctrl Pts',(-0.284870348510406,2.35457999376525,
15.6177566220856));
#69195=CARTESIAN_POINT('Ctrl Pts',(-0.336659423831911,2.34831425975964,
15.6212544147238));
#69196=CARTESIAN_POINT('Ctrl Pts',(-0.388223137926654,2.34034139237763,
15.6247522073619));
#69197=CARTESIAN_POINT('Ctrl Pts',(-0.439445221994505,2.33068358199182,
15.62825));
#69198=CARTESIAN_POINT('Ctrl Pts',(-2.36929349484953,0.173162376944586,
14.8369729823432));
#69199=CARTESIAN_POINT('Ctrl Pts',(-2.36976752448848,0.166738132832525,
14.8374071698954));
#69200=CARTESIAN_POINT('Ctrl Pts',(-2.37374016789726,0.109425107004542,
14.8412794730826));
#69201=CARTESIAN_POINT('Ctrl Pts',(-2.37542909742077,0.0519633377314283,
14.8451517762699));
#69202=CARTESIAN_POINT('Ctrl Pts',(-2.37517539399571,0.000929234209626874,
14.848589891905));
#69203=CARTESIAN_POINT('Origin',(0.,0.,15.5));
#69204=CARTESIAN_POINT('',(-2.86750655814837,8.90676632684412E-12,15.1324934418516));
#69205=CARTESIAN_POINT('Ctrl Pts',(-0.439445221994173,2.33068358199189,
15.62825));
#69206=CARTESIAN_POINT('Ctrl Pts',(-0.147008436989358,2.39880934021625,
15.6154874245605));
#69207=CARTESIAN_POINT('Ctrl Pts',(0.156480113641278,2.40931707764128,15.6043391916112));
#69208=CARTESIAN_POINT('Ctrl Pts',(0.737928439613964,2.32205123249246,15.5805131341436));
#69209=CARTESIAN_POINT('Ctrl Pts',(1.01352850236858,2.22934105143109,15.5679821521404));
#69210=CARTESIAN_POINT('Ctrl Pts',(1.47507484108102,1.97772793770723,15.5442630334499));
#69211=CARTESIAN_POINT('Ctrl Pts',(1.74286514902497,1.79346046158376,15.5295935945513));
#69212=CARTESIAN_POINT('Ctrl Pts',(2.17583696066496,1.25931375699315,15.5037713171893));
#69213=CARTESIAN_POINT('Ctrl Pts',(2.3203740697325,0.994251451750397,15.4932862058718));
#69214=CARTESIAN_POINT('Ctrl Pts',(2.51613707821668,0.414921897144935,15.4691143190916));
#69215=CARTESIAN_POINT('Ctrl Pts',(2.56173394912988,0.10148589177416,15.4553705111695));
#69216=CARTESIAN_POINT('Ctrl Pts',(2.53656022337087,-0.536980409493823,
15.4277868133117));
#69217=CARTESIAN_POINT('Ctrl Pts',(2.46062401708309,-0.853728603629975,
15.4157681065155));
#69218=CARTESIAN_POINT('Ctrl Pts',(2.20286218964617,-1.42534776432417,15.3936829887307));
#69219=CARTESIAN_POINT('Ctrl Pts',(2.03089606467517,-1.67805785252003,15.3829262679689));
#69220=CARTESIAN_POINT('Ctrl Pts',(1.57719177316252,-2.14967050654236,15.357096870092));
#69221=CARTESIAN_POINT('Ctrl Pts',(1.28448753171242,-2.35379022866316,15.3416926900889));
#69222=CARTESIAN_POINT('Ctrl Pts',(0.688989948483511,-2.61018154805751,
15.3167193293302));
#69223=CARTESIAN_POINT('Ctrl Pts',(0.398757154749054,-2.67942819397912,
15.3071940127235));
#69224=CARTESIAN_POINT('Ctrl Pts',(-0.251140580273949,-2.72678822036303,
15.2849170067093));
#69225=CARTESIAN_POINT('Ctrl Pts',(-0.609715051811953,-2.68297212826165,
15.2717461797437));
#69226=CARTESIAN_POINT('Ctrl Pts',(-1.17927502173795,-2.49854219510547,
15.2477763655208));
#69227=CARTESIAN_POINT('Ctrl Pts',(-1.49930249907036,-2.36318439438247,
15.2331919507368));
#69228=CARTESIAN_POINT('Ctrl Pts',(-2.09484079639828,-1.87954071233988,
15.2068720036005));
#69229=CARTESIAN_POINT('Ctrl Pts',(-2.32001767675477,-1.61164092749457,
15.1963836430683));
#69230=CARTESIAN_POINT('Ctrl Pts',(-2.59888433046962,-1.12346182881195,
15.1769355703592));
#69231=CARTESIAN_POINT('Ctrl Pts',(-2.68470675960721,-0.92393846071841,
15.168981896123));
#69232=CARTESIAN_POINT('Ctrl Pts',(-2.81771204745999,-0.484244810756474,
15.1513296903239));
#69233=CARTESIAN_POINT('Ctrl Pts',(-2.85842499981825,-0.243042999797827,
15.1415750001833));
#69234=CARTESIAN_POINT('Ctrl Pts',(-2.86750655814837,1.78013159768398E-11,
15.1324934418516));
#69235=CARTESIAN_POINT('Ctrl Pts',(0.261217229955146,2.92775537770323,15.060614691318));
#69236=CARTESIAN_POINT('Ctrl Pts',(0.163263701748706,2.92398569950982,15.0730743864785));
#69237=CARTESIAN_POINT('Ctrl Pts',(0.0657522159450944,2.91542515906648,
15.0854400947226));
#69238=CARTESIAN_POINT('Ctrl Pts',(-0.0308985911385236,2.90209534740483,
15.0977401687025));
#69239=CARTESIAN_POINT('Ctrl Pts',(-0.131043112735575,2.88828369231249,
15.1104848633563));
#69240=CARTESIAN_POINT('Ctrl Pts',(-0.230263368948763,2.86935169178861,
15.1231588590619));
#69241=CARTESIAN_POINT('Ctrl Pts',(-0.328080927958953,2.84531552794264,
15.1358321367556));
#69242=CARTESIAN_POINT('Ctrl Pts',(-0.401444097216596,2.82728840505817,
15.1453370950259));
#69243=CARTESIAN_POINT('Ctrl Pts',(-0.474017960878834,2.80639013673891,
15.1548424738783));
#69244=CARTESIAN_POINT('Ctrl Pts',(-0.545597552831274,2.78262387417559,
15.1643920731548));
#69245=CARTESIAN_POINT('Ctrl Pts',(-0.599282246795606,2.7647991772531,15.1715542726122));
#69246=CARTESIAN_POINT('Ctrl Pts',(-0.652407612168172,2.74536119848702,
15.1787416045881));
#69247=CARTESIAN_POINT('Ctrl Pts',(-0.704886515140488,2.72430928904873,
15.1859768832463));
#69248=CARTESIAN_POINT('Ctrl Pts',(-0.720596781816833,2.71800711631664,
15.1881428613968));
#69249=CARTESIAN_POINT('Ctrl Pts',(-0.736249110096228,2.71156029066323,
15.1903131609141));
#69250=CARTESIAN_POINT('Ctrl Pts',(-0.751841153536472,2.70496875253283,
15.1924884555304));
#69251=CARTESIAN_POINT('Ctrl Pts',(-0.76457047729845,2.69958742947065,15.1942643631947));
#69252=CARTESIAN_POINT('Ctrl Pts',(-0.777250594925623,2.69411346937544,
15.1960423418424));
#69253=CARTESIAN_POINT('Ctrl Pts',(-0.789880380926013,2.68854724896585,
15.1978227525559));
#69254=CARTESIAN_POINT('Ctrl Pts',(-0.873086561955101,2.65187648169916,
15.2095522605717));
#69255=CARTESIAN_POINT('Ctrl Pts',(-0.954109753653407,2.61120393346883,
15.2213864180752));
#69256=CARTESIAN_POINT('Ctrl Pts',(-1.0326800470441,2.56659382923925,15.2334440248114));
#69257=CARTESIAN_POINT('Ctrl Pts',(-1.07396798549143,2.54315164571067,15.2397801819423));
#69258=CARTESIAN_POINT('Ctrl Pts',(-1.11457874886226,2.51862142780173,15.2461783007471));
#69259=CARTESIAN_POINT('Ctrl Pts',(-1.15447370792355,2.49300700336368,15.252657017934));
#69260=CARTESIAN_POINT('Ctrl Pts',(-1.23233138917397,2.44301874068001,15.2653006678968));
#69261=CARTESIAN_POINT('Ctrl Pts',(-1.30746996628184,2.38890091090125,15.2782511407249));
#69262=CARTESIAN_POINT('Ctrl Pts',(-1.37967108001291,2.33085874954981,15.2914219968078));
#69263=CARTESIAN_POINT('Ctrl Pts',(-1.45359796468599,2.27142924844285,15.3049076663268));
#69264=CARTESIAN_POINT('Ctrl Pts',(-1.52444526031354,2.20788342659833,15.318623759732));
#69265=CARTESIAN_POINT('Ctrl Pts',(-1.59188833385002,2.1404469597675,15.332487740417));
#69266=CARTESIAN_POINT('Ctrl Pts',(-1.60226264324965,2.13007366663248,15.3346203422928));
#69267=CARTESIAN_POINT('Ctrl Pts',(-1.61255750286032,2.11960704884808,15.3367567393357));
#69268=CARTESIAN_POINT('Ctrl Pts',(-1.6227675606002,2.10905212039588,15.3388958302459));
#69269=CARTESIAN_POINT('Ctrl Pts',(-1.68513439043447,2.04457869199203,15.3519621930614));
#69270=CARTESIAN_POINT('Ctrl Pts',(-1.74412898638654,1.97703074697555,15.365082540821));
#69271=CARTESIAN_POINT('Ctrl Pts',(-1.79953647467951,1.90668242393888,15.3782125582993));
#69272=CARTESIAN_POINT('Ctrl Pts',(-1.85482014934552,1.83649130133295,15.3913132354279));
#69273=CARTESIAN_POINT('Ctrl Pts',(-1.90653200235803,1.76351139803357,15.404423277528));
#69274=CARTESIAN_POINT('Ctrl Pts',(-1.95441360534623,1.68803174082651,15.41752372735));
#69275=CARTESIAN_POINT('Ctrl Pts',(-2.00152977687848,1.61375869535139,15.4304147544343));
#69276=CARTESIAN_POINT('Ctrl Pts',(-2.04493641973501,1.53706478161179,15.4432963377886));
#69277=CARTESIAN_POINT('Ctrl Pts',(-2.08435494788096,1.4582510974481,15.45617771612));
#69278=CARTESIAN_POINT('Ctrl Pts',(-2.1059680281026,1.41503775188416,15.4632405435856));
#69279=CARTESIAN_POINT('Ctrl Pts',(-2.12638166130199,1.37118763733681,15.470303805537));
#69280=CARTESIAN_POINT('Ctrl Pts',(-2.14554686211721,1.32675413515881,15.4773728232848));
#69281=CARTESIAN_POINT('Ctrl Pts',(-2.15238081888792,1.31090996864141,15.479893504501));
#69282=CARTESIAN_POINT('Ctrl Pts',(-2.15905601977847,1.29499164910449,15.4824149433682));
#69283=CARTESIAN_POINT('Ctrl Pts',(-2.16557018945707,1.27900167913697,15.484937467835));
#69284=CARTESIAN_POINT('Ctrl Pts',(-2.1701386561413,1.26778771808245,15.4867065450244));
#69285=CARTESIAN_POINT('Ctrl Pts',(-2.17462683200284,1.25654108535781,15.4884757499118));
#69286=CARTESIAN_POINT('Ctrl Pts',(-2.1790311425866,1.2452704312927,15.4902440024149));
#69287=CARTESIAN_POINT('Ctrl Pts',(-2.21002477719553,1.1659575564956,15.5026873964345));
#69288=CARTESIAN_POINT('Ctrl Pts',(-2.2369126125938,1.08534359103648,15.5150992820502));
#69289=CARTESIAN_POINT('Ctrl Pts',(-2.25954646256793,1.00373624547512,15.5275444054577));
#69290=CARTESIAN_POINT('Ctrl Pts',(-2.28183631964793,0.923369181483772,
15.5398003858769));
#69291=CARTESIAN_POINT('Ctrl Pts',(-2.30000078071459,0.842038814791743,
15.5520888107296));
#69292=CARTESIAN_POINT('Ctrl Pts',(-2.31387996442088,0.760032592464827,
15.5644938859947));
#69293=CARTESIAN_POINT('Ctrl Pts',(-2.32735702168778,0.680402365073205,
15.5765395446794));
#69294=CARTESIAN_POINT('Ctrl Pts',(-2.33679399591497,0.600134965111233,
15.588695508872));
#69295=CARTESIAN_POINT('Ctrl Pts',(-2.34202168375654,0.519485938537849,
15.601056230854));
#69296=CARTESIAN_POINT('Ctrl Pts',(-2.3458041924598,0.46113210139823,15.6099998671025));
#69297=CARTESIAN_POINT('Ctrl Pts',(-2.34738263953659,0.402578305857887,
15.6190510917899));
#69298=CARTESIAN_POINT('Ctrl Pts',(-2.34668236863854,0.343918483395395,
15.62825));
#69299=CARTESIAN_POINT('',(-2.86810422470753,0.00112209329583249,15.1318955557932));
#69300=CARTESIAN_POINT('Ctrl Pts',(-2.86810422470753,0.00112209329583249,
15.1318955557932));
#69301=CARTESIAN_POINT('Ctrl Pts',(-2.87043208924124,0.0628907887003932,
15.1295435255677));
#69302=CARTESIAN_POINT('Ctrl Pts',(-2.87069405598972,0.124617231014218,
15.1272626996305));
#69303=CARTESIAN_POINT('Ctrl Pts',(-2.86887882812214,0.18622628149455,15.1250833127955));
#69304=CARTESIAN_POINT('Ctrl Pts',(-2.86624429184131,0.27564275730815,15.121920253331));
#69305=CARTESIAN_POINT('Ctrl Pts',(-2.85923588778213,0.364817170574697,
15.1189701933795));
#69306=CARTESIAN_POINT('Ctrl Pts',(-2.84798023700843,0.453530392715298,
15.1161343222149));
#69307=CARTESIAN_POINT('Ctrl Pts',(-2.84725382473312,0.459255727912805,
15.1159513019998));
#69308=CARTESIAN_POINT('Ctrl Pts',(-2.84650970988206,0.464979155137534,
15.1157687573921));
#69309=CARTESIAN_POINT('Ctrl Pts',(-2.84574792123122,0.470700620581005,
15.115586661831));
#69310=CARTESIAN_POINT('Ctrl Pts',(-2.83292253676448,0.56702654240334,15.1125209223));
#69311=CARTESIAN_POINT('Ctrl Pts',(-2.81509017073285,0.662792526882216,
15.1095819301958));
#69312=CARTESIAN_POINT('Ctrl Pts',(-2.79237326851397,0.75767385608828,15.1066596911336));
#69313=CARTESIAN_POINT('Ctrl Pts',(-2.77861012505902,0.815158161495671,
15.1048892386733));
#69314=CARTESIAN_POINT('Ctrl Pts',(-2.76305343525744,0.87231684260555,15.1031252999957));
#69315=CARTESIAN_POINT('Ctrl Pts',(-2.74572684796513,0.929069661288577,
15.1013474925125));
#69316=CARTESIAN_POINT('Ctrl Pts',(-2.73593206408982,0.961152239579201,
15.1003424913674));
#69317=CARTESIAN_POINT('Ctrl Pts',(-2.72557164273762,0.993105009075931,
15.0993331185811));
#69318=CARTESIAN_POINT('Ctrl Pts',(-2.71464968609205,1.02491266185944,15.0983161987151));
#69319=CARTESIAN_POINT('Ctrl Pts',(-2.7095518477653,1.03975892766194,15.0978415499652));
#69320=CARTESIAN_POINT('Ctrl Pts',(-2.70433399449945,1.05456668921369,15.0973654813685));
#69321=CARTESIAN_POINT('Ctrl Pts',(-2.69899954771354,1.06932740672487,15.0968879351064));
#69322=CARTESIAN_POINT('Ctrl Pts',(-2.66530865040951,1.16255203483741,15.0938718843853));
#69323=CARTESIAN_POINT('Ctrl Pts',(-2.62693751439746,1.25398885395718,15.0907912075745));
#69324=CARTESIAN_POINT('Ctrl Pts',(-2.58413151251978,1.34326828686256,15.0875945741555));
#69325=CARTESIAN_POINT('Ctrl Pts',(-2.54084885367928,1.43354187155657,15.0843623453175));
#69326=CARTESIAN_POINT('Ctrl Pts',(-2.49303197702603,1.52160928443245,15.0810114657988));
#69327=CARTESIAN_POINT('Ctrl Pts',(-2.44092724967875,1.60708697826089,15.0775259806253));
#69328=CARTESIAN_POINT('Ctrl Pts',(-2.38908958411024,1.69212655781216,15.0740583602391));
#69329=CARTESIAN_POINT('Ctrl Pts',(-2.33300828307443,1.77460269145118,15.070457600858));
#69330=CARTESIAN_POINT('Ctrl Pts',(-2.27291614853868,1.85414146323808,15.0667444052748));
#69331=CARTESIAN_POINT('Ctrl Pts',(-2.23194216665565,1.90837518649277,15.0642125529829));
#69332=CARTESIAN_POINT('Ctrl Pts',(-2.18910328969542,1.96124339077654,15.0616291892213));
#69333=CARTESIAN_POINT('Ctrl Pts',(-2.14446881854968,2.0126287210334,15.0590102206127));
#69334=CARTESIAN_POINT('Ctrl Pts',(-2.86750655814837,1.78005205161276E-11,
15.1324934418516));
#69335=CARTESIAN_POINT('Ctrl Pts',(-2.8675210427035,0.000387639407476004,
15.1324789572965));
#69336=CARTESIAN_POINT('Ctrl Pts',(-2.8675354467886,0.0007752834867927,
15.1324644746078));
#69337=CARTESIAN_POINT('Ctrl Pts',(-2.8675497703958,0.00116293222919048,
15.1324499937912));
#69338=CARTESIAN_POINT('',(-2.,-2.44929359829471E-16,16.));
#69339=CARTESIAN_POINT('',(-2.5,3.06161699786838E-16,15.5));
#69340=CARTESIAN_POINT('Origin',(0.,0.,16.));
#69341=CARTESIAN_POINT('Ctrl Pts',(1.70912691251745,-2.39920179129963,-0.331459347220305));
#69342=CARTESIAN_POINT('Ctrl Pts',(2.50276811089229,-1.8338774509613,-0.278813689627446));
#69343=CARTESIAN_POINT('Ctrl Pts',(3.47164055573234,0.135559128113983,-0.173547661664216));
#69344=CARTESIAN_POINT('Ctrl Pts',(1.7822571658123,2.98575720466778,-0.0156612633306156));
#69345=CARTESIAN_POINT('Ctrl Pts',(-1.52260497856303,3.12258994484077,0.142199847780495));
#69346=CARTESIAN_POINT('Ctrl Pts',(-3.44759473877435,0.435419189166611,
0.300060958891607));
#69347=CARTESIAN_POINT('Ctrl Pts',(-2.25033077153724,-2.64835158515141,
0.457922070002716));
#69348=CARTESIAN_POINT('Ctrl Pts',(0.985382290881231,-3.33221894822028,
0.615783181113829));
#69349=CARTESIAN_POINT('Ctrl Pts',(3.32847435827679,-0.998535563052339,
0.77364429222494));
#69350=CARTESIAN_POINT('Ctrl Pts',(2.65685902325779,2.23988877671352,0.93150540333605));
#69351=CARTESIAN_POINT('Ctrl Pts',(-0.421236688919228,3.44936780038012,
1.08936651444716));
#69352=CARTESIAN_POINT('Ctrl Pts',(-3.11778136245101,1.534669043428,1.24722762555827));
#69353=CARTESIAN_POINT('Ctrl Pts',(-2.99040402529488,-1.77010166332876,
1.40508873666939));
#69354=CARTESIAN_POINT('Ctrl Pts',(-0.154463996640659,-3.47157902841105,
1.5629498477805));
#69355=CARTESIAN_POINT('Ctrl Pts',(2.82137950689542,-2.02868629898774,1.72081095889161));
#69356=CARTESIAN_POINT('Ctrl Pts',(3.24175982869864,1.25169549534852,1.87867207000272));
#69357=CARTESIAN_POINT('Ctrl Pts',(0.725915687453796,3.39835072617039,2.03653318111383));
#69358=CARTESIAN_POINT('Ctrl Pts',(-2.44742623153422,2.46695170965159,2.19439429222494));
#69359=CARTESIAN_POINT('Ctrl Pts',(-3.40401210913808,-0.698889657279975,
2.35225540333606));
#69360=CARTESIAN_POINT('Ctrl Pts',(-1.27741406313663,-3.23171125442164,
2.51011651444716));
#69361=CARTESIAN_POINT('Ctrl Pts',(2.00620167327619,-2.83741076670449,2.66797762555828));
#69362=CARTESIAN_POINT('Ctrl Pts',(3.47270034769341,0.126874545576242,2.82583873666938));
#69363=CARTESIAN_POINT('Ctrl Pts',(1.79380080602483,2.97624317288409,2.9836998477805));
#69364=CARTESIAN_POINT('Ctrl Pts',(-1.50983373834399,3.12987970032478,3.14156095889161));
#69365=CARTESIAN_POINT('Ctrl Pts',(-3.44593643717389,0.448627793146361,
3.29942207000272));
#69366=CARTESIAN_POINT('Ctrl Pts',(-2.26088234184521,-2.63896870992823,
3.45728318111383));
#69367=CARTESIAN_POINT('Ctrl Pts',(0.971965844637692,-3.33631941315407,
3.61514429222494));
#69368=CARTESIAN_POINT('Ctrl Pts',(3.32445600610991,-1.01179893649521,3.77300540333605));
#69369=CARTESIAN_POINT('Ctrl Pts',(2.66582027065906,2.22915838561566,3.93086651444717));
#69370=CARTESIAN_POINT('Ctrl Pts',(-0.40738206985568,3.45105558846889,4.08872762555827));
#69371=CARTESIAN_POINT('Ctrl Pts',(-3.11159811670885,1.54715932752985,4.24658873666939));
#69372=CARTESIAN_POINT('Ctrl Pts',(-2.99748429181114,-1.75807643320396,
4.4044498477805));
#69373=CARTESIAN_POINT('Ctrl Pts',(-0.168399187629091,-3.47093453388311,
4.56231095889161));
#69374=CARTESIAN_POINT('Ctrl Pts',(2.81321347412892,-2.03999381708313,4.72017207000272));
#69375=CARTESIAN_POINT('Ctrl Pts',(3.24675814243868,1.2386712192005,4.87803318111383));
#69376=CARTESIAN_POINT('Ctrl Pts',(0.739551751054495,3.39540984747235,5.03589429222495));
#69377=CARTESIAN_POINT('Ctrl Pts',(-2.43750360973441,2.47675614005708,5.19375540333605));
#69378=CARTESIAN_POINT('Ctrl Pts',(-3.40679017196424,-0.68521934370669,
5.35161651444717));
#69379=CARTESIAN_POINT('Ctrl Pts',(-1.290376670055,-3.2265574338858,5.50947762555827));
#69380=CARTESIAN_POINT('Ctrl Pts',(1.99479544995775,-2.84544125534347,5.66733873666938));
#69381=CARTESIAN_POINT('Ctrl Pts',(3.47318166970145,0.112933228207418,5.8251998477805));
#69382=CARTESIAN_POINT('Ctrl Pts',(1.80573372884392,2.96901844475568,5.98306095889161));
#69383=CARTESIAN_POINT('Ctrl Pts',(-1.49725746582663,3.13591532184942,6.14092207000272));
#69384=CARTESIAN_POINT('Ctrl Pts',(-3.44410776976812,0.462457019631576,
6.29878318111384));
#69385=CARTESIAN_POINT('Ctrl Pts',(-2.27145759682837,-2.62987170991179,
6.45664429222494));
#69386=CARTESIAN_POINT('Ctrl Pts',(0.958565205016858,-3.34019424173425,
6.61450540333606));
#69387=CARTESIAN_POINT('Ctrl Pts',(3.32036761015448,-1.02513597060133,6.77236651444716));
#69388=CARTESIAN_POINT('Ctrl Pts',(2.67474718310955,2.21843916554662,6.93022762555828));
#69389=CARTESIAN_POINT('Ctrl Pts',(-0.393525399738489,3.45266311483532,
7.08808873666939));
#69390=CARTESIAN_POINT('Ctrl Pts',(-3.10536236726555,1.55963758378497,7.2459498477805));
#69391=CARTESIAN_POINT('Ctrl Pts',(-3.00451749289248,-1.74602962737945,
7.4038109588916));
#69392=CARTESIAN_POINT('Ctrl Pts',(-0.182331017612658,-3.47023057228191,
7.56167207000273));
#69393=CARTESIAN_POINT('Ctrl Pts',(2.80500176969189,-2.05127031295465,7.71953318111383));
#69394=CARTESIAN_POINT('Ctrl Pts',(3.25170431452417,1.22562795157771,7.87739429222495));
#69395=CARTESIAN_POINT('Ctrl Pts',(0.753175804487954,3.39241374721859,8.03525540333604));
#69396=CARTESIAN_POINT('Ctrl Pts',(-2.42754166081253,2.48652092486737,8.19311651444717));
#69397=CARTESIAN_POINT('Ctrl Pts',(-3.4095133623985,-0.671538127294123,
8.35097762555827));
#69398=CARTESIAN_POINT('Ctrl Pts',(-1.30331847021638,-3.22135154709579,
8.50883873666939));
#69399=CARTESIAN_POINT('Ctrl Pts',(1.98335707505572,-2.85342592993231,8.6666998477805));
#69400=CARTESIAN_POINT('Ctrl Pts',(3.47360702767608,0.0989901109348193,
8.82456095889161));
#69401=CARTESIAN_POINT('Ctrl Pts',(1.81763755172645,2.96174586271981,8.98242207000272));
#69402=CARTESIAN_POINT('Ctrl Pts',(-1.48465706514355,3.14190041594302,9.14028318111382));
#69403=CARTESIAN_POINT('Ctrl Pts',(-3.44222360370688,0.476278791115081,
9.29814429222495));
#69404=CARTESIAN_POINT('Ctrl Pts',(-2.28199624872525,-2.62073233001576,
9.45600540333604));
#69405=CARTESIAN_POINT('Ctrl Pts',(0.945149118703501,-3.34401524640603,
9.61386651444717));
#69406=CARTESIAN_POINT('Ctrl Pts',(3.31622570907301,-1.03845648501127,9.77172762555827));
#69407=CARTESIAN_POINT('Ctrl Pts',(2.68363099400492,2.20768419680356,9.92958873666939));
#69408=CARTESIAN_POINT('Ctrl Pts',(-0.379662388241621,3.45421500426974,
10.0874498477804));
#69409=CARTESIAN_POINT('Ctrl Pts',(-3.09907657727214,1.57209070761236,10.2453109588916));
#69410=CARTESIAN_POINT('Ctrl Pts',(-3.01150227846558,-1.73395468559392,
10.4031720700027));
#69411=CARTESIAN_POINT('Ctrl Pts',(-0.19625990944859,-3.46947069054991,
10.5610331811138));
#69412=CARTESIAN_POINT('Ctrl Pts',(2.79674486473763,-2.06251375419229,10.7188942922249));
#69413=CARTESIAN_POINT('Ctrl Pts',(3.25659808795613,1.21256493395727,10.876755403336));
#69414=CARTESIAN_POINT('Ctrl Pts',(0.766787720893258,3.38936298066535,11.0346165144471));
#69415=CARTESIAN_POINT('Ctrl Pts',(-2.41754059357168,2.49624564153576,11.1924776255582));
#69416=CARTESIAN_POINT('Ctrl Pts',(-3.41218161174795,-0.657846090039483,
11.3503387366693));
#69417=CARTESIAN_POINT('Ctrl Pts',(-1.31623926718511,-3.21609374974792,
11.5081998477805));
#69418=CARTESIAN_POINT('Ctrl Pts',(1.97188673755754,-2.86136462550139,11.6660609588915));
#69419=CARTESIAN_POINT('Ctrl Pts',(3.47397641551634,0.0850454018936421,
11.8239220700027));
#69420=CARTESIAN_POINT('Ctrl Pts',(1.82951207635102,2.95442554793994,11.9817831811138));
#69421=CARTESIAN_POINT('Ctrl Pts',(-1.47203272427312,3.14783489304223,12.1396442922249));
#69422=CARTESIAN_POINT('Ctrl Pts',(-3.44028399952346,0.490092864148866,
12.297505403336));
#69423=CARTESIAN_POINT('Ctrl Pts',(-2.29249806934856,-2.61155067396514,
12.4553665144471));
#69424=CARTESIAN_POINT('Ctrl Pts',(0.931717690008006,-3.3477824508677,12.6132276255582));
#69425=CARTESIAN_POINT('Ctrl Pts',(3.3120305835413,-1.05176010108855,12.7710887366694));
#69426=CARTESIAN_POINT('Ctrl Pts',(2.69247115139201,2.19689333884833,12.9289498477804));
#69427=CARTESIAN_POINT('Ctrl Pts',(-0.365792477741649,3.45571183163002,
13.0868109588916));
#69428=CARTESIAN_POINT('Ctrl Pts',(-3.09274234008898,1.58451735220887,13.2446720700027));
#69429=CARTESIAN_POINT('Ctrl Pts',(-3.01843568553144,-1.72184961279198,
13.4025331811139));
#69430=CARTESIAN_POINT('Ctrl Pts',(-0.210191084142041,-3.4686590840217,
13.5603942922249));
#69431=CARTESIAN_POINT('Ctrl Pts',(2.78845329525541,-2.07371596827588,13.718255403336));
#69432=CARTESIAN_POINT('Ctrl Pts',(3.26141951023774,1.19946711027502,13.8761165144471));
#69433=CARTESIAN_POINT('Ctrl Pts',(0.780425247323911,3.38628676205265,14.0339776255582));
#69434=CARTESIAN_POINT('Ctrl Pts',(-2.40757310028838,2.50587441647701,14.1918387366693));
#69435=CARTESIAN_POINT('Ctrl Pts',(-3.41465630905069,-0.64403700912367,
14.3496998477805));
#69436=CARTESIAN_POINT('Ctrl Pts',(-1.3294036198624,-3.21098749848051,14.5075609588917));
#69437=CARTESIAN_POINT('Ctrl Pts',(1.96089086179741,-2.86886848447928,14.6654220700027));
#69438=CARTESIAN_POINT('Ctrl Pts',(3.47331888567816,0.0703548346390749,
14.8232831811138));
#69439=CARTESIAN_POINT('Ctrl Pts',(1.84324590483098,2.94849643456436,14.9811442922249));
#69440=CARTESIAN_POINT('Ctrl Pts',(-1.46382348530112,3.15085562308053,15.1390307759807));
#69441=CARTESIAN_POINT('Ctrl Pts',(-2.77399534817744,1.38993107123141,15.244296889366));
#69442=CARTESIAN_POINT('Ctrl Pts',(-2.91479286562129,0.42575414026495,15.2969426323811));
#69443=CARTESIAN_POINT('Ctrl Pts',(1.59731828398619,-2.24224945505684,-0.220201080228989));
#69444=CARTESIAN_POINT('Ctrl Pts',(2.33904061472963,-1.71390782133067,-0.16755542263613));
#69445=CARTESIAN_POINT('Ctrl Pts',(3.24453081540399,0.126691044598195,-0.0622893946728999));
#69446=CARTESIAN_POINT('Ctrl Pts',(1.66566446111606,2.79043325550034,0.0955970036607006));
#69447=CARTESIAN_POINT('Ctrl Pts',(-1.42299834712965,2.91831459428533,0.253458114771811));
#69448=CARTESIAN_POINT('Ctrl Pts',(-3.22205804126471,0.406934691017055,
0.411319225882923));
#69449=CARTESIAN_POINT('Ctrl Pts',(-2.10311736364774,-2.47510022714181,
0.569180336994034));
#69450=CARTESIAN_POINT('Ctrl Pts',(0.920919996293564,-3.11422996926394,
0.727041448105144));
#69451=CARTESIAN_POINT('Ctrl Pts',(3.11073034501781,-0.933212800285599,
0.884902559216257));
#69452=CARTESIAN_POINT('Ctrl Pts',(2.48305112086282,2.09335846913207,1.04276367032736));
#69453=CARTESIAN_POINT('Ctrl Pts',(-0.393679989571658,3.22371511172612,
1.20062478143848));
#69454=CARTESIAN_POINT('Ctrl Pts',(-2.91382058245102,1.43427319819356,1.35848589254958));
#69455=CARTESIAN_POINT('Ctrl Pts',(-2.79477608779421,-1.65430415415129,
1.5163470036607));
#69456=CARTESIAN_POINT('Ctrl Pts',(-0.144359183770769,-3.24447331311172,
1.67420811477181));
#69457=CARTESIAN_POINT('Ctrl Pts',(2.63680891069109,-1.89597255423958,1.83206922588292));
#69458=CARTESIAN_POINT('Ctrl Pts',(3.02968855545379,1.16981137331599,1.98993033699403));
#69459=CARTESIAN_POINT('Ctrl Pts',(0.678427325501767,3.17603550125726,2.14779144810514));
#69460=CARTESIAN_POINT('Ctrl Pts',(-2.28731912165539,2.30556727103035,2.30565255921625));
#69461=CARTESIAN_POINT('Ctrl Pts',(-3.18132652468021,-0.653169299416062,
2.46351367032736));
#69462=CARTESIAN_POINT('Ctrl Pts',(-1.1938474693279,-3.02029734447755,2.62137478143847));
#69463=CARTESIAN_POINT('Ctrl Pts',(1.87495884045709,-2.65179142850224,2.77923589254959));
#69464=CARTESIAN_POINT('Ctrl Pts',(3.2455212772967,0.118574594980136,2.9370970036607));
#69465=CARTESIAN_POINT('Ctrl Pts',(1.67645293296106,2.781541618015,3.09495811477181));
#69466=CARTESIAN_POINT('Ctrl Pts',(-1.41106258310788,2.92512746443273,3.25281922588292));
#69467=CARTESIAN_POINT('Ctrl Pts',(-3.22050822337385,0.419279207090299,
3.41068033699403));
#69468=CARTESIAN_POINT('Ctrl Pts',(-2.11297866537686,-2.46633116614313,
3.56854144810514));
#69469=CARTESIAN_POINT('Ctrl Pts',(0.908381234698991,-3.1180621876695,3.72640255921625));
#69470=CARTESIAN_POINT('Ctrl Pts',(3.10697486767988,-0.94560850288233,3.88426367032737));
#69471=CARTESIAN_POINT('Ctrl Pts',(2.4914261363263,2.08333004481237,4.04212478143847));
#69472=CARTESIAN_POINT('Ctrl Pts',(-0.380731719793802,3.22529248714156,
4.19998589254959));
#69473=CARTESIAN_POINT('Ctrl Pts',(-2.90804183576698,1.44594638584389,4.3578470036607));
#69474=CARTESIAN_POINT('Ctrl Pts',(-2.80139317344133,-1.64306559731458,
4.5157081147718));
#69475=CARTESIAN_POINT('Ctrl Pts',(-0.157382754573871,-3.24387098049039,
4.67356922588293));
#69476=CARTESIAN_POINT('Ctrl Pts',(2.62917708806279,-1.9065403507373,4.83143033699403));
#69477=CARTESIAN_POINT('Ctrl Pts',(3.03435988668589,1.15763912661238,4.98929144810515));
#69478=CARTESIAN_POINT('Ctrl Pts',(0.691171337401332,3.17328701062093,5.14715255921625));
#69479=CARTESIAN_POINT('Ctrl Pts',(-2.27804562352611,2.31473030967662,5.30501367032737));
#69480=CARTESIAN_POINT('Ctrl Pts',(-3.18392285062523,-0.64039327812794,
5.46287478143848));
#69481=CARTESIAN_POINT('Ctrl Pts',(-1.2059620811143,-3.01548067948094,5.62073589254959));
#69482=CARTESIAN_POINT('Ctrl Pts',(1.86429879589028,-2.6592965741052,5.77859700366071));
#69483=CARTESIAN_POINT('Ctrl Pts',(3.2459711119101,0.105545298575644,5.93645811477181));
#69484=CARTESIAN_POINT('Ctrl Pts',(1.68760522110346,2.77478952122698,6.09431922588292));
#69485=CARTESIAN_POINT('Ctrl Pts',(-1.39930903228071,2.93076824426359,6.25218033699404));
#69486=CARTESIAN_POINT('Ctrl Pts',(-3.21879918476404,0.43220374543584,6.41004144810514));
#69487=CARTESIAN_POINT('Ctrl Pts',(-2.12286210236372,-2.45782927880566,
6.56790255921625));
#69488=CARTESIAN_POINT('Ctrl Pts',(0.895857245680565,-3.12168353052771,
6.72576367032737));
#69489=CARTESIAN_POINT('Ctrl Pts',(3.10315392871742,-0.958073047367486,
6.88362478143849));
#69490=CARTESIAN_POINT('Ctrl Pts',(2.49976906298218,2.07331206072884,7.04148589254958));
#69491=CARTESIAN_POINT('Ctrl Pts',(-0.367781533139289,3.2267948514413,7.1993470036607));
#69492=CARTESIAN_POINT('Ctrl Pts',(-2.90221402009851,1.45760833249197,7.3572081147718));
#69493=CARTESIAN_POINT('Ctrl Pts',(-2.80796627260669,-1.63180687622944,
7.51506922588292));
#69494=CARTESIAN_POINT('Ctrl Pts',(-0.170403184244221,-3.24321307104634,
7.67293033699403));
#69495=CARTESIAN_POINT('Ctrl Pts',(2.62150258153908,-1.9170791544405,7.83079144810515));
#69496=CARTESIAN_POINT('Ctrl Pts',(3.03898248729561,1.14544913082903,7.98865255921625));
#69497=CARTESIAN_POINT('Ctrl Pts',(0.703904124821557,3.17048691094375,8.14651367032737));
#69498=CARTESIAN_POINT('Ctrl Pts',(-2.26873537099862,2.32385629628559,8.30437478143848));
#69499=CARTESIAN_POINT('Ctrl Pts',(-3.18646789385143,-0.627607067248622,
8.46223589254958));
#69500=CARTESIAN_POINT('Ctrl Pts',(-1.21805724729189,-3.01061535432976,
8.62009700366071));
#69501=CARTESIAN_POINT('Ctrl Pts',(1.85360870305031,-2.6667589027474,8.77795811477182));
#69502=CARTESIAN_POINT('Ctrl Pts',(3.24636864357678,0.0925143200145056,
8.93581922588293));
#69503=CARTESIAN_POINT('Ctrl Pts',(1.69873031298536,2.7679927010654,9.09368033699404));
#69504=CARTESIAN_POINT('Ctrl Pts',(-1.38753293171776,2.93636180209542,9.25154144810513));
#69505=CARTESIAN_POINT('Ctrl Pts',(-3.2170382781411,0.445121316475167,9.40940255921626));
#69506=CARTESIAN_POINT('Ctrl Pts',(-2.13271133078565,-2.44928778401944,
9.56726367032736));
#69507=CARTESIAN_POINT('Ctrl Pts',(0.883318820470059,-3.12525457056035,
9.72512478143848));
#69508=CARTESIAN_POINT('Ctrl Pts',(3.09928298485748,-0.970522152851265,
9.88298589254958));
#69509=CARTESIAN_POINT('Ctrl Pts',(2.50807170772477,2.06326066659819,10.0408470036607));
#69510=CARTESIAN_POINT('Ctrl Pts',(-0.354825419949051,3.22824521849724,
10.1987081147718));
#69511=CARTESIAN_POINT('Ctrl Pts',(-2.8963394374609,1.46924679083965,10.3565692258829));
#69512=CARTESIAN_POINT('Ctrl Pts',(-2.81449412353686,-1.62052185979746,
10.514430336994));
#69513=CARTESIAN_POINT('Ctrl Pts',(-0.183420867976338,-3.24250289968617,
10.6722914481051));
#69514=CARTESIAN_POINT('Ctrl Pts',(2.61378583145108,-1.92758706589651,10.8301525592163));
#69515=CARTESIAN_POINT('Ctrl Pts',(3.04355611709647,1.1332406770645,10.9880136703274));
#69516=CARTESIAN_POINT('Ctrl Pts',(0.716625569200582,3.16763572115793,11.1458747814385));
#69517=CARTESIAN_POINT('Ctrl Pts',(-2.25938855921644,2.33294483595297,11.3037358925496));
#69518=CARTESIAN_POINT('Ctrl Pts',(-3.18896159015968,-0.61481074341118,
11.4615970036607));
#69519=CARTESIAN_POINT('Ctrl Pts',(-1.23013278427552,-3.00570151453487,
11.6194581147718));
#69520=CARTESIAN_POINT('Ctrl Pts',(1.84288873856135,-2.67417826025129,11.7773192258829));
#69521=CARTESIAN_POINT('Ctrl Pts',(3.24671386659492,0.0794818538159997,
11.935180336994));
#69522=CARTESIAN_POINT('Ctrl Pts',(1.70982802325928,2.76115127076741,12.0930414481051));
#69523=CARTESIAN_POINT('Ctrl Pts',(-1.37573445710014,2.94190805422394,12.2509025592163));
#69524=CARTESIAN_POINT('Ctrl Pts',(-3.21522556007834,0.458031692686313,
12.4087636703274));
#69525=CARTESIAN_POINT('Ctrl Pts',(-2.14252613738304,-2.440706778724,12.5666247814385));
#69526=CARTESIAN_POINT('Ctrl Pts',(0.870766056554023,-3.12877532991534,
12.7244858925496));
#69527=CARTESIAN_POINT('Ctrl Pts',(3.09536229841439,-0.982955465467049,
12.8823470036607));
#69528=CARTESIAN_POINT('Ctrl Pts',(2.51633355470891,2.05317573107611,13.0402081147718));
#69529=CARTESIAN_POINT('Ctrl Pts',(-0.341862859078587,3.22964412556086,
13.1980692258829));
#69530=CARTESIAN_POINT('Ctrl Pts',(-2.89041957697911,1.48086050218972,13.355930336994));
#69531=CARTESIAN_POINT('Ctrl Pts',(-2.82097395706795,-1.6092086834769,13.5137914481051));
#69532=CARTESIAN_POINT('Ctrl Pts',(-0.196440685224712,-3.24174438729166,
13.6716525592163));
#69533=CARTESIAN_POINT('Ctrl Pts',(2.60603668453876,-1.93805644721967,13.8295136703274));
#69534=CARTESIAN_POINT('Ctrl Pts',(3.04806212885536,1.12099969420077,13.9873747814385));
#69535=CARTESIAN_POINT('Ctrl Pts',(0.729370948233867,3.1647607443498,14.1452358925496));
#69536=CARTESIAN_POINT('Ctrl Pts',(-2.2500731250317,2.34194371026325,14.3030970036607));
#69537=CARTESIAN_POINT('Ctrl Pts',(-3.19127439631823,-0.601905032740824,
14.4609581147718));
#69538=CARTESIAN_POINT('Ctrl Pts',(-1.24243594390296,-3.00092930689345,
14.6188192258829));
#69539=CARTESIAN_POINT('Ctrl Pts',(1.83261219720478,-2.68119122754943,14.776680336994));
#69540=CARTESIAN_POINT('Ctrl Pts',(3.24609935141463,0.0657523223774665,
14.9345414481051));
#69541=CARTESIAN_POINT('Ctrl Pts',(1.72266340440009,2.75561003147542,15.0924025592163));
#69542=CARTESIAN_POINT('Ctrl Pts',(-1.36806225475429,2.94473117244051,15.2502890429721));
#69543=CARTESIAN_POINT('Ctrl Pts',(-2.5925245555989,1.29900377631302,15.3555551563574));
#69544=CARTESIAN_POINT('Ctrl Pts',(-2.72411130161863,0.397901915736784,
15.4082008993725));
#69545=CARTESIAN_POINT('Ctrl Pts',(1.48550965545491,-2.08529711881406,-0.108942813237673));
#69546=CARTESIAN_POINT('Ctrl Pts',(2.17531311856699,-1.59393819170005,-0.0562971556448137));
#69547=CARTESIAN_POINT('Ctrl Pts',(3.01742107507566,0.117822961082407,0.0489688723184162));
#69548=CARTESIAN_POINT('Ctrl Pts',(1.54907175641981,2.59510930633288,0.206855270652017));
#69549=CARTESIAN_POINT('Ctrl Pts',(-1.32339171569626,2.71403924372989,0.364716381763127));
#69550=CARTESIAN_POINT('Ctrl Pts',(-2.99652134375508,0.378450192867501,
0.52257749287424));
#69551=CARTESIAN_POINT('Ctrl Pts',(-1.95590395575824,-2.30184886913221,
0.680438603985348));
#69552=CARTESIAN_POINT('Ctrl Pts',(0.856457701705894,-2.8962409903076,0.838299715096462));
#69553=CARTESIAN_POINT('Ctrl Pts',(2.89298633175884,-0.86789003751886,0.996160826207572));
#69554=CARTESIAN_POINT('Ctrl Pts',(2.30924321846785,1.94682816155061,1.15402193731868));
#69555=CARTESIAN_POINT('Ctrl Pts',(-0.366123290224087,2.99806242307211,
1.31188304842979));
#69556=CARTESIAN_POINT('Ctrl Pts',(-2.70985980245103,1.33387735295911,1.46974415954091));
#69557=CARTESIAN_POINT('Ctrl Pts',(-2.59914815029355,-1.53850664497382,
1.62760527065202));
#69558=CARTESIAN_POINT('Ctrl Pts',(-0.134254370900873,-3.0173675978124,
1.78546638176313));
#69559=CARTESIAN_POINT('Ctrl Pts',(2.45223831448674,-1.76325880949142,1.94332749287424));
#69560=CARTESIAN_POINT('Ctrl Pts',(2.81761728220894,1.08792725128345,2.10118860398535));
#69561=CARTESIAN_POINT('Ctrl Pts',(0.630938963549732,2.95372027634413,2.25904971509646));
#69562=CARTESIAN_POINT('Ctrl Pts',(-2.12721201177655,2.14418283240911,2.41691082620757));
#69563=CARTESIAN_POINT('Ctrl Pts',(-2.95864094022234,-0.607448941552151,
2.57477193731869));
#69564=CARTESIAN_POINT('Ctrl Pts',(-1.11028087551918,-2.80888343453346,
2.73263304842979));
#69565=CARTESIAN_POINT('Ctrl Pts',(1.743716007638,-2.46617209029998,2.8904941595409));
#69566=CARTESIAN_POINT('Ctrl Pts',(3.01834220689999,0.110274644384027,3.04835527065202));
#69567=CARTESIAN_POINT('Ctrl Pts',(1.55910505989728,2.5868400631459,3.20621638176313));
#69568=CARTESIAN_POINT('Ctrl Pts',(-1.31229142787177,2.72037522854068,3.36407749287424));
#69569=CARTESIAN_POINT('Ctrl Pts',(-2.99508000957381,0.389930621034239,
3.52193860398535));
#69570=CARTESIAN_POINT('Ctrl Pts',(-1.9650749889085,-2.29369362235803,3.67979971509646));
#69571=CARTESIAN_POINT('Ctrl Pts',(0.844796624760288,-2.89980496218494,
3.83766082620758));
#69572=CARTESIAN_POINT('Ctrl Pts',(2.88949372924982,-0.879418069269448,
3.99552193731869));
#69573=CARTESIAN_POINT('Ctrl Pts',(2.31703200199353,1.93750170400908,4.1533830484298));
#69574=CARTESIAN_POINT('Ctrl Pts',(-0.354081369731924,2.99952938581424,
4.31124415954091));
#69575=CARTESIAN_POINT('Ctrl Pts',(-2.7044855548251,1.34473344415793,4.46910527065202));
#69576=CARTESIAN_POINT('Ctrl Pts',(-2.60530205507152,-1.52805476142519,
4.62696638176313));
#69577=CARTESIAN_POINT('Ctrl Pts',(-0.146366321518651,-3.01680742709766,
4.78482749287424));
#69578=CARTESIAN_POINT('Ctrl Pts',(2.44514070199668,-1.77308688439148,4.94268860398535));
#69579=CARTESIAN_POINT('Ctrl Pts',(2.8219616309331,1.07660703402426,5.10054971509647));
#69580=CARTESIAN_POINT('Ctrl Pts',(0.642790923748172,2.95116417376951,5.25841082620757));
#69581=CARTESIAN_POINT('Ctrl Pts',(-2.11858763731782,2.15270447929615,5.41627193731869));
#69582=CARTESIAN_POINT('Ctrl Pts',(-2.96105552928621,-0.595567212549187,
5.57413304842979));
#69583=CARTESIAN_POINT('Ctrl Pts',(-1.1215474921736,-2.80440392507609,5.73199415954091));
#69584=CARTESIAN_POINT('Ctrl Pts',(1.73380214182281,-2.47315189286694,5.88985527065202));
#69585=CARTESIAN_POINT('Ctrl Pts',(3.01876055411874,0.0981573689438738,
6.04771638176313));
#69586=CARTESIAN_POINT('Ctrl Pts',(1.569476713363,2.58056059769827,6.20557749287424));
#69587=CARTESIAN_POINT('Ctrl Pts',(-1.30136059873477,2.72562116667776,6.36343860398535));
#69588=CARTESIAN_POINT('Ctrl Pts',(-2.99349059975995,0.4019504712401,6.52129971509647));
#69589=CARTESIAN_POINT('Ctrl Pts',(-1.97426660789908,-2.28578684769951,
6.67916082620757));
#69590=CARTESIAN_POINT('Ctrl Pts',(0.833149286344271,-2.90317281932119,
6.83702193731869));
#69591=CARTESIAN_POINT('Ctrl Pts',(2.88594024728037,-0.891010124133642,
6.9948830484298));
#69592=CARTESIAN_POINT('Ctrl Pts',(2.3247909428548,1.92818495591104,7.15274415954091));
#69593=CARTESIAN_POINT('Ctrl Pts',(-0.342037666540088,3.00092658804729,
7.31060527065203));
#69594=CARTESIAN_POINT('Ctrl Pts',(-2.69906567293149,1.35557908119896,7.46846638176313));
#69595=CARTESIAN_POINT('Ctrl Pts',(-2.6114150523209,-1.51758412507944,7.62632749287424));
#69596=CARTESIAN_POINT('Ctrl Pts',(-0.158475350875785,-3.01619556981077,
7.78418860398534));
#69597=CARTESIAN_POINT('Ctrl Pts',(2.43800339338629,-1.78288799592635,7.94204971509647));
#69598=CARTESIAN_POINT('Ctrl Pts',(2.82626066006705,1.06527031008035,8.09991082620757));
#69599=CARTESIAN_POINT('Ctrl Pts',(0.65463244515516,2.94856007466891,8.2577719373187));
#69600=CARTESIAN_POINT('Ctrl Pts',(-2.10992908118473,2.1611916677038,8.41563304842979));
#69601=CARTESIAN_POINT('Ctrl Pts',(-2.96342242530435,-0.583676007203117,
8.57349415954092));
#69602=CARTESIAN_POINT('Ctrl Pts',(-1.13279602436738,-2.79987916156373,
8.73135527065201));
#69603=CARTESIAN_POINT('Ctrl Pts',(1.72386033104489,-2.48009187556249,8.88921638176315));
#69604=CARTESIAN_POINT('Ctrl Pts',(3.01913025947748,0.0860385290941875,
9.04707749287423));
#69605=CARTESIAN_POINT('Ctrl Pts',(1.57982307424428,2.574239539411,9.20493860398536));
#69606=CARTESIAN_POINT('Ctrl Pts',(-1.29040879829197,2.7308231882478,9.36279971509646));
#69607=CARTESIAN_POINT('Ctrl Pts',(-2.99185295257532,0.413963841835261,
9.52066082620758));
#69608=CARTESIAN_POINT('Ctrl Pts',(-1.98342641284605,-2.27784323802312,
9.67852193731868));
#69609=CARTESIAN_POINT('Ctrl Pts',(0.821488522236616,-2.90649389471465,
9.8363830484298));
#69610=CARTESIAN_POINT('Ctrl Pts',(2.88234026064193,-0.902587820691261,
9.9942441595409));
#69611=CARTESIAN_POINT('Ctrl Pts',(2.33251242144462,1.91883713639282,10.1521052706521));
#69612=CARTESIAN_POINT('Ctrl Pts',(-0.329988451656481,3.00227543272473,
10.3099663817632));
#69613=CARTESIAN_POINT('Ctrl Pts',(-2.69360229764966,1.36640287406693,10.4678274928743));
#69614=CARTESIAN_POINT('Ctrl Pts',(-2.61748596860813,-1.50708903400101,
10.6256886039854));
#69615=CARTESIAN_POINT('Ctrl Pts',(-0.170581826504084,-3.0155351088224,
10.7835497150965));
#69616=CARTESIAN_POINT('Ctrl Pts',(2.43082679816454,-1.79266037760072,10.9414108262076));
#69617=CARTESIAN_POINT('Ctrl Pts',(2.83051414623682,1.05391642017174,11.0992719373187));
#69618=CARTESIAN_POINT('Ctrl Pts',(0.666463417507903,2.94590846165049,11.2571330484298));
#69619=CARTESIAN_POINT('Ctrl Pts',(-2.10123652486119,2.16964403037017,11.414994159541));
#69620=CARTESIAN_POINT('Ctrl Pts',(-2.96574156857143,-0.571775396782877,
11.5728552706521));
#69621=CARTESIAN_POINT('Ctrl Pts',(-1.14402630136591,-2.79530927932181,
11.7307163817632));
#69622=CARTESIAN_POINT('Ctrl Pts',(1.71389073956514,-2.48699189500119,11.8885774928743));
#69623=CARTESIAN_POINT('Ctrl Pts',(3.01945131767349,0.0739183057383534,
12.0464386039854));
#69624=CARTESIAN_POINT('Ctrl Pts',(1.59014397016754,2.56787699359488,12.2042997150965));
#69625=CARTESIAN_POINT('Ctrl Pts',(-1.27943618992718,2.73598121540565,12.3621608262076));
#69626=CARTESIAN_POINT('Ctrl Pts',(-2.99016712063321,0.42597052122376,12.5200219373187));
#69627=CARTESIAN_POINT('Ctrl Pts',(-1.99255420541753,-2.26986288348284,
12.6778830484298));
#69628=CARTESIAN_POINT('Ctrl Pts',(0.809814423100042,-2.90976820896299,
12.8357441595409));
#69629=CARTESIAN_POINT('Ctrl Pts',(2.87869401328747,-0.914150829845545,
12.9936052706521));
#69630=CARTESIAN_POINT('Ctrl Pts',(2.34019595802583,1.9094581233039,13.1514663817632));
#69631=CARTESIAN_POINT('Ctrl Pts',(-0.317933240415524,3.00357641949169,
13.3093274928743));
#69632=CARTESIAN_POINT('Ctrl Pts',(-2.68809681386924,1.37720365217055,13.4671886039854));
#69633=CARTESIAN_POINT('Ctrl Pts',(-2.62351222860445,-1.49656775416184,
13.6250497150965));
#69634=CARTESIAN_POINT('Ctrl Pts',(-0.182690286307381,-3.01482969056162,
13.7829108262076));
#69635=CARTESIAN_POINT('Ctrl Pts',(2.42362007382213,-1.80239692616347,13.9407719373187));
#69636=CARTESIAN_POINT('Ctrl Pts',(2.83470474747299,1.04253227812653,14.0986330484299));
#69637=CARTESIAN_POINT('Ctrl Pts',(0.678316649143826,2.94323472664697,14.2564941595409));
#69638=CARTESIAN_POINT('Ctrl Pts',(-2.09257314977501,2.17801300404947,14.4143552706521));
#69639=CARTESIAN_POINT('Ctrl Pts',(-2.96789248358577,-0.559773056357977,
14.5722163817632));
#69640=CARTESIAN_POINT('Ctrl Pts',(-1.15546826794353,-2.79087111530639,
14.7300774928743));
#69641=CARTESIAN_POINT('Ctrl Pts',(1.70433353261215,-2.49351397061956,14.8879386039854));
#69642=CARTESIAN_POINT('Ctrl Pts',(3.01887981715109,0.0611498101158578,
15.0457997150965));
#69643=CARTESIAN_POINT('Ctrl Pts',(1.6020809039692,2.56272362838647,15.2036608262076));
#69644=CARTESIAN_POINT('Ctrl Pts',(-1.27230102420747,2.73860672180048,15.3615473099633));
#69645=CARTESIAN_POINT('Ctrl Pts',(-2.41105376302034,1.20807648139464,15.4668134233488));
#69646=CARTESIAN_POINT('Ctrl Pts',(-2.53342973761595,0.370049691208616,
15.5194591663637));
#69647=CARTESIAN_POINT('Ctrl Pts',(1.37370102692364,-1.92834478257128,0.00231545375364296));
#69648=CARTESIAN_POINT('Ctrl Pts',(2.01158562240434,-1.47396856206942,0.0549611113465025));
#69649=CARTESIAN_POINT('Ctrl Pts',(2.79031133474731,0.108954877566618,0.160227139309733));
#69650=CARTESIAN_POINT('Ctrl Pts',(1.43247905172356,2.39978535716542,0.318113537643333));
#69651=CARTESIAN_POINT('Ctrl Pts',(-1.22378508426288,2.50976389317445,0.475974648754443));
#69652=CARTESIAN_POINT('Ctrl Pts',(-2.77098464624544,0.349965694717946,
0.633835759865555));
#69653=CARTESIAN_POINT('Ctrl Pts',(-1.80869054786874,-2.1285975111226,0.791696870976666));
#69654=CARTESIAN_POINT('Ctrl Pts',(0.791995407118226,-2.67825201135127,
0.949557982087777));
#69655=CARTESIAN_POINT('Ctrl Pts',(2.67524231849987,-0.802567274752119,
1.10741909319888));
#69656=CARTESIAN_POINT('Ctrl Pts',(2.13543531607289,1.80029785396915,1.26528020430999));
#69657=CARTESIAN_POINT('Ctrl Pts',(-0.338566590876518,2.77240973441811,
1.42314131542111));
#69658=CARTESIAN_POINT('Ctrl Pts',(-2.50589902245105,1.23348150772466,1.58100242653222));
#69659=CARTESIAN_POINT('Ctrl Pts',(-2.40352021279288,-1.42270913579635,
1.73886353764333));
#69660=CARTESIAN_POINT('Ctrl Pts',(-0.12414955803098,-2.79026188251307,
1.89672464875444));
#69661=CARTESIAN_POINT('Ctrl Pts',(2.26766771828241,-1.63054506474326,2.05458575986555));
#69662=CARTESIAN_POINT('Ctrl Pts',(2.60554600896408,1.00604312925092,2.21244687097666));
#69663=CARTESIAN_POINT('Ctrl Pts',(0.583450601597702,2.731405051431,2.37030798208778));
#69664=CARTESIAN_POINT('Ctrl Pts',(-1.96710490189772,1.98279839378788,2.52816909319888));
#69665=CARTESIAN_POINT('Ctrl Pts',(-2.73595535576447,-0.561728583688241,
2.68603020431));
#69666=CARTESIAN_POINT('Ctrl Pts',(-1.02671428171045,-2.59746952458937,
2.8438913154211));
#69667=CARTESIAN_POINT('Ctrl Pts',(1.61247317481889,-2.28055275209774,3.00175242653222));
#69668=CARTESIAN_POINT('Ctrl Pts',(2.79116313650327,0.101974693787918,3.15961353764333));
#69669=CARTESIAN_POINT('Ctrl Pts',(1.44175718683351,2.39213850827682,3.31747464875444));
#69670=CARTESIAN_POINT('Ctrl Pts',(-1.21352027263567,2.51562299264861,3.47533575986556));
#69671=CARTESIAN_POINT('Ctrl Pts',(-2.76965179577376,0.360582034978182,
3.63319687097666));
#69672=CARTESIAN_POINT('Ctrl Pts',(-1.81717131244015,-2.12105607857293,
3.79105798208778));
#69673=CARTESIAN_POINT('Ctrl Pts',(0.781212014821587,-2.68154773670037,
3.94891909319888));
#69674=CARTESIAN_POINT('Ctrl Pts',(2.67201259081977,-0.813227635656568,
4.10678020431));
#69675=CARTESIAN_POINT('Ctrl Pts',(2.14263786766077,1.79167336320579,4.26464131542111));
#69676=CARTESIAN_POINT('Ctrl Pts',(-0.327431019670046,2.77376628448691,
4.42250242653222));
#69677=CARTESIAN_POINT('Ctrl Pts',(-2.50092927388322,1.24352050247198,4.58036353764333));
#69678=CARTESIAN_POINT('Ctrl Pts',(-2.4092109367017,-1.4130439255358,4.73822464875444));
#69679=CARTESIAN_POINT('Ctrl Pts',(-0.135349888463429,-2.78974387370495,
4.89608575986555));
#69680=CARTESIAN_POINT('Ctrl Pts',(2.26110431593055,-1.63963341804565,5.05394687097667));
#69681=CARTESIAN_POINT('Ctrl Pts',(2.6095633751803,0.995574941436156,5.21180798208777));
#69682=CARTESIAN_POINT('Ctrl Pts',(0.594410510095007,2.72904133691807,5.36966909319889));
#69683=CARTESIAN_POINT('Ctrl Pts',(-1.95912965110952,1.99067864891568,5.52753020430999));
#69684=CARTESIAN_POINT('Ctrl Pts',(-2.7381882079472,-0.550741146970434,
5.68539131542111));
#69685=CARTESIAN_POINT('Ctrl Pts',(-1.03713290323291,-2.59332717067123,
5.84325242653222));
#69686=CARTESIAN_POINT('Ctrl Pts',(1.60330548775534,-2.28700721162866,6.00111353764333));
#69687=CARTESIAN_POINT('Ctrl Pts',(2.79154999632737,0.0907694393121017,
6.15897464875444));
#69688=CARTESIAN_POINT('Ctrl Pts',(1.45134820562253,2.38633167416956,6.31683575986555));
#69689=CARTESIAN_POINT('Ctrl Pts',(-1.20341216518885,2.52047408909194,6.47469687097668));
#69690=CARTESIAN_POINT('Ctrl Pts',(-2.76818201475586,0.371697197044361,
6.63255798208777));
#69691=CARTESIAN_POINT('Ctrl Pts',(-1.82567111343442,-2.11374441659337,
6.79041909319889));
#69692=CARTESIAN_POINT('Ctrl Pts',(0.770441327007976,-2.68466210811466,
6.94828020430999));
#69693=CARTESIAN_POINT('Ctrl Pts',(2.66872656584332,-0.823947200899797,
7.10614131542111));
#69694=CARTESIAN_POINT('Ctrl Pts',(2.14981282272741,1.78305785109325,7.26400242653222));
#69695=CARTESIAN_POINT('Ctrl Pts',(-0.316293799940889,2.77505832465327,
7.42186353764333));
#69696=CARTESIAN_POINT('Ctrl Pts',(-2.49591732576446,1.25354982990597,7.57972464875445));
#69697=CARTESIAN_POINT('Ctrl Pts',(-2.41486383203512,-1.40336137392943,
7.73758575986554));
#69698=CARTESIAN_POINT('Ctrl Pts',(-0.146547517507347,-2.7891780685752,
7.89544687097668));
#69699=CARTESIAN_POINT('Ctrl Pts',(2.25450420523348,-1.64869683741221,8.05330798208776));
#69700=CARTESIAN_POINT('Ctrl Pts',(2.61353883283848,0.98509148933167,8.21116909319889));
#69701=CARTESIAN_POINT('Ctrl Pts',(0.605360765488762,2.72663323839408,8.36903020430999));
#69702=CARTESIAN_POINT('Ctrl Pts',(-1.95112279137082,1.99852703912202,8.52689131542112));
#69703=CARTESIAN_POINT('Ctrl Pts',(-2.74037695675728,-0.539744947157614,
8.68475242653222));
#69704=CARTESIAN_POINT('Ctrl Pts',(-1.04753480144288,-2.58914296879769,
8.84261353764335));
#69705=CARTESIAN_POINT('Ctrl Pts',(1.59411195903949,-2.29342484837757,9.00047464875443));
#69706=CARTESIAN_POINT('Ctrl Pts',(2.79189187537818,0.0795627381738728,
9.15833575986557));
#69707=CARTESIAN_POINT('Ctrl Pts',(1.46091583550319,2.38048637775659,9.31619687097666));
#69708=CARTESIAN_POINT('Ctrl Pts',(-1.19328466486618,2.5252845744002,9.47405798208777));
#69709=CARTESIAN_POINT('Ctrl Pts',(-2.76666762700954,0.38280636719535,9.63191909319889));
#69710=CARTESIAN_POINT('Ctrl Pts',(-1.83414149490645,-2.10639869202682,
9.78978020431));
#69711=CARTESIAN_POINT('Ctrl Pts',(0.759658224003173,-2.68773321886896,
9.94764131542111));
#69712=CARTESIAN_POINT('Ctrl Pts',(2.66539753642639,-0.834653488531258,
10.1055024265322));
#69713=CARTESIAN_POINT('Ctrl Pts',(2.15695313516446,1.77441360618746,10.2633635376433));
#69714=CARTESIAN_POINT('Ctrl Pts',(-0.305151483363911,2.77630564695223,
10.4212246487544));
#69715=CARTESIAN_POINT('Ctrl Pts',(-2.49086515783842,1.26355895729423,10.5790857598655));
#69716=CARTESIAN_POINT('Ctrl Pts',(-2.42047781367941,-1.39365620820457,
10.7369468709767));
#69717=CARTESIAN_POINT('Ctrl Pts',(-0.157742785031831,-2.78856731795865,
10.8948079820878));
#69718=CARTESIAN_POINT('Ctrl Pts',(2.247867764878,-1.65773368930495,11.0526690931989));
#69719=CARTESIAN_POINT('Ctrl Pts',(2.61747217537717,0.974592163278993,11.21053020431));
#69720=CARTESIAN_POINT('Ctrl Pts',(0.616301265815223,2.72418120214306,11.3683913154211));
#69721=CARTESIAN_POINT('Ctrl Pts',(-1.94308449050595,2.00634322478738,11.5262524265322));
#69722=CARTESIAN_POINT('Ctrl Pts',(-2.74252154698318,-0.528740050154576,
11.6841135376433));
#69723=CARTESIAN_POINT('Ctrl Pts',(-1.05791981845631,-2.58491704410876,
11.8419746487544));
#69724=CARTESIAN_POINT('Ctrl Pts',(1.58489274056894,-2.2998055297511,11.9998357598655));
#69725=CARTESIAN_POINT('Ctrl Pts',(2.79218876875207,0.0683547576607113,
12.1576968709766));
#69726=CARTESIAN_POINT('Ctrl Pts',(1.4704599170758,2.37460271642234,12.3155579820878));
#69727=CARTESIAN_POINT('Ctrl Pts',(-1.18313792275421,2.53005437658735,12.4734190931989));
#69728=CARTESIAN_POINT('Ctrl Pts',(-2.7651086811881,0.393909349761204,12.63128020431));
#69729=CARTESIAN_POINT('Ctrl Pts',(-1.84258227345201,-2.09901898824168,
12.7891413154211));
#69730=CARTESIAN_POINT('Ctrl Pts',(0.74886278964606,-2.69076108801064,12.9470024265322));
#69731=CARTESIAN_POINT('Ctrl Pts',(2.66202572816055,-0.845346194224041,
13.1048635376433));
#69732=CARTESIAN_POINT('Ctrl Pts',(2.16405836134274,1.76574051553168,13.2627246487544));
#69733=CARTESIAN_POINT('Ctrl Pts',(-0.294003621752462,2.77750871342253,
13.4205857598655));
#69734=CARTESIAN_POINT('Ctrl Pts',(-2.48577405075937,1.2735468021514,13.5784468709767));
#69735=CARTESIAN_POINT('Ctrl Pts',(-2.42605050014095,-1.38392682484676,
13.7363079820877));
#69736=CARTESIAN_POINT('Ctrl Pts',(-0.168939887390049,-2.78791499383159,
13.8941690931989));
#69737=CARTESIAN_POINT('Ctrl Pts',(2.24120346310549,-1.66673740510728,14.05203020431));
#69738=CARTESIAN_POINT('Ctrl Pts',(2.62134736609061,0.964064862052277,14.2098913154211));
#69739=CARTESIAN_POINT('Ctrl Pts',(0.627262350053781,2.72170870894412,14.3677524265322));
#69740=CARTESIAN_POINT('Ctrl Pts',(-1.93507317451832,2.0140822978357,14.5256135376433));
#69741=CARTESIAN_POINT('Ctrl Pts',(-2.74451057085332,-0.517641079975128,
14.6834746487544));
#69742=CARTESIAN_POINT('Ctrl Pts',(-1.06850059198409,-2.58081292371933,
14.8413357598655));
#69743=CARTESIAN_POINT('Ctrl Pts',(1.57605486801951,-2.30583671368971,14.9991968709767));
#69744=CARTESIAN_POINT('Ctrl Pts',(2.79166028288756,0.0565472978542511,
15.1570579820878));
#69745=CARTESIAN_POINT('Ctrl Pts',(1.4814984035383,2.36983722529753,15.3149190931989));
#69746=CARTESIAN_POINT('Ctrl Pts',(-1.17653979366064,2.53248227116047,15.4728055769547));
#69747=CARTESIAN_POINT('Ctrl Pts',(-2.2295829704418,1.11714918647624,15.57807169034));
#69748=CARTESIAN_POINT('Ctrl Pts',(-2.34274817361327,0.34219746668045,15.6307174333551));
#69749=CARTESIAN_POINT('Ctrl Pts',(1.29200104020317,2.64812001020929,3.10255293678452E-15));
#69750=CARTESIAN_POINT('Ctrl Pts',(1.36315737313149,2.60529414881161,2.09107015119386E-15));
#69751=CARTESIAN_POINT('Ctrl Pts',(1.43224767624703,2.55934891308958,1.31609841305187E-15));
#69752=CARTESIAN_POINT('Ctrl Pts',(1.49903325513989,2.51027466650741,1.66186508998578E-15));
#69753=CARTESIAN_POINT('Ctrl Pts',(1.57400867069288,2.45518250302776,1.95949932089937E-15));
#69754=CARTESIAN_POINT('Ctrl Pts',(1.64608024297622,2.39614668551523,1.83946245349909E-15));
#69755=CARTESIAN_POINT('Ctrl Pts',(1.71509586361607,2.3334939900483,1.70696790036118E-15));
#69756=CARTESIAN_POINT('Ctrl Pts',(1.74960367393599,2.30216764231483,1.64072062379222E-15));
#69757=CARTESIAN_POINT('Ctrl Pts',(1.78334695259876,2.26993667275488,1.11913045518732E-15));
#69758=CARTESIAN_POINT('Ctrl Pts',(1.81630324354019,2.23683999242427,1.31838984174237E-15));
#69759=CARTESIAN_POINT('Ctrl Pts',(1.83676158255619,2.21629450362181,1.44208446773989E-15));
#69760=CARTESIAN_POINT('Ctrl Pts',(1.85691660316518,2.19541538445973,1.46191677087001E-15));
#69761=CARTESIAN_POINT('Ctrl Pts',(1.87676245786726,2.17421177399615,2.54657406273395E-15));
#69762=CARTESIAN_POINT('Ctrl Pts',(1.88888624454376,2.16125853746939,3.20918869037616E-15));
#69763=CARTESIAN_POINT('Ctrl Pts',(1.90089366672971,2.1481851241337,1.96170375495304E-15));
#69764=CARTESIAN_POINT('Ctrl Pts',(1.91277473204615,2.1350036118777,1.54737334057131E-15));
#69765=CARTESIAN_POINT('Ctrl Pts',(1.9776543595374,2.06302255780864,-1.97990253103911E-15));
#69766=CARTESIAN_POINT('Ctrl Pts',(2.03884298327229,1.98774253915799,-1.66382442733107E-15));
#69767=CARTESIAN_POINT('Ctrl Pts',(2.09617256623861,1.90953752585601,-9.71445146547012E-16));
#69768=CARTESIAN_POINT('Ctrl Pts',(2.1535084707902,1.83132388908891,-2.78989518885305E-16));
#69769=CARTESIAN_POINT('Ctrl Pts',(2.20698482442042,1.75018364400972,1.25908428358211E-15));
#69770=CARTESIAN_POINT('Ctrl Pts',(2.25638533273427,1.66647271728721,-1.98452365651747E-15));
#69771=CARTESIAN_POINT('Ctrl Pts',(2.26598195715652,1.65021089425715,-2.61463229783777E-15));
#69772=CARTESIAN_POINT('Ctrl Pts',(2.27542461416388,1.63385203033854,-2.47328191587402E-15));
#69773=CARTESIAN_POINT('Ctrl Pts',(2.28471149018554,1.61739870311764,-1.85962356624714E-15));
#69774=CARTESIAN_POINT('Ctrl Pts',(2.29658165337844,1.59636863027905,-1.51468754041748E-15));
#69775=CARTESIAN_POINT('Ctrl Pts',(2.30819775718845,1.57518341353175,-2.25374764460409E-15));
#69776=CARTESIAN_POINT('Ctrl Pts',(2.319554459588,1.55385101519017,-2.52575738102223E-15));
#69777=CARTESIAN_POINT('Ctrl Pts',(2.32539410160174,1.54288184780102,-2.66562540160156E-15));
#69778=CARTESIAN_POINT('Ctrl Pts',(2.33116442149476,1.53187508817643,-2.94361108551474E-15));
#69779=CARTESIAN_POINT('Ctrl Pts',(2.33686168047272,1.52083799385098,-2.56739074444567E-15));
#69780=CARTESIAN_POINT('Ctrl Pts',(2.38042908971752,1.43643642333951,-3.13104787203378E-16));
#69781=CARTESIAN_POINT('Ctrl Pts',(2.41979213021192,1.3501422097958,-1.59953211202993E-15));
#69782=CARTESIAN_POINT('Ctrl Pts',(2.45479061001924,1.26230270075925,-1.83186799063151E-15));
#69783=CARTESIAN_POINT('Ctrl Pts',(2.48943950316612,1.17534058756353,-2.06188315346638E-15));
#69784=CARTESIAN_POINT('Ctrl Pts',(2.51981079469772,1.08686297282194,-1.65071434113658E-15));
#69785=CARTESIAN_POINT('Ctrl Pts',(2.54569935642937,0.997197819015192,-3.8441472227646E-15));
#69786=CARTESIAN_POINT('Ctrl Pts',(2.57084179381203,0.910116870356819,-5.97436401313909E-15));
#69787=CARTESIAN_POINT('Ctrl Pts',(2.59175618069638,0.82191508220806,-3.21503687969247E-15));
#69788=CARTESIAN_POINT('Ctrl Pts',(2.60820620752898,0.732896562075562,-4.85722573273506E-15));
#69789=CARTESIAN_POINT('Ctrl Pts',(2.61778223009678,0.681076381694317,-5.8131899799285E-15));
#69790=CARTESIAN_POINT('Ctrl Pts',(2.62584449121432,0.628979560875543,-2.63541690974722E-15));
#69791=CARTESIAN_POINT('Ctrl Pts',(2.63233843305125,0.576668196894127,-3.19189119579733E-15));
#69792=CARTESIAN_POINT('Ctrl Pts',(2.63414224296016,0.562137768524487,-3.34548576625677E-15));
#69793=CARTESIAN_POINT('Ctrl Pts',(2.63582527555606,0.547588319420663,-4.76400556623387E-15));
#69794=CARTESIAN_POINT('Ctrl Pts',(2.63738542604938,0.53302926152673,-4.71844785465692E-15));
#69795=CARTESIAN_POINT('Ctrl Pts',(2.64690685377399,0.444176924480302,-4.60028352020783E-15));
#69796=CARTESIAN_POINT('Ctrl Pts',(2.65183263786071,0.355196731306933,-1.12077890731655E-15));
#69797=CARTESIAN_POINT('Ctrl Pts',(2.65198717743402,0.26638198029663,-3.05311331771918E-15));
#69798=CARTESIAN_POINT('Ctrl Pts',(2.65207998114263,0.213047173580212,-3.85426492076651E-15));
#69799=CARTESIAN_POINT('Ctrl Pts',(2.65045121279154,0.159772024913009,-2.51411300564142E-15));
#69800=CARTESIAN_POINT('Ctrl Pts',(2.64705383408491,0.106621318043218,-3.10862446895044E-15));
#69801=CARTESIAN_POINT('Ctrl Pts',(2.64122335367285,0.0154056538352043,
-4.35916179998321E-15));
#69802=CARTESIAN_POINT('Ctrl Pts',(2.6301863282489,-0.0754450034552312,
-4.42204053305948E-15));
#69803=CARTESIAN_POINT('Ctrl Pts',(2.61414363949405,-0.165586435036926,
-3.66373598126302E-15));
#69804=CARTESIAN_POINT('Ctrl Pts',(2.5981009507392,-0.255727866618621,-2.90543142946655E-15));
#69805=CARTESIAN_POINT('Ctrl Pts',(2.57705193629621,-0.345160943019199,
-4.87329601145403E-15));
#69806=CARTESIAN_POINT('Ctrl Pts',(2.55115372858487,-0.433510589178545,
-1.60982338570648E-15));
#69807=CARTESIAN_POINT('Ctrl Pts',(2.54730992415644,-0.446623417870877,
-1.20154213111825E-15));
#69808=CARTESIAN_POINT('Ctrl Pts',(2.54335838534963,-0.4597150170452,-1.8738946464181E-15));
#69809=CARTESIAN_POINT('Ctrl Pts',(2.53930241226215,-0.472774949708627,
-1.97064586870965E-15));
#69810=CARTESIAN_POINT('Ctrl Pts',(2.51300579541806,-0.557448106520195,
-3.25376286445461E-15));
#69811=CARTESIAN_POINT('Ctrl Pts',(2.48237490705924,-0.640633082256515,
-3.13037515801062E-15));
#69812=CARTESIAN_POINT('Ctrl Pts',(2.44762844889866,-0.722031078368415,
-1.77635683940025E-15));
#69813=CARTESIAN_POINT('Ctrl Pts',(2.41285997251622,-0.80348065496454,-3.32163561638838E-16));
#69814=CARTESIAN_POINT('Ctrl Pts',(2.37397005509929,-0.883141781461181,
-2.97904560551731E-15));
#69815=CARTESIAN_POINT('Ctrl Pts',(2.33113438836156,-0.96068640220217,-3.02535774210355E-15));
#69816=CARTESIAN_POINT('Ctrl Pts',(2.28891526221294,-1.03711491083859,-3.47404387143521E-15));
#69817=CARTESIAN_POINT('Ctrl Pts',(2.24286247134769,-1.11148803976047,-3.0687412209896E-15));
#69818=CARTESIAN_POINT('Ctrl Pts',(2.19311210718949,-1.18345333934342,-1.33226762955019E-15));
#69819=CARTESIAN_POINT('Ctrl Pts',(2.1665899473663,-1.22181838871659,1.22294838671581E-16));
#69820=CARTESIAN_POINT('Ctrl Pts',(2.13901644806922,-1.25949841971484,-1.28609992312022E-16));
#69821=CARTESIAN_POINT('Ctrl Pts',(2.11040940577999,-1.29643454214332,-1.88737914186277E-15));
#69822=CARTESIAN_POINT('Ctrl Pts',(2.09658409753436,-1.31428515643645,-2.18989034168364E-15));
#69823=CARTESIAN_POINT('Ctrl Pts',(2.08251135224091,-1.33196908693401,-1.95637260965346E-15));
#69824=CARTESIAN_POINT('Ctrl Pts',(2.06822143203954,-1.34944529769313,-1.60982338570648E-15));
#69825=CARTESIAN_POINT('Ctrl Pts',(2.01420303007452,-1.41550843620673,-2.99806603525348E-16));
#69826=CARTESIAN_POINT('Ctrl Pts',(1.95704446263552,-1.47866336737798,-6.19616046821105E-16));
#69827=CARTESIAN_POINT('Ctrl Pts',(1.8969065179103,-1.53861547303735,-1.0547118733939E-15));
#69828=CARTESIAN_POINT('Ctrl Pts',(1.83769520508206,-1.59764381028979,-1.48310355214476E-15));
#69829=CARTESIAN_POINT('Ctrl Pts',(1.77559497936228,-1.65356778346114,2.20446172603681E-16));
#69830=CARTESIAN_POINT('Ctrl Pts',(1.71073303306612,-1.70606397784894,8.88178419700125E-16));
#69831=CARTESIAN_POINT('Ctrl Pts',(1.64789827301082,-1.75691946348473,1.5350414560931E-15));
#69832=CARTESIAN_POINT('Ctrl Pts',(1.58247114995395,-1.80455837340375,-6.98079953837882E-16));
#69833=CARTESIAN_POINT('Ctrl Pts',(1.51455134937916,-1.8486411040293,-4.9960036108132E-16));
#69834=CARTESIAN_POINT('Ctrl Pts',(1.46978363624784,-1.87769718225669,-3.68777281570644E-16));
#69835=CARTESIAN_POINT('Ctrl Pts',(1.42393267971699,-1.90520735301187,1.69235332884175E-16));
#69836=CARTESIAN_POINT('Ctrl Pts',(1.37702479013106,-1.93106208855762,-2.22044604925031E-16));
#69837=CARTESIAN_POINT('Ctrl Pts',(-1.03727419333506,2.12829183996564,-0.33162583102735));
#69838=CARTESIAN_POINT('Ctrl Pts',(-1.74153389301133,1.78505394459699,-0.278960867360666));
#69839=CARTESIAN_POINT('Ctrl Pts',(-2.77088494568995,0.350890813503785,
-0.173630940027297));
#69840=CARTESIAN_POINT('Ctrl Pts',(-1.80617750337226,-2.13380867727772,
-0.0156360490272432));
#69841=CARTESIAN_POINT('Ctrl Pts',(0.799331096145292,-2.67619672977392,
0.14235884197281));
#69842=CARTESIAN_POINT('Ctrl Pts',(2.6785330878346,-0.794154761772425,0.300353732972864));
#69843=CARTESIAN_POINT('Ctrl Pts',(2.12850244685976,1.81002105660491,0.458348623972918));
#69844=CARTESIAN_POINT('Ctrl Pts',(-0.352738835506404,2.771329446129,0.616343514972972));
#69845=CARTESIAN_POINT('Ctrl Pts',(-2.51382108425654,1.21907270575297,0.774338405973023));
#69846=CARTESIAN_POINT('Ctrl Pts',(-2.39456021962358,-1.43931956546868,
0.932333296973079));
#69847=CARTESIAN_POINT('Ctrl Pts',(-0.103009617793377,-2.79189425785633,
1.09032818797313));
#69848=CARTESIAN_POINT('Ctrl Pts',(2.28196265616274,-1.61184802118412,1.24832307897318));
#69849=CARTESIAN_POINT('Ctrl Pts',(2.59684801618063,1.03043335678079,1.40631796997323));
#69850=CARTESIAN_POINT('Ctrl Pts',(0.555976476186501,2.73793099838751,1.56431286097329));
#69851=CARTESIAN_POINT('Ctrl Pts',(-1.98924983312574,1.96170350529848,1.72230775197334));
#69852=CARTESIAN_POINT('Ctrl Pts',(-2.72991498642861,-0.594103134059335,
1.8803026429734));
#69853=CARTESIAN_POINT('Ctrl Pts',(-0.994116232242361,-2.61096200673646,
2.03829753397345));
#69854=CARTESIAN_POINT('Ctrl Pts',(1.64350205501279,-2.25926839472914,2.1962924249735));
#69855=CARTESIAN_POINT('Ctrl Pts',(2.79020532811094,0.141938289250975,2.35428731597356));
#69856=CARTESIAN_POINT('Ctrl Pts',(1.40575267279317,2.41438420716175,2.51228220697361));
#69857=CARTESIAN_POINT('Ctrl Pts',(-1.25393904248897,2.49660349308063,2.67027709797367));
#69858=CARTESIAN_POINT('Ctrl Pts',(-2.77611054256664,0.314010001336946,
2.82827198897372));
#69859=CARTESIAN_POINT('Ctrl Pts',(-1.7799124222889,-2.15343997555266,2.98626687997377));
#69860=CARTESIAN_POINT('Ctrl Pts',(0.830946655855235,-2.66738067760568,
3.14426177097383));
#69861=CARTESIAN_POINT('Ctrl Pts',(2.68800621811034,-0.761586880528364,
3.30225666197388));
#69862=CARTESIAN_POINT('Ctrl Pts',(2.1066206787299,1.83508618713756,3.46025155297393));
#69863=CARTESIAN_POINT('Ctrl Pts',(-0.385801684362841,2.76704699413756,
3.61824644397398));
#69864=CARTESIAN_POINT('Ctrl Pts',(-2.52824114267486,1.1888602645272,3.77624133497404));
#69865=CARTESIAN_POINT('Ctrl Pts',(-2.37716759400457,-1.46781001274115,
3.93423622597408));
#69866=CARTESIAN_POINT('Ctrl Pts',(-0.0696285472027664,-2.7929453754341,
4.09223111697415));
#69867=CARTESIAN_POINT('Ctrl Pts',(2.30107456105757,-1.58443929156132,4.25022600797419));
#69868=CARTESIAN_POINT('Ctrl Pts',(2.58434053922803,1.0614028365637,4.40822089897426));
#69869=CARTESIAN_POINT('Ctrl Pts',(0.523202520475101,2.7443853823577,4.56621578997431));
#69870=CARTESIAN_POINT('Ctrl Pts',(-2.01256260784032,1.93777804553689,4.72421068097436));
#69871=CARTESIAN_POINT('Ctrl Pts',(-2.72261639883674,-0.626699249266954,
4.88220557197441));
#69872=CARTESIAN_POINT('Ctrl Pts',(-0.962828204728596,-2.62266159701306,
5.04020046297447));
#69873=CARTESIAN_POINT('Ctrl Pts',(1.67039685162278,-2.23945671142426,5.19819535397451));
#69874=CARTESIAN_POINT('Ctrl Pts',(2.78830881513536,0.175288207517705,5.3561902449746));
#69875=CARTESIAN_POINT('Ctrl Pts',(1.37678542300575,2.43101910795819,5.51418513597462));
#69876=CARTESIAN_POINT('Ctrl Pts',(-1.2836992416995,2.48143270332224,5.67218002697469));
#69877=CARTESIAN_POINT('Ctrl Pts',(-2.77966646474201,0.280795920636377,
5.83017491797473));
#69878=CARTESIAN_POINT('Ctrl Pts',(-1.7540383054339,-2.17456699766373,5.98816980897479));
#69879=CARTESIAN_POINT('Ctrl Pts',(0.862778921897542,-2.65725507548423,
6.14616469997484));
#69880=CARTESIAN_POINT('Ctrl Pts',(2.69691974792615,-0.729394185268462,
6.30415959097489));
#69881=CARTESIAN_POINT('Ctrl Pts',(2.08452949938132,1.86014213716763,6.46215448197495));
#69882=CARTESIAN_POINT('Ctrl Pts',(-0.418857394511624,2.76223650097533,
6.620149372975));
#69883=CARTESIAN_POINT('Ctrl Pts',(-2.5422746462691,1.15854720542358,6.77814426397505));
#69884=CARTESIAN_POINT('Ctrl Pts',(-2.35944829289878,-1.49612691887905,
6.93613915497512));
#69885=CARTESIAN_POINT('Ctrl Pts',(-0.0362306387250156,-2.79357823321186,
7.09413404597515));
#69886=CARTESIAN_POINT('Ctrl Pts',(2.3198539124191,-1.55681399958096,7.25212893697523));
#69887=CARTESIAN_POINT('Ctrl Pts',(2.5714655034136,1.09222578664457,7.41012382797526));
#69888=CARTESIAN_POINT('Ctrl Pts',(0.490352783225777,2.75044471899368,7.56811871897533));
#69889=CARTESIAN_POINT('Ctrl Pts',(-2.03558715979207,1.91357699587635,7.72611360997538));
#69890=CARTESIAN_POINT('Ctrl Pts',(-2.71492886967243,-0.659206520656943,
7.88410850097543));
#69891=CARTESIAN_POINT('Ctrl Pts',(-0.931402394462092,-2.63398587388918,
8.0421033919755));
#69892=CARTESIAN_POINT('Ctrl Pts',(1.69705278236641,-2.21932509067958,8.20009828297554));
#69893=CARTESIAN_POINT('Ctrl Pts',(2.78601373789173,0.208613174406663,8.3580931739756));
#69894=CARTESIAN_POINT('Ctrl Pts',(1.34762133439256,2.44730642612392,8.51608806497565));
#69895=CARTESIAN_POINT('Ctrl Pts',(-1.31327591890231,2.46590720934279,8.6740829559757));
#69896=CARTESIAN_POINT('Ctrl Pts',(-2.78282502490651,0.247541683382087,
8.83207784697575));
#69897=CARTESIAN_POINT('Ctrl Pts',(-1.72791343690234,-2.19538314624801,
8.99007273797581));
#69898=CARTESIAN_POINT('Ctrl Pts',(0.894487847747497,-2.64674960933017,
9.14806762897587));
#69899=CARTESIAN_POINT('Ctrl Pts',(2.70544774003657,-0.697097217171796,
9.30606251997591));
#69900=CARTESIAN_POINT('Ctrl Pts',(2.06214032543822,1.88493216919308,9.46405741097597));
#69901=CARTESIAN_POINT('Ctrl Pts',(-0.451853226630304,2.75703113254833,
9.62205230197602));
#69902=CARTESIAN_POINT('Ctrl Pts',(-2.55594471878539,1.12806852574304,9.78004719297607));
#69903=CARTESIAN_POINT('Ctrl Pts',(-2.34139169650468,-1.52422994583995,
9.93804208397613));
#69904=CARTESIAN_POINT('Ctrl Pts',(-0.00282755092387669,-2.79381173474703,
10.0960369749762));
#69905=CARTESIAN_POINT('Ctrl Pts',(2.33830162879016,-1.52896615301492,10.2540318659762));
#69906=CARTESIAN_POINT('Ctrl Pts',(2.55822286341245,1.12289259742877,10.4120267569763));
#69907=CARTESIAN_POINT('Ctrl Pts',(0.457432947542771,2.7561108654668,10.5700216479763));
#69908=CARTESIAN_POINT('Ctrl Pts',(-2.05832071413818,1.88910239057596,10.7280165389764));
#69909=CARTESIAN_POINT('Ctrl Pts',(-2.70685322748717,-0.691619555106155,
10.8860114299764));
#69910=CARTESIAN_POINT('Ctrl Pts',(-0.899843435489688,-2.64493360895804,
11.0440063209765));
#69911=CARTESIAN_POINT('Ctrl Pts',(1.72346611079269,-2.19887620608651,11.2020012119765));
#69912=CARTESIAN_POINT('Ctrl Pts',(2.78332038555639,0.241908319069164,11.3599961029766));
#69913=CARTESIAN_POINT('Ctrl Pts',(1.31826459668171,2.46324388910665,11.5179909939767));
#69914=CARTESIAN_POINT('Ctrl Pts',(-1.34266485711555,2.45002920164021,11.6759858849767));
#69915=CARTESIAN_POINT('Ctrl Pts',(-2.78558576494693,0.214252058101096,
11.8339807759768));
#69916=CARTESIAN_POINT('Ctrl Pts',(-1.70154155624011,-2.21588545226976,
11.9919756669768));
#69917=CARTESIAN_POINT('Ctrl Pts',(0.926068905704722,-2.63586577921336,
12.1499705579768));
#69918=CARTESIAN_POINT('Ctrl Pts',(2.71358896739729,-0.66470059075221,12.3079654489769));
#69919=CARTESIAN_POINT('Ctrl Pts',(2.03945637158195,1.90945273151837,12.465960339977));
#69920=CARTESIAN_POINT('Ctrl Pts',(-0.484784490030591,2.7514316495538,12.623955230977));
#69921=CARTESIAN_POINT('Ctrl Pts',(-2.56924935619517,1.09742855008785,12.7819501219771));
#69922=CARTESIAN_POINT('Ctrl Pts',(-2.32300048113579,-1.55211501365623,
12.9399450129771));
#69923=CARTESIAN_POINT('Ctrl Pts',(0.0305761225400629,-2.79364596629274,
13.0979399039772));
#69924=CARTESIAN_POINT('Ctrl Pts',(2.35641472627957,-1.50089950416469,13.2559347949772));
#69925=CARTESIAN_POINT('Ctrl Pts',(2.54461517470071,1.15339844793961,13.4139296859773));
#69926=CARTESIAN_POINT('Ctrl Pts',(0.424446453969621,2.76138384673405,13.5719245769773));
#69927=CARTESIAN_POINT('Ctrl Pts',(-2.08075760311621,1.86435613311354,13.7299194679774));
#69928=CARTESIAN_POINT('Ctrl Pts',(-2.69839524633484,-0.72393067103507,
13.8879143589774));
#69929=CARTESIAN_POINT('Ctrl Pts',(-0.86814701313444,-2.65550906063268,
14.0459092499775));
#69930=CARTESIAN_POINT('Ctrl Pts',(1.74961619768082,-2.17810185464822,14.2039041409775));
#69931=CARTESIAN_POINT('Ctrl Pts',(2.78026136217266,0.275147623930244,14.3618990319776));
#69932=CARTESIAN_POINT('Ctrl Pts',(1.28865784862374,2.47886983416738,14.5198939229777));
#69933=CARTESIAN_POINT('Ctrl Pts',(-1.37174423913667,2.4337233465313,14.6778888139777));
#69934=CARTESIAN_POINT('Ctrl Pts',(-2.78817303762162,0.181080103603136,
14.8358837049778));
#69935=CARTESIAN_POINT('Ctrl Pts',(-1.67449675827739,-2.23635459951884,
14.9938785959778));
#69936=CARTESIAN_POINT('Ctrl Pts',(0.956694219915353,-2.62406084291086,
15.1518734869779));
#69937=CARTESIAN_POINT('Ctrl Pts',(2.72293688569169,-0.633270369947463,
15.3098683779779));
#69938=CARTESIAN_POINT('Ctrl Pts',(2.01312970789309,1.93633043049701,15.4678886471889));
#69939=CARTESIAN_POINT('Ctrl Pts',(0.330396509531936,2.47203073808571,15.573243952733));
#69940=CARTESIAN_POINT('Ctrl Pts',(-0.439790560653197,2.32640238805053,
15.6259342946106));
#69941=CARTESIAN_POINT('Ctrl Pts',(-1.12170252862657,2.30152292796285,-0.22036464634795));
#69942=CARTESIAN_POINT('Ctrl Pts',(-1.88328504076518,1.93034738187355,-0.167699682681266));
#69943=CARTESIAN_POINT('Ctrl Pts',(-2.99641952926692,0.379451369086483,
-0.062369755347896));
#69944=CARTESIAN_POINT('Ctrl Pts',(-1.95319028054399,-2.30748880506914,
0.0956251356521572));
#69945=CARTESIAN_POINT('Ctrl Pts',(0.864392190143294,-2.89402422057555,
0.253620026652211));
#69946=CARTESIAN_POINT('Ctrl Pts',(2.89655074515435,-0.858794531016792,
0.411614917652264));
#69947=CARTESIAN_POINT('Ctrl Pts',(2.30175067708376,1.95734667757734,0.569609808652319));
#69948=CARTESIAN_POINT('Ctrl Pts',(-0.381449809775129,2.9969002095631,0.727604699652371));
#69949=CARTESIAN_POINT('Ctrl Pts',(-2.71843210295174,1.3182984262109,0.885599590652427));
#69950=CARTESIAN_POINT('Ctrl Pts',(-2.58946406895983,-1.55647215216739,
1.04359448165247));
#69951=CARTESIAN_POINT('Ctrl Pts',(-0.111394026279792,-3.01913888229157,
1.20158937265253));
#69952=CARTESIAN_POINT('Ctrl Pts',(2.46770169169952,-1.74304346212535,1.35958426365258));
#69953=CARTESIAN_POINT('Ctrl Pts',(2.80821696415988,1.11430488612263,1.51757915465264));
#69954=CARTESIAN_POINT('Ctrl Pts',(0.601229861113374,2.96078331441178,1.67557404565269));
#69955=CARTESIAN_POINT('Ctrl Pts',(-2.15116367709187,2.12137523178328,1.83356893665274));
#69956=CARTESIAN_POINT('Ctrl Pts',(-2.95211484377831,-0.642459816335227,
1.9915638276528));
#69957=CARTESIAN_POINT('Ctrl Pts',(-1.07503175015829,-2.82347975484453,
2.14955871865285));
#69958=CARTESIAN_POINT('Ctrl Pts',(1.77727395779847,-2.44316024393295,2.3075536096529));
#69959=CARTESIAN_POINT('Ctrl Pts',(3.01731248308272,0.153491274520022,2.46554850065296));
#69960=CARTESIAN_POINT('Ctrl Pts',(1.52017310160377,2.6109016185411,2.62354339165301));
#69961=CARTESIAN_POINT('Ctrl Pts',(-1.35600268833558,2.69981309586282,2.78153828265307));
#69962=CARTESIAN_POINT('Ctrl Pts',(-3.0020704605904,0.339568664463957,2.93953317365312));
#69963=CARTESIAN_POINT('Ctrl Pts',(-1.92478736831974,-2.32871798155565,
3.09752806465317));
#69964=CARTESIAN_POINT('Ctrl Pts',(0.898581080119023,-2.88449059092087,
3.25552295565323));
#69965=CARTESIAN_POINT('Ctrl Pts',(2.90679493541049,-0.823575805844403,
3.41351784665328));
#69966=CARTESIAN_POINT('Ctrl Pts',(2.2780878550452,1.9844519699672,3.57151273765333));
#69967=CARTESIAN_POINT('Ctrl Pts',(-0.417203790163499,2.99226918985935,
3.72950762865338));
#69968=CARTESIAN_POINT('Ctrl Pts',(-2.73402587371621,1.2856268607399,3.88750251965344));
#69969=CARTESIAN_POINT('Ctrl Pts',(-2.57065578060014,-1.58728156297948,
4.04549741065349));
#69970=CARTESIAN_POINT('Ctrl Pts',(-0.0752959226825514,-3.02027555497893,
4.20349230165355));
#69971=CARTESIAN_POINT('Ctrl Pts',(2.48836919908102,-1.71340381474775,4.3614871926536));
#69972=CARTESIAN_POINT('Ctrl Pts',(2.79469144832751,1.14779510886793,4.51948208365366));
#69973=CARTESIAN_POINT('Ctrl Pts',(0.565788288161118,2.96776304924624,4.67747697465371));
#69974=CARTESIAN_POINT('Ctrl Pts',(-2.17637398167157,2.09550237301017,4.83547186565376));
#69975=CARTESIAN_POINT('Ctrl Pts',(-2.94422219185483,-0.677709073558362,
4.99346675665382));
#69976=CARTESIAN_POINT('Ctrl Pts',(-1.04119705167313,-2.83613162653042,
5.15146164765387));
#69977=CARTESIAN_POINT('Ctrl Pts',(1.80635784088181,-2.4217360000809,5.30945653865392));
#69978=CARTESIAN_POINT('Ctrl Pts',(3.01526160452625,0.189555690167927,5.46745142965398));
#69979=CARTESIAN_POINT('Ctrl Pts',(1.48884807921076,2.62889050750288,5.62544632065403));
#69980=CARTESIAN_POINT('Ctrl Pts',(-1.38818520181308,2.68340748841342,5.78344121165409));
#69981=CARTESIAN_POINT('Ctrl Pts',(-3.00591581500234,0.303651142802643,
5.94143610265413));
#69982=CARTESIAN_POINT('Ctrl Pts',(-1.89680724263192,-2.35156462545811,
6.0994309936542));
#69983=CARTESIAN_POINT('Ctrl Pts',(0.933004315114162,-2.87354082124909,
6.25742588465425));
#69984=CARTESIAN_POINT('Ctrl Pts',(2.9164339768497,-0.78876280470318,6.4154207756543));
#69985=CARTESIAN_POINT('Ctrl Pts',(2.25419857688244,2.0115473346128,6.57341566665436));
#69986=CARTESIAN_POINT('Ctrl Pts',(-0.452950050793218,2.98706714937797,
6.73141055765441));
#69987=CARTESIAN_POINT('Ctrl Pts',(-2.74920162624943,1.25284648765685,6.88940544865445));
#69988=CARTESIAN_POINT('Ctrl Pts',(-2.55149422719067,-1.61790330737633,
7.04740033965452));
#69989=CARTESIAN_POINT('Ctrl Pts',(-0.0391796106880552,-3.02095992385085,
7.20539523065456));
#69990=CARTESIAN_POINT('Ctrl Pts',(2.50867708492601,-1.68352997804427,7.36339012165463));
#69991=CARTESIAN_POINT('Ctrl Pts',(2.78076845639151,1.18112687521052,7.52138501265468));
#69992=CARTESIAN_POINT('Ctrl Pts',(0.530264765476331,2.97431558209632,7.67937990365473));
#69993=CARTESIAN_POINT('Ctrl Pts',(-2.20127260376274,2.0693314928571,7.83737479465478));
#69994=CARTESIAN_POINT('Ctrl Pts',(-2.93590894068373,-0.712862255572524,
7.99536968565484));
#69995=CARTESIAN_POINT('Ctrl Pts',(-1.00721335568747,-2.84837763639784,
8.1533645766549));
#69996=CARTESIAN_POINT('Ctrl Pts',(1.83518341574924,-2.3999657776655,8.31135946765493));
#69997=CARTESIAN_POINT('Ctrl Pts',(3.0127797207928,0.225593123535039,8.469354358655));
#69998=CARTESIAN_POINT('Ctrl Pts',(1.45731019640918,2.646503522546,8.62734924965505));
#69999=CARTESIAN_POINT('Ctrl Pts',(-1.42016925561481,2.66661830579726,8.78534414065509));
#70000=CARTESIAN_POINT('Ctrl Pts',(-3.00933146435147,0.267690196068054,
8.94333903165517));
#70001=CARTESIAN_POINT('Ctrl Pts',(-1.86855595547932,-2.37407509246219,
9.1013339226552));
#70002=CARTESIAN_POINT('Ctrl Pts',(0.967294170713062,-2.86218026873064,
9.25932881365528));
#70003=CARTESIAN_POINT('Ctrl Pts',(2.92565609996415,-0.753837043497722,
9.41732370465531));
#70004=CARTESIAN_POINT('Ctrl Pts',(2.22998704902682,2.03835513701099,9.57531859565539));
#70005=CARTESIAN_POINT('Ctrl Pts',(-0.488631559655073,2.98143809298718,
9.73331348665541));
#70006=CARTESIAN_POINT('Ctrl Pts',(-2.76398436644151,1.21988701340545,9.89130837765549));
#70007=CARTESIAN_POINT('Ctrl Pts',(-2.53196792453725,-1.64829376402382,
10.0493032686556));
#70008=CARTESIAN_POINT('Ctrl Pts',(-0.00305769780212466,-3.02121243110894,
10.2072981596556));
#70009=CARTESIAN_POINT('Ctrl Pts',(2.52862634254158,-1.65341547205285,10.3652930506557));
#70010=CARTESIAN_POINT('Ctrl Pts',(2.76644793933786,1.21428979338836,10.5232879416557));
#70011=CARTESIAN_POINT('Ctrl Pts',(0.494665438736237,2.9804429212968,10.6812828326558));
#70012=CARTESIAN_POINT('Ctrl Pts',(-2.22585654266583,2.0428647911605,10.8392777236558));
#70013=CARTESIAN_POINT('Ctrl Pts',(-2.92717598625596,-0.74791353028442,
10.9972726146559));
#70014=CARTESIAN_POINT('Ctrl Pts',(-0.973085673433698,-2.86021645605457,
11.1552675056559));
#70015=CARTESIAN_POINT('Ctrl Pts',(1.86374664182347,-2.37785246789358,11.313262396656));
#70016=CARTESIAN_POINT('Ctrl Pts',(3.00986714459602,0.261598307312764,11.471257287656));
#70017=CARTESIAN_POINT('Ctrl Pts',(1.42556398394764,2.66373820614507,11.6292521786561));
#70018=CARTESIAN_POINT('Ctrl Pts',(-1.45195028952006,2.6494479168066,11.7872470696561));
#70019=CARTESIAN_POINT('Ctrl Pts',(-3.01231691323675,0.23169098091872,11.9452419606562));
#70020=CARTESIAN_POINT('Ctrl Pts',(-1.840037550786,-2.3962461718692,12.1032368516563));
#70021=CARTESIAN_POINT('Ctrl Pts',(1.00144575068579,-2.8504105555327,12.2612317426563));
#70022=CARTESIAN_POINT('Ctrl Pts',(2.93445997783494,-0.718803512337577,
12.4192266336564));
#70023=CARTESIAN_POINT('Ctrl Pts',(2.20545674781687,2.06487153637807,12.5772215246564));
#70024=CARTESIAN_POINT('Ctrl Pts',(-0.52424324426491,2.97538284330073,12.7352164156565));
#70025=CARTESIAN_POINT('Ctrl Pts',(-2.77837192714716,1.18675311458651,12.8932113066565));
#70026=CARTESIAN_POINT('Ctrl Pts',(-2.51207976679037,-1.67844852086771,
13.0512061976566));
#70027=CARTESIAN_POINT('Ctrl Pts',(0.0330648484162935,-3.02103317002684,
13.2092010886566));
#70028=CARTESIAN_POINT('Ctrl Pts',(2.54821374516441,-1.62306435449139,13.3671959796567));
#70029=CARTESIAN_POINT('Ctrl Pts',(2.75173266064415,1.24727865002413,13.5251908706567));
#70030=CARTESIAN_POINT('Ctrl Pts',(0.458994028525444,2.98614509383602,13.6831857616568));
#70031=CARTESIAN_POINT('Ctrl Pts',(-2.25011966929414,2.01610432633067,13.8411806526569));
#70032=CARTESIAN_POINT('Ctrl Pts',(-2.91802957260121,-0.782854590876773,
13.9991755436569));
#70033=CARTESIAN_POINT('Ctrl Pts',(-0.938809339044251,-2.87165269052473,
14.157170434657));
#70034=CARTESIAN_POINT('Ctrl Pts',(1.89202519996625,-2.35538720009011,14.315165325657));
#70035=CARTESIAN_POINT('Ctrl Pts',(3.00655913376658,0.297543106240599,14.4731602166571));
#70036=CARTESIAN_POINT('Ctrl Pts',(1.39354741169084,2.6806360160004,14.6311551076571));
#70037=CARTESIAN_POINT('Ctrl Pts',(-1.48339657108533,2.63181485601649,14.7891499986572));
#70038=CARTESIAN_POINT('Ctrl Pts',(-3.01511477548001,0.195819014298005,
14.9471448896572));
#70039=CARTESIAN_POINT('Ctrl Pts',(-1.81079145707627,-2.41838139356435,
15.1051397806573));
#70040=CARTESIAN_POINT('Ctrl Pts',(1.03456379470036,-2.83764476324185,15.2631346716573));
#70041=CARTESIAN_POINT('Ctrl Pts',(2.94456876455265,-0.68481504682045,15.4211295626574));
#70042=CARTESIAN_POINT('Ctrl Pts',(2.17698724050641,2.09393693017821,15.5791498318682));
#70043=CARTESIAN_POINT('Ctrl Pts',(0.357288943051609,2.67324025563383,15.6845051374125));
#70044=CARTESIAN_POINT('Ctrl Pts',(-0.475587059931246,2.51575856995826,
15.73719547929));
#70045=CARTESIAN_POINT('Ctrl Pts',(-1.20613086391808,2.47475401596006,-0.109103461668549));
#70046=CARTESIAN_POINT('Ctrl Pts',(-2.02503618851906,2.0756408191501,-0.0564384980018643));
#70047=CARTESIAN_POINT('Ctrl Pts',(-3.22195411284388,0.408011924669176,
0.0488914293315046));
#70048=CARTESIAN_POINT('Ctrl Pts',(-2.10020305771572,-2.48116893286055,
0.206886320331559));
#70049=CARTESIAN_POINT('Ctrl Pts',(0.929453284141298,-3.11185171137717,
0.364881211331612));
#70050=CARTESIAN_POINT('Ctrl Pts',(3.11456840247411,-0.923434300261156,
0.522876102331665));
#70051=CARTESIAN_POINT('Ctrl Pts',(2.47499890730776,2.10467229854974,0.68087099333172));
#70052=CARTESIAN_POINT('Ctrl Pts',(-0.410160784043849,3.22247097299719,
0.838865884331773));
#70053=CARTESIAN_POINT('Ctrl Pts',(-2.92304312164692,1.41752414666883,0.996860775331826));
#70054=CARTESIAN_POINT('Ctrl Pts',(-2.78436791829607,-1.6736247388661,1.15485566633188));
#70055=CARTESIAN_POINT('Ctrl Pts',(-0.119778434766208,-3.24638350672681,
1.31285055733193));
#70056=CARTESIAN_POINT('Ctrl Pts',(2.6534407272363,-1.87423890306657,1.47084544833198));
#70057=CARTESIAN_POINT('Ctrl Pts',(3.01958591213912,1.19817641546448,1.62884033933204));
#70058=CARTESIAN_POINT('Ctrl Pts',(0.646483246040247,3.18363563043606,1.78683523033209));
#70059=CARTESIAN_POINT('Ctrl Pts',(-2.31307752105799,2.28104695826807,1.94483012133214));
#70060=CARTESIAN_POINT('Ctrl Pts',(-3.17431470112801,-0.690816498611117,
2.1028250123322));
#70061=CARTESIAN_POINT('Ctrl Pts',(-1.15594726807422,-3.0359975029526,2.26081990333225));
#70062=CARTESIAN_POINT('Ctrl Pts',(1.91104586058415,-2.62705209313675,2.41881479433231));
#70063=CARTESIAN_POINT('Ctrl Pts',(3.24441963805449,0.165044259789067,2.57680968533236));
#70064=CARTESIAN_POINT('Ctrl Pts',(1.63459353041437,2.80741902992046,2.73480457633241));
#70065=CARTESIAN_POINT('Ctrl Pts',(-1.45806633418219,2.903022698645,2.89279946733247));
#70066=CARTESIAN_POINT('Ctrl Pts',(-3.22803037861418,0.365127327590972,
3.05079435833252));
#70067=CARTESIAN_POINT('Ctrl Pts',(-2.06966231435056,-2.50399598755864,
3.20878924933257));
#70068=CARTESIAN_POINT('Ctrl Pts',(0.9662155043828,-3.10160050423604,3.36678414033263));
#70069=CARTESIAN_POINT('Ctrl Pts',(3.12558365271064,-0.885564731160449,
3.52477903133268));
#70070=CARTESIAN_POINT('Ctrl Pts',(2.44955503136051,2.13381775279686,3.68277392233274));
#70071=CARTESIAN_POINT('Ctrl Pts',(-0.448605895964152,3.21749138558114,
3.84076881333278));
#70072=CARTESIAN_POINT('Ctrl Pts',(-2.93981060475756,1.3823934569526,3.99876370433284));
#70073=CARTESIAN_POINT('Ctrl Pts',(-2.76414396719572,-1.70675311321781,
4.15675859533289));
#70074=CARTESIAN_POINT('Ctrl Pts',(-0.0809632981623413,-3.24760573452376,
4.31475348633295));
#70075=CARTESIAN_POINT('Ctrl Pts',(2.67566383710448,-1.84236833793416,4.472748377333));
#70076=CARTESIAN_POINT('Ctrl Pts',(3.00504235742698,1.23418738117217,4.63074326833305));
#70077=CARTESIAN_POINT('Ctrl Pts',(0.60837405584714,3.19114071613476,4.78873815933311));
#70078=CARTESIAN_POINT('Ctrl Pts',(-2.34018535550283,2.25322670048346,4.94673305033316));
#70079=CARTESIAN_POINT('Ctrl Pts',(-3.16582798487292,-0.72871889784977,
5.10472794133323));
#70080=CARTESIAN_POINT('Ctrl Pts',(-1.11956589861766,-3.04960165604779,
5.26272283233327));
#70081=CARTESIAN_POINT('Ctrl Pts',(1.94231883014085,-2.60401528873755,5.42071772333333));
#70082=CARTESIAN_POINT('Ctrl Pts',(3.24221439391714,0.203823172818145,5.57871261433338));
#70083=CARTESIAN_POINT('Ctrl Pts',(1.60091073541578,2.82676190704757,5.73670750533343));
#70084=CARTESIAN_POINT('Ctrl Pts',(-1.49267116192667,2.88538227350458,5.8947023963335));
#70085=CARTESIAN_POINT('Ctrl Pts',(-3.23216516526265,0.326506364968914,
6.05269728733353));
#70086=CARTESIAN_POINT('Ctrl Pts',(-2.03957617982994,-2.52856225325249,
6.21069217833361));
#70087=CARTESIAN_POINT('Ctrl Pts',(1.00322970833078,-3.08982656701393,6.36868706933365));
#70088=CARTESIAN_POINT('Ctrl Pts',(3.13594820577326,-0.848131424137899,
6.5266819603337));
#70089=CARTESIAN_POINT('Ctrl Pts',(2.42386765438354,2.16295253205797,6.68467685133376));
#70090=CARTESIAN_POINT('Ctrl Pts',(-0.487042707074808,3.21189779778061,
6.84267174233381));
#70091=CARTESIAN_POINT('Ctrl Pts',(-2.95612860622976,1.34714576989012,7.00066663333385));
#70092=CARTESIAN_POINT('Ctrl Pts',(-2.74354016148256,-1.73967969587362,
7.15866152433392));
#70093=CARTESIAN_POINT('Ctrl Pts',(-0.0421285826510928,-3.24834161448985,
7.31665641533396));
#70094=CARTESIAN_POINT('Ctrl Pts',(2.69750025743292,-1.81024595650758,7.47465130633402));
#70095=CARTESIAN_POINT('Ctrl Pts',(2.99007140936943,1.27002796377647,7.63264619733409));
#70096=CARTESIAN_POINT('Ctrl Pts',(0.570176747726886,3.19818644519895,7.79064108833413));
#70097=CARTESIAN_POINT('Ctrl Pts',(-2.36695804773341,2.22508598983787,7.94863597933417));
#70098=CARTESIAN_POINT('Ctrl Pts',(-3.15688901169502,-0.766517990488109,
8.10663087033424));
#70099=CARTESIAN_POINT('Ctrl Pts',(-1.08302431691284,-3.06276939890652,
8.2646257613343));
#70100=CARTESIAN_POINT('Ctrl Pts',(1.97331404913207,-2.58060646465142,8.42262065233434));
#70101=CARTESIAN_POINT('Ctrl Pts',(3.23954570369386,0.24257307266342,8.5806155433344));
#70102=CARTESIAN_POINT('Ctrl Pts',(1.56699905842581,2.84570061896807,8.73861043433446));
#70103=CARTESIAN_POINT('Ctrl Pts',(-1.52706259232731,2.86732940225174,8.89660532533451));
#70104=CARTESIAN_POINT('Ctrl Pts',(-3.23583790379643,0.287838708754021,
9.05460021633457));
#70105=CARTESIAN_POINT('Ctrl Pts',(-2.0091984740563,-2.55276703867637,9.21259510733461));
#70106=CARTESIAN_POINT('Ctrl Pts',(1.04010049367863,-3.07761092813111,9.37058999833468));
#70107=CARTESIAN_POINT('Ctrl Pts',(3.14586445989173,-0.810576869823648,
9.52858488933471));
#70108=CARTESIAN_POINT('Ctrl Pts',(2.39783377261543,2.19177810482891,9.68657978033478));
#70109=CARTESIAN_POINT('Ctrl Pts',(-0.525409892679846,3.20584505342603,
9.84457467133482));
#70110=CARTESIAN_POINT('Ctrl Pts',(-2.97202401409764,1.31170550106787,10.0025695623349));
#70111=CARTESIAN_POINT('Ctrl Pts',(-2.72254415256981,-1.77235758220769,
10.1605644533349));
#70112=CARTESIAN_POINT('Ctrl Pts',(-0.00328784468036826,-3.24861312747085,
10.318559344335));
#70113=CARTESIAN_POINT('Ctrl Pts',(2.71895105629298,-1.77786479109078,10.476554235335));
#70114=CARTESIAN_POINT('Ctrl Pts',(2.97467301526326,1.30568698934795,10.6345491263351));
#70115=CARTESIAN_POINT('Ctrl Pts',(0.531897929929706,3.2047749771268,10.7925440173351));
#70116=CARTESIAN_POINT('Ctrl Pts',(-2.39339237119349,2.19662719174505,10.9505389083352));
#70117=CARTESIAN_POINT('Ctrl Pts',(-3.14749874502475,-0.804207505462682,
11.1085337993352));
#70118=CARTESIAN_POINT('Ctrl Pts',(-1.04632791137771,-3.0754993031511,11.2665286903353));
#70119=CARTESIAN_POINT('Ctrl Pts',(2.00402717285426,-2.55682872970066,11.4245235813353));
#70120=CARTESIAN_POINT('Ctrl Pts',(3.23641390363566,0.281288295556363,11.5825184723354));
#70121=CARTESIAN_POINT('Ctrl Pts',(1.53286337121357,2.86423252318349,11.7405133633355));
#70122=CARTESIAN_POINT('Ctrl Pts',(-1.56123572192459,2.84886663197299,11.8985082543355));
#70123=CARTESIAN_POINT('Ctrl Pts',(-3.23904806152655,0.249129903736346,
12.0565031453356));
#70124=CARTESIAN_POINT('Ctrl Pts',(-1.9785335453319,-2.57660689146864,12.2144980363356));
#70125=CARTESIAN_POINT('Ctrl Pts',(1.07682259566685,-3.06495533185205,12.3724929273357));
#70126=CARTESIAN_POINT('Ctrl Pts',(3.15533098827258,-0.772906433922943,
12.5304878183357));
#70127=CARTESIAN_POINT('Ctrl Pts',(2.37145712405178,2.22029034123777,12.6884827093358));
#70128=CARTESIAN_POINT('Ctrl Pts',(-0.56370199849923,3.19933403704765,12.8464776003358));
#70129=CARTESIAN_POINT('Ctrl Pts',(-2.98749449809915,1.27607767908515,13.0044724913359));
#70130=CARTESIAN_POINT('Ctrl Pts',(-2.70115905244496,-1.80478202807917,
13.1624673823359));
#70131=CARTESIAN_POINT('Ctrl Pts',(0.0355535742925287,-3.24842037376092,
13.320462273336));
#70132=CARTESIAN_POINT('Ctrl Pts',(2.74001276404922,-1.7452292048181,13.478457164336));
#70133=CARTESIAN_POINT('Ctrl Pts',(2.95885014658758,1.34115885210865,13.6364520553361));
#70134=CARTESIAN_POINT('Ctrl Pts',(0.493541603081266,3.21090634093799,13.7944469463361));
#70135=CARTESIAN_POINT('Ctrl Pts',(-2.41948173547208,2.1678525195478,13.9524418373362));
#70136=CARTESIAN_POINT('Ctrl Pts',(-3.13766389886759,-0.841778510718479,
14.1104367283363));
#70137=CARTESIAN_POINT('Ctrl Pts',(-1.00947166495406,-3.08779632041677,
14.2684316193363));
#70138=CARTESIAN_POINT('Ctrl Pts',(2.03443420225168,-2.53267254553199,14.4264265103364));
#70139=CARTESIAN_POINT('Ctrl Pts',(3.23285690536049,0.319938588550955,14.5844214013364));
#70140=CARTESIAN_POINT('Ctrl Pts',(1.49843697475794,2.88240219783341,14.7424162923365));
#70141=CARTESIAN_POINT('Ctrl Pts',(-1.595048903034,2.82990636550169,14.9004111833365));
#70142=CARTESIAN_POINT('Ctrl Pts',(-3.2420565133384,0.210557924992872,15.0584060743366));
#70143=CARTESIAN_POINT('Ctrl Pts',(-1.94708615587513,-2.60040818760985,
15.2164009653366));
#70144=CARTESIAN_POINT('Ctrl Pts',(1.11243336948536,-3.05122868357283,15.3743958563367));
#70145=CARTESIAN_POINT('Ctrl Pts',(3.16620064341362,-0.736359723693434,
15.5323907473367));
#70146=CARTESIAN_POINT('Ctrl Pts',(2.34084477311972,2.2515434298594,15.6904110165477));
#70147=CARTESIAN_POINT('Ctrl Pts',(0.384181376571284,2.87444977318196,15.7957663220919));
#70148=CARTESIAN_POINT('Ctrl Pts',(-0.511383559209293,2.70511475186599,
15.8484566639694));
#70149=CARTESIAN_POINT('Ctrl Pts',(-1.29055919920959,2.64798510395726,0.00215772301085195));
#70150=CARTESIAN_POINT('Ctrl Pts',(-2.16678733627292,2.22093425642666,0.0548226866775366));
#70151=CARTESIAN_POINT('Ctrl Pts',(-3.44748869642086,0.436572480251873,
0.160152614010905));
#70152=CARTESIAN_POINT('Ctrl Pts',(-2.24721583488744,-2.65484906065196,
0.318147505010959));
#70153=CARTESIAN_POINT('Ctrl Pts',(0.994514378139303,-3.32967920217881,
0.476142396011012));
#70154=CARTESIAN_POINT('Ctrl Pts',(3.33258605979387,-0.988074069505522,
0.634137287011066));
#70155=CARTESIAN_POINT('Ctrl Pts',(2.64824713753178,2.25199791952217,0.79213217801112));
#70156=CARTESIAN_POINT('Ctrl Pts',(-0.43887175831257,3.44804173643128,0.950127069011173));
#70157=CARTESIAN_POINT('Ctrl Pts',(-3.12765414034211,1.51674986712676,1.10812196001123));
#70158=CARTESIAN_POINT('Ctrl Pts',(-2.97927176763231,-1.79077732556482,
1.26611685101128));
#70159=CARTESIAN_POINT('Ctrl Pts',(-0.128162843252621,-3.47362813116205,
1.42411174201133));
#70160=CARTESIAN_POINT('Ctrl Pts',(2.83917976277308,-2.0054343440078,1.58210663301139));
#70161=CARTESIAN_POINT('Ctrl Pts',(3.23095486011837,1.28204794480633,1.74010152401144));
#70162=CARTESIAN_POINT('Ctrl Pts',(0.691736630967119,3.40648794646033,1.89809641501149));
#70163=CARTESIAN_POINT('Ctrl Pts',(-2.47499136502412,2.44071868475286,2.05609130601155));
#70164=CARTESIAN_POINT('Ctrl Pts',(-3.39651455847771,-0.73917318088701,
2.2140861970116));
#70165=CARTESIAN_POINT('Ctrl Pts',(-1.23686278599015,-3.24851525106067,
2.37208108801165));
#70166=CARTESIAN_POINT('Ctrl Pts',(2.04481776336984,-2.81094394234055,2.53007597901171));
#70167=CARTESIAN_POINT('Ctrl Pts',(3.47152679302626,0.176597245058115,2.68807087001176));
#70168=CARTESIAN_POINT('Ctrl Pts',(1.74901395922498,3.00393644129981,2.84606576101181));
#70169=CARTESIAN_POINT('Ctrl Pts',(-1.5601299800288,3.10623230142719,3.00406065201187));
#70170=CARTESIAN_POINT('Ctrl Pts',(-3.45399029663795,0.390685990717984,
3.16205554301192));
#70171=CARTESIAN_POINT('Ctrl Pts',(-2.21453726038139,-2.67927399356163,
3.32005043401198));
#70172=CARTESIAN_POINT('Ctrl Pts',(1.03384992864659,-3.31871041755122,3.47804532501203));
#70173=CARTESIAN_POINT('Ctrl Pts',(3.3443723700108,-0.947553656476489,3.63604021601208));
#70174=CARTESIAN_POINT('Ctrl Pts',(2.62102220767581,2.28318353562651,3.79403510701214));
#70175=CARTESIAN_POINT('Ctrl Pts',(-0.480008001764807,3.44271358130293,
3.95202999801219));
#70176=CARTESIAN_POINT('Ctrl Pts',(-3.1455953357989,1.47916005316529,4.11002488901225));
#70177=CARTESIAN_POINT('Ctrl Pts',(-2.9576321537913,-1.82622466345613,4.2680197800123));
#70178=CARTESIAN_POINT('Ctrl Pts',(-0.086630673642128,-3.47493591406859,
4.42601467101235));
#70179=CARTESIAN_POINT('Ctrl Pts',(2.86295847512794,-1.97133286112058,4.5840095620124));
#70180=CARTESIAN_POINT('Ctrl Pts',(3.21539326652644,1.3205796534764,4.74200445301246));
#70181=CARTESIAN_POINT('Ctrl Pts',(0.650959823533161,3.41451838302329,4.89999934401251));
#70182=CARTESIAN_POINT('Ctrl Pts',(-2.50399672933409,2.41095102795676,5.05799423501256));
#70183=CARTESIAN_POINT('Ctrl Pts',(-3.387433777891,-0.779728722141183,5.21598912601263));
#70184=CARTESIAN_POINT('Ctrl Pts',(-1.1979347455622,-3.26307168556515,5.37398401701266));
#70185=CARTESIAN_POINT('Ctrl Pts',(2.07827981939988,-2.7862945773942,5.53197890801273));
#70186=CARTESIAN_POINT('Ctrl Pts',(3.46916718330803,0.218090655468369,5.68997379901277));
#70187=CARTESIAN_POINT('Ctrl Pts',(1.7129733916208,3.02463330659226,5.84796869001284));
#70188=CARTESIAN_POINT('Ctrl Pts',(-1.59715712204027,3.08735705859576,6.00596358101288));
#70189=CARTESIAN_POINT('Ctrl Pts',(-3.45841451552297,0.349361587135177,
6.16395847201295));
#70190=CARTESIAN_POINT('Ctrl Pts',(-2.18234511702796,-2.70555988104687,
6.321953363013));
#70191=CARTESIAN_POINT('Ctrl Pts',(1.0734551015474,-3.30611231277879,6.47994825401305));
#70192=CARTESIAN_POINT('Ctrl Pts',(3.35546243469681,-0.907500043572617,
6.63794314501309));
#70193=CARTESIAN_POINT('Ctrl Pts',(2.59353673188465,2.31435772950313,6.79593803601317));
#70194=CARTESIAN_POINT('Ctrl Pts',(-0.521135363356403,3.43672844618325,
6.95393292701321));
#70195=CARTESIAN_POINT('Ctrl Pts',(-3.16305558621008,1.44144505212338,7.11192781801326));
#70196=CARTESIAN_POINT('Ctrl Pts',(-2.93558609577446,-1.86145608437091,
7.26992270901332));
#70197=CARTESIAN_POINT('Ctrl Pts',(-0.0450775546141294,-3.47572330512885,
7.42791760001339));
#70198=CARTESIAN_POINT('Ctrl Pts',(2.88632342993983,-1.93696193497089,7.58591249101342));
#70199=CARTESIAN_POINT('Ctrl Pts',(3.19937436234735,1.35892905234243,7.74390738201349));
#70200=CARTESIAN_POINT('Ctrl Pts',(0.610088729977438,3.42205730830159,7.90190227301353));
#70201=CARTESIAN_POINT('Ctrl Pts',(-2.53264349170409,2.38084048681862,8.0598971640136));
#70202=CARTESIAN_POINT('Ctrl Pts',(-3.37786908270631,-0.820173725403692,
8.21789205501364));
#70203=CARTESIAN_POINT('Ctrl Pts',(-1.15883527813821,-3.27716116141519,
8.3758869460137));
#70204=CARTESIAN_POINT('Ctrl Pts',(2.1114446825149,-2.76124715163735,8.53388183701374));
#70205=CARTESIAN_POINT('Ctrl Pts',(3.46631168659493,0.259553021791801,8.6918767280138));
#70206=CARTESIAN_POINT('Ctrl Pts',(1.67668792044244,3.04489771539016,8.84987161901386));
#70207=CARTESIAN_POINT('Ctrl Pts',(-1.63395592903981,3.06804049870621,9.0078665100139));
#70208=CARTESIAN_POINT('Ctrl Pts',(-3.46234434324138,0.307987221439991,
9.16586140101396));
#70209=CARTESIAN_POINT('Ctrl Pts',(-2.14984099263328,-2.73145898489056,
9.32385629201401));
#70210=CARTESIAN_POINT('Ctrl Pts',(1.1129068166442,-3.29304158753158,9.48185118301408));
#70211=CARTESIAN_POINT('Ctrl Pts',(3.3660728198193,-0.867316696149578,9.63984607401411));
#70212=CARTESIAN_POINT('Ctrl Pts',(2.56568049620403,2.34520107264683,9.79784096501418));
#70213=CARTESIAN_POINT('Ctrl Pts',(-0.562188225704613,3.43025201386488,
9.95583585601423));
#70214=CARTESIAN_POINT('Ctrl Pts',(-3.18006366175377,1.40352398873029,10.1138307470143));
#70215=CARTESIAN_POINT('Ctrl Pts',(-2.91312038060238,-1.89642140039157,
10.2718256380144));
#70216=CARTESIAN_POINT('Ctrl Pts',(-0.00351799155861674,-3.47601382383277,
10.4298205290144));
#70217=CARTESIAN_POINT('Ctrl Pts',(2.90927577004438,-1.90231411012871,10.5878154200145));
#70218=CARTESIAN_POINT('Ctrl Pts',(3.18289809118866,1.39708418530755,10.7458103110145));
#70219=CARTESIAN_POINT('Ctrl Pts',(0.569130421123177,3.42910703295679,10.9038052020146));
#70220=CARTESIAN_POINT('Ctrl Pts',(-2.56092819972115,2.35038959232959,11.0618000930147));
#70221=CARTESIAN_POINT('Ctrl Pts',(-3.36782150379354,-0.860501480640944,
11.2197949840147));
#70222=CARTESIAN_POINT('Ctrl Pts',(-1.11957014932173,-3.29078215024765,
11.3777898750148));
#70223=CARTESIAN_POINT('Ctrl Pts',(2.14430770388506,-2.73580499150773,11.5357847660148));
#70224=CARTESIAN_POINT('Ctrl Pts',(3.46296066267528,0.300978283799964,11.6937796570149));
#70225=CARTESIAN_POINT('Ctrl Pts',(1.64016275847952,3.06472684022192,11.8517745480149));
#70226=CARTESIAN_POINT('Ctrl Pts',(-1.67052115432913,3.04828534713938,12.009769439015));
#70227=CARTESIAN_POINT('Ctrl Pts',(-3.46577920981637,0.266568826553971,
12.167764330015));
#70228=CARTESIAN_POINT('Ctrl Pts',(-2.1170295398778,-2.75696761106808,12.3257592210151));
#70229=CARTESIAN_POINT('Ctrl Pts',(1.15219944064791,-3.2795001081714,12.4837541120151));
#70230=CARTESIAN_POINT('Ctrl Pts',(3.37620199871023,-0.82700935550831,12.6417490030152));
#70231=CARTESIAN_POINT('Ctrl Pts',(2.5374575002867,2.37570914609746,12.7997438940152));
#70232=CARTESIAN_POINT('Ctrl Pts',(-0.603160752733551,3.42328523079457,
12.9577387850153));
#70233=CARTESIAN_POINT('Ctrl Pts',(-3.19661706905115,1.36540224358379,13.1157336760154));
#70234=CARTESIAN_POINT('Ctrl Pts',(-2.89023833809954,-1.93111553529064,
13.2737285670154));
#70235=CARTESIAN_POINT('Ctrl Pts',(0.0380423001687606,-3.47580757749502,
13.4317234580155));
#70236=CARTESIAN_POINT('Ctrl Pts',(2.93181178293406,-1.8673940551448,13.5897183490155));
#70237=CARTESIAN_POINT('Ctrl Pts',(3.165967632531,1.43503905419316,13.7477132400156));
#70238=CARTESIAN_POINT('Ctrl Pts',(0.528089177637088,3.43566758803995,13.9057081310156));
#70239=CARTESIAN_POINT('Ctrl Pts',(-2.58884380165001,2.31960071276493,14.0637030220157));
#70240=CARTESIAN_POINT('Ctrl Pts',(-3.35729822513396,-0.90070243056019,
14.2216979130157));
#70241=CARTESIAN_POINT('Ctrl Pts',(-1.08013399086388,-3.30393995030882,
14.3796928040158));
#70242=CARTESIAN_POINT('Ctrl Pts',(2.1768432045371,-2.70995789097388,14.5376876950158));
#70243=CARTESIAN_POINT('Ctrl Pts',(3.45915467695442,0.342334070861309,14.6956825860159));
#70244=CARTESIAN_POINT('Ctrl Pts',(1.60332653782504,3.08416837966642,14.8536774770159));
#70245=CARTESIAN_POINT('Ctrl Pts',(-1.70670123498267,3.02799787498689,15.011672368016));
#70246=CARTESIAN_POINT('Ctrl Pts',(-3.4689982511968,0.225296835687742,15.1696672590161));
#70247=CARTESIAN_POINT('Ctrl Pts',(-2.083380854674,-2.78243498165535,15.3276621500161));
#70248=CARTESIAN_POINT('Ctrl Pts',(1.19030294427037,-3.26481260390381,15.4856570410162));
#70249=CARTESIAN_POINT('Ctrl Pts',(3.38783252227459,-0.787904400566419,
15.6436519320162));
#70250=CARTESIAN_POINT('Ctrl Pts',(2.50470230573304,2.4091499295406,15.8016722012271));
#70251=CARTESIAN_POINT('Ctrl Pts',(0.411073810090958,3.07565929073008,15.9070275067712));
#70252=CARTESIAN_POINT('Ctrl Pts',(-0.547180058487341,2.89447093377372,
15.9597178486488));
#70253=CARTESIAN_POINT('',(-1.37838761780672,-1.93231671732536,-0.00102187466432732));
#70254=CARTESIAN_POINT('Ctrl Pts',(-1.37994859234592,-1.93347131995892,
-3.54317269968263E-16));
#70255=CARTESIAN_POINT('Ctrl Pts',(-1.43831895271373,-1.90176082500493,
-3.157397654546E-15));
#70256=CARTESIAN_POINT('Ctrl Pts',(-1.49514575458196,-1.86752259046863,
-4.34169899202657E-15));
#70257=CARTESIAN_POINT('Ctrl Pts',(-1.55024291463986,-1.83079524515745,
-4.08700850940136E-15));
#70258=CARTESIAN_POINT('Ctrl Pts',(-1.61848165101461,-1.78530782562802,
-3.78829000146298E-15));
#70259=CARTESIAN_POINT('Ctrl Pts',(-1.68406861913595,-1.7360041391636,-3.23024659681305E-15));
#70260=CARTESIAN_POINT('Ctrl Pts',(-1.74691851112218,-1.68324606443273,
-1.38083988687754E-15));
#70261=CARTESIAN_POINT('Ctrl Pts',(-1.78341473484423,-1.65261004521818,
-3.06910260178252E-16));
#70262=CARTESIAN_POINT('Ctrl Pts',(-1.81898770098065,-1.6208082297802,-6.08222538088405E-16));
#70263=CARTESIAN_POINT('Ctrl Pts',(-1.8536174249306,-1.58790418430479,9.99200722162641E-16));
#70264=CARTESIAN_POINT('Ctrl Pts',(-1.86599100473682,-1.57614720832583,
1.20135119786233E-15));
#70265=CARTESIAN_POINT('Ctrl Pts',(-1.87824533378606,-1.56424827137885,
-1.41288533260964E-15));
#70266=CARTESIAN_POINT('Ctrl Pts',(-1.89037564784624,-1.55221386701802,
-9.99200722162641E-16));
#70267=CARTESIAN_POINT('Ctrl Pts',(-1.95007879268067,-1.49298277184718,
9.89920292723067E-16));
#70268=CARTESIAN_POINT('Ctrl Pts',(-2.00663609510422,-1.43061741633727,
-1.65749671126755E-16));
#70269=CARTESIAN_POINT('Ctrl Pts',(-2.05996340201355,-1.36549876184075,
-1.87350135405495E-16));
#70270=CARTESIAN_POINT('Ctrl Pts',(-2.1147730212604,-1.29857003684645,-2.09551016929213E-16));
#70271=CARTESIAN_POINT('Ctrl Pts',(-2.16617121071363,-1.22873232295192,
-1.7198130603224E-15));
#70272=CARTESIAN_POINT('Ctrl Pts',(-2.2140407003356,-1.15635106472184,1.94289029309402E-16));
#70273=CARTESIAN_POINT('Ctrl Pts',(-2.22834382104116,-1.13472397236174,
7.66211425954361E-16));
#70274=CARTESIAN_POINT('Ctrl Pts',(-2.24233169959178,-1.11286950794349,
1.53050669563487E-15));
#70275=CARTESIAN_POINT('Ctrl Pts',(-2.25600064404541,-1.09079672684346,
6.66133814775094E-16));
#70276=CARTESIAN_POINT('Ctrl Pts',(-2.26668277274188,-1.07354709288677,
8.73288649491799E-17));
#70277=CARTESIAN_POINT('Ctrl Pts',(-2.27717011522814,-1.05616412126237,
1.79116184180511E-15));
#70278=CARTESIAN_POINT('Ctrl Pts',(-2.28746078556243,-1.03865201740679,
1.04083408558608E-15));
#70279=CARTESIAN_POINT('Ctrl Pts',(-2.3043278418407,-1.00994857713634,-1.81981144522876E-16));
#70280=CARTESIAN_POINT('Ctrl Pts',(-2.32064206145016,-0.980939786561838,
8.03113917588522E-16));
#70281=CARTESIAN_POINT('Ctrl Pts',(-2.33639567929063,-0.951653513157818,
1.1518563880486E-15));
#70282=CARTESIAN_POINT('Ctrl Pts',(-2.37855893182263,-0.873271229560512,
2.08523670738533E-15));
#70283=CARTESIAN_POINT('Ctrl Pts',(-2.41671657812553,-0.792890901649699,
2.49401152098159E-15));
#70284=CARTESIAN_POINT('Ctrl Pts',(-2.45076495402598,-0.710905122334628,
2.48412401759879E-15));
#70285=CARTESIAN_POINT('Ctrl Pts',(-2.48531718185078,-0.62770610768645,
2.47409019776256E-15));
#70286=CARTESIAN_POINT('Ctrl Pts',(-2.51563826586878,-0.542853018948936,
3.90133880310071E-16));
#70287=CARTESIAN_POINT('Ctrl Pts',(-2.54158369978739,-0.456717097481997,
1.08246744900953E-15));
#70288=CARTESIAN_POINT('Ctrl Pts',(-2.56086666911763,-0.392699808848862,
1.59701837205101E-15));
#70289=CARTESIAN_POINT('Ctrl Pts',(-2.57773198353371,-0.327973042405811,
9.74482875872416E-16));
#70290=CARTESIAN_POINT('Ctrl Pts',(-2.59210443472119,-0.262679462931668,
1.36002320516582E-15));
#70291=CARTESIAN_POINT('Ctrl Pts',(-2.5985839551262,-0.233243211940112,
1.53383603625654E-15));
#70292=CARTESIAN_POINT('Ctrl Pts',(-2.60455661090768,-0.203691668580144,
2.53601366117178E-15));
#70293=CARTESIAN_POINT('Ctrl Pts',(-2.61001448404778,-0.174037544115253,
3.24740234702858E-15));
#70294=CARTESIAN_POINT('Ctrl Pts',(-2.61367527686472,-0.154147450841394,
3.72455645530154E-15));
#70295=CARTESIAN_POINT('Ctrl Pts',(-2.61710457712665,-0.134210532287337,
4.62273400142151E-15));
#70296=CARTESIAN_POINT('Ctrl Pts',(-2.62029962849891,-0.114231655457859,
4.24660306919122E-15));
#70297=CARTESIAN_POINT('Ctrl Pts',(-2.62289997143562,-0.0979715315368936,
3.94048297941976E-15));
#70298=CARTESIAN_POINT('Ctrl Pts',(-2.62534443718676,-0.0816875079929038,
3.10814855031425E-15));
#70299=CARTESIAN_POINT('Ctrl Pts',(-2.62763003749086,-0.0653963791800208,
2.80331313717852E-15));
#70300=CARTESIAN_POINT('Ctrl Pts',(-2.64049518650456,0.0263028559853445,
1.08746062892512E-15));
#70301=CARTESIAN_POINT('Ctrl Pts',(-2.64834915604118,0.118337335855572,
-1.43867851364987E-16));
#70302=CARTESIAN_POINT('Ctrl Pts',(-2.651061018059,0.210311484632908,1.11022302462516E-15));
#70303=CARTESIAN_POINT('Ctrl Pts',(-2.65226580187014,0.251172326652904,
1.66737098243456E-15));
#70304=CARTESIAN_POINT('Ctrl Pts',(-2.65245512561064,0.292021668535638,
3.00696151315835E-15));
#70305=CARTESIAN_POINT('Ctrl Pts',(-2.65161463128253,0.332826444242183,
2.4980018054066E-15));
#70306=CARTESIAN_POINT('Ctrl Pts',(-2.64976919202174,0.422419833034951,
1.50902187236961E-15));
#70307=CARTESIAN_POINT('Ctrl Pts',(-2.64296288001183,0.511797898314078,
2.96934449413589E-15));
#70308=CARTESIAN_POINT('Ctrl Pts',(-2.63144647848012,0.600691769744574,
1.72084568816899E-15));
#70309=CARTESIAN_POINT('Ctrl Pts',(-2.6199300769484,0.68958564117507,4.72346882202091E-16));
#70310=CARTESIAN_POINT('Ctrl Pts',(-2.60370331353105,0.777996048559996,
1.9168699501881E-15));
#70311=CARTESIAN_POINT('Ctrl Pts',(-2.58296460883121,0.865656938831558,
2.05391259555654E-15));
#70312=CARTESIAN_POINT('Ctrl Pts',(-2.57869408333521,0.88370811764552,1.96966790296377E-15));
#70313=CARTESIAN_POINT('Ctrl Pts',(-2.57423206760738,0.901727502426253,
-1.21291301995112E-15));
#70314=CARTESIAN_POINT('Ctrl Pts',(-2.56958003501042,0.919712740461558,
-3.05311331771918E-16));
#70315=CARTESIAN_POINT('Ctrl Pts',(-2.56604635272843,0.933374320783267,
4.12631142411499E-16));
#70316=CARTESIAN_POINT('Ctrl Pts',(-2.56240532303519,0.94700728407811,2.96072359195587E-16));
#70317=CARTESIAN_POINT('Ctrl Pts',(-2.5586586911495,0.960608258314246,4.16333634234434E-16));
#70318=CARTESIAN_POINT('Ctrl Pts',(-2.53410521411211,1.0497419706143,2.12171029893344E-15));
#70319=CARTESIAN_POINT('Ctrl Pts',(-2.5050122305201,1.13753405978208,1.37195759662732E-17));
#70320=CARTESIAN_POINT('Ctrl Pts',(-2.47166814999145,1.22370371724256,5.82867087928207E-16));
#70321=CARTESIAN_POINT('Ctrl Pts',(-2.43774488106874,1.31137014608583,1.16190072145076E-15));
#70322=CARTESIAN_POINT('Ctrl Pts',(-2.3994213674271,1.39735806555781,5.22902315393273E-16));
#70323=CARTESIAN_POINT('Ctrl Pts',(-2.35694651643052,1.48137454593671,-1.4432899320127E-15));
#70324=CARTESIAN_POINT('Ctrl Pts',(-2.31397714205714,1.56636920781853,-3.43237403205193E-15));
#70325=CARTESIAN_POINT('Ctrl Pts',(-2.26675893828999,1.64934713164981,-7.02071007117468E-16));
#70326=CARTESIAN_POINT('Ctrl Pts',(-2.21549747648264,1.72999528429546,-1.38777878078145E-15));
#70327=CARTESIAN_POINT('Ctrl Pts',(-2.1844953421251,1.77877003194907,-1.80248417113962E-15));
#70328=CARTESIAN_POINT('Ctrl Pts',(-2.15201333894673,1.82669238798436,3.6817056606625E-16));
#70329=CARTESIAN_POINT('Ctrl Pts',(-2.11808850376185,1.87368930169053,-5.55111512312578E-16));
#70330=CARTESIAN_POINT('Ctrl Pts',(-2.1089145366433,1.88639822536441,-8.91198155137096E-16));
#70331=CARTESIAN_POINT('Ctrl Pts',(-2.09963412322397,1.89904053530927,-2.70664328051753E-15));
#70332=CARTESIAN_POINT('Ctrl Pts',(-2.09025911328956,1.91160012317952,-2.4980018054066E-15));
#70333=CARTESIAN_POINT('Ctrl Pts',(-2.03145402967863,1.9903805852799,-9.44997988912952E-16));
#70334=CARTESIAN_POINT('Ctrl Pts',(-1.96883756375649,2.06603912302116,-8.89268907589407E-16));
#70335=CARTESIAN_POINT('Ctrl Pts',(-1.90268196527423,2.13826743811982,-1.4432899320127E-15));
#70336=CARTESIAN_POINT('Ctrl Pts',(-1.8363597619551,2.21067765145431,-1.96590601829329E-15));
#70337=CARTESIAN_POINT('Ctrl Pts',(-1.76648017671596,2.27964124288177,-1.24430221715273E-15));
#70338=CARTESIAN_POINT('Ctrl Pts',(-1.69326751955099,2.34483179094349,-1.4432899320127E-15));
#70339=CARTESIAN_POINT('Ctrl Pts',(-1.62146081065517,2.40877044429517,-8.49003099635195E-16));
#70340=CARTESIAN_POINT('Ctrl Pts',(-1.54644728359594,2.46908034426638,-2.45521957121142E-15));
#70341=CARTESIAN_POINT('Ctrl Pts',(-1.46839770083036,2.5254261196735,-1.99840144432528E-15));
#70342=CARTESIAN_POINT('Ctrl Pts',(-1.41023968234419,2.56741172077001,-9.78062777089129E-16));
#70343=CARTESIAN_POINT('Ctrl Pts',(-1.35039506896439,2.6071958124341,2.30014117106762E-15));
#70344=CARTESIAN_POINT('Ctrl Pts',(-1.28892185405328,2.64462557919714,7.7715611723761E-16));
#70345=CARTESIAN_POINT('Ctrl Pts',(-1.37733488469885,-1.93084092506131,
-0.00102187466432729));
#70346=CARTESIAN_POINT('Ctrl Pts',(-1.36944737626449,-1.93646735465424,
-0.000681249776216117));
#70347=CARTESIAN_POINT('Ctrl Pts',(-1.36152539135263,-1.94204545278975,
-0.000340624888104793));
#70348=CARTESIAN_POINT('Ctrl Pts',(-1.35356952483514,-1.9475748006014,6.38378239159465E-15));
#70349=CARTESIAN_POINT('Origin',(-1.44337567297407,-2.5,-6.));
#70350=CARTESIAN_POINT('',(-1.44337567297407,-2.5,-6.));
#70351=CARTESIAN_POINT('',(1.44337567297406,-2.5,-6.));
#70352=CARTESIAN_POINT('',(-0.721687836487033,-2.5,-6.));
#70353=CARTESIAN_POINT('',(-1.44337567297407,-2.5,-3.));
#70354=CARTESIAN_POINT('',(-1.44337567297407,-2.5,-6.));
#70355=CARTESIAN_POINT('',(1.44337567297406,-2.5,-3.));
#70356=CARTESIAN_POINT('',(-1.44337567297407,-2.5,-3.));
#70357=CARTESIAN_POINT('',(1.44337567297406,-2.5,-6.));
#70358=CARTESIAN_POINT('Origin',(-2.88675134594813,3.53525079574969E-16,
-6.));
#70359=CARTESIAN_POINT('',(-2.88675134594813,3.53525079574969E-16,-6.));
#70360=CARTESIAN_POINT('',(-2.52590742770461,-0.625,-6.));
#70361=CARTESIAN_POINT('',(-2.88675134594813,5.55111512312578E-16,-3.));
#70362=CARTESIAN_POINT('',(-2.88675134594813,3.53525079574969E-16,-6.));
#70363=CARTESIAN_POINT('',(-2.88675134594813,3.53525079574969E-16,-3.));
#70364=CARTESIAN_POINT('Origin',(-1.44337567297406,2.5,-6.));
#70365=CARTESIAN_POINT('',(-1.44337567297406,2.5,-6.));
#70366=CARTESIAN_POINT('',(-1.80421959121758,1.875,-6.));
#70367=CARTESIAN_POINT('',(-1.44337567297406,2.5,-3.));
#70368=CARTESIAN_POINT('',(-1.44337567297406,2.5,-6.));
#70369=CARTESIAN_POINT('',(-1.44337567297406,2.5,-3.));
#70370=CARTESIAN_POINT('Origin',(1.44337567297406,2.5,-6.));
#70371=CARTESIAN_POINT('',(1.44337567297406,2.5,-6.));
#70372=CARTESIAN_POINT('',(0.721687836487033,2.5,-6.));
#70373=CARTESIAN_POINT('',(1.44337567297406,2.5,-3.));
#70374=CARTESIAN_POINT('',(1.44337567297406,2.5,-6.));
#70375=CARTESIAN_POINT('',(1.44337567297406,2.5,-3.));
#70376=CARTESIAN_POINT('Origin',(2.88675134594813,0.,-6.));
#70377=CARTESIAN_POINT('',(2.88675134594813,0.,-6.));
#70378=CARTESIAN_POINT('',(2.52590742770461,0.625,-6.));
#70379=CARTESIAN_POINT('',(2.88675134594813,0.,-3.));
#70380=CARTESIAN_POINT('',(2.88675134594813,0.,-6.));
#70381=CARTESIAN_POINT('',(2.88675134594813,0.,-3.));
#70382=CARTESIAN_POINT('Origin',(1.44337567297406,-2.5,-6.));
#70383=CARTESIAN_POINT('',(1.80421959121758,-1.875,-6.));
#70384=CARTESIAN_POINT('',(1.44337567297406,-2.5,-3.));
#70385=CARTESIAN_POINT('Origin',(0.,0.,-3.));
#70386=CARTESIAN_POINT('Origin',(0.,0.,0.));
#70387=CARTESIAN_POINT('',(-5.,-6.12323399573677E-16,0.));
#70388=CARTESIAN_POINT('Origin',(0.,0.,0.));
#70389=CARTESIAN_POINT('Origin',(0.,0.,-6.));
#70390=CARTESIAN_POINT('',(-5.,-6.12323399573677E-16,-6.));
#70391=CARTESIAN_POINT('',(-5.,-6.12323399573677E-16,-6.));
#70392=CARTESIAN_POINT('Origin',(0.,0.,-6.));
#70393=CARTESIAN_POINT('Origin',(0.,0.,-6.));
#70394=CARTESIAN_POINT('Origin',(0.,0.,16.));
#94389=UNCERTAINTY_MEASURE_WITH_UNIT(LENGTH_MEASURE(0.01),#94413,
'DISTANCE_ACCURACY_VALUE',
'Maximum model space distance between geometric entities at asserted c
onnectivities');
#94394=UNCERTAINTY_MEASURE_WITH_UNIT(LENGTH_MEASURE(0.01),#94413,
'DISTANCE_ACCURACY_VALUE',
'Maximum model space distance between geometric entities at asserted c
onnectivities');
#94407=(
GEOMETRIC_REPRESENTATION_CONTEXT(3)
GLOBAL_UNCERTAINTY_ASSIGNED_CONTEXT((#94389))
GLOBAL_UNIT_ASSIGNED_CONTEXT((#94413,#94415,#94416))
REPRESENTATION_CONTEXT('','3D')
);
#94412=(
GEOMETRIC_REPRESENTATION_CONTEXT(3)
GLOBAL_UNCERTAINTY_ASSIGNED_CONTEXT((#94394))
GLOBAL_UNIT_ASSIGNED_CONTEXT((#94413,#94415,#94416))
REPRESENTATION_CONTEXT('','3D')
);
#94413=(
LENGTH_UNIT()
NAMED_UNIT(*)
SI_UNIT(.MILLI.,.METRE.)
);
#94415=(
NAMED_UNIT(*)
PLANE_ANGLE_UNIT()
SI_UNIT($,.RADIAN.)
);
#94416=(
NAMED_UNIT(*)
SI_UNIT($,.STERADIAN.)
SOLID_ANGLE_UNIT()
);
#94429=SHAPE_DEFINITION_REPRESENTATION(#94463,#94498);
#94463=PRODUCT_DEFINITION_SHAPE('',$,#94516);
#94498=SHAPE_REPRESENTATION('',(#8773),#94407);
#94503=PRODUCT_DEFINITION_CONTEXT('part definition',#94556,'design');
#94516=PRODUCT_DEFINITION('Socket head cap screw M6x16',
'Socket head cap screw M6x16',#94533,#94503);
#94533=PRODUCT_DEFINITION_FORMATION('',$,#94570);
#94556=APPLICATION_CONTEXT(
'Core Data for Automotive Mechanical Design Process');
#94557=PRODUCT_CONTEXT('part definition',#94556,'mechanical');
#94570=PRODUCT('Socket head cap screw M6x16',
'Socket head cap screw M6x16',$,(#94557));
#94578=PRESENTATION_STYLE_ASSIGNMENT((#94585));
#94585=SURFACE_STYLE_USAGE(.BOTH.,#94592);
#94592=SURFACE_SIDE_STYLE('',(#94599));
#94599=SURFACE_STYLE_FILL_AREA(#94606);
#94606=FILL_AREA_STYLE('Opaque(64,72,82)',(#94613));
#94613=FILL_AREA_STYLE_COLOUR('Opaque(64,72,82)',#94620);
#94620=COLOUR_RGB('Opaque(64,72,82)',0.250980392156863,0.282352941176471,
0.32156862745098);
ENDSEC;
END-ISO-10303-21;
